ISO-10303-21;
HEADER;
FILE_DESCRIPTION (('STEP AP214'),
    '1' );
FILE_NAME ('Injection Molded Chain Links 8.step',
    '2026-10-08T22:59:04',
    ( '' ),
    ( '' ),
    'SwSTEP 2.0',
    'SolidWorks 2020',
    '' );
FILE_SCHEMA (( 'AUTOMOTIVE_DESIGN' ));
ENDSEC;

DATA;
#3=CARTESIAN_POINT ( 'NONE',  ( -23.15000000000000213, 3.470628026992396808, -231.7731008717366876 ) ) ;
#40=LINE ( 'NONE', #161717, #239034 ) ;
#60=FACE_OUTER_BOUND ( 'NONE', #199534, .T. ) ;
#69=AXIS2_PLACEMENT_3D ( 'NONE', #162469, #21667, #98580 ) ;
#101=CARTESIAN_POINT ( 'NONE',  ( -20.54999999999999716, 23.49882452903949925, -253.1653563615082305 ) ) ;
#129=ORIENTED_EDGE ( 'NONE', *, *, #240704, .T. ) ;
#140=EDGE_CURVE ( 'NONE', #198947, #93557, #66106, .T. ) ;
#164=DIRECTION ( 'NONE',  ( 2.952720810173289605E-16, -0.4721928772777346794, -0.8814952561688429444 ) ) ;
#199=CARTESIAN_POINT ( 'NONE',  ( -22.50000000000000000, 1.619487989037824871, -230.7814958294534335 ) ) ;
#212=DIRECTION ( 'NONE',  ( -0.7070776581708964059, -0.3339045366652730884, -0.6233369439636241571 ) ) ;
#219=ADVANCED_FACE ( 'NONE', ( #251471 ), #75440, .T. ) ;
#244=DIRECTION ( 'NONE',  ( -1.000000000000000000, 0.000000000000000000, 0.000000000000000000 ) ) ;
#260=VERTEX_POINT ( 'NONE', #174569 ) ;
#316=EDGE_CURVE ( 'NONE', #120394, #176327, #185325, .T. ) ;
#322=EDGE_LOOP ( 'NONE', ( #244833, #202567, #58686, #132622 ) ) ;
#332=CYLINDRICAL_SURFACE ( 'NONE', #17646, 0.1000000000000075273 ) ;
#352=CARTESIAN_POINT ( 'NONE',  ( -18.59999999999999787, 10.63601275468165142, -265.6051570720007931 ) ) ;
#367=FACE_OUTER_BOUND ( 'NONE', #189454, .T. ) ;
#371=DIRECTION ( 'NONE',  ( 0.000000000000000000, -0.8814952561688430555, 0.4721928772777346239 ) ) ;
#395=ORIENTED_EDGE ( 'NONE', *, *, #245882, .T. ) ;
#400=EDGE_CURVE ( 'NONE', #236903, #41196, #35696, .T. ) ;
#404=CARTESIAN_POINT ( 'NONE',  ( -20.94999999999999929, 43.24695311518262031, -245.0026972281755491 ) ) ;
#412=EDGE_CURVE ( 'NONE', #54594, #188452, #201762, .T. ) ;
#444=AXIS2_PLACEMENT_3D ( 'NONE', #191508, #53247, #36272 ) ;
#457=DIRECTION ( 'NONE',  ( 1.000000000000000000, 0.000000000000000000, 0.000000000000000000 ) ) ;
#506=CARTESIAN_POINT ( 'NONE',  ( 21.14999999999999858, 10.21728496540352360, -227.9671432372868765 ) ) ;
#531=CARTESIAN_POINT ( 'NONE',  ( -21.05000000000000071, 40.27305497204160645, -251.4871534980821082 ) ) ;
#570=CARTESIAN_POINT ( 'NONE',  ( -23.25000000000000000, 23.68770167995059595, -252.8127582590406348 ) ) ;
#606=DIRECTION ( 'NONE',  ( -0.000000000000000000, 0.4721928772777331806, 0.8814952561688438326 ) ) ;
#636=DIRECTION ( 'NONE',  ( 1.000000000000000000, 0.000000000000000000, 0.000000000000000000 ) ) ;
#642=FACE_OUTER_BOUND ( 'NONE', #91854, .T. ) ;
#643=DIRECTION ( 'NONE',  ( -1.000000000000000000, 0.000000000000000000, 0.000000000000000000 ) ) ;
#647=CIRCLE ( 'NONE', #158927, 11.80000000000001670 ) ;
#658=CIRCLE ( 'NONE', #225521, 0.1000000000000013933 ) ;
#697=AXIS2_PLACEMENT_3D ( 'NONE', #238510, #41624, #258027 ) ;
#724=CARTESIAN_POINT ( 'NONE',  ( -18.52186455168981638, 8.844482643606943029, -245.4073368711099477 ) ) ;
#726=EDGE_CURVE ( 'NONE', #253511, #179129, #72550, .T. ) ;
#786=DIRECTION ( 'NONE',  ( 0.000000000000000000, 0.9424537609900496271, 0.3343365196859450217 ) ) ;
#802=ORIENTED_EDGE ( 'NONE', *, *, #150859, .T. ) ;
#804=DIRECTION ( 'NONE',  ( -3.265361837132812600E-16, 0.4721928772777346239, 0.8814952561688430555 ) ) ;
#807=ORIENTED_EDGE ( 'NONE', *, *, #217651, .F. ) ;
#853=DIRECTION ( 'NONE',  ( -1.000000000000000000, 0.000000000000000000, -0.000000000000000000 ) ) ;
#867=CARTESIAN_POINT ( 'NONE',  ( -18.50000000000000000, 16.56538529403860238, -240.6448716151659823 ) ) ;
#916=DIRECTION ( 'NONE',  ( -0.000000000000000000, 0.5474227397873200340, -0.8368562265788217491 ) ) ;
#957=EDGE_LOOP ( 'NONE', ( #50520, #79684, #17049, #193542 ) ) ;
#974=LINE ( 'NONE', #144343, #138543 ) ;
#1013=ORIENTED_EDGE ( 'NONE', *, *, #141561, .F. ) ;
#1024=AXIS2_PLACEMENT_3D ( 'NONE', #181277, #82122, #221642 ) ;
#1029=EDGE_CURVE ( 'NONE', #88325, #70494, #117580, .T. ) ;
#1030=CARTESIAN_POINT ( 'NONE',  ( 21.10642757222115407, 22.98234816118409185, -230.0602600960314419 ) ) ;
#1032=VECTOR ( 'NONE', #248459, 999.9999999999998863 ) ;
#1054=ORIENTED_EDGE ( 'NONE', *, *, #171013, .T. ) ;
#1056=B_SPLINE_CURVE_WITH_KNOTS ( 'NONE', 3,
 ( #24582, #242312, #4960, #182362, #88352, #44128 ),
 .UNSPECIFIED., .F., .F.,
 ( 4, 2, 4 ),
 ( 0.000000000000000000, 0.0002113392456166024729, 0.0004226784912332049457 ),
 .UNSPECIFIED. ) ;
#1063=AXIS2_PLACEMENT_3D ( 'NONE', #82994, #24366, #21792 ) ;
#1070=ORIENTED_EDGE ( 'NONE', *, *, #6774, .F. ) ;
#1083=CYLINDRICAL_SURFACE ( 'NONE', #136111, 0.09999999999999438505 ) ;
#1126=CARTESIAN_POINT ( 'NONE',  ( -22.39999999999999858, 10.80758397488570743, -226.8651660546161111 ) ) ;
#1130=VERTEX_POINT ( 'NONE', #101710 ) ;
#1156=ORIENTED_EDGE ( 'NONE', *, *, #29802, .T. ) ;
#1187=ORIENTED_EDGE ( 'NONE', *, *, #165921, .F. ) ;
#1249=VECTOR ( 'NONE', #185443, 1000.000000000000000 ) ;
#1252=DIRECTION ( 'NONE',  ( 0.000000000000000000, -0.4721928772777346239, -0.8814952561688430555 ) ) ;
#1254=FACE_BOUND ( 'NONE', #25184, .T. ) ;
#1255=VERTEX_POINT ( 'NONE', #130282 ) ;
#1284=CARTESIAN_POINT ( 'NONE',  ( -18.47140463609786210, 37.97412965213577962, -261.2273517166002534 ) ) ;
#1287=DIRECTION ( 'NONE',  ( -1.000000000000000000, 0.000000000000000000, 0.000000000000000000 ) ) ;
#1293=CIRCLE ( 'NONE', #172041, 0.1000000000000053346 ) ;
#1299=CARTESIAN_POINT ( 'NONE',  ( -18.54148534481894472, 46.44433919924418319, -243.0795225066946159 ) ) ;
#1304=ORIENTED_EDGE ( 'NONE', *, *, #48349, .T. ) ;
#1306=AXIS2_PLACEMENT_3D ( 'NONE', #80522, #239639, #121000 ) ;
#1314=DIRECTION ( 'NONE',  ( -0.000000000000000000, -0.8814952561688430555, 0.4721928772777346239 ) ) ;
#1317=ORIENTED_EDGE ( 'NONE', *, *, #97114, .T. ) ;
#1325=CIRCLE ( 'NONE', #163847, 0.09999999999999564793 ) ;
#1381=ORIENTED_EDGE ( 'NONE', *, *, #10400, .F. ) ;
#1401=AXIS2_PLACEMENT_3D ( 'NONE', #177812, #119103, #201198 ) ;
#1404=AXIS2_PLACEMENT_3D ( 'NONE', #179154, #203814, #100818 ) ;
#1407=ADVANCED_FACE ( 'NONE', ( #79280 ), #5302, .F. ) ;
#1437=EDGE_CURVE ( 'NONE', #26265, #126765, #32201, .T. ) ;
#1438=EDGE_LOOP ( 'NONE', ( #59081, #252539, #235616, #116783 ) ) ;
#1457=ORIENTED_EDGE ( 'NONE', *, *, #165449, .F. ) ;
#1462=ORIENTED_EDGE ( 'NONE', *, *, #232577, .T. ) ;
#1463=VERTEX_POINT ( 'NONE', #200529 ) ;
#1479=VERTEX_POINT ( 'NONE', #244777 ) ;
#1485=ADVANCED_FACE ( 'NONE', ( #218794 ), #100951, .F. ) ;
#1509=LINE ( 'NONE', #6648, #175588 ) ;
#1512=CIRCLE ( 'NONE', #51558, 0.1000000000000013933 ) ;
#1519=CARTESIAN_POINT ( 'NONE',  ( -18.59999999999999787, 13.71992543034163958, -238.5823796952984992 ) ) ;
#1533=FACE_OUTER_BOUND ( 'NONE', #81379, .T. ) ;
#1535=ORIENTED_EDGE ( 'NONE', *, *, #187968, .T. ) ;
#1538=CARTESIAN_POINT ( 'NONE',  ( 18.59999999999999787, 45.99141771592758943, -256.5205054824189119 ) ) ;
#1542=AXIS2_PLACEMENT_3D ( 'NONE', #201731, #59621, #160067 ) ;
#1594=CARTESIAN_POINT ( 'NONE',  ( -23.15000000000000213, 28.42524210734032053, -258.3567845160494585 ) ) ;
#1632=EDGE_LOOP ( 'NONE', ( #167534, #95771, #153789, #255852, #194006, #42861, #88956, #101450, #103179, #1381, #99248, #94098, #160662, #52035, #31709, #102029, #113560, #203152 ) ) ;
#1641=CYLINDRICAL_SURFACE ( 'NONE', #28968, 11.80000000000000604 ) ;
#1668=ADVANCED_FACE ( 'NONE', ( #191265 ), #92132, .T. ) ;
#1685=ORIENTED_EDGE ( 'NONE', *, *, #121618, .F. ) ;
#1816=AXIS2_PLACEMENT_3D ( 'NONE', #183721, #5041, #10225 ) ;
#1818=DIRECTION ( 'NONE',  ( 1.000000000000000000, 0.000000000000000000, 0.000000000000000000 ) ) ;
#1878=ORIENTED_EDGE ( 'NONE', *, *, #194972, .T. ) ;
#1917=EDGE_LOOP ( 'NONE', ( #93620, #204400, #64244, #37138, #52393, #59076 ) ) ;
#1918=DIRECTION ( 'NONE',  ( -0.000000000000000000, 0.8814952561688430555, -0.4721928772777346239 ) ) ;
#1943=VECTOR ( 'NONE', #227255, 1000.000000000000000 ) ;
#1967=ORIENTED_EDGE ( 'NONE', *, *, #232485, .F. ) ;
#1996=FACE_OUTER_BOUND ( 'NONE', #62739, .T. ) ;
#2021=ORIENTED_EDGE ( 'NONE', *, *, #250072, .F. ) ;
#2047=DIRECTION ( 'NONE',  ( 0.000000000000000000, -0.8814952561688476074, 0.4721928772777262417 ) ) ;
#2060=AXIS2_PLACEMENT_3D ( 'NONE', #76641, #152367, #231897 ) ;
#2075=VERTEX_POINT ( 'NONE', #235196 ) ;
#2108=CARTESIAN_POINT ( 'NONE',  ( -21.14999999999999858, 1.572268701310051586, -230.8696453550703325 ) ) ;
#2133=ORIENTED_EDGE ( 'NONE', *, *, #155455, .T. ) ;
#2162=CIRCLE ( 'NONE', #181272, 2.000000000000006661 ) ;
#2186=CYLINDRICAL_SURFACE ( 'NONE', #18211, 0.09999999999999939493 ) ;
#2189=ORIENTED_EDGE ( 'NONE', *, *, #193610, .F. ) ;
#2203=ADVANCED_FACE ( 'NONE', ( #120419 ), #199938, .T. ) ;
#2205=CARTESIAN_POINT ( 'NONE',  ( -21.05000000000000782, 10.01651311888701201, -228.1334776613236386 ) ) ;
#2206=DIRECTION ( 'NONE',  ( 0.000000000000000000, 0.8814952561688430555, -0.4721928772777346239 ) ) ;
#2209=B_SPLINE_CURVE_WITH_KNOTS ( 'NONE', 3,
 ( #113554, #173585, #210106, #212668 ),
 .UNSPECIFIED., .F., .F.,
 ( 4, 4 ),
 ( 6.254634441385501517E-18, 0.0001058379652594648159 ),
 .UNSPECIFIED. ) ;
#2224=CYLINDRICAL_SURFACE ( 'NONE', #27248, 0.09999999999999983902 ) ;
#2229=DIRECTION ( 'NONE',  ( 1.000000000000000000, 0.000000000000000000, 0.000000000000000000 ) ) ;
#2317=DIRECTION ( 'NONE',  ( 0.000000000000000000, 0.4646089985449745052, 0.8855159391400224678 ) ) ;
#2331=CARTESIAN_POINT ( 'NONE',  ( 21.08750232978087880, 22.97271790860457230, -230.0531648411424044 ) ) ;
#2333=CARTESIAN_POINT ( 'NONE',  ( 21.05000000000000071, 28.15345123516638282, -259.0759448016705733 ) ) ;
#2336=CARTESIAN_POINT ( 'NONE',  ( -23.25000000000000000, 7.128833340093095217, -233.7327013124392749 ) ) ;
#2338=SPHERICAL_SURFACE ( 'NONE', #28389, 0.1000000000000000056 ) ;
#2388=DIRECTION ( 'NONE',  ( 1.000000000000000000, 0.000000000000000000, 0.000000000000000000 ) ) ;
#2394=DIRECTION ( 'NONE',  ( 0.000000000000000000, 0.4721928772778128947, 0.8814952561688012000 ) ) ;
#2414=CARTESIAN_POINT ( 'NONE',  ( -20.85000000000000142, 42.15997144203495139, -239.2817429668763793 ) ) ;
#2425=AXIS2_PLACEMENT_3D ( 'NONE', #153513, #135160, #16531 ) ;
#2461=DIRECTION ( 'NONE',  ( 1.000000000000000000, 0.000000000000000000, 0.000000000000000000 ) ) ;
#2488=CYLINDRICAL_SURFACE ( 'NONE', #129690, 0.1000000000000013933 ) ;
#2489=DIRECTION ( 'NONE',  ( 0.000000000000000000, -0.4721928772777347350, -0.8814952561688431665 ) ) ;
#2500=DIRECTION ( 'NONE',  ( 1.000000000000000000, 0.000000000000000000, 0.000000000000000000 ) ) ;
#2501=AXIS2_PLACEMENT_3D ( 'NONE', #233664, #34202, #113703 ) ;
#2537=DIRECTION ( 'NONE',  ( 1.000000000000000000, 0.000000000000000000, 0.000000000000000000 ) ) ;
#2546=EDGE_LOOP ( 'NONE', ( #121682, #240910, #99758, #98790 ) ) ;
#2548=ADVANCED_FACE ( 'NONE', ( #119975 ), #159831, .T. ) ;
#2555=AXIS2_PLACEMENT_3D ( 'NONE', #240546, #38496, #121896 ) ;
#2584=DIRECTION ( 'NONE',  ( 0.000000000000000000, -0.4721928772777346794, -0.8814952561688431665 ) ) ;
#2589=CARTESIAN_POINT ( 'NONE',  ( -18.51697539158857353, 46.41023286455060060, -243.0722154975327385 ) ) ;
#2591=AXIS2_PLACEMENT_3D ( 'NONE', #61545, #237618, #58937 ) ;
#2620=ORIENTED_EDGE ( 'NONE', *, *, #144929, .T. ) ;
#2635=ORIENTED_EDGE ( 'NONE', *, *, #233065, .T. ) ;
#2647=EDGE_CURVE ( 'NONE', #234687, #108265, #87058, .T. ) ;
#2650=ORIENTED_EDGE ( 'NONE', *, *, #214883, .T. ) ;
#2694=VERTEX_POINT ( 'NONE', #64942 ) ;
#2716=ORIENTED_EDGE ( 'NONE', *, *, #55006, .T. ) ;
#2732=AXIS2_PLACEMENT_3D ( 'NONE', #99635, #38413, #241744 ) ;
#2753=CARTESIAN_POINT ( 'NONE',  ( 20.85000000000000142, 43.00579525902548994, -254.2551217332645876 ) ) ;
#2759=ORIENTED_EDGE ( 'NONE', *, *, #250214, .T. ) ;
#2775=CYLINDRICAL_SURFACE ( 'NONE', #125101, 0.1000000000000075273 ) ;
#2778=CIRCLE ( 'NONE', #52842, 11.80000000000000959 ) ;
#2786=ADVANCED_FACE ( 'NONE', ( #171790 ), #135175, .T. ) ;
#2811=CARTESIAN_POINT ( 'NONE',  ( 18.59999999999999076, 34.53503747617446606, -235.1972745784239578 ) ) ;
#2829=CARTESIAN_POINT ( 'NONE',  ( -20.54999999999999716, 19.28991295610541812, -237.9781866380819793 ) ) ;
#2834=DIRECTION ( 'NONE',  ( 0.000000000000000000, -0.8814952561689786137, 0.4721928772774816596 ) ) ;
#2852=AXIS2_PLACEMENT_3D ( 'NONE', #112691, #13597, #31893 ) ;
#2867=DIRECTION ( 'NONE',  ( 0.000000000000000000, -0.8814952561688440547, 0.4721928772777328476 ) ) ;
#2929=EDGE_LOOP ( 'NONE', ( #211555, #73148, #61901, #229163 ) ) ;
#2945=CARTESIAN_POINT ( 'NONE',  ( 20.01093837587850288, 34.49798355602222699, -235.0639822023744614 ) ) ;
#2953=CIRCLE ( 'NONE', #240477, 0.9750000000000036415 ) ;
#2965=CIRCLE ( 'NONE', #202889, 0.1000000000000013933 ) ;
#2970=ORIENTED_EDGE ( 'NONE', *, *, #184693, .F. ) ;
#2987=VERTEX_POINT ( 'NONE', #146714 ) ;
#3013=AXIS2_PLACEMENT_3D ( 'NONE', #51744, #214687, #96017 ) ;
#3042=EDGE_CURVE ( 'NONE', #15820, #122934, #14467, .T. ) ;
#3056=LINE ( 'NONE', #158337, #235204 ) ;
#3129=DIRECTION ( 'NONE',  ( -1.000000000000000000, 0.000000000000000000, 0.000000000000000000 ) ) ;
#3142=EDGE_CURVE ( 'NONE', #183490, #176803, #185137, .T. ) ;
#3172=CARTESIAN_POINT ( 'NONE',  ( -23.25000000000000000, 43.62273694548321146, -253.2814864317374770 ) ) ;
#3174=VECTOR ( 'NONE', #70464, 1000.000000000000000 ) ;
#3278=DIRECTION ( 'NONE',  ( 0.000000000000000000, -0.8814952561688429444, 0.4721928772777349570 ) ) ;
#3298=ORIENTED_EDGE ( 'NONE', *, *, #77797, .T. ) ;
#3304=CARTESIAN_POINT ( 'NONE',  ( -21.14999999999999858, 10.30543449102040476, -228.0143625250146329 ) ) ;
#3326=LINE ( 'NONE', #39936, #119321 ) ;
#3338=EDGE_CURVE ( 'NONE', #3782, #136922, #3056, .T. ) ;
#3361=EDGE_LOOP ( 'NONE', ( #54331, #120515, #209399, #88518, #138557, #223536 ) ) ;
#3382=EDGE_LOOP ( 'NONE', ( #256344, #215257, #222788, #187858 ) ) ;
#3393=CIRCLE ( 'NONE', #245024, 0.09999999999999983902 ) ;
#3411=CARTESIAN_POINT ( 'NONE',  ( 23.14999999999999858, 28.08470566095357057, -239.2860081655328770 ) ) ;
#3426=EDGE_CURVE ( 'NONE', #121993, #223188, #5613, .T. ) ;
#3445=FACE_OUTER_BOUND ( 'NONE', #188794, .T. ) ;
#3452=ORIENTED_EDGE ( 'NONE', *, *, #212330, .T. ) ;
#3461=CARTESIAN_POINT ( 'NONE',  ( 21.70464131381650219, 10.47921085838517286, -227.4781768778995570 ) ) ;
#3490=ORIENTED_EDGE ( 'NONE', *, *, #228821, .F. ) ;
#3513=CARTESIAN_POINT ( 'NONE',  ( 18.59999999999997655, 42.20719072976272912, -239.1935934412594804 ) ) ;
#3542=DIRECTION ( 'NONE',  ( 1.000000000000000000, 0.000000000000000000, 0.000000000000000000 ) ) ;
#3616=DIRECTION ( 'NONE',  ( 0.000000000000000000, 0.8814952561688444987, -0.4721928772777320149 ) ) ;
#3617=CARTESIAN_POINT ( 'NONE',  ( 21.02374657821582815, 36.02918351771350558, -236.0543695115171943 ) ) ;
#3649=CARTESIAN_POINT ( 'NONE',  ( 20.94788355080264353, 46.36250628750308778, -243.0620573837410063 ) ) ;
#3659=CARTESIAN_POINT ( 'NONE',  ( -23.15000000000000213, 20.06933876993645782, -235.7297789824848451 ) ) ;
#3666=DIRECTION ( 'NONE',  ( 0.000000000000000000, 0.8496786552930077896, 0.5273008465188219196 ) ) ;
#3699=CIRCLE ( 'NONE', #145157, 0.09999999999999913125 ) ;
#3700=CARTESIAN_POINT ( 'NONE',  ( 23.14999999999999858, 28.36802138732021206, -238.7571110118315971 ) ) ;
#3719=CIRCLE ( 'NONE', #57866, 0.09999999999999939493 ) ;
#3722=ORIENTED_EDGE ( 'NONE', *, *, #247076, .T. ) ;
#3735=CARTESIAN_POINT ( 'NONE',  ( 22.40736611211992368, -3.140208063160686791, -228.2318569537739847 ) ) ;
#3776=EDGE_CURVE ( 'NONE', #194531, #154195, #66290, .T. ) ;
#3782=VERTEX_POINT ( 'NONE', #147084 ) ;
#3798=LINE ( 'NONE', #208438, #32156 ) ;
#3823=DIRECTION ( 'NONE',  ( -1.000000000000000000, 0.000000000000000000, 0.000000000000000000 ) ) ;
#3825=DIRECTION ( 'NONE',  ( -1.000000000000000000, 0.000000000000000000, -0.000000000000000000 ) ) ;
#3834=CARTESIAN_POINT ( 'NONE',  ( 20.95035502843362707, 18.75477178125364830, -228.0741875901196636 ) ) ;
#3835=ORIENTED_EDGE ( 'NONE', *, *, #241766, .F. ) ;
#3839=DIRECTION ( 'NONE',  ( -1.000000000000000000, -0.000000000000000000, -0.000000000000000000 ) ) ;
#3876=VERTEX_POINT ( 'NONE', #136499 ) ;
#3877=DIRECTION ( 'NONE',  ( 1.000000000000000000, 0.000000000000000000, 0.000000000000000000 ) ) ;
#3907=AXIS2_PLACEMENT_3D ( 'NONE', #83576, #212, #160613 ) ;
#3915=CARTESIAN_POINT ( 'NONE',  ( 21.05000000000000071, 28.40523720341322544, -239.6697522603257937 ) ) ;
#3925=DIRECTION ( 'NONE',  ( 1.000000000000000000, 0.000000000000000000, 0.000000000000000000 ) ) ;
#3955=ORIENTED_EDGE ( 'NONE', *, *, #88344, .T. ) ;
#3997=ADVANCED_FACE ( 'NONE', ( #76540 ), #219910, .T. ) ;
#4100=CARTESIAN_POINT ( 'NONE',  ( -21.05000000000000071, 18.24178995542692050, -237.7003448530951459 ) ) ;
#4112=DIRECTION ( 'NONE',  ( -2.952720810173288619E-16, 0.4721928772777346239, 0.8814952561688430555 ) ) ;
#4113=CARTESIAN_POINT ( 'NONE',  ( 18.59999999999999787, 16.52766025697963315, -240.8672687545768270 ) ) ;
#4125=DIRECTION ( 'NONE',  ( 0.000000000000000000, 0.8814952561688437216, -0.4721928772777334582 ) ) ;
#4130=VECTOR ( 'NONE', #187871, 1000.000000000000000 ) ;
#4131=DIRECTION ( 'NONE',  ( 2.557131231893036985E-16, -0.8496786552930077896, -0.5273008465188220306 ) ) ;
#4149=DIRECTION ( 'NONE',  ( 0.000000000000000000, 0.8814952561688476074, -0.4721928772777262417 ) ) ;
#4155=DIRECTION ( 'NONE',  ( 0.000000000000000000, 0.8814952561688429444, -0.4721928772777345684 ) ) ;
#4214=ORIENTED_EDGE ( 'NONE', *, *, #33008, .F. ) ;
#4216=DIRECTION ( 'NONE',  ( 0.000000000000000000, 0.8814952561688449428, -0.4721928772777310157 ) ) ;
#4227=CARTESIAN_POINT ( 'NONE',  ( 19.75857864376269291, 34.58225676390223668, -235.1091250528070589 ) ) ;
#4229=CARTESIAN_POINT ( 'NONE',  ( 20.85000000000000142, 46.01276039807270024, -256.6622985126337539 ) ) ;
#4234=DIRECTION ( 'NONE',  ( 1.000000000000000000, -0.000000000000000000, -0.000000000000000000 ) ) ;
#4276=EDGE_CURVE ( 'NONE', #213072, #257480, #21560, .T. ) ;
#4392=CARTESIAN_POINT ( 'NONE',  ( -23.25000000000000000, 42.20719072976272912, -239.1935934412594804 ) ) ;
#4411=LINE ( 'NONE', #142627, #230215 ) ;
#4419=ADVANCED_FACE ( 'NONE', ( #78783 ), #158382, .T. ) ;
#4424=DIRECTION ( 'NONE',  ( 2.952720810173289605E-16, -0.4721928772777354011, -0.8814952561688425003 ) ) ;
#4439=CYLINDRICAL_SURFACE ( 'NONE', #132897, 0.1000000000000013933 ) ;
#4501=AXIS2_PLACEMENT_3D ( 'NONE', #40352, #119871, #22044 ) ;
#4505=ORIENTED_EDGE ( 'NONE', *, *, #81415, .F. ) ;
#4514=CARTESIAN_POINT ( 'NONE',  ( 21.05000000000000071, 30.48727911274996671, -240.1192265702093209 ) ) ;
#4537=CARTESIAN_POINT ( 'NONE',  ( -23.25000000000000000, 12.62988036037870643, -223.4632815780722410 ) ) ;
#4557=CARTESIAN_POINT ( 'NONE',  ( -23.25000000000000000, 40.09675592080785123, -251.3927149226265385 ) ) ;
#4561=VERTEX_POINT ( 'NONE', #129496 ) ;
#4607=TOROIDAL_SURFACE ( 'NONE', #125448, 0.2000000000000000111, 0.1000000000000000056 ) ;
#4615=CARTESIAN_POINT ( 'NONE',  ( -18.59999999999999787, 22.25400410509136151, -231.2278641261850680 ) ) ;
#4619=CARTESIAN_POINT ( 'NONE',  ( -23.25000000000000000, 1.580567032079710055, -244.0902705724231794 ) ) ;
#4633=VERTEX_POINT ( 'NONE', #133350 ) ;
#4664=EDGE_CURVE ( 'NONE', #195479, #141753, #238865, .T. ) ;
#4667=EDGE_CURVE ( 'NONE', #230514, #46846, #113497, .T. ) ;
#4674=CARTESIAN_POINT ( 'NONE',  ( 23.24999999999999645, -0.5844558071354983841, -223.2480615698803490 ) ) ;
#4680=ADVANCED_FACE ( 'NONE', ( #61515 ), #67520, .T. ) ;
#4696=CARTESIAN_POINT ( 'NONE',  ( 23.24999999999999645, 36.65892442174935439, -249.5511627012433848 ) ) ;
#4708=ORIENTED_EDGE ( 'NONE', *, *, #21185, .T. ) ;
#4714=CARTESIAN_POINT ( 'NONE',  ( -21.45000000000000284, 21.65523568329831505, -232.7692078405380300 ) ) ;
#4750=AXIS2_PLACEMENT_3D ( 'NONE', #53847, #112544, #250751 ) ;
#4755=ORIENTED_EDGE ( 'NONE', *, *, #229318, .F. ) ;
#4773=AXIS2_PLACEMENT_3D ( 'NONE', #245058, #126391, #243776 ) ;
#4775=CARTESIAN_POINT ( 'NONE',  ( -23.15000000000000213, 28.62564411244411744, -258.1944495455016977 ) ) ;
#4781=ADVANCED_FACE ( 'NONE', ( #187891 ), #28855, .F. ) ;
#4783=ORIENTED_EDGE ( 'NONE', *, *, #77886, .F. ) ;
#4798=ADVANCED_FACE ( 'NONE', ( #143609 ), #159316, .T. ) ;
#4834=FACE_OUTER_BOUND ( 'NONE', #224629, .T. ) ;
#4845=CARTESIAN_POINT ( 'NONE',  ( -21.05000000000000071, 18.18127959618848166, -237.5711165786817389 ) ) ;
#4862=ADVANCED_FACE ( 'NONE', ( #65354 ), #247849, .T. ) ;
#4903=AXIS2_PLACEMENT_3D ( 'NONE', #58003, #77562, #160992 ) ;
#4928=TOROIDAL_SURFACE ( 'NONE', #146407, 12.77500000000000036, 0.1000000000000000056 ) ;
#4934=CYLINDRICAL_SURFACE ( 'NONE', #161394, 3.999999999999994671 ) ;
#4960=CARTESIAN_POINT ( 'NONE',  ( 21.05000000000000426, 18.68963942977167747, -227.9427330617897951 ) ) ;
#5002=VERTEX_POINT ( 'NONE', #74388 ) ;
#5004=DIRECTION ( 'NONE',  ( 0.000000000000000000, 0.3488585713686311318, 0.9371753822965249725 ) ) ;
#5016=CARTESIAN_POINT ( 'NONE',  ( -21.55000000000000426, 21.67479455268075128, -232.7326951115107647 ) ) ;
#5023=LINE ( 'NONE', #84540, #16809 ) ;
#5037=ORIENTED_EDGE ( 'NONE', *, *, #400, .F. ) ;
#5041=DIRECTION ( 'NONE',  ( -1.000000000000000000, -1.394253735153569469E-16, -2.602809386958778209E-16 ) ) ;
#5090=DIRECTION ( 'NONE',  ( 1.000000000000000000, 0.000000000000000000, 0.000000000000000000 ) ) ;
#5091=CIRCLE ( 'NONE', #150860, 7.900000000000000355 ) ;
#5100=ORIENTED_EDGE ( 'NONE', *, *, #205800, .F. ) ;
#5127=VERTEX_POINT ( 'NONE', #40399 ) ;
#5151=DIRECTION ( 'NONE',  ( 0.000000000000000000, -0.8814952561688476074, 0.4721928772777262417 ) ) ;
#5160=ORIENTED_EDGE ( 'NONE', *, *, #161803, .T. ) ;
#5161=DIRECTION ( 'NONE',  ( -1.000000000000000000, -8.674042436075348305E-17, -1.619280515896124405E-16 ) ) ;
#5167=AXIS2_PLACEMENT_3D ( 'NONE', #198540, #19927, #99422 ) ;
#5175=DIRECTION ( 'NONE',  ( 1.000000000000000000, 0.000000000000000000, 0.000000000000000000 ) ) ;
#5193=ORIENTED_EDGE ( 'NONE', *, *, #215598, .T. ) ;
#5194=CARTESIAN_POINT ( 'NONE',  ( 21.04999999999999716, 18.86217927868475641, -229.9540340038553552 ) ) ;
#5201=EDGE_CURVE ( 'NONE', #121060, #158295, #151109, .T. ) ;
#5202=DIRECTION ( 'NONE',  ( 1.000000000000000000, 0.000000000000000000, 0.000000000000000000 ) ) ;
#5211=VERTEX_POINT ( 'NONE', #203281 ) ;
#5250=VECTOR ( 'NONE', #75745, 1000.000000000000000 ) ;
#5255=SPHERICAL_SURFACE ( 'NONE', #48957, 0.1000000000000000056 ) ;
#5258=AXIS2_PLACEMENT_3D ( 'NONE', #114103, #256122, #115391 ) ;
#5279=CARTESIAN_POINT ( 'NONE',  ( 18.59999999999999076, 36.65892442174935439, -249.5511627012433848 ) ) ;
#5283=CARTESIAN_POINT ( 'NONE',  ( -20.64999999999999858, 11.60058429089262333, -246.3380203656811887 ) ) ;
#5293=AXIS2_PLACEMENT_3D ( 'NONE', #33222, #153170, #96961 ) ;
#5302=TOROIDAL_SURFACE ( 'NONE', #96876, 0.2000000000000000111, 0.1000000000000000056 ) ;
#5305=CIRCLE ( 'NONE', #151089, 0.1000000000000013933 ) ;
#5322=ADVANCED_FACE ( 'NONE', ( #208442 ), #252479, .F. ) ;
#5324=AXIS2_PLACEMENT_3D ( 'NONE', #23396, #102872, #182453 ) ;
#5351=DIRECTION ( 'NONE',  ( -2.812466655313718795E-14, -0.8096735173027139743, 0.5868805631290339164 ) ) ;
#5357=CARTESIAN_POINT ( 'NONE',  ( 23.14999999999999503, 28.91254064196106910, -237.8576372133405528 ) ) ;
#5366=FACE_OUTER_BOUND ( 'NONE', #139534, .T. ) ;
#5378=CARTESIAN_POINT ( 'NONE',  ( -18.59999999999999787, 7.128833340093095217, -233.7327013124392749 ) ) ;
#5405=EDGE_CURVE ( 'NONE', #89629, #9372, #194275, .T. ) ;
#5415=AXIS2_PLACEMENT_3D ( 'NONE', #88065, #107656, #232452 ) ;
#5460=ORIENTED_EDGE ( 'NONE', *, *, #190126, .F. ) ;
#5479=CIRCLE ( 'NONE', #38834, 0.09999999999999939493 ) ;
#5504=CARTESIAN_POINT ( 'NONE',  ( 19.97071067695909363, 34.41526977942278620, -235.0529015606424537 ) ) ;
#5509=DIRECTION ( 'NONE',  ( -3.265361837132812600E-16, 0.4721928772777346239, 0.8814952561688430555 ) ) ;
#5520=ORIENTED_EDGE ( 'NONE', *, *, #136132, .T. ) ;
#5555=ORIENTED_EDGE ( 'NONE', *, *, #109757, .F. ) ;
#5560=AXIS2_PLACEMENT_3D ( 'NONE', #50988, #227078, #210112 ) ;
#5577=DIRECTION ( 'NONE',  ( 1.000000000000000000, -0.000000000000000000, -0.000000000000000000 ) ) ;
#5581=DIRECTION ( 'NONE',  ( 0.000000000000000000, 0.8814952561688425003, -0.4721928772777359007 ) ) ;
#5584=DIRECTION ( 'NONE',  ( 1.000000000000000000, 0.000000000000000000, 0.000000000000000000 ) ) ;
#5586=CARTESIAN_POINT ( 'NONE',  ( 20.94999999999999574, 4.313202326203132486, -245.5540684919841681 ) ) ;
#5613=LINE ( 'NONE', #43495, #1943 ) ;
#5621=CIRCLE ( 'NONE', #205546, 11.79999999999999005 ) ;
#5640=DIRECTION ( 'NONE',  ( 0.000000000000000000, -0.8814952561688430555, 0.4721928772777345684 ) ) ;
#5649=ORIENTED_EDGE ( 'NONE', *, *, #5201, .T. ) ;
#5659=EDGE_LOOP ( 'NONE', ( #189875, #147682, #217332, #52542 ) ) ;
#5693=ORIENTED_EDGE ( 'NONE', *, *, #151891, .T. ) ;
#5707=DIRECTION ( 'NONE',  ( 1.000000000000000000, 0.000000000000000000, 0.000000000000000000 ) ) ;
#5725=DIRECTION ( 'NONE',  ( 0.000000000000000000, -0.8814952561688430555, 0.4721928772777346239 ) ) ;
#5730=EDGE_CURVE ( 'NONE', #252297, #221637, #31944, .T. ) ;
#5737=CARTESIAN_POINT ( 'NONE',  ( 21.05000000000000071, 24.07562609839690992, -252.7152152143214892 ) ) ;
#5742=CARTESIAN_POINT ( 'NONE',  ( 21.05000000000000071, 14.88773611405353314, -236.3451124650200370 ) ) ;
#5801=EDGE_CURVE ( 'NONE', #109224, #231948, #229923, .T. ) ;
#5811=AXIS2_PLACEMENT_3D ( 'NONE', #13241, #193159, #54900 ) ;
#5842=CIRCLE ( 'NONE', #135014, 0.3999999999999994671 ) ;
#5866=AXIS2_PLACEMENT_3D ( 'NONE', #24498, #103982, #227801 ) ;
#5898=LINE ( 'NONE', #224948, #78373 ) ;
#5949=EDGE_LOOP ( 'NONE', ( #245874, #16097, #62746, #24845 ) ) ;
#5966=CIRCLE ( 'NONE', #126795, 0.09999999999999939493 ) ;
#6032=VECTOR ( 'NONE', #33427, 1000.000000000000000 ) ;
#6074=LINE ( 'NONE', #4775, #45466 ) ;
#6093=AXIS2_PLACEMENT_3D ( 'NONE', #129224, #146201, #70562 ) ;
#6097=DIRECTION ( 'NONE',  ( 1.000000000000000000, 0.000000000000000000, 0.000000000000000000 ) ) ;
#6132=AXIS2_PLACEMENT_3D ( 'NONE', #186248, #205796, #5004 ) ;
#6155=CARTESIAN_POINT ( 'NONE',  ( 21.05000000000000071, 18.71171618620643429, -229.8673829423568691 ) ) ;
#6182=AXIS2_PLACEMENT_3D ( 'NONE', #146848, #47751, #107741 ) ;
#6204=LINE ( 'NONE', #81867, #134721 ) ;
#6220=ORIENTED_EDGE ( 'NONE', *, *, #75887, .F. ) ;
#6236=CYLINDRICAL_SURFACE ( 'NONE', #240486, 0.09999999999998304689 ) ;
#6310=ADVANCED_FACE ( 'NONE', ( #249073 ), #138074, .T. ) ;
#6324=EDGE_CURVE ( 'NONE', #218161, #132362, #252898, .T. ) ;
#6331=AXIS2_PLACEMENT_3D ( 'NONE', #97898, #139602, #174963 ) ;
#6334=ORIENTED_EDGE ( 'NONE', *, *, #161570, .F. ) ;
#6336=CARTESIAN_POINT ( 'NONE',  ( 20.94999999999999929, 7.128833340093095217, -233.7327013124392749 ) ) ;
#6374=CIRCLE ( 'NONE', #152154, 2.000000000000003553 ) ;
#6378=DIRECTION ( 'NONE',  ( -1.000000000000000000, -1.394253735153569469E-16, -2.602809386958778209E-16 ) ) ;
#6383=DIRECTION ( 'NONE',  ( 0.000000000000000000, -0.8814952561688476074, 0.4721928772777262417 ) ) ;
#6392=DIRECTION ( 'NONE',  ( -1.000000000000000000, 0.000000000000000000, 0.000000000000000000 ) ) ;
#6413=AXIS2_PLACEMENT_3D ( 'NONE', #131595, #92464, #211138 ) ;
#6460=LINE ( 'NONE', #199564, #197511 ) ;
#6477=EDGE_CURVE ( 'NONE', #178909, #150487, #106720, .T. ) ;
#6549=ORIENTED_EDGE ( 'NONE', *, *, #88998, .F. ) ;
#6560=ORIENTED_EDGE ( 'NONE', *, *, #203534, .F. ) ;
#6637=CARTESIAN_POINT ( 'NONE',  ( -23.15000000000000213, -7.761787541757065867, -236.6467894636467975 ) ) ;
#6644=AXIS2_PLACEMENT_3D ( 'NONE', #237677, #232569, #16091 ) ;
#6648=CARTESIAN_POINT ( 'NONE',  ( -21.64999999999999858, 21.35054858842499925, -233.1262234518674177 ) ) ;
#6657=ADVANCED_FACE ( 'NONE', ( #49255 ), #105340, .F. ) ;
#6668=LINE ( 'NONE', #107048, #26196 ) ;
#6674=ORIENTED_EDGE ( 'NONE', *, *, #249816, .F. ) ;
#6683=VERTEX_POINT ( 'NONE', #170550 ) ;
#6687=LINE ( 'NONE', #139761, #77800 ) ;
#6703=CARTESIAN_POINT ( 'NONE',  ( -23.15000000000000213, 23.34004772283015328, -229.2004250369967338 ) ) ;
#6715=CARTESIAN_POINT ( 'NONE',  ( 22.49999999999999645, 12.55707850971095141, -223.4244300710886364 ) ) ;
#6737=DIRECTION ( 'NONE',  ( 1.000000000000000000, 0.000000000000000000, 0.000000000000000000 ) ) ;
#6759=AXIS2_PLACEMENT_3D ( 'NONE', #55558, #214663, #192549 ) ;
#6774=EDGE_CURVE ( 'NONE', #114431, #207366, #164992, .T. ) ;
#6782=CARTESIAN_POINT ( 'NONE',  ( -23.25000000000000000, 43.00579525902548994, -254.2551217332645876 ) ) ;
#6786=CARTESIAN_POINT ( 'NONE',  ( 23.25000000000000000, 11.39998237908105594, -245.7725481090871540 ) ) ;
#6798=CARTESIAN_POINT ( 'NONE',  ( -18.59999999999999787, 14.77103648604101060, -236.4083752604501001 ) ) ;
#6821=CARTESIAN_POINT ( 'NONE',  ( -18.50000000000000000, 36.65892442174935439, -249.5511627012433848 ) ) ;
#6833=EDGE_CURVE ( 'NONE', #2694, #179081, #153548, .T. ) ;
#6837=ORIENTED_EDGE ( 'NONE', *, *, #121046, .T. ) ;
#6850=EDGE_CURVE ( 'NONE', #161618, #138960, #73630, .T. ) ;
#6899=LINE ( 'NONE', #250328, #63716 ) ;
#6915=DIRECTION ( 'NONE',  ( 0.000000000000000000, 0.4721928772777512218, 0.8814952561688340626 ) ) ;
#6949=FACE_OUTER_BOUND ( 'NONE', #146185, .T. ) ;
#6952=TOROIDAL_SURFACE ( 'NONE', #186021, 0.2000000000000000111, 0.1000000000000000056 ) ;
#6955=( LENGTH_UNIT ( ) NAMED_UNIT ( * ) SI_UNIT ( .MILLI., .METRE. ) );
#7036=EDGE_CURVE ( 'NONE', #136922, #116426, #111177, .T. ) ;
#7047=CARTESIAN_POINT ( 'NONE',  ( -23.25000000000000000, 20.01397631055648674, -237.6853859230195098 ) ) ;
#7068=DIRECTION ( 'NONE',  ( 0.000000000000000000, 0.8814952561688444987, -0.4721928772777320149 ) ) ;
#7086=ORIENTED_EDGE ( 'NONE', *, *, #216150, .F. ) ;
#7092=VECTOR ( 'NONE', #95438, 1000.000000000000000 ) ;
#7144=AXIS2_PLACEMENT_3D ( 'NONE', #54493, #111927, #31130 ) ;
#7150=VERTEX_POINT ( 'NONE', #112470 ) ;
#7151=CARTESIAN_POINT ( 'NONE',  ( -20.54999999999999716, 21.35054858842500281, -233.1262234518673893 ) ) ;
#7169=VECTOR ( 'NONE', #250079, 1000.000000000000000 ) ;
#7184=DIRECTION ( 'NONE',  ( 2.715809747126116508E-16, -0.4721928772777347905, -0.8814952561688429444 ) ) ;
#7199=EDGE_CURVE ( 'NONE', #94319, #137100, #158053, .T. ) ;
#7203=DIRECTION ( 'NONE',  ( 1.000000000000000000, 8.674042436075353235E-17, 1.619280515896125144E-16 ) ) ;
#7268=CARTESIAN_POINT ( 'NONE',  ( 21.05000000000000071, 23.68770167995059239, -252.8127582590406348 ) ) ;
#7289=VERTEX_POINT ( 'NONE', #79722 ) ;
#7292=CARTESIAN_POINT ( 'NONE',  ( 21.05000000000000071, 36.65892442174935439, -249.5511627012433848 ) ) ;
#7294=ORIENTED_EDGE ( 'NONE', *, *, #240733, .T. ) ;
#7309=ORIENTED_EDGE ( 'NONE', *, *, #165586, .F. ) ;
#7320=DIRECTION ( 'NONE',  ( 0.000000000000000000, 0.8814952561688437216, -0.4721928772777334582 ) ) ;
#7329=CIRCLE ( 'NONE', #61503, 0.09999999999999638345 ) ;
#7420=PLANE ( 'NONE',  #84336 ) ;
#7422=VECTOR ( 'NONE', #116765, 1000.000000000000000 ) ;
#7424=AXIS2_PLACEMENT_3D ( 'NONE', #22645, #23933, #160865 ) ;
#7446=ORIENTED_EDGE ( 'NONE', *, *, #221006, .T. ) ;
#7455=( BOUNDED_CURVE ( )  B_SPLINE_CURVE ( 3, ( #37478, #119587, #118292, #40065 ),
 .UNSPECIFIED., .F., .F. ) 
 B_SPLINE_CURVE_WITH_KNOTS ( ( 4, 4 ),
 ( 3.192897208853993085, 4.712388980384689674 ),
 .UNSPECIFIED. ) 
 CURVE ( )  GEOMETRIC_REPRESENTATION_ITEM ( )  RATIONAL_B_SPLINE_CURVE ( ( 1.000000000000000000, 0.8166740347213228279, 0.8166740347213228279, 1.000000000000000000 ) ) 
 REPRESENTATION_ITEM ( '' )  );
#7464=CARTESIAN_POINT ( 'NONE',  ( 22.59999999999999787, 12.54152817314149715, -223.4164406214577241 ) ) ;
#7528=EDGE_CURVE ( 'NONE', #157387, #18238, #244458, .T. ) ;
#7549=EDGE_LOOP ( 'NONE', ( #65986, #141549, #225808, #15787, #230435, #122686, #63645, #8949, #113853, #7446, #242313, #9996 ) ) ;
#7593=CARTESIAN_POINT ( 'NONE',  ( -20.94999999999999929, 4.436385504674529301, -245.3241086753762659 ) ) ;
#7611=EDGE_CURVE ( 'NONE', #59542, #39875, #182309, .T. ) ;
#7618=CARTESIAN_POINT ( 'NONE',  ( 20.94999999999999929, 28.52545328903799415, -239.5221046041717443 ) ) ;
#7631=VECTOR ( 'NONE', #126894, 1000.000000000000000 ) ;
#7641=DIRECTION ( 'NONE',  ( -1.000000000000000000, -0.000000000000000000, -0.000000000000000000 ) ) ;
#7677=AXIS2_PLACEMENT_3D ( 'NONE', #245443, #5509, #66795 ) ;
#7696=DIRECTION ( 'NONE',  ( -1.000000000000000000, -0.000000000000000000, -0.000000000000000000 ) ) ;
#7710=VECTOR ( 'NONE', #65599, 1000.000000000000000 ) ;
#7737=LINE ( 'NONE', #225465, #19392 ) ;
#7768=AXIS2_PLACEMENT_3D ( 'NONE', #104633, #126804, #26435 ) ;
#7797=TOROIDAL_SURFACE ( 'NONE', #228368, 0.6000000000000013101, 0.1000000000000000056 ) ;
#7803=ORIENTED_EDGE ( 'NONE', *, *, #230075, .T. ) ;
#7833=CARTESIAN_POINT ( 'NONE',  ( -20.54999999999999716, 38.33376540847015690, -250.4483291680710693 ) ) ;
#7924=CARTESIAN_POINT ( 'NONE',  ( -21.05000000000000071, 1.316055977212907457, -230.7323992127457473 ) ) ;
#7998=ADVANCED_FACE ( 'NONE', ( #175689 ), #78237, .T. ) ;
#8015=EDGE_CURVE ( 'NONE', #54485, #165408, #55677, .T. ) ;
#8061=EDGE_CURVE ( 'NONE', #7150, #234336, #244819, .T. ) ;
#8072=EDGE_CURVE ( 'NONE', #153027, #239741, #199052, .T. ) ;
#8096=EDGE_CURVE ( 'NONE', #226091, #226316, #240751, .T. ) ;
#8116=AXIS2_PLACEMENT_3D ( 'NONE', #30061, #151280, #109551 ) ;
#8174=DIRECTION ( 'NONE',  ( 1.000000000000000000, 0.000000000000000000, 0.000000000000000000 ) ) ;
#8180=AXIS2_PLACEMENT_3D ( 'NONE', #169793, #217734, #76950 ) ;
#8182=CIRCLE ( 'NONE', #153975, 0.09999999999999986677 ) ;
#8220=FACE_OUTER_BOUND ( 'NONE', #58531, .T. ) ;
#8237=EDGE_CURVE ( 'NONE', #35657, #237528, #115845, .T. ) ;
#8260=EDGE_LOOP ( 'NONE', ( #68690, #62572, #195289 ) ) ;
#8274=DIRECTION ( 'NONE',  ( 0.000000000000000000, 0.9994937237965558774, 0.03181660087586650476 ) ) ;
#8298=EDGE_CURVE ( 'NONE', #105344, #76904, #51524, .T. ) ;
#8328=ORIENTED_EDGE ( 'NONE', *, *, #146178, .T. ) ;
#8335=CARTESIAN_POINT ( 'NONE',  ( -23.15000000000000213, 31.44980407958351165, -233.5445995079518866 ) ) ;
#8401=CARTESIAN_POINT ( 'NONE',  ( -2.995603634470829482E-16, 29.00069016757795026, -237.9048565010683376 ) ) ;
#8415=CARTESIAN_POINT ( 'NONE',  ( 21.04999999999999716, 10.12429514711028666, -228.1852862148587064 ) ) ;
#8443=ADVANCED_FACE ( 'NONE', ( #13716 ), #55370, .T. ) ;
#8447=DIRECTION ( 'NONE',  ( 1.000000000000000000, 0.000000000000000000, 0.000000000000000000 ) ) ;
#8465=ADVANCED_FACE ( 'NONE', ( #194943 ), #116665, .F. ) ;
#8526=DIRECTION ( 'NONE',  ( -1.000000000000000000, 0.000000000000000000, 0.000000000000000000 ) ) ;
#8530=CARTESIAN_POINT ( 'NONE',  ( -18.59999999999999787, 31.40887384169439756, -233.4092306946072313 ) ) ;
#8551=TOROIDAL_SURFACE ( 'NONE', #158425, 4.099999999999999645, 0.1000000000000000056 ) ;
#8562=EDGE_LOOP ( 'NONE', ( #255701, #145115, #165249, #119098 ) ) ;
#8570=DIRECTION ( 'NONE',  ( 0.000000000000000000, -0.8814952561688429444, 0.4721928772777348460 ) ) ;
#8623=CARTESIAN_POINT ( 'NONE',  ( 20.94999999999999574, 18.81166555858608902, -229.8642012822692777 ) ) ;
#8731=CIRCLE ( 'NONE', #83529, 0.09999999999999939493 ) ;
#8736=CARTESIAN_POINT ( 'NONE',  ( 18.48536876927990846, 8.873546741997410336, -245.4030630292437820 ) ) ;
#8747=VECTOR ( 'NONE', #120856, 1000.000000000000114 ) ;
#8748=AXIS2_PLACEMENT_3D ( 'NONE', #226713, #131477, #71530 ) ;
#8760=CARTESIAN_POINT ( 'NONE',  ( -21.05000000000000071, 1.658775325997247752, -230.6916041481598540 ) ) ;
#8768=DIRECTION ( 'NONE',  ( 1.000000000000000000, 0.000000000000000000, 0.000000000000000000 ) ) ;
#8780=CARTESIAN_POINT ( 'NONE',  ( 21.04999999999999716, 1.529241108124774984, -230.7757353094251584 ) ) ;
#8782=EDGE_CURVE ( 'NONE', #123203, #203424, #114032, .T. ) ;
#8798=CARTESIAN_POINT ( 'NONE',  ( -18.50000000000000000, 22.38308386859736032, -231.4104522272575082 ) ) ;
#8840=CARTESIAN_POINT ( 'NONE',  ( -21.00219873199062093, 18.70228113215760501, -226.7667091168536047 ) ) ;
#8842=DIRECTION ( 'NONE',  ( 0.000000000000000000, 0.8814952561688444987, -0.4721928772777320149 ) ) ;
#8843=AXIS2_PLACEMENT_3D ( 'NONE', #51309, #168777, #73507 ) ;
#8852=ORIENTED_EDGE ( 'NONE', *, *, #142713, .F. ) ;
#8885=ORIENTED_EDGE ( 'NONE', *, *, #197393, .T. ) ;
#8887=AXIS2_PLACEMENT_3D ( 'NONE', #189514, #173846, #74735 ) ;
#8911=DIRECTION ( 'NONE',  ( 1.000000000000000000, 0.000000000000000000, 0.000000000000000000 ) ) ;
#8934=DIRECTION ( 'NONE',  ( -1.000000000000000000, -0.000000000000000000, -0.000000000000000000 ) ) ;
#8949=ORIENTED_EDGE ( 'NONE', *, *, #84400, .T. ) ;
#8951=ORIENTED_EDGE ( 'NONE', *, *, #106969, .T. ) ;
#8952=DIRECTION ( 'NONE',  ( 0.000000000000000000, 0.8814952561688476074, -0.4721928772777262417 ) ) ;
#8962=LINE ( 'NONE', #152356, #78719 ) ;
#8966=CARTESIAN_POINT ( 'NONE',  ( 20.95017935633852346, 18.75476199923615894, -228.0766203067306321 ) ) ;
#8990=( BOUNDED_SURFACE ( )  B_SPLINE_SURFACE ( 3, 2, ( 
 ( #51878, #11510, #153624 ),
 ( #252654, #36213, #171889 ),
 ( #133999, #213530, #71492 ),
 ( #114445, #253937, #234378 ) ),
 .UNSPECIFIED., .F., .F., .F. ) 
 B_SPLINE_SURFACE_WITH_KNOTS ( ( 4, 4 ),
 ( 3, 3 ),
 ( 0.04058434257139476725, 0.04256401539001602313 ),
 ( 0.000000000000000000, 1.000000000000000000 ),
 .UNSPECIFIED. ) 
 GEOMETRIC_REPRESENTATION_ITEM ( )  RATIONAL_B_SPLINE_SURFACE ( (
 ( 1.000000000000000000, 0.7103081912008347709, 1.000000000000000000),
 ( 1.000000000000000000, 0.7104998333557990264, 1.000000000000000000),
 ( 1.000000000000000000, 0.7107238315752896218, 1.000000000000000000),
 ( 1.000000000000000000, 0.7110073749539418397, 1.000000000000000000) ) ) 
 REPRESENTATION_ITEM ( '' )  SURFACE ( )  );
#9003=DIRECTION ( 'NONE',  ( -1.000000000000000000, -0.000000000000000000, -0.000000000000000000 ) ) ;
#9019=EDGE_CURVE ( 'NONE', #138276, #142373, #199441, .T. ) ;
#9036=ADVANCED_FACE ( 'NONE', ( #65056 ), #228665, .F. ) ;
#9046=DIRECTION ( 'NONE',  ( -1.836970198721029441E-16, 0.4721928772777346239, 0.8814952561688430555 ) ) ;
#9050=DIRECTION ( 'NONE',  ( -0.7071067811865388020, -0.6233112732207694018, 0.3338907855510774847 ) ) ;
#9054=DIRECTION ( 'NONE',  ( 1.000000000000000000, -0.000000000000000000, 0.000000000000000000 ) ) ;
#9093=EDGE_CURVE ( 'NONE', #215045, #71039, #91458, .T. ) ;
#9094=EDGE_CURVE ( 'NONE', #71933, #19158, #178793, .T. ) ;
#9113=LINE ( 'NONE', #112073, #255473 ) ;
#9120=DIRECTION ( 'NONE',  ( -1.000000000000000000, 0.000000000000000000, 0.000000000000000000 ) ) ;
#9121=DIRECTION ( 'NONE',  ( -1.000000000000000000, -1.394253735153569469E-16, -2.602809386958778209E-16 ) ) ;
#9135=EDGE_LOOP ( 'NONE', ( #193769, #94768, #110377, #143501 ) ) ;
#9141=CARTESIAN_POINT ( 'NONE',  ( -18.50000000000000000, 14.81796439977981272, -236.5325475414793743 ) ) ;
#9156=ORIENTED_EDGE ( 'NONE', *, *, #78223, .F. ) ;
#9163=FACE_OUTER_BOUND ( 'NONE', #97026, .T. ) ;
#9179=DIRECTION ( 'NONE',  ( 0.000000000000000000, 0.8814952561688476074, -0.4721928772777262417 ) ) ;
#9190=CARTESIAN_POINT ( 'NONE',  ( -21.05000000000000071, 1.658775325997240868, -230.6916041481598540 ) ) ;
#9198=CARTESIAN_POINT ( 'NONE',  ( -20.64999999999999858, 29.14863708059993286, -237.4168895852561434 ) ) ;
#9258=EDGE_CURVE ( 'NONE', #76756, #159519, #16455, .T. ) ;
#9286=CARTESIAN_POINT ( 'NONE',  ( 22.48660254037844908, 12.63302488529802936, -223.3515224085915065 ) ) ;
#9296=AXIS2_PLACEMENT_3D ( 'NONE', #147100, #105382, #226639 ) ;
#9300=DIRECTION ( 'NONE',  ( 0.000000000000000000, -0.8454177738465993297, -0.5341055959866553016 ) ) ;
#9313=VERTEX_POINT ( 'NONE', #45181 ) ;
#9360=CIRCLE ( 'NONE', #217634, 0.09999999999999939493 ) ;
#9361=EDGE_LOOP ( 'NONE', ( #239588, #228154, #121598, #131714 ) ) ;
#9372=VERTEX_POINT ( 'NONE', #170318 ) ;
#9377=VECTOR ( 'NONE', #120298, 1000.000000000000000 ) ;
#9386=EDGE_CURVE ( 'NONE', #17591, #108265, #37297, .T. ) ;
#9404=VECTOR ( 'NONE', #164383, 1000.000000000000000 ) ;
#9406=ADVANCED_FACE ( 'NONE', ( #248518 ), #41594, .T. ) ;
#9422=AXIS2_PLACEMENT_3D ( 'NONE', #67820, #226894, #127809 ) ;
#9425=LINE ( 'NONE', #88950, #126444 ) ;
#9429=AXIS2_PLACEMENT_3D ( 'NONE', #214931, #132847, #251485 ) ;
#9433=DIRECTION ( 'NONE',  ( 0.000000000000000000, 0.4721928772778128947, 0.8814952561688012000 ) ) ;
#9457=ORIENTED_EDGE ( 'NONE', *, *, #147447, .F. ) ;
#9489=VECTOR ( 'NONE', #16033, 1000.000000000000000 ) ;
#9498=DIRECTION ( 'NONE',  ( -0.000000000000000000, 0.9371753822965315228, -0.3488585713686134238 ) ) ;
#9512=ORIENTED_EDGE ( 'NONE', *, *, #170955, .F. ) ;
#9520=ORIENTED_EDGE ( 'NONE', *, *, #243357, .F. ) ;
#9547=FACE_OUTER_BOUND ( 'NONE', #246459, .T. ) ;
#9593=CARTESIAN_POINT ( 'NONE',  ( -23.15000000000000213, 11.31726856452598184, -246.8669175193824969 ) ) ;
#9595=VECTOR ( 'NONE', #206965, 1000.000000000000000 ) ;
#9609=DIRECTION ( 'NONE',  ( -0.000000000000000000, 0.4721928772777345684, 0.8814952561688429444 ) ) ;
#9666=DIRECTION ( 'NONE',  ( -3.265361837132813586E-16, 0.4721928772777345129, 0.8814952561688430555 ) ) ;
#9673=ORIENTED_EDGE ( 'NONE', *, *, #129870, .T. ) ;
#9674=CARTESIAN_POINT ( 'NONE',  ( 21.05000000000000071, 22.90266353732884852, -230.0169390150674076 ) ) ;
#9681=CARTESIAN_POINT ( 'NONE',  ( 21.05000000000000426, 10.05455514295651653, -228.1997025080316348 ) ) ;
#9688=CIRCLE ( 'NONE', #63869, 0.1000000000000013933 ) ;
#9702=DIRECTION ( 'NONE',  ( -1.000000000000000000, -0.000000000000000000, -0.000000000000000000 ) ) ;
#9725=ORIENTED_EDGE ( 'NONE', *, *, #89843, .F. ) ;
#9735=VERTEX_POINT ( 'NONE', #29219 ) ;
#9740=EDGE_CURVE ( 'NONE', #132362, #141820, #70817, .T. ) ;
#9755=EDGE_CURVE ( 'NONE', #128122, #12130, #141691, .T. ) ;
#9762=ADVANCED_FACE ( 'NONE', ( #89139 ), #184378, .T. ) ;
#9807=CARTESIAN_POINT ( 'NONE',  ( 21.05000000000000071, 14.80592234317787081, -236.3146577222204314 ) ) ;
#9821=AXIS2_PLACEMENT_3D ( 'NONE', #53195, #14088, #74079 ) ;
#9826=ADVANCED_FACE ( 'NONE', ( #150425 ), #229939, .T. ) ;
#9827=DIRECTION ( 'NONE',  ( 0.000000000000000000, 0.8814952561688437216, -0.4721928772777334582 ) ) ;
#9846=CARTESIAN_POINT ( 'NONE',  ( 18.59999999999997655, 43.62273694548321856, -253.2814864317374770 ) ) ;
#9851=DIRECTION ( 'NONE',  ( 0.000000000000000000, 0.8814952561688429444, -0.4721928772777347350 ) ) ;
#9882=CARTESIAN_POINT ( 'NONE',  ( 18.49999999999999289, 43.35377423437995503, -245.1717807829448930 ) ) ;
#9886=ORIENTED_EDGE ( 'NONE', *, *, #46404, .F. ) ;
#9895=DIRECTION ( 'NONE',  ( 1.000000000000000000, 0.000000000000000000, 0.000000000000000000 ) ) ;
#9928=CARTESIAN_POINT ( 'NONE',  ( 21.07199075132371746, 22.03847052870693091, -231.7647718156920575 ) ) ;
#9984=ORIENTED_EDGE ( 'NONE', *, *, #67063, .F. ) ;
#9985=CARTESIAN_POINT ( 'NONE',  ( -21.93340585899525763, 0.6726324846117338607, -230.2742912564596054 ) ) ;
#9996=ORIENTED_EDGE ( 'NONE', *, *, #109292, .T. ) ;
#10012=EDGE_LOOP ( 'NONE', ( #172084, #112810, #153334 ) ) ;
#10021=CARTESIAN_POINT ( 'NONE',  ( 18.49999999999999289, 46.32970330538243786, -243.0551226933711746 ) ) ;
#10025=AXIS2_PLACEMENT_3D ( 'NONE', #22935, #243226, #123297 ) ;
#10039=DIRECTION ( 'NONE',  ( 0.000000000000000000, 0.5273008465188219196, -0.8496786552930077896 ) ) ;
#10050=CARTESIAN_POINT ( 'NONE',  ( -21.05000000000000071, 28.55432187084631224, -258.5393726171218418 ) ) ;
#10058=CARTESIAN_POINT ( 'NONE',  ( 21.05000000000000071, 1.618246818147480726, -230.7412754484373352 ) ) ;
#10060=ORIENTED_EDGE ( 'NONE', *, *, #154410, .F. ) ;
#10079=DIRECTION ( 'NONE',  ( 0.000000000000000000, 0.8814952561688438326, -0.4721928772777331806 ) ) ;
#10091=EDGE_LOOP ( 'NONE', ( #211173, #172407, #208181, #213723, #53390 ) ) ;
#10092=EDGE_CURVE ( 'NONE', #67400, #2075, #647, .T. ) ;
#10097=CIRCLE ( 'NONE', #172656, 0.09999999999999986677 ) ;
#10140=CARTESIAN_POINT ( 'NONE',  ( -18.50000000000000000, 16.50669723772569952, -240.7258389668962479 ) ) ;
#10163=CYLINDRICAL_SURFACE ( 'NONE', #138508, 0.1000000000000013933 ) ;
#10169=CARTESIAN_POINT ( 'NONE',  ( -22.47071067811865319, 10.68684811775433374, -226.8807012965928038 ) ) ;
#10200=CARTESIAN_POINT ( 'NONE',  ( 20.94999999999999574, 14.77103648604101060, -236.4083752604501001 ) ) ;
#10209=DIRECTION ( 'NONE',  ( -1.000000000000000000, 0.000000000000000000, 0.000000000000000000 ) ) ;
#10225=DIRECTION ( 'NONE',  ( 2.952720810173290591E-16, -0.4721928772777312933, -0.8814952561688448318 ) ) ;
#10236=B_SPLINE_CURVE_WITH_KNOTS ( 'NONE', 3,
 ( #68387, #168812, #86625, #8415, #9681, #247003 ),
 .UNSPECIFIED., .F., .F.,
 ( 4, 2, 4 ),
 ( 0.000000000000000000, 0.0001895189928937418447, 0.0003790379857874836894 ),
 .UNSPECIFIED. ) ;
#10256=CARTESIAN_POINT ( 'NONE',  ( 21.14999999999999503, 7.128833340093095217, -233.7327013124392749 ) ) ;
#10262=CARTESIAN_POINT ( 'NONE',  ( 20.95420533658165141, 18.77923608808111666, -228.0098942474668888 ) ) ;
#10264=AXIS2_PLACEMENT_3D ( 'NONE', #250504, #211393, #130558 ) ;
#10292=CARTESIAN_POINT ( 'NONE',  ( -2.995603634470829482E-16, 28.91254064196106910, -237.8576372133405528 ) ) ;
#10304=CIRCLE ( 'NONE', #156057, 0.1000000000000013933 ) ;
#10327=EDGE_LOOP ( 'NONE', ( #47152, #78985, #215056 ) ) ;
#10337=CARTESIAN_POINT ( 'NONE',  ( -21.05000000000000426, 1.372110199356192384, -230.7624259250305556 ) ) ;
#10344=CARTESIAN_POINT ( 'NONE',  ( 21.05000000000000071, 20.02733907826963033, -235.1395327601354666 ) ) ;
#10346=DIRECTION ( 'NONE',  ( 1.000000000000000000, -3.448943450116723568E-16, -6.438528483529607644E-16 ) ) ;
#10353=DIRECTION ( 'NONE',  ( 0.000000000000000000, -0.8814952561688439436, 0.4721928772777331806 ) ) ;
#10398=LINE ( 'NONE', #89908, #206368 ) ;
#10400=EDGE_CURVE ( 'NONE', #155399, #104681, #196494, .T. ) ;
#10410=CARTESIAN_POINT ( 'NONE',  ( 23.14999999999999858, 36.65892442174935439, -249.5511627012433848 ) ) ;
#10438=ORIENTED_EDGE ( 'NONE', *, *, #9019, .T. ) ;
#10535=ORIENTED_EDGE ( 'NONE', *, *, #241272, .T. ) ;
#10538=CARTESIAN_POINT ( 'NONE',  ( -18.59999999999999787, 43.30036367478129478, -245.0872390055602352 ) ) ;
#10541=VECTOR ( 'NONE', #246208, 1000.000000000000000 ) ;
#10607=CARTESIAN_POINT ( 'NONE',  ( -22.59999999999999787, 12.54152817314149715, -223.4164406214577241 ) ) ;
#10618=EDGE_CURVE ( 'NONE', #126382, #71039, #25909, .T. ) ;
#10634=( BOUNDED_SURFACE ( )  B_SPLINE_SURFACE ( 3, 2, ( 
 ( #77020, #156607, #9674 ),
 ( #236099, #155317, #188308 ),
 ( #56163, #74507, #136999 ),
 ( #216535, #248290, #69673 ),
 ( #213979, #129628, #212701 ),
 ( #34092, #15805, #95309 ) ),
 .UNSPECIFIED., .F., .F., .F. ) 
 B_SPLINE_SURFACE_WITH_KNOTS ( ( 4, 2, 4 ),
 ( 3, 3 ),
 ( 0.0001342700090130055928, 0.0002909192928057414561, 0.0004475685765984773194 ),
 ( 0.000000000000000000, 1.000000000000000000 ),
 .UNSPECIFIED. ) 
 GEOMETRIC_REPRESENTATION_ITEM ( )  RATIONAL_B_SPLINE_SURFACE ( (
 ( 1.000000000000000000, 0.7250110520819893489, 1.000000000000000000),
 ( 1.000000000000000000, 0.7257599279128809089, 1.000000000000000000),
 ( 1.000000000000000000, 0.7137594617291853627, 1.000000000000000000),
 ( 1.000000000000000000, 0.6959270178800760487, 1.000000000000000000),
 ( 1.000000000000000000, 0.6919879549345794301, 1.000000000000000000),
 ( 1.000000000000000000, 0.7071067811865708874, 1.000000000000000000) ) ) 
 REPRESENTATION_ITEM ( '' )  SURFACE ( )  );
#10703=CARTESIAN_POINT ( 'NONE',  ( 21.05000000000000071, 13.50240476722978933, -238.5648941131444474 ) ) ;
#10708=ORIENTED_EDGE ( 'NONE', *, *, #89086, .T. ) ;
#10712=DIRECTION ( 'NONE',  ( 0.000000000000000000, -0.8814952561688431665, 0.4721928772777346794 ) ) ;
#10721=EDGE_CURVE ( 'NONE', #137100, #132943, #226651, .T. ) ;
#10737=LINE ( 'NONE', #88963, #239933 ) ;
#10754=CARTESIAN_POINT ( 'NONE',  ( 18.52928932188134326, 33.71149860592453251, -236.3111109633100000 ) ) ;
#10759=CARTESIAN_POINT ( 'NONE',  ( 18.41815437325366389, 37.99504821466788229, -261.0425665635218593 ) ) ;
#10767=CARTESIAN_POINT ( 'NONE',  ( -20.54999999999999716, 23.68770167995059595, -252.8127582590406348 ) ) ;
#10775=CARTESIAN_POINT ( 'NONE',  ( 21.08479644141222664, 1.563360853806263107, -230.6850037888585234 ) ) ;
#10779=ADVANCED_FACE ( 'NONE', ( #190116 ), #115706, .F. ) ;
#10798=FACE_OUTER_BOUND ( 'NONE', #3361, .T. ) ;
#10801=CARTESIAN_POINT ( 'NONE',  ( 21.14999999999999858, 23.07408735703284464, -230.1204787304871502 ) ) ;
#10830=CARTESIAN_POINT ( 'NONE',  ( -21.14999999999999858, 1.363275264940686293, -230.6442496871288483 ) ) ;
#10836=CARTESIAN_POINT ( 'NONE',  ( 20.94999999999999574, 18.65488991999774271, -228.0822300706204544 ) ) ;
#10847=ADVANCED_FACE ( 'NONE', ( #236930 ), #56981, .F. ) ;
#10858=EDGE_LOOP ( 'NONE', ( #217082, #226134, #52695, #225958 ) ) ;
#10896=ORIENTED_EDGE ( 'NONE', *, *, #192111, .T. ) ;
#10906=ORIENTED_EDGE ( 'NONE', *, *, #160337, .T. ) ;
#10928=ORIENTED_EDGE ( 'NONE', *, *, #116491, .T. ) ;
#10956=ORIENTED_EDGE ( 'NONE', *, *, #77388, .F. ) ;
#11002=ADVANCED_FACE ( 'NONE', ( #125955 ), #117755, .F. ) ;
#11054=DIRECTION ( 'NONE',  ( 0.000000000000000000, 0.8814952561688476074, -0.4721928772777262417 ) ) ;
#11098=DIRECTION ( 'NONE',  ( 1.000000000000000000, 1.394253735153569469E-16, 2.602809386958778209E-16 ) ) ;
#11136=DIRECTION ( 'NONE',  ( 0.000000000000000000, 0.8814952561688444987, -0.4721928772777320149 ) ) ;
#11143=ORIENTED_EDGE ( 'NONE', *, *, #138214, .T. ) ;
#11193=AXIS2_PLACEMENT_3D ( 'NONE', #30261, #245455, #25129 ) ;
#11221=DIRECTION ( 'NONE',  ( 0.000000000000000000, 0.3488585713686159218, 0.9371753822965306346 ) ) ;
#11244=VECTOR ( 'NONE', #14672, 1000.000000000000000 ) ;
#11245=CARTESIAN_POINT ( 'NONE',  ( -21.05000000000000071, 18.62343931468261360, -223.9512205031617498 ) ) ;
#11280=CARTESIAN_POINT ( 'NONE',  ( -20.00857864376270001, 30.09302283515540211, -235.6538990729184491 ) ) ;
#11331=VERTEX_POINT ( 'NONE', #39734 ) ;
#11337=CARTESIAN_POINT ( 'NONE',  ( -20.85000000000000142, 42.94477010600543565, -254.3363632230312703 ) ) ;
#11340=CARTESIAN_POINT ( 'NONE',  ( -20.96077737575309996, 36.10128815642492839, -236.0658802525699400 ) ) ;
#11348=CARTESIAN_POINT ( 'NONE',  ( 21.05000000000000071, 1.316055977212909456, -230.7323992127457473 ) ) ;
#11375=AXIS2_PLACEMENT_3D ( 'NONE', #30016, #109508, #172107 ) ;
#11383=VERTEX_POINT ( 'NONE', #228304 ) ;
#11397=AXIS2_PLACEMENT_3D ( 'NONE', #23737, #4131, #246591 ) ;
#11403=DIRECTION ( 'NONE',  ( 0.000000000000000000, 0.8814952561688430555, -0.4721928772777346239 ) ) ;
#11424=EDGE_CURVE ( 'NONE', #108480, #142601, #6668, .T. ) ;
#11457=CARTESIAN_POINT ( 'NONE',  ( -21.05000000000000071, 16.53615870702968138, -240.8540256063542984 ) ) ;
#11461=CARTESIAN_POINT ( 'NONE',  ( -21.40925344232282157, 10.18571439685150004, -227.8165249505043448 ) ) ;
#11483=CARTESIAN_POINT ( 'NONE',  ( -23.25000000000000000, 7.128833340093095217, -233.7327013124392749 ) ) ;
#11494=EDGE_CURVE ( 'NONE', #202163, #11913, #54779, .T. ) ;
#11502=CARTESIAN_POINT ( 'NONE',  ( -18.50000000000000000, 1.006414599850381730, -224.3937905772586703 ) ) ;
#11510=CARTESIAN_POINT ( 'NONE',  ( 22.47007471830798409, 10.77449791745510232, -226.9269314985139374 ) ) ;
#11515=AXIS2_PLACEMENT_3D ( 'NONE', #150484, #193467, #132192 ) ;
#11530=AXIS2_PLACEMENT_3D ( 'NONE', #65836, #86658, #67127 ) ;
#11546=CARTESIAN_POINT ( 'NONE',  ( -20.94999999999999929, 42.92545512184477730, -254.1955779480491344 ) ) ;
#11551=AXIS2_PLACEMENT_3D ( 'NONE', #77641, #137618, #116793 ) ;
#11565=DIRECTION ( 'NONE',  ( 1.000000000000000000, -0.000000000000000000, -0.000000000000000000 ) ) ;
#11588=CARTESIAN_POINT ( 'NONE',  ( -20.95000000000000284, 35.97645343225767789, -235.9694016464868298 ) ) ;
#11628=AXIS2_PLACEMENT_3D ( 'NONE', #116980, #253905, #97375 ) ;
#11630=CIRCLE ( 'NONE', #86593, 0.09999999999999954758 ) ;
#11640=CARTESIAN_POINT ( 'NONE',  ( -20.94999999999999929, 43.08613539620618837, -254.3146655184800409 ) ) ;
#11647=ORIENTED_EDGE ( 'NONE', *, *, #134734, .F. ) ;
#11656=ORIENTED_EDGE ( 'NONE', *, *, #215097, .F. ) ;
#11684=ADVANCED_FACE ( 'NONE', ( #102879 ), #123762, .F. ) ;
#11701=ORIENTED_EDGE ( 'NONE', *, *, #205800, .T. ) ;
#11715=EDGE_CURVE ( 'NONE', #2987, #33556, #176411, .T. ) ;
#11765=EDGE_CURVE ( 'NONE', #188452, #227951, #101308, .T. ) ;
#11820=CIRCLE ( 'NONE', #82473, 11.75000000000000533 ) ;
#11864=AXIS2_PLACEMENT_3D ( 'NONE', #225907, #104670, #5581 ) ;
#11913=VERTEX_POINT ( 'NONE', #96156 ) ;
#11937=FACE_OUTER_BOUND ( 'NONE', #18043, .T. ) ;
#11942=AXIS2_PLACEMENT_3D ( 'NONE', #236050, #36607, #135652 ) ;
#11961=CIRCLE ( 'NONE', #191016, 0.1000000000000013933 ) ;
#11968=VECTOR ( 'NONE', #200230, 1000.000000000000114 ) ;
#11993=DIRECTION ( 'NONE',  ( -1.000000000000000000, -1.541880601228652843E-16, -2.878400969107353907E-16 ) ) ;
#12054=ORIENTED_EDGE ( 'NONE', *, *, #229318, .T. ) ;
#12064=CARTESIAN_POINT ( 'NONE',  ( 23.25000000000000355, 2.513905990859601314, -256.7358755158824692 ) ) ;
#12065=CARTESIAN_POINT ( 'NONE',  ( 18.46932045258611765, 37.97547201091887814, -261.2271751612549906 ) ) ;
#12069=EDGE_CURVE ( 'NONE', #248870, #107706, #234839, .T. ) ;
#12130=VERTEX_POINT ( 'NONE', #163860 ) ;
#12152=DIRECTION ( 'NONE',  ( 1.000000000000000000, 0.000000000000000000, 0.000000000000000000 ) ) ;
#12161=EDGE_CURVE ( 'NONE', #104349, #149025, #230753, .T. ) ;
#12164=LINE ( 'NONE', #214195, #89805 ) ;
#12204=ORIENTED_EDGE ( 'NONE', *, *, #236920, .F. ) ;
#12208=CARTESIAN_POINT ( 'NONE',  ( 21.05000000000000071, 28.55432187084631934, -258.5393726171218418 ) ) ;
#12218=CARTESIAN_POINT ( 'NONE',  ( -21.05000000000000071, 9.997527148596390134, -228.1702915402975691 ) ) ;
#12233=AXIS2_PLACEMENT_3D ( 'NONE', #204778, #247772, #27490 ) ;
#12278=CARTESIAN_POINT ( 'NONE',  ( 20.94999999999999574, 18.14639373905162145, -237.6648341169113792 ) ) ;
#12298=CIRCLE ( 'NONE', #120634, 7.900000000000013678 ) ;
#12299=DIRECTION ( 'NONE',  ( -1.000000000000000000, -0.000000000000000000, -0.000000000000000000 ) ) ;
#12303=EDGE_LOOP ( 'NONE', ( #174671, #76672, #112137, #113608 ) ) ;
#12313=TOROIDAL_SURFACE ( 'NONE', #187094, 0.4000000000000015210, 0.1000000000000000056 ) ;
#12348=ORIENTED_EDGE ( 'NONE', *, *, #46754, .T. ) ;
#12355=EDGE_CURVE ( 'NONE', #95915, #128122, #60035, .T. ) ;
#12372=ADVANCED_FACE ( 'NONE', ( #192404 ), #73766, .F. ) ;
#12396=DIRECTION ( 'NONE',  ( 0.000000000000000000, -0.4721928772777346239, -0.8814952561688430555 ) ) ;
#12411=CARTESIAN_POINT ( 'NONE',  ( 21.05000000000000071, 1.626809808086280951, -230.7491004397056145 ) ) ;
#12413=VERTEX_POINT ( 'NONE', #42317 ) ;
#12415=VECTOR ( 'NONE', #125040, 1000.000000000000000 ) ;
#12417=CARTESIAN_POINT ( 'NONE',  ( 18.59999999999999076, 19.00443933019177223, -232.7770257915295531 ) ) ;
#12502=DIRECTION ( 'NONE',  ( 1.000000000000000000, 0.000000000000000000, 0.000000000000000000 ) ) ;
#12503=EDGE_CURVE ( 'NONE', #92492, #256102, #241795, .T. ) ;
#12508=CARTESIAN_POINT ( 'NONE',  ( 18.49999999999999645, 14.81796439977981272, -236.5325475414793743 ) ) ;
#12516=DIRECTION ( 'NONE',  ( 1.000000000000000000, 0.000000000000000000, 0.000000000000000000 ) ) ;
#12550=AXIS2_PLACEMENT_3D ( 'NONE', #252289, #21112, #73701 ) ;
#12561=DIRECTION ( 'NONE',  ( -1.000000000000000000, 0.000000000000000000, 0.000000000000000000 ) ) ;
#12578=EDGE_CURVE ( 'NONE', #19158, #134779, #89248, .T. ) ;
#12587=EDGE_LOOP ( 'NONE', ( #206396, #79602, #111325, #34296 ) ) ;
#12621=FACE_OUTER_BOUND ( 'NONE', #172055, .T. ) ;
#12629=CARTESIAN_POINT ( 'NONE',  ( 23.15000000000000213, 11.36448785225375424, -246.7787679937655980 ) ) ;
#12630=CARTESIAN_POINT ( 'NONE',  ( 20.94999999999999929, 11.43341603104965110, -245.8667934851861787 ) ) ;
#12631=CIRCLE ( 'NONE', #62689, 0.1000000000000013933 ) ;
#12652=CARTESIAN_POINT ( 'NONE',  ( 21.05000000000000071, 1.560925708358002373, -230.7692066839898359 ) ) ;
#12673=CARTESIAN_POINT ( 'NONE',  ( 18.39999999999999858, 8.794517532467700960, -245.5155488533044945 ) ) ;
#12674=AXIS2_PLACEMENT_3D ( 'NONE', #121801, #22713, #102181 ) ;
#12696=ORIENTED_EDGE ( 'NONE', *, *, #248754, .F. ) ;
#12702=DIRECTION ( 'NONE',  ( -1.000000000000000000, 0.000000000000000000, 0.000000000000000000 ) ) ;
#12714=CIRCLE ( 'NONE', #237726, 0.5000000000000008882 ) ;
#12762=DIRECTION ( 'NONE',  ( 0.000000000000000000, -0.4721928772777346239, -0.8814952561688430555 ) ) ;
#12765=DIRECTION ( 'NONE',  ( 1.000000000000000000, 0.000000000000000000, 0.000000000000000000 ) ) ;
#12766=ORIENTED_EDGE ( 'NONE', *, *, #130555, .F. ) ;
#12773=LINE ( 'NONE', #14050, #7169 ) ;
#12816=ORIENTED_EDGE ( 'NONE', *, *, #126816, .F. ) ;
#12849=DIRECTION ( 'NONE',  ( 0.000000000000000000, 0.8814952561688428334, -0.4721928772777349570 ) ) ;
#12868=ORIENTED_EDGE ( 'NONE', *, *, #45600, .T. ) ;
#12870=CARTESIAN_POINT ( 'NONE',  ( 23.14999999999999503, 28.81810206650552075, -238.0339362645743222 ) ) ;
#12875=CYLINDRICAL_SURFACE ( 'NONE', #121006, 0.1000000000000076522 ) ;
#12884=CARTESIAN_POINT ( 'NONE',  ( -20.54999999999999716, 25.27005795345702666, -235.3392409252341224 ) ) ;
#12932=ORIENTED_EDGE ( 'NONE', *, *, #87980, .T. ) ;
#12953=CARTESIAN_POINT ( 'NONE',  ( -22.59999999999999787, 7.128833340093095217, -233.7327013124392749 ) ) ;
#12971=DIRECTION ( 'NONE',  ( 1.000000000000000000, 0.000000000000000000, 0.000000000000000000 ) ) ;
#12980=ORIENTED_EDGE ( 'NONE', *, *, #240302, .F. ) ;
#12983=CARTESIAN_POINT ( 'NONE',  ( 20.94999999999999929, 24.04029978241812060, -253.0016354099517457 ) ) ;
#12986=EDGE_CURVE ( 'NONE', #147651, #236113, #205380, .T. ) ;
#13007=ORIENTED_EDGE ( 'NONE', *, *, #157994, .F. ) ;
#13070=DIRECTION ( 'NONE',  ( 2.978066053179066765E-16, -0.4721928772777322925, -0.8814952561688443877 ) ) ;
#13082=DIRECTION ( 'NONE',  ( 0.000000000000000000, 0.8814952561688437216, -0.4721928772777334582 ) ) ;
#13126=CARTESIAN_POINT ( 'NONE',  ( 20.94999999999999929, 20.93186404871370598, -233.6960508434578401 ) ) ;
#13152=VERTEX_POINT ( 'NONE', #37542 ) ;
#13162=CARTESIAN_POINT ( 'NONE',  ( 20.94999999999999574, 36.09166453643263850, -236.0643439437599511 ) ) ;
#13213=EDGE_CURVE ( 'NONE', #134581, #203424, #102593, .T. ) ;
#13241=CARTESIAN_POINT ( 'NONE',  ( -18.50000000000000000, 18.18127959618848166, -237.5711165786817389 ) ) ;
#13248=DIRECTION ( 'NONE',  ( 0.000000000000000000, -0.5868805631290353597, -0.8096735173027127530 ) ) ;
#13249=EDGE_LOOP ( 'NONE', ( #88311, #232927, #40668, #50470 ) ) ;
#13260=CARTESIAN_POINT ( 'NONE',  ( 20.21567752745113111, 18.89280262299452318, -228.4652292927793269 ) ) ;
#13296=EDGE_LOOP ( 'NONE', ( #196236, #110209, #202151, #58024 ) ) ;
#13318=FACE_OUTER_BOUND ( 'NONE', #186627, .T. ) ;
#13326=CARTESIAN_POINT ( 'NONE',  ( 18.58143601961928582, 33.87351802927719291, -236.2204290509960458 ) ) ;
#13331=CARTESIAN_POINT ( 'NONE',  ( 21.53551880898956838, 10.24532516527459158, -227.7052014679549927 ) ) ;
#13370=DIRECTION ( 'NONE',  ( 0.000000000000000000, 0.8814952561688476074, -0.4721928772777262417 ) ) ;
#13385=CIRCLE ( 'NONE', #96555, 0.1000000000000013933 ) ;
#13387=CARTESIAN_POINT ( 'NONE',  ( -21.37071067811865532, 21.73808232493841075, -232.4027708824187073 ) ) ;
#13400=AXIS2_PLACEMENT_3D ( 'NONE', #125723, #104839, #248249 ) ;
#13412=CARTESIAN_POINT ( 'NONE',  ( -22.50000000000000000, 12.62988036037869755, -223.4632815780722694 ) ) ;
#13413=CARTESIAN_POINT ( 'NONE',  ( -21.05000000000000071, 36.02918351690955490, -236.0543695120161374 ) ) ;
#13415=CARTESIAN_POINT ( 'NONE',  ( -20.85000000000000142, 28.60154115857408641, -258.4512230915049713 ) ) ;
#13439=DIRECTION ( 'NONE',  ( 0.000000000000000000, -0.8814952561688430555, 0.4721928772777346239 ) ) ;
#13513=CARTESIAN_POINT ( 'NONE',  ( 23.15000000000000213, 28.51339163295720525, -258.4040038037771865 ) ) ;
#13551=AXIS2_PLACEMENT_3D ( 'NONE', #181474, #60210, #180187 ) ;
#13554=AXIS2_PLACEMENT_3D ( 'NONE', #75127, #119369, #78915 ) ;
#13567=VECTOR ( 'NONE', #19083, 1000.000000000000000 ) ;
#13597=DIRECTION ( 'NONE',  ( -1.000000000000000000, -0.000000000000000000, -0.000000000000000000 ) ) ;
#13604=ORIENTED_EDGE ( 'NONE', *, *, #15503, .F. ) ;
#13621=PLANE ( 'NONE',  #76053 ) ;
#13625=CARTESIAN_POINT ( 'NONE',  ( -22.50000000000000000, 12.55707850971102069, -223.4244300710886648 ) ) ;
#13626=FACE_OUTER_BOUND ( 'NONE', #23249, .T. ) ;
#13633=CARTESIAN_POINT ( 'NONE',  ( -20.85000000000000142, 43.35377423437995503, -245.1717807829448930 ) ) ;
#13654=ORIENTED_EDGE ( 'NONE', *, *, #227439, .F. ) ;
#13671=EDGE_CURVE ( 'NONE', #235869, #248947, #135856, .T. ) ;
#13676=DIRECTION ( 'NONE',  ( 0.000000000000000000, -0.8096735173027302945, 0.5868805631290110458 ) ) ;
#13681=EDGE_CURVE ( 'NONE', #53624, #227815, #118301, .T. ) ;
#13704=ADVANCED_FACE ( 'NONE', ( #38082 ), #75907, .F. ) ;
#13716=FACE_OUTER_BOUND ( 'NONE', #41760, .T. ) ;
#13718=CARTESIAN_POINT ( 'NONE',  ( 18.59999999999998721, 43.18640298906419162, -245.2812653309023574 ) ) ;
#13722=EDGE_CURVE ( 'NONE', #97044, #196423, #14258, .T. ) ;
#13741=DIRECTION ( 'NONE',  ( -1.000000000000000000, -1.541880601228652843E-16, -2.878400969107353907E-16 ) ) ;
#13779=DIRECTION ( 'NONE',  ( 0.000000000000000000, 0.8814952561688476074, -0.4721928772777262417 ) ) ;
#13782=CARTESIAN_POINT ( 'NONE',  ( -22.39999999999999858, -3.275978944802467652, -228.2735455795363748 ) ) ;
#13797=CARTESIAN_POINT ( 'NONE',  ( 18.59999999999999076, 28.95347087985017609, -237.9930060266852081 ) ) ;
#13801=ORIENTED_EDGE ( 'NONE', *, *, #136665, .T. ) ;
#13806=DIRECTION ( 'NONE',  ( 1.000000000000000000, 0.000000000000000000, 0.000000000000000000 ) ) ;
#13824=CARTESIAN_POINT ( 'NONE',  ( -20.54999999999999716, 11.60058429089262333, -246.3380203656811887 ) ) ;
#13827=CIRCLE ( 'NONE', #151212, 0.09999999999999986677 ) ;
#13848=PLANE ( 'NONE',  #73921 ) ;
#13854=EDGE_CURVE ( 'NONE', #45747, #161618, #179956, .T. ) ;
#13869=CARTESIAN_POINT ( 'NONE',  ( 18.49713797159812145, 8.901728458076256345, -245.3988228286745823 ) ) ;
#13871=VERTEX_POINT ( 'NONE', #117402 ) ;
#13874=ORIENTED_EDGE ( 'NONE', *, *, #97856, .F. ) ;
#13899=AXIS2_PLACEMENT_3D ( 'NONE', #13633, #256029, #38339 ) ;
#13919=CIRCLE ( 'NONE', #159665, 0.1000000000000013933 ) ;
#13971=CIRCLE ( 'NONE', #5560, 0.09999999999999939493 ) ;
#13974=ORIENTED_EDGE ( 'NONE', *, *, #95592, .T. ) ;
#13991=FACE_OUTER_BOUND ( 'NONE', #202479, .T. ) ;
#13998=DIRECTION ( 'NONE',  ( 0.000000000000000000, -0.5273008465187821736, 0.8496786552930323255 ) ) ;
#14041=ORIENTED_EDGE ( 'NONE', *, *, #100464, .F. ) ;
#14045=DIRECTION ( 'NONE',  ( 0.000000000000000000, -0.8814952561688428334, 0.4721928772777350680 ) ) ;
#14050=CARTESIAN_POINT ( 'NONE',  ( 21.05000000000000071, 16.53042682864194290, -240.8665456014163624 ) ) ;
#14058=TOROIDAL_SURFACE ( 'NONE', #159788, 12.77500000000000036, 0.1000000000000000056 ) ;
#14065=ADVANCED_FACE ( 'NONE', ( #22173 ), #43009, .T. ) ;
#14066=DIRECTION ( 'NONE',  ( 0.000000000000000000, 0.8814952561688476074, -0.4721928772777262417 ) ) ;
#14071=DIRECTION ( 'NONE',  ( 0.000000000000000000, 0.8814952561688430555, -0.4721928772777346239 ) ) ;
#14088=DIRECTION ( 'NONE',  ( 1.000000000000000000, 0.000000000000000000, 0.000000000000000000 ) ) ;
#14096=ORIENTED_EDGE ( 'NONE', *, *, #108087, .T. ) ;
#14098=CIRCLE ( 'NONE', #47379, 0.09999999999998464284 ) ;
#14123=CARTESIAN_POINT ( 'NONE',  ( 21.13461538461537614, 22.12278086513518005, -231.6846110910352081 ) ) ;
#14162=DIRECTION ( 'NONE',  ( 1.000000000000000000, 0.000000000000000000, 0.000000000000000000 ) ) ;
#14228=ORIENTED_EDGE ( 'NONE', *, *, #67657, .F. ) ;
#14232=DIRECTION ( 'NONE',  ( 6.938893903906854773E-14, -0.5273008465188072647, 0.8496786552930167824 ) ) ;
#14258=CIRCLE ( 'NONE', #222497, 0.09999999999999022171 ) ;
#14301=VECTOR ( 'NONE', #97079, 1000.000000000000000 ) ;
#14411=CIRCLE ( 'NONE', #131081, 12.97500000000000320 ) ;
#14427=CIRCLE ( 'NONE', #197549, 11.70000000000001172 ) ;
#14464=CARTESIAN_POINT ( 'NONE',  ( 21.05000000000000071, 36.02918351690956200, -236.0543695120161090 ) ) ;
#14467=CIRCLE ( 'NONE', #139314, 0.09999999999998304689 ) ;
#14481=ORIENTED_EDGE ( 'NONE', *, *, #412, .T. ) ;
#14500=DIRECTION ( 'NONE',  ( 0.000000000000000000, -0.8814952561683926380, 0.4721928772785753958 ) ) ;
#14518=CARTESIAN_POINT ( 'NONE',  ( 20.94999999999999574, 7.128833340093095217, -233.7327013124392749 ) ) ;
#14521=CARTESIAN_POINT ( 'NONE',  ( -23.15000000000000213, -2.001034438968700258, -225.8925473383868905 ) ) ;
#14545=FACE_OUTER_BOUND ( 'NONE', #239805, .T. ) ;
#14605=CARTESIAN_POINT ( 'NONE',  ( 20.95512820512820440, 18.86447962780959386, -229.9497396848627204 ) ) ;
#14638=EDGE_CURVE ( 'NONE', #1255, #104063, #241544, .T. ) ;
#14644=CYLINDRICAL_SURFACE ( 'NONE', #98845, 0.09999999999999983902 ) ;
#14672=DIRECTION ( 'NONE',  ( -0.000000000000000000, -0.8814952561688430555, 0.4721928772777346239 ) ) ;
#14686=EDGE_CURVE ( 'NONE', #100546, #124483, #235349, .T. ) ;
#14722=CARTESIAN_POINT ( 'NONE',  ( -20.64999999999999858, 19.73066058418984170, -238.2142830767208466 ) ) ;
#14723=EDGE_LOOP ( 'NONE', ( #184292, #87683, #51984, #57120, #229485 ) ) ;
#14755=EDGE_CURVE ( 'NONE', #35113, #201330, #231463, .T. ) ;
#14796=AXIS2_PLACEMENT_3D ( 'NONE', #66833, #104631, #47243 ) ;
#14803=AXIS2_PLACEMENT_3D ( 'NONE', #181910, #123218, #64524 ) ;
#14810=DIRECTION ( 'NONE',  ( 0.000000000000000000, 0.4859085964047519801, 0.8740096314915323239 ) ) ;
#14817=ADVANCED_FACE ( 'NONE', ( #53619 ), #95310, .T. ) ;
#14830=DIRECTION ( 'NONE',  ( 0.000000000000000000, 0.8814952561688476074, -0.4721928772777262417 ) ) ;
#14845=AXIS2_PLACEMENT_3D ( 'NONE', #6336, #183716, #102855 ) ;
#14874=DIRECTION ( 'NONE',  ( 0.7071359030027322135, 0.3338770338705078222, 0.6232856014206827888 ) ) ;
#14891=CARTESIAN_POINT ( 'NONE',  ( -18.43459694179580310, 38.00868472153695876, -261.0447666131053097 ) ) ;
#14914=AXIS2_PLACEMENT_3D ( 'NONE', #72784, #37489, #132741 ) ;
#14929=DIRECTION ( 'NONE',  ( -1.000000000000000000, 0.000000000000000000, 0.000000000000000000 ) ) ;
#14938=VECTOR ( 'NONE', #155306, 1000.000000000000000 ) ;
#14947=VECTOR ( 'NONE', #166614, 1000.000000000000000 ) ;
#14952=CARTESIAN_POINT ( 'NONE',  ( -21.12230431290520727, 10.17345785877508391, -228.0379268863081847 ) ) ;
#14961=DIRECTION ( 'NONE',  ( -0.000000000000000000, 0.4721928772777346239, 0.8814952561688430555 ) ) ;
#14972=DIRECTION ( 'NONE',  ( 1.000000000000000000, 0.000000000000000000, 0.000000000000000000 ) ) ;
#14974=ORIENTED_EDGE ( 'NONE', *, *, #93525, .F. ) ;
#14977=ORIENTED_EDGE ( 'NONE', *, *, #200593, .F. ) ;
#15013=ORIENTED_EDGE ( 'NONE', *, *, #160659, .F. ) ;
#15026=DIRECTION ( 'NONE',  ( 1.000000000000000000, 0.000000000000000000, 0.000000000000000000 ) ) ;
#15059=ORIENTED_EDGE ( 'NONE', *, *, #219723, .F. ) ;
#15105=AXIS2_PLACEMENT_3D ( 'NONE', #179958, #102953, #196930 ) ;
#15112=DIRECTION ( 'NONE',  ( 0.000000000000000000, 0.8814952561688436106, -0.4721928772777334027 ) ) ;
#15127=EDGE_LOOP ( 'NONE', ( #3955, #20582, #243279, #245828 ) ) ;
#15237=ORIENTED_EDGE ( 'NONE', *, *, #85909, .T. ) ;
#15247=VERTEX_POINT ( 'NONE', #92422 ) ;
#15256=EDGE_CURVE ( 'NONE', #118730, #235869, #139854, .T. ) ;
#15257=DIRECTION ( 'NONE',  ( -1.000000000000000000, 0.000000000000000000, 0.000000000000000000 ) ) ;
#15291=ORIENTED_EDGE ( 'NONE', *, *, #69356, .T. ) ;
#15294=EDGE_CURVE ( 'NONE', #194512, #109477, #173240, .T. ) ;
#15319=DIRECTION ( 'NONE',  ( 0.000000000000000000, -0.8814952561688476074, 0.4721928772777262417 ) ) ;
#15339=ORIENTED_EDGE ( 'NONE', *, *, #180098, .T. ) ;
#15346=DIRECTION ( 'NONE',  ( 1.000000000000000000, 0.000000000000000000, 0.000000000000000000 ) ) ;
#15375=DIRECTION ( 'NONE',  ( 0.000000000000000000, -0.9446535261619708468, 0.3280696808755038663 ) ) ;
#15381=ORIENTED_EDGE ( 'NONE', *, *, #139933, .T. ) ;
#15385=CARTESIAN_POINT ( 'NONE',  ( 23.24999999999999645, 36.65892442174935439, -249.5511627012433848 ) ) ;
#15397=DIRECTION ( 'NONE',  ( 1.000000000000000000, 3.448943450116723568E-16, 6.438528483529607644E-16 ) ) ;
#15431=CARTESIAN_POINT ( 'NONE',  ( -23.15000000000000213, 7.128833340093095217, -233.7327013124392749 ) ) ;
#15503=EDGE_CURVE ( 'NONE', #48651, #181045, #83234, .T. ) ;
#15546=ORIENTED_EDGE ( 'NONE', *, *, #216461, .F. ) ;
#15570=EDGE_CURVE ( 'NONE', #1130, #120155, #132536, .T. ) ;
#15586=DIRECTION ( 'NONE',  ( 0.000000000000000000, 0.8814952561688437216, -0.4721928772777334582 ) ) ;
#15587=DIRECTION ( 'NONE',  ( 0.000000000000000000, 0.8814952561688722543, -0.4721928772776801675 ) ) ;
#15600=VECTOR ( 'NONE', #8934, 1000.000000000000000 ) ;
#15653=CARTESIAN_POINT ( 'NONE',  ( -21.05000000000000071, 16.44800918141279311, -240.8068063186265135 ) ) ;
#15671=EDGE_LOOP ( 'NONE', ( #250005, #217592, #97912, #69773 ) ) ;
#15745=EDGE_LOOP ( 'NONE', ( #61527, #176850, #31869, #11656 ) ) ;
#15787=ORIENTED_EDGE ( 'NONE', *, *, #13671, .T. ) ;
#15805=CARTESIAN_POINT ( 'NONE',  ( 21.13461538461538325, 22.93928069810350223, -230.1603595318553630 ) ) ;
#15816=CARTESIAN_POINT ( 'NONE',  ( 20.94999999999999929, 7.128833340093095217, -233.7327013124392749 ) ) ;
#15818=ORIENTED_EDGE ( 'NONE', *, *, #182618, .F. ) ;
#15820=VERTEX_POINT ( 'NONE', #121958 ) ;
#15827=EDGE_CURVE ( 'NONE', #84354, #153027, #102351, .T. ) ;
#15834=VERTEX_POINT ( 'NONE', #81506 ) ;
#15847=VERTEX_POINT ( 'NONE', #4557 ) ;
#15859=ORIENTED_EDGE ( 'NONE', *, *, #214614, .F. ) ;
#15893=CARTESIAN_POINT ( 'NONE',  ( 20.95159278453404283, 18.81431913549488399, -229.8868573851966062 ) ) ;
#15947=EDGE_CURVE ( 'NONE', #29656, #102316, #247023, .T. ) ;
#15949=ORIENTED_EDGE ( 'NONE', *, *, #216838, .T. ) ;
#15965=CARTESIAN_POINT ( 'NONE',  ( -20.85000000000000142, 46.46967969402479781, -243.0849751855955674 ) ) ;
#15984=TOROIDAL_SURFACE ( 'NONE', #170115, 11.65000000000000036, 0.1000000000000000056 ) ;
#16033=DIRECTION ( 'NONE',  ( 1.000000000000000000, 0.000000000000000000, 0.000000000000000000 ) ) ;
#16035=EDGE_CURVE ( 'NONE', #4561, #39320, #19627, .T. ) ;
#16036=DIRECTION ( 'NONE',  ( 0.000000000000000000, -0.8814952561688430555, 0.4721928772777346239 ) ) ;
#16046=VECTOR ( 'NONE', #139764, 1000.000000000000000 ) ;
#16051=ORIENTED_EDGE ( 'NONE', *, *, #208238, .T. ) ;
#16052=CARTESIAN_POINT ( 'NONE',  ( -20.92356734117541706, 46.42459709376391430, -243.0752906381742662 ) ) ;
#16070=DIRECTION ( 'NONE',  ( 0.000000000000000000, 0.5826443254699606999, 0.8127272543711416830 ) ) ;
#16078=CLOSED_SHELL ( 'NONE', ( #114748, #235998, #2548, #163033, #16117, #129052, #101375, #101041, #24713, #38558, #109404, #82852, #133080, #224577, #184670, #212507, #167420, #167536, #98380, #84554, #86889, #239566, #158134, #44216, #250729, #135563, #123821, #181916, #11684, #164566, #9826, #252335, #57627, #214030, #170477, #71359, #127141, #113343, #193406, #211503, #168401, #22585, #4419, #184841, #199110, #61050, #90876, #37472, #165377, #75791, #48707, #234951, #77646, #150367, #10779, #127628, #95580, #253796, #27238, #181306, #148597, #93442, #244860, #233250, #94758, #173673, #102306, #65682, #128795, #88767, #31397, #188094, #36521, #233343, #161380, #212716, #224946, #224406, #22824, #2203, #86779, #162433, #171137, #141806, #192281, #83168, #49105, #26121, #72362, #226620, #64778, #4781, #238146, #29951, #133260, #109120, #109649, #81396, #225110, #214704, #153229, #167715, #73443, #164590, #94601, #216156, #61190, #152830, #70300, #218904, #185313, #170999, #68481, #1668, #31645, #197933, #134786, #206350, #46707, #32985, #197564, #115266, #235003, #137212, #223461, #84492, #68412, #220721, #155183, #155254, #133572, #50882, #135093, #16780, #34429, #6310, #134908, #117942, #8443, #148892, #62168, #26534, #62046, #39476, #163069, #130713, #184340, #74687, #16899, #46988, #1485, #145326, #108479, #143812, #114865, #81060, #5322, #126335, #221014, #141412, #92968, #217844, #255160, #192306, #246848, #194113, #53872, #22607, #137393, #140284, #87681, #140139, #28026, #211901, #150602, #61195, #189269, #198027, #175014, #11002, #212630, #40502, #253105, #253351, #9762, #99425, #6657, #26298, #241828, #219, #72067, #65200, #77569, #20185, #170513, #159468, #136476, #181663, #218940, #129177, #114151, #220976, #75003, #255647, #64358, #170613, #217774, #123983, #123299, #126728, #234135, #26542, #217447, #133245, #42168, #33988, #172153, #199469, #225327, #199826, #203284, #126298, #12372, #136185, #151621, #89141, #130262, #223543, #123946, #141541, #144995, #196008, #203691, #222672, #128333, #119580, #93613, #118357, #74494, #72248, #169686, #149729, #72439, #37896, #103420, #142730, #149839, #183868, #16891, #202549, #92541, #148613, #156583, #184665, #37822, #78025, #210336, #60111, #41762, #234833, #51253, #4862, #3997, #223974, #155333, #231097, #41639, #226929, #30051, #166524, #4798, #82182, #39723, #13704, #201126, #236157, #91176, #136472, #159472, #91474, #187211, #92554, #125357, #253147, #59040, #51086, #92935, #197871, #235903, #58563, #59552, #140678, #66635, #199705, #193029, #66215, #125048, #183827, #130115, #177528, #37015, #10847, #64224, #9406, #203989, #28157, #194119, #202941, #233230, #229609, #249309, #181154, #39060, #183228, #123312, #78946, #54931, #50475, #86745, #241600, #26167, #128196, #44119, #7998, #50647, #240987, #222935, #37118, #97388, #192166, #71742, #248282, #99150, #82905, #210176, #150999, #180365, #8465, #208358, #242412, #106672, #105587, #41517, #240749, #137531, #76656, #73150, #16555, #30651, #222290, #127053, #220006, #51415, #14817, #253342, #20739, #204281, #67345, #1407, #149524, #154261, #48897, #214788, #157103, #155432, #67671, #229486, #137211, #108127, #214320, #195181, #235073, #43783, #17694, #17369, #48947, #243945, #241318, #2786, #161899, #108364, #122889, #212297, #88428, #66693, #156186, #98184, #101952, #151522, #209010, #186810, #81337, #229664, #111771, #37879, #198566, #157744, #42649, #105353, #111672, #16970, #149655, #91780, #91009, #128846, #138297, #240926, #9036, #221169, #74949, #189581, #191747, #107061, #150390, #240409, #190197, #213370, #81887, #254412, #42065, #78474, #178621, #112303, #128472, #205684, #237560, #164711, #204954, #107592, #46235, #201476, #106873, #49739, #95415, #162090, #217856, #232589, #141314, #160100, #98281, #19968, #110031, #16810, #198584, #134435, #227134, #254618, #130086, #134695, #68982, #180700, #107903, #203685, #24601, #142043, #138617, #228955, #24836, #102849, #108243, #116162, #209022, #183295, #39040, #117845, #127055, #87095, #20452, #247488, #14065, #85605, #4680, #31164, #174015, #153907, #238113, #228221, #126105 ) ) ;
#16091=DIRECTION ( 'NONE',  ( 1.000000000000000000, 0.000000000000000000, 0.000000000000000000 ) ) ;
#16097=ORIENTED_EDGE ( 'NONE', *, *, #75206, .F. ) ;
#16110=DIRECTION ( 'NONE',  ( 0.000000000000000000, -0.8496786552930076786, -0.5273008465188218086 ) ) ;
#16117=ADVANCED_FACE ( 'NONE', ( #37009 ), #244453, .T. ) ;
#16121=AXIS2_PLACEMENT_3D ( 'NONE', #140477, #141762, #136627 ) ;
#16130=DIRECTION ( 'NONE',  ( -1.000000000000000000, 0.000000000000000000, 0.000000000000000000 ) ) ;
#16153=CARTESIAN_POINT ( 'NONE',  ( 20.94999999999999929, 36.65892442174935439, -249.5511627012433848 ) ) ;
#16159=AXIS2_PLACEMENT_3D ( 'NONE', #200960, #87421, #104401 ) ;
#16167=VERTEX_POINT ( 'NONE', #404 ) ;
#16170=CARTESIAN_POINT ( 'NONE',  ( -23.25000000000000000, 36.65892442174935439, -249.5511627012433848 ) ) ;
#16179=CARTESIAN_POINT ( 'NONE',  ( -18.33682934331562109, 38.25511225049375241, -261.1960286750406794 ) ) ;
#16200=CIRCLE ( 'NONE', #45210, 0.09999999999999485689 ) ;
#16202=EDGE_CURVE ( 'NONE', #41248, #199581, #248760, .T. ) ;
#16226=AXIS2_PLACEMENT_3D ( 'NONE', #54724, #75603, #170882 ) ;
#16237=EDGE_CURVE ( 'NONE', #34543, #56882, #53110, .T. ) ;
#16282=DIRECTION ( 'NONE',  ( 7.304098846218136639E-16, -0.4721928772777346239, -0.8814952561688430555 ) ) ;
#16289=CYLINDRICAL_SURFACE ( 'NONE', #174158, 0.1000000000000013933 ) ;
#16325=CARTESIAN_POINT ( 'NONE',  ( -20.54999999999999716, 29.19585636832770703, -237.3287400596392445 ) ) ;
#16342=AXIS2_PLACEMENT_3D ( 'NONE', #176020, #93882, #74364 ) ;
#16384=ORIENTED_EDGE ( 'NONE', *, *, #252970, .F. ) ;
#16395=CARTESIAN_POINT ( 'NONE',  ( -20.64999999999999858, 27.91464654983916205, -239.9322955902566719 ) ) ;
#16399=CIRCLE ( 'NONE', #249627, 1.999999999999997335 ) ;
#16412=DIRECTION ( 'NONE',  ( 0.000000000000000000, -0.8814952561688444987, 0.4721928772777320149 ) ) ;
#16413=PLANE ( 'NONE',  #145898 ) ;
#16451=ORIENTED_EDGE ( 'NONE', *, *, #36735, .T. ) ;
#16455=CIRCLE ( 'NONE', #58097, 0.1000000000000015737 ) ;
#16490=CARTESIAN_POINT ( 'NONE',  ( -18.47079683080355750, 8.922807857279824617, -245.4386816022545190 ) ) ;
#16491=ORIENTED_EDGE ( 'NONE', *, *, #251691, .F. ) ;
#16531=DIRECTION ( 'NONE',  ( 1.000000000000000000, 0.000000000000000000, 0.000000000000000000 ) ) ;
#16553=DIRECTION ( 'NONE',  ( 0.000000000000000000, 0.8814952561688476074, -0.4721928772777262417 ) ) ;
#16555=ADVANCED_FACE ( 'NONE', ( #201841 ), #2338, .T. ) ;
#16597=AXIS2_PLACEMENT_3D ( 'NONE', #178212, #80330, #158649 ) ;
#16605=CARTESIAN_POINT ( 'NONE',  ( -20.94999999999999929, 43.17747518314619271, -245.0773422074893233 ) ) ;
#16612=VERTEX_POINT ( 'NONE', #206980 ) ;
#16620=DIRECTION ( 'NONE',  ( 0.000000000000000000, 0.8814952561688438326, -0.4721928772777331806 ) ) ;
#16632=CYLINDRICAL_SURFACE ( 'NONE', #39152, 0.1000000000000013933 ) ;
#16633=EDGE_CURVE ( 'NONE', #1479, #116380, #204196, .T. ) ;
#16634=DIRECTION ( 'NONE',  ( 1.000000000000000000, 0.000000000000000000, 0.000000000000000000 ) ) ;
#16648=ORIENTED_EDGE ( 'NONE', *, *, #9094, .T. ) ;
#16649=ORIENTED_EDGE ( 'NONE', *, *, #234861, .T. ) ;
#16698=VECTOR ( 'NONE', #239513, 1000.000000000000000 ) ;
#16722=ORIENTED_EDGE ( 'NONE', *, *, #128289, .T. ) ;
#16733=FACE_OUTER_BOUND ( 'NONE', #74538, .T. ) ;
#16765=DIRECTION ( 'NONE',  ( 1.000000000000000000, 1.394253735153569469E-16, 2.602809386958778209E-16 ) ) ;
#16771=DIRECTION ( 'NONE',  ( 0.000000000000000000, -0.8814952561688476074, 0.4721928772777262417 ) ) ;
#16772=FACE_OUTER_BOUND ( 'NONE', #178100, .T. ) ;
#16780=ADVANCED_FACE ( 'NONE', ( #94723 ), #138956, .T. ) ;
#16795=CARTESIAN_POINT ( 'NONE',  ( 23.25000000000000000, 11.31726856452598184, -246.8669175193824969 ) ) ;
#16809=VECTOR ( 'NONE', #65020, 1000.000000000000000 ) ;
#16810=ADVANCED_FACE ( 'NONE', ( #75194 ), #94685, .T. ) ;
#16820=AXIS2_PLACEMENT_3D ( 'NONE', #222050, #123001, #248068 ) ;
#16825=EDGE_CURVE ( 'NONE', #248838, #196126, #44931, .T. ) ;
#16846=DIRECTION ( 'NONE',  ( 0.7071067811865708874, -0.3338907855511046296, -0.6233112732207185536 ) ) ;
#16852=ORIENTED_EDGE ( 'NONE', *, *, #213353, .T. ) ;
#16855=CARTESIAN_POINT ( 'NONE',  ( -23.15000000000000213, 7.128833340093095217, -233.7327013124392749 ) ) ;
#16870=ORIENTED_EDGE ( 'NONE', *, *, #91639, .T. ) ;
#16880=VERTEX_POINT ( 'NONE', #64581 ) ;
#16891=ADVANCED_FACE ( 'NONE', ( #106263 ), #183265, .T. ) ;
#16895=VERTEX_POINT ( 'NONE', #241936 ) ;
#16899=ADVANCED_FACE ( 'NONE', ( #184529 ), #86694, .F. ) ;
#16924=EDGE_CURVE ( 'NONE', #198003, #231948, #111565, .T. ) ;
#16925=B_SPLINE_CURVE_WITH_KNOTS ( 'NONE', 3,
 ( #57188, #79322, #158909, #238418, #40248, #213716, #194180, #27106, #121074, #144422, #62356, #182315, #204411, #3649, #41527, #161472, #46612, #102727, #240994 ),
 .UNSPECIFIED., .F., .F.,
 ( 4, 3, 3, 3, 3, 3, 4 ),
 ( 1.387778780781445521E-17, 2.646747978908964204E-05, 5.271166642128792909E-05, 9.008788829885240981E-05, 0.0001426648776561058600, 0.0001897378458659877839, 0.0001917382627806327297 ),
 .UNSPECIFIED. ) ;
#16962=FACE_OUTER_BOUND ( 'NONE', #66118, .T. ) ;
#16970=ADVANCED_FACE ( 'NONE', ( #84097 ), #53304, .F. ) ;
#17015=CIRCLE ( 'NONE', #141881, 11.75000000000000533 ) ;
#17049=ORIENTED_EDGE ( 'NONE', *, *, #27153, .F. ) ;
#17067=DIRECTION ( 'NONE',  ( 0.000000000000000000, -0.4721928772777342354, -0.8814952561688431665 ) ) ;
#17081=DIRECTION ( 'NONE',  ( 4.408576920032446123E-17, -0.9371753822965315228, 0.3488585713686134238 ) ) ;
#17138=LINE ( 'NONE', #217855, #52112 ) ;
#17146=LINE ( 'NONE', #96621, #142505 ) ;
#17149=CARTESIAN_POINT ( 'NONE',  ( -21.05000000000000071, 18.14639373905162145, -237.6648341169113792 ) ) ;
#17156=AXIS2_PLACEMENT_3D ( 'NONE', #123632, #3666, #144440 ) ;
#17211=CARTESIAN_POINT ( 'NONE',  ( -18.59999999999999787, 45.93315328338058379, -256.6017782078560003 ) ) ;
#17216=EDGE_CURVE ( 'NONE', #68656, #125839, #164709, .T. ) ;
#17222=FACE_OUTER_BOUND ( 'NONE', #14723, .T. ) ;
#17230=CARTESIAN_POINT ( 'NONE',  ( -23.15000000000000213, 19.28991295610541812, -237.9781866380819793 ) ) ;
#17243=CARTESIAN_POINT ( 'NONE',  ( -20.94999999999999929, 16.44800918141279666, -240.8068063186265135 ) ) ;
#17248=CARTESIAN_POINT ( 'NONE',  ( -18.59999999999999787, 43.08613539620618837, -254.3146655184800409 ) ) ;
#17253=ORIENTED_EDGE ( 'NONE', *, *, #252209, .T. ) ;
#17284=ORIENTED_EDGE ( 'NONE', *, *, #90939, .F. ) ;
#17322=CARTESIAN_POINT ( 'NONE',  ( -20.94999999999999929, 46.32970330538243786, -243.0551226933711746 ) ) ;
#17338=CARTESIAN_POINT ( 'NONE',  ( 21.05000000000000071, 11.27293161222461748, -225.9964495734431864 ) ) ;
#17350=ORIENTED_EDGE ( 'NONE', *, *, #253780, .F. ) ;
#17369=ADVANCED_FACE ( 'NONE', ( #193266 ), #14644, .F. ) ;
#17416=DIRECTION ( 'NONE',  ( 0.000000000000000000, 0.8814952561688442767, -0.4721928772777324035 ) ) ;
#17433=CARTESIAN_POINT ( 'NONE',  ( -18.43634282235085564, 37.95953089239920075, -261.2289615770415594 ) ) ;
#17480=CARTESIAN_POINT ( 'NONE',  ( -21.14999999999999858, -3.275978944802464099, -228.2735455795363748 ) ) ;
#17488=EDGE_CURVE ( 'NONE', #56714, #129778, #19775, .T. ) ;
#17510=CARTESIAN_POINT ( 'NONE',  ( 21.07933241753356768, 10.03486121375300222, -228.1099367534912687 ) ) ;
#17518=ORIENTED_EDGE ( 'NONE', *, *, #7199, .T. ) ;
#17528=DIRECTION ( 'NONE',  ( 0.000000000000000000, -0.8814952561688476074, 0.4721928772777262417 ) ) ;
#17545=LINE ( 'NONE', #198756, #203794 ) ;
#17582=ORIENTED_EDGE ( 'NONE', *, *, #9386, .F. ) ;
#17591=VERTEX_POINT ( 'NONE', #27507 ) ;
#17646=AXIS2_PLACEMENT_3D ( 'NONE', #11588, #92378, #51955 ) ;
#17694=ADVANCED_FACE ( 'NONE', ( #67862 ), #88686, .F. ) ;
#17742=CARTESIAN_POINT ( 'NONE',  ( 21.05000000000000071, 10.21728496540352893, -227.9671432372869049 ) ) ;
#17749=ORIENTED_EDGE ( 'NONE', *, *, #117481, .F. ) ;
#17753=LINE ( 'NONE', #118162, #127554 ) ;
#17760=CARTESIAN_POINT ( 'NONE',  ( -20.85000000000000142, 43.27008861172207332, -245.2265230569236110 ) ) ;
#17829=VECTOR ( 'NONE', #245104, 1000.000000000000000 ) ;
#17831=ORIENTED_EDGE ( 'NONE', *, *, #103926, .F. ) ;
#17836=FACE_OUTER_BOUND ( 'NONE', #250083, .T. ) ;
#17864=AXIS2_PLACEMENT_3D ( 'NONE', #158460, #235388, #196265 ) ;
#17866=VERTEX_POINT ( 'NONE', #42865 ) ;
#17870=DIRECTION ( 'NONE',  ( -1.000000000000000000, -1.394253735153569469E-16, -2.602809386958778209E-16 ) ) ;
#17892=VERTEX_POINT ( 'NONE', #79401 ) ;
#17939=DIRECTION ( 'NONE',  ( 0.000000000000000000, -0.8814952561688449428, 0.4721928772777310157 ) ) ;
#17960=CIRCLE ( 'NONE', #43108, 7.900000000000007461 ) ;
#17964=CARTESIAN_POINT ( 'NONE',  ( -21.55000000000000426, 29.52010233258345906, -236.9352117192826199 ) ) ;
#17974=DIRECTION ( 'NONE',  ( 0.000000000000000000, 0.8814952561688437216, -0.4721928772777334582 ) ) ;
#17983=EDGE_CURVE ( 'NONE', #185172, #111286, #65755, .T. ) ;
#18041=DIRECTION ( 'NONE',  ( 0.000000000000000000, 0.8814952561688436106, -0.4721928772777334027 ) ) ;
#18043=EDGE_LOOP ( 'NONE', ( #67699, #16852, #252501, #122915, #215323, #130953, #47247 ) ) ;
#18091=ORIENTED_EDGE ( 'NONE', *, *, #74992, .F. ) ;
#18160=CIRCLE ( 'NONE', #197226, 0.1000000000000013933 ) ;
#18182=TOROIDAL_SURFACE ( 'NONE', #163932, 12.97499999999999609, 0.1000000000000000056 ) ;
#18206=ORIENTED_EDGE ( 'NONE', *, *, #106835, .T. ) ;
#18211=AXIS2_PLACEMENT_3D ( 'NONE', #101252, #180853, #140420 ) ;
#18238=VERTEX_POINT ( 'NONE', #116956 ) ;
#18287=LINE ( 'NONE', #40464, #170080 ) ;
#18307=AXIS2_PLACEMENT_3D ( 'NONE', #159193, #40545, #241289 ) ;
#18342=ORIENTED_EDGE ( 'NONE', *, *, #211172, .F. ) ;
#18346=EDGE_LOOP ( 'NONE', ( #218892, #76411, #209500, #160825 ) ) ;
#18350=DIRECTION ( 'NONE',  ( 0.000000000000000000, 0.8814952561688429444, -0.4721928772777349015 ) ) ;
#18359=CARTESIAN_POINT ( 'NONE',  ( 18.59999999999999076, 30.76917518201224055, -234.8152055956155380 ) ) ;
#18371=CARTESIAN_POINT ( 'NONE',  ( 23.25000000000000000, 28.37802281961254991, -258.4449340416662722 ) ) ;
#18374=VERTEX_POINT ( 'NONE', #202903 ) ;
#18385=EDGE_LOOP ( 'NONE', ( #44764, #106456, #205013, #37117 ) ) ;
#18390=DIRECTION ( 'NONE',  ( 1.000000000000000000, 0.000000000000000000, 0.000000000000000000 ) ) ;
#18455=FACE_OUTER_BOUND ( 'NONE', #237125, .T. ) ;
#18509=CARTESIAN_POINT ( 'NONE',  ( -20.54999999999999716, 27.91464654983916205, -239.9322955902566719 ) ) ;
#18553=VERTEX_POINT ( 'NONE', #78776 ) ;
#18560=ORIENTED_EDGE ( 'NONE', *, *, #118066, .F. ) ;
#18563=TOROIDAL_SURFACE ( 'NONE', #93003, 11.89999999999999858, 0.1000000000000000056 ) ;
#18614=CIRCLE ( 'NONE', #89890, 0.09999999999999939493 ) ;
#18627=SPHERICAL_SURFACE ( 'NONE', #6644, 0.1000000000000000056 ) ;
#18632=AXIS2_PLACEMENT_3D ( 'NONE', #110544, #53142, #36167 ) ;
#18642=CYLINDRICAL_SURFACE ( 'NONE', #101110, 0.09999999999999216460 ) ;
#18671=VERTEX_POINT ( 'NONE', #225976 ) ;
#18731=ORIENTED_EDGE ( 'NONE', *, *, #217651, .T. ) ;
#18757=CARTESIAN_POINT ( 'NONE',  ( 21.14999999999999503, 4.184122562697137226, -245.3714803909117279 ) ) ;
#18770=ORIENTED_EDGE ( 'NONE', *, *, #213862, .F. ) ;
#18777=CARTESIAN_POINT ( 'NONE',  ( -21.14999999999999858, 10.21728496540352182, -227.9671432372868765 ) ) ;
#18789=CARTESIAN_POINT ( 'NONE',  ( -20.85000000000000142, 43.26562470876307742, -245.1245614952171081 ) ) ;
#18826=CARTESIAN_POINT ( 'NONE',  ( -23.15000000000000213, 23.34004772283015328, -229.2004250369967338 ) ) ;
#18893=TOROIDAL_SURFACE ( 'NONE', #239664, 0.2000000000000000111, 0.1000000000000000056 ) ;
#18924=DIRECTION ( 'NONE',  ( 0.000000000000000000, -0.8814952561688430555, 0.4721928772777346239 ) ) ;
#18999=DIRECTION ( 'NONE',  ( 0.000000000000000000, 0.8814952561688429444, -0.4721928772777345684 ) ) ;
#19002=CARTESIAN_POINT ( 'NONE',  ( -23.25000000000000000, 24.26958830762006869, -252.6664436919618879 ) ) ;
#19018=EDGE_CURVE ( 'NONE', #91747, #257602, #232918, .T. ) ;
#19032=CARTESIAN_POINT ( 'NONE',  ( -18.51555513499602412, 9.055083425720873436, -245.3745321141128670 ) ) ;
#19039=ORIENTED_EDGE ( 'NONE', *, *, #212330, .F. ) ;
#19043=CARTESIAN_POINT ( 'NONE',  ( 21.04999999999999716, 10.01651311888475249, -228.1334776613284987 ) ) ;
#19066=EDGE_LOOP ( 'NONE', ( #158436, #99733, #129575, #39325 ) ) ;
#19067=DIRECTION ( 'NONE',  ( -1.000000000000000000, -0.000000000000000000, -0.000000000000000000 ) ) ;
#19083=DIRECTION ( 'NONE',  ( 1.000000000000000000, 0.000000000000000000, 0.000000000000000000 ) ) ;
#19095=CARTESIAN_POINT ( 'NONE',  ( 21.05000000000000071, 11.46684968301824625, -245.9610388612851750 ) ) ;
#19111=ORIENTED_EDGE ( 'NONE', *, *, #104104, .F. ) ;
#19122=B_SPLINE_CURVE_WITH_KNOTS ( 'NONE', 3,
 ( #57406, #59969, #1284, #136956, #159123, #37887, #61279, #202079 ),
 .UNSPECIFIED., .F., .F.,
 ( 4, 2, 2, 4 ),
 ( 0.000000000000000000, 0.0001094981963948526792, 0.0002189963927897053584, 0.0004379927855794107168 ),
 .UNSPECIFIED. ) ;
#19144=ORIENTED_EDGE ( 'NONE', *, *, #36135, .T. ) ;
#19158=VERTEX_POINT ( 'NONE', #55694 ) ;
#19159=DIRECTION ( 'NONE',  ( 1.000000000000000000, 0.000000000000000000, 0.000000000000000000 ) ) ;
#19184=CARTESIAN_POINT ( 'NONE',  ( -22.48660254037843487, 12.58580559757028183, -223.4396719342083770 ) ) ;
#19201=LINE ( 'NONE', #158743, #209340 ) ;
#19215=AXIS2_PLACEMENT_3D ( 'NONE', #2108, #81625, #118227 ) ;
#19249=CARTESIAN_POINT ( 'NONE',  ( 20.94999999999999929, 46.32970330538243786, -243.0551226933711746 ) ) ;
#19255=ORIENTED_EDGE ( 'NONE', *, *, #134150, .T. ) ;
#19269=CARTESIAN_POINT ( 'NONE',  ( 22.00356870068858228, 0.7342531111018623102, -230.3072997391775800 ) ) ;
#19279=CARTESIAN_POINT ( 'NONE',  ( -21.05000000000000071, 18.92285928089247804, -233.3572654221044900 ) ) ;
#19290=EDGE_LOOP ( 'NONE', ( #156411, #38523, #109732, #129186 ) ) ;
#19296=AXIS2_PLACEMENT_3D ( 'NONE', #152728, #75735, #117421 ) ;
#19319=VERTEX_POINT ( 'NONE', #867 ) ;
#19336=CYLINDRICAL_SURFACE ( 'NONE', #103511, 0.09999999999999939493 ) ;
#19356=CIRCLE ( 'NONE', #252379, 12.87500000000000000 ) ;
#19368=ORIENTED_EDGE ( 'NONE', *, *, #256839, .F. ) ;
#19381=DIRECTION ( 'NONE',  ( -1.000000000000000000, 0.000000000000000000, 0.000000000000000000 ) ) ;
#19392=VECTOR ( 'NONE', #46830, 1000.000000000000000 ) ;
#19399=CIRCLE ( 'NONE', #185982, 0.1000000000000013933 ) ;
#19400=EDGE_LOOP ( 'NONE', ( #143498, #183961, #162501, #61480 ) ) ;
#19416=DIRECTION ( 'NONE',  ( 0.000000000000000000, 0.8814952561688437216, -0.4721928772777334582 ) ) ;
#19477=EDGE_CURVE ( 'NONE', #28426, #129778, #112744, .T. ) ;
#19486=CARTESIAN_POINT ( 'NONE',  ( -18.59999999999999787, 1.091828907200461884, -220.1187534104809913 ) ) ;
#19518=AXIS2_PLACEMENT_3D ( 'NONE', #62620, #3925, #70350 ) ;
#19549=CARTESIAN_POINT ( 'NONE',  ( 22.57856590037849287, -3.230736822513305295, -228.1880465021345685 ) ) ;
#19556=CIRCLE ( 'NONE', #240134, 12.87500000000000178 ) ;
#19570=VERTEX_POINT ( 'NONE', #153284 ) ;
#19588=DIRECTION ( 'NONE',  ( 0.000000000000000000, 0.8814952561688430555, -0.4721928772777346239 ) ) ;
#19591=DIRECTION ( 'NONE',  ( -0.000000000000000000, 0.4721928772777347905, 0.8814952561688430555 ) ) ;
#19594=VERTEX_POINT ( 'NONE', #94540 ) ;
#19597=ORIENTED_EDGE ( 'NONE', *, *, #48994, .T. ) ;
#19600=AXIS2_PLACEMENT_3D ( 'NONE', #211217, #190392, #127840 ) ;
#19611=CARTESIAN_POINT ( 'NONE',  ( 20.04142135623730070, 34.35873842494069663, -235.1028360029684166 ) ) ;
#19627=CIRCLE ( 'NONE', #206868, 0.1000000000000075273 ) ;
#19656=CARTESIAN_POINT ( 'NONE',  ( -18.59999999999999787, 22.34215363070824623, -231.2750834139128528 ) ) ;
#19658=TOROIDAL_SURFACE ( 'NONE', #28040, 0.4000000000000012990, 0.1000000000000000056 ) ;
#19666=ORIENTED_EDGE ( 'NONE', *, *, #181840, .T. ) ;
#19678=EDGE_CURVE ( 'NONE', #62589, #135784, #50548, .T. ) ;
#19682=ORIENTED_EDGE ( 'NONE', *, *, #255911, .T. ) ;
#19683=ORIENTED_EDGE ( 'NONE', *, *, #182989, .T. ) ;
#19705=CARTESIAN_POINT ( 'NONE',  ( 20.94999999999999574, 14.81796439977981272, -236.5325475414793743 ) ) ;
#19709=VERTEX_POINT ( 'NONE', #83924 ) ;
#19716=EDGE_LOOP ( 'NONE', ( #126538, #153068, #256599, #61537, #148896 ) ) ;
#19754=CYLINDRICAL_SURFACE ( 'NONE', #172752, 0.1000000000000075273 ) ;
#19770=VERTEX_POINT ( 'NONE', #186962 ) ;
#19775=LINE ( 'NONE', #80992, #36957 ) ;
#19802=CARTESIAN_POINT ( 'NONE',  ( -23.15000000000000213, 26.18196512540240661, -241.1028522842020152 ) ) ;
#19808=AXIS2_PLACEMENT_3D ( 'NONE', #5283, #65288, #204783 ) ;
#19837=EDGE_CURVE ( 'NONE', #196423, #26265, #233750, .T. ) ;
#19846=EDGE_LOOP ( 'NONE', ( #124840, #182489, #109143, #1685, #72668 ) ) ;
#19889=EDGE_CURVE ( 'NONE', #62655, #182152, #121354, .T. ) ;
#19892=CARTESIAN_POINT ( 'NONE',  ( -20.87600722750343252, 46.46487552657982434, -243.0839400145317200 ) ) ;
#19894=AXIS2_PLACEMENT_3D ( 'NONE', #153084, #51333, #252128 ) ;
#19898=EDGE_CURVE ( 'NONE', #83686, #141820, #183682, .T. ) ;
#19900=CARTESIAN_POINT ( 'NONE',  ( 21.05000000000000071, 17.83900070254454562, -239.4698447713637677 ) ) ;
#19904=CARTESIAN_POINT ( 'NONE',  ( 20.94999999999999929, 16.44800918141279666, -240.8068063186265135 ) ) ;
#19921=EDGE_CURVE ( 'NONE', #195613, #207366, #42202, .T. ) ;
#19925=DIRECTION ( 'NONE',  ( 0.000000000000000000, 0.8814952561688476074, -0.4721928772777262417 ) ) ;
#19927=DIRECTION ( 'NONE',  ( 1.000000000000000000, 0.000000000000000000, 0.000000000000000000 ) ) ;
#19968=ADVANCED_FACE ( 'NONE', ( #193375 ), #63026, .T. ) ;
#20018=ORIENTED_EDGE ( 'NONE', *, *, #70319, .F. ) ;
#20058=TOROIDAL_SURFACE ( 'NONE', #49264, 4.149999999999999467, 0.1000000000000000056 ) ;
#20116=CIRCLE ( 'NONE', #11942, 0.09999999999999939493 ) ;
#20147=TOROIDAL_SURFACE ( 'NONE', #232550, 0.4000000000000003553, 0.1000000000000000056 ) ;
#20177=EDGE_CURVE ( 'NONE', #76904, #31642, #198823, .T. ) ;
#20184=AXIS2_PLACEMENT_3D ( 'NONE', #230054, #31881, #166261 ) ;
#20185=ADVANCED_FACE ( 'NONE', ( #202339 ), #163226, .T. ) ;
#20191=DIRECTION ( 'NONE',  ( 1.000000000000000000, 3.448943450116723568E-16, 6.438528483529607644E-16 ) ) ;
#20225=TOROIDAL_SURFACE ( 'NONE', #11864, 0.2000000000000000111, 0.1000000000000000056 ) ;
#20262=ORIENTED_EDGE ( 'NONE', *, *, #16237, .T. ) ;
#20267=CIRCLE ( 'NONE', #49293, 4.000000000000010658 ) ;
#20285=AXIS2_PLACEMENT_3D ( 'NONE', #106386, #103817, #221209 ) ;
#20307=DIRECTION ( 'NONE',  ( 0.000000000000000000, -0.8496786552930076786, -0.5273008465188218086 ) ) ;
#20314=DIRECTION ( 'NONE',  ( 1.000000000000000000, 0.000000000000000000, 0.000000000000000000 ) ) ;
#20357=DIRECTION ( 'NONE',  ( 0.000000000000000000, 0.8814952561688438326, -0.4721928772777330696 ) ) ;
#20398=ORIENTED_EDGE ( 'NONE', *, *, #228667, .T. ) ;
#20403=ORIENTED_EDGE ( 'NONE', *, *, #140, .F. ) ;
#20452=ADVANCED_FACE ( 'NONE', ( #190031 ), #191343, .T. ) ;
#20469=ORIENTED_EDGE ( 'NONE', *, *, #189107, .T. ) ;
#20488=CARTESIAN_POINT ( 'NONE',  ( -21.05000000000000071, 16.44800918141279311, -240.8068063186265135 ) ) ;
#20528=DIRECTION ( 'NONE',  ( -1.000000000000000000, 0.000000000000000000, 0.000000000000000000 ) ) ;
#20530=AXIS2_PLACEMENT_3D ( 'NONE', #49321, #166742, #67598 ) ;
#20532=CARTESIAN_POINT ( 'NONE',  ( 18.59999999999997655, 36.65892442174935439, -249.5511627012433848 ) ) ;
#20547=DIRECTION ( 'NONE',  ( -0.000000000000000000, -0.4721928772777343464, -0.8814952561688431665 ) ) ;
#20564=DIRECTION ( 'NONE',  ( 0.000000000000000000, 0.8814952561688428334, -0.4721928772777350125 ) ) ;
#20574=CARTESIAN_POINT ( 'NONE',  ( 21.07016717457008426, 1.556953976783223004, -230.7479980709940435 ) ) ;
#20576=ORIENTED_EDGE ( 'NONE', *, *, #25672, .T. ) ;
#20582=ORIENTED_EDGE ( 'NONE', *, *, #66136, .F. ) ;
#20613=CARTESIAN_POINT ( 'NONE',  ( 18.49999999999999289, 43.18640298906419162, -245.2812653309023574 ) ) ;
#20637=FACE_OUTER_BOUND ( 'NONE', #114303, .T. ) ;
#20651=CARTESIAN_POINT ( 'NONE',  ( 21.05933563467872460, 22.94152016742551226, -230.0368372691647778 ) ) ;
#20661=VERTEX_POINT ( 'NONE', #122928 ) ;
#20679=CIRCLE ( 'NONE', #49878, 11.80000000000000782 ) ;
#20680=DIRECTION ( 'NONE',  ( 1.000000000000000000, 1.394253735153569469E-16, 2.602809386958778209E-16 ) ) ;
#20717=ORIENTED_EDGE ( 'NONE', *, *, #94085, .T. ) ;
#20726=DIRECTION ( 'NONE',  ( 0.000000000000000000, 0.8814952561688437216, -0.4721928772777334582 ) ) ;
#20737=CARTESIAN_POINT ( 'NONE',  ( -18.59999999999999787, 31.44980407958351165, -233.5445995079518866 ) ) ;
#20739=ADVANCED_FACE ( 'NONE', ( #86319 ), #184161, .T. ) ;
#20783=DIRECTION ( 'NONE',  ( 0.000000000000000000, -0.9446535261619708468, 0.3280696808755038663 ) ) ;
#20785=DIRECTION ( 'NONE',  ( 0.000000000000000000, 0.8814952561688430555, -0.4721928772777346239 ) ) ;
#20814=EDGE_CURVE ( 'NONE', #57307, #172354, #212422, .T. ) ;
#20841=VECTOR ( 'NONE', #178387, 1000.000000000000000 ) ;
#20900=ORIENTED_EDGE ( 'NONE', *, *, #32023, .F. ) ;
#20923=EDGE_LOOP ( 'NONE', ( #176936, #14481, #21869, #236083 ) ) ;
#20945=VECTOR ( 'NONE', #184005, 1000.000000000000000 ) ;
#20946=VERTEX_POINT ( 'NONE', #8760 ) ;
#20967=ORIENTED_EDGE ( 'NONE', *, *, #62578, .F. ) ;
#20969=B_SPLINE_CURVE_WITH_KNOTS ( 'NONE', 3,
 ( #221624, #39193, #122569, #63861, #160427, #202094, #179971, #1299, #143395, #239943, #2589, #61295, #140834, #121307, #58700, #200809, #44310, #157876, #22187 ),
 .UNSPECIFIED., .F., .F.,
 ( 4, 3, 3, 3, 3, 3, 4 ),
 ( 0.000000000000000000, 2.646747978908389238E-05, 5.271166642128361261E-05, 9.008788829883987372E-05, 0.0001426648776560936627, 0.0001897378458659669401, 0.0001917382627806129159 ),
 .UNSPECIFIED. ) ;
#20988=ORIENTED_EDGE ( 'NONE', *, *, #112739, .T. ) ;
#20993=AXIS2_PLACEMENT_3D ( 'NONE', #249772, #151985, #112828 ) ;
#21002=ORIENTED_EDGE ( 'NONE', *, *, #162874, .T. ) ;
#21030=VERTEX_POINT ( 'NONE', #12629 ) ;
#21047=AXIS2_PLACEMENT_3D ( 'NONE', #115076, #236299, #58916 ) ;
#21055=CARTESIAN_POINT ( 'NONE',  ( -20.94999999999999929, 43.08613539620618837, -254.3146655184800409 ) ) ;
#21109=AXIS2_PLACEMENT_3D ( 'NONE', #221473, #224050, #182386 ) ;
#21112=DIRECTION ( 'NONE',  ( -0.000000000000000000, 0.8814952561688430555, -0.4721928772777346239 ) ) ;
#21129=CYLINDRICAL_SURFACE ( 'NONE', #125584, 0.5000000000000008882 ) ;
#21146=CYLINDRICAL_SURFACE ( 'NONE', #195017, 0.09999999999999507894 ) ;
#21151=DIRECTION ( 'NONE',  ( 1.000000000000000000, -0.000000000000000000, -0.000000000000000000 ) ) ;
#21173=CARTESIAN_POINT ( 'NONE',  ( -23.25000000000000000, 12.67709964810647882, -223.3751320524553705 ) ) ;
#21185=EDGE_CURVE ( 'NONE', #30609, #134482, #219776, .T. ) ;
#21207=CARTESIAN_POINT ( 'NONE',  ( -20.64999999999999858, 29.19585636832770703, -237.3287400596392445 ) ) ;
#21212=VERTEX_POINT ( 'NONE', #107537 ) ;
#21242=AXIS2_PLACEMENT_3D ( 'NONE', #163914, #29567, #109058 ) ;
#21259=( BOUNDED_CURVE ( )  B_SPLINE_CURVE ( 3, ( #172275, #13162, #155265, #14464 ),
 .UNSPECIFIED., .F., .F. ) 
 B_SPLINE_CURVE_WITH_KNOTS ( ( 4, 4 ),
 ( 4.712388980384689674, 6.283185307179586232 ),
 .UNSPECIFIED. ) 
 CURVE ( )  GEOMETRIC_REPRESENTATION_ITEM ( )  RATIONAL_B_SPLINE_CURVE ( ( 1.000000000000000000, 0.8047378541243649375, 0.8047378541243649375, 1.000000000000000000 ) ) 
 REPRESENTATION_ITEM ( '' )  );
#21296=ORIENTED_EDGE ( 'NONE', *, *, #56498, .F. ) ;
#21315=ORIENTED_EDGE ( 'NONE', *, *, #65380, .F. ) ;
#21344=TOROIDAL_SURFACE ( 'NONE', #121125, 0.6000000000000009770, 0.1000000000000000056 ) ;
#21359=CARTESIAN_POINT ( 'NONE',  ( -21.05000000000000071, 33.13294339707397995, -247.6623911921324463 ) ) ;
#21365=AXIS2_PLACEMENT_3D ( 'NONE', #230593, #169366, #127633 ) ;
#21403=CARTESIAN_POINT ( 'NONE',  ( 21.08035267497491105, 10.04573058037006028, -228.1122867900675715 ) ) ;
#21406=DIRECTION ( 'NONE',  ( 0.000000000000000000, 0.8814952561688429444, -0.4721928772777348460 ) ) ;
#21408=VECTOR ( 'NONE', #251061, 1000.000000000000000 ) ;
#21420=AXIS2_PLACEMENT_3D ( 'NONE', #132390, #15026, #172852 ) ;
#21437=DIRECTION ( 'NONE',  ( -7.304098846218132695E-16, -0.4721928772777346794, -0.8814952561688431665 ) ) ;
#21538=CARTESIAN_POINT ( 'NONE',  ( -18.59999999999999787, 22.43030315632513094, -231.3223027016406093 ) ) ;
#21560=CIRCLE ( 'NONE', #38316, 0.09999999999999469036 ) ;
#21566=ORIENTED_EDGE ( 'NONE', *, *, #158184, .F. ) ;
#21587=AXIS2_PLACEMENT_3D ( 'NONE', #181871, #184427, #99727 ) ;
#21609=ORIENTED_EDGE ( 'NONE', *, *, #81415, .T. ) ;
#21616=ORIENTED_EDGE ( 'NONE', *, *, #88512, .T. ) ;
#21646=CARTESIAN_POINT ( 'NONE',  ( 22.50000000000000355, -3.119487940400186954, -228.1911993711476043 ) ) ;
#21667=DIRECTION ( 'NONE',  ( -0.000000000000000000, 0.4721928772777345684, 0.8814952561688429444 ) ) ;
#21681=VECTOR ( 'NONE', #162992, 1000.000000000000000 ) ;
#21688=DIRECTION ( 'NONE',  ( 0.000000000000000000, 0.8814952561688368382, -0.4721928772777462813 ) ) ;
#21708=VERTEX_POINT ( 'NONE', #142503 ) ;
#21732=VERTEX_POINT ( 'NONE', #43424 ) ;
#21734=CIRCLE ( 'NONE', #84199, 0.09999999999999939493 ) ;
#21792=DIRECTION ( 'NONE',  ( 1.000000000000000000, 0.000000000000000000, 0.000000000000000000 ) ) ;
#21801=CARTESIAN_POINT ( 'NONE',  ( -23.15000000000000213, 1.627786319807483340, -244.0021210468063089 ) ) ;
#21802=CARTESIAN_POINT ( 'NONE',  ( -21.05000000000000071, 10.21728496540351827, -227.9671432372868480 ) ) ;
#21834=DIRECTION ( 'NONE',  ( -1.000000000000000000, -0.000000000000000000, -0.000000000000000000 ) ) ;
#21843=AXIS2_PLACEMENT_3D ( 'NONE', #71630, #233282, #14232 ) ;
#21869=ORIENTED_EDGE ( 'NONE', *, *, #162010, .T. ) ;
#21886=CARTESIAN_POINT ( 'NONE',  ( -20.93284271247462058, 36.02367271998545561, -235.8812521208699309 ) ) ;
#21902=CARTESIAN_POINT ( 'NONE',  ( -22.47120815636973745, -3.126878263853650530, -228.2062078246864303 ) ) ;
#21921=CARTESIAN_POINT ( 'NONE',  ( -20.64999999999999858, 19.73066058418984170, -238.2142830767208466 ) ) ;
#21922=CARTESIAN_POINT ( 'NONE',  ( 21.05000000000000071, 36.02918351690956200, -236.0543695120161090 ) ) ;
#21943=VECTOR ( 'NONE', #90599, 1000.000000000000000 ) ;
#21961=DIRECTION ( 'NONE',  ( 2.710505431213776862E-16, -0.4721928772777346239, -0.8814952561688430555 ) ) ;
#21978=TOROIDAL_SURFACE ( 'NONE', #221848, 1.900000000000002576, 0.1000000000000000056 ) ;
#22020=ORIENTED_EDGE ( 'NONE', *, *, #48335, .T. ) ;
#22044=DIRECTION ( 'NONE',  ( 0.000000000000000000, 0.8814952561688476074, -0.4721928772777262417 ) ) ;
#22085=CARTESIAN_POINT ( 'NONE',  ( 18.59999999999999076, 18.26942912180536638, -237.6183358664095238 ) ) ;
#22097=DIRECTION ( 'NONE',  ( 2.694716079187271467E-16, -0.4721928772777345129, -0.8814952561688430555 ) ) ;
#22103=DIRECTION ( 'NONE',  ( 1.296989514748957725E-15, -0.5986962832864934914, -0.8009761297185696849 ) ) ;
#22107=AXIS2_PLACEMENT_3D ( 'NONE', #206953, #127415, #28353 ) ;
#22134=DIRECTION ( 'NONE',  ( 0.7071067811865476838, -0.3338907855510733769, -0.6233112732207617412 ) ) ;
#22160=DIRECTION ( 'NONE',  ( 0.000000000000000000, 0.9424537609900496271, 0.3343365196859450217 ) ) ;
#22170=CARTESIAN_POINT ( 'NONE',  ( 18.59999999999999432, 18.11150788191476124, -237.7585516551410478 ) ) ;
#22173=FACE_OUTER_BOUND ( 'NONE', #80954, .T. ) ;
#22175=CARTESIAN_POINT ( 'NONE',  ( -23.25000000000000000, 27.77927773649450316, -239.9732258281457860 ) ) ;
#22185=CARTESIAN_POINT ( 'NONE',  ( 18.44444291854883033, 38.02111363811317091, -261.0467631091868839 ) ) ;
#22187=CARTESIAN_POINT ( 'NONE',  ( -18.50000000000000000, 46.32970330538243786, -243.0551226933711746 ) ) ;
#22198=DIRECTION ( 'NONE',  ( 0.000000000000000000, 0.03181660087583047802, -0.9994937237965568766 ) ) ;
#22200=CARTESIAN_POINT ( 'NONE',  ( -23.15000000000000213, 23.34004772283015328, -229.2004250369967338 ) ) ;
#22216=EDGE_LOOP ( 'NONE', ( #65696, #89565, #211231, #9457 ) ) ;
#22220=DIRECTION ( 'NONE',  ( -1.000000000000000000, 0.000000000000000000, 0.000000000000000000 ) ) ;
#22233=AXIS2_PLACEMENT_3D ( 'NONE', #7151, #230068, #47557 ) ;
#22253=DIRECTION ( 'NONE',  ( 0.000000000000000000, 0.8814952561688476074, -0.4721928772777262417 ) ) ;
#22254=ORIENTED_EDGE ( 'NONE', *, *, #77312, .T. ) ;
#22274=CARTESIAN_POINT ( 'NONE',  ( 20.94999999999999929, 18.82290990851282331, -233.3604470821920529 ) ) ;
#22322=EDGE_CURVE ( 'NONE', #235787, #214842, #161981, .T. ) ;
#22377=DIRECTION ( 'NONE',  ( 2.659396599871503240E-15, 0.9858629823651696711, 0.1675535138457361073 ) ) ;
#22388=EDGE_CURVE ( 'NONE', #31578, #81676, #199387, .T. ) ;
#22398=AXIS2_PLACEMENT_3D ( 'NONE', #78466, #160616, #64052 ) ;
#22414=SPHERICAL_SURFACE ( 'NONE', #187635, 0.1000000000000000056 ) ;
#22468=FACE_BOUND ( 'NONE', #45603, .T. ) ;
#22469=CIRCLE ( 'NONE', #255623, 0.09999999999999939493 ) ;
#22475=CARTESIAN_POINT ( 'NONE',  ( -20.85000000000000142, 36.65892442174935439, -249.5511627012433848 ) ) ;
#22477=CARTESIAN_POINT ( 'NONE',  ( -23.15000000000000213, 28.42524210734032053, -258.3567845160494585 ) ) ;
#22480=AXIS2_PLACEMENT_3D ( 'NONE', #159276, #103112, #238801 ) ;
#22485=ORIENTED_EDGE ( 'NONE', *, *, #187398, .T. ) ;
#22501=AXIS2_PLACEMENT_3D ( 'NONE', #55903, #76774, #19381 ) ;
#22553=ORIENTED_EDGE ( 'NONE', *, *, #85293, .F. ) ;
#22585=ADVANCED_FACE ( 'NONE', ( #256805 ), #216101, .F. ) ;
#22607=ADVANCED_FACE ( 'NONE', ( #200746 ), #126337, .F. ) ;
#22617=ORIENTED_EDGE ( 'NONE', *, *, #87980, .F. ) ;
#22624=ORIENTED_EDGE ( 'NONE', *, *, #123355, .F. ) ;
#22634=CARTESIAN_POINT ( 'NONE',  ( -20.64999999999999858, 11.36448785225375602, -246.7787679937655980 ) ) ;
#22645=CARTESIAN_POINT ( 'NONE',  ( -23.15000000000000213, 2.272311100394799332, -217.9150152700588592 ) ) ;
#22660=CARTESIAN_POINT ( 'NONE',  ( -23.15000000000000213, 35.97645343225766368, -235.9694016464868298 ) ) ;
#22662=AXIS2_PLACEMENT_3D ( 'NONE', #252493, #235501, #129971 ) ;
#22686=CARTESIAN_POINT ( 'NONE',  ( 21.08621493067296271, 10.07738939570518255, -228.1092937118111195 ) ) ;
#22690=CIRCLE ( 'NONE', #47583, 0.3999999999999994671 ) ;
#22693=EDGE_CURVE ( 'NONE', #99386, #194512, #183754, .T. ) ;
#22704=ORIENTED_EDGE ( 'NONE', *, *, #226216, .T. ) ;
#22710=CARTESIAN_POINT ( 'NONE',  ( 20.94999999999999929, 20.97908333644147660, -233.6079013178409411 ) ) ;
#22713=DIRECTION ( 'NONE',  ( 1.000000000000000000, 0.000000000000000000, 0.000000000000000000 ) ) ;
#22721=CARTESIAN_POINT ( 'NONE',  ( -18.45068461519106151, 8.880466068112633948, -245.4328380456663581 ) ) ;
#22729=CIRCLE ( 'NONE', #251657, 11.64999999999999325 ) ;
#22738=CARTESIAN_POINT ( 'NONE',  ( 18.59999999999999076, 29.08883969319483498, -237.9520757887960940 ) ) ;
#22745=AXIS2_PLACEMENT_3D ( 'NONE', #24099, #125731, #7068 ) ;
#22759=EDGE_CURVE ( 'NONE', #30618, #201330, #8962, .T. ) ;
#22770=ORIENTED_EDGE ( 'NONE', *, *, #13671, .F. ) ;
#22783=CARTESIAN_POINT ( 'NONE',  ( 21.05000000000000071, 7.128833340093095217, -233.7327013124392749 ) ) ;
#22784=AXIS2_PLACEMENT_3D ( 'NONE', #86601, #145303, #141460 ) ;
#22791=DIRECTION ( 'NONE',  ( -3.787827842127534447E-15, -0.2438576117979244784, 0.9698110461157951612 ) ) ;
#22824=ADVANCED_FACE ( 'NONE', ( #88471 ), #247570, .F. ) ;
#22846=VERTEX_POINT ( 'NONE', #11546 ) ;
#22880=DIRECTION ( 'NONE',  ( 1.000000000000000000, 0.000000000000000000, 0.000000000000000000 ) ) ;
#22885=ORIENTED_EDGE ( 'NONE', *, *, #49141, .F. ) ;
#22935=CARTESIAN_POINT ( 'NONE',  ( 20.94999999999999929, 28.50120599808395028, -258.2149742250584268 ) ) ;
#22962=VECTOR ( 'NONE', #16110, 1000.000000000000114 ) ;
#23001=ORIENTED_EDGE ( 'NONE', *, *, #128538, .T. ) ;
#23012=ORIENTED_EDGE ( 'NONE', *, *, #235109, .T. ) ;
#23052=CYLINDRICAL_SURFACE ( 'NONE', #20285, 0.09999999999999939493 ) ;
#23068=CARTESIAN_POINT ( 'NONE',  ( 21.05000000000000071, 18.56623428888383387, -239.8594038951179073 ) ) ;
#23079=FACE_OUTER_BOUND ( 'NONE', #102954, .T. ) ;
#23147=ORIENTED_EDGE ( 'NONE', *, *, #146560, .T. ) ;
#23149=CARTESIAN_POINT ( 'NONE',  ( 23.14999999999999858, 20.66107731230508548, -234.7421556583769302 ) ) ;
#23155=CARTESIAN_POINT ( 'NONE',  ( -20.64999999999999858, 25.30967299857550401, -243.4716794062925374 ) ) ;
#23194=CARTESIAN_POINT ( 'NONE',  ( -22.39999999999999858, 12.54173083476182526, -223.4160622903444846 ) ) ;
#23195=EDGE_LOOP ( 'NONE', ( #245697, #251295, #807, #105704 ) ) ;
#23202=EDGE_CURVE ( 'NONE', #246412, #220499, #91409, .T. ) ;
#23210=CIRCLE ( 'NONE', #168981, 0.4999999999999970024 ) ;
#23211=EDGE_LOOP ( 'NONE', ( #159291, #50543, #35795, #10708, #28136, #168586, #238435, #59772 ) ) ;
#23249=EDGE_LOOP ( 'NONE', ( #31604, #75251, #204849, #87713 ) ) ;
#23297=ORIENTED_EDGE ( 'NONE', *, *, #115565, .F. ) ;
#23298=CARTESIAN_POINT ( 'NONE',  ( -20.94999999999999929, 13.54362637910787370, -238.4879411198429580 ) ) ;
#23314=CARTESIAN_POINT ( 'NONE',  ( -21.55000000000000071, 21.39776787615277343, -233.0380739262505472 ) ) ;
#23315=CARTESIAN_POINT ( 'NONE',  ( -21.33487959338958007, 10.30459399514276164, -227.8041537064418662 ) ) ;
#23371=CARTESIAN_POINT ( 'NONE',  ( 22.39999999999999503, 12.54173083476182882, -223.4160622903444562 ) ) ;
#23396=CARTESIAN_POINT ( 'NONE',  ( -20.64999999999999858, 38.33376540847015690, -250.4483291680710693 ) ) ;
#23403=DIRECTION ( 'NONE',  ( 0.000000000000000000, 0.8814952561688476074, -0.4721928772777262417 ) ) ;
#23421=FACE_OUTER_BOUND ( 'NONE', #163247, .T. ) ;
#23473=CYLINDRICAL_SURFACE ( 'NONE', #15105, 0.1000000000000053763 ) ;
#23493=DIRECTION ( 'NONE',  ( 0.000000000000000000, 0.1397316906016290161, -0.9901894034181595305 ) ) ;
#23497=DIRECTION ( 'NONE',  ( 1.000000000000000000, 0.000000000000000000, 0.000000000000000000 ) ) ;
#23524=DIRECTION ( 'NONE',  ( 1.000000000000000000, 0.000000000000000000, 0.000000000000000000 ) ) ;
#23541=AXIS2_PLACEMENT_3D ( 'NONE', #4615, #26793, #84108 ) ;
#23586=DIRECTION ( 'NONE',  ( 0.000000000000000000, 0.8814952561688428334, -0.4721928772777349570 ) ) ;
#23595=ORIENTED_EDGE ( 'NONE', *, *, #141500, .T. ) ;
#23622=ORIENTED_EDGE ( 'NONE', *, *, #172451, .T. ) ;
#23627=DIRECTION ( 'NONE',  ( 0.000000000000000000, -0.8814952561688444987, 0.4721928772777320149 ) ) ;
#23629=ORIENTED_EDGE ( 'NONE', *, *, #105893, .T. ) ;
#23630=DIRECTION ( 'NONE',  ( 1.000000000000000000, 0.000000000000000000, 0.000000000000000000 ) ) ;
#23660=ORIENTED_EDGE ( 'NONE', *, *, #151970, .T. ) ;
#23702=CARTESIAN_POINT ( 'NONE',  ( -21.05000000000000071, 3.338403738567107926, -231.7022719401450388 ) ) ;
#23707=CIRCLE ( 'NONE', #136066, 0.1000000000000076522 ) ;
#23733=CARTESIAN_POINT ( 'NONE',  ( 21.97500000000000497, 22.53103078161933936, -230.9224853114453140 ) ) ;
#23737=CARTESIAN_POINT ( 'NONE',  ( 23.14999999999999503, 38.38020821401235594, -234.4776589466471819 ) ) ;
#23760=FACE_OUTER_BOUND ( 'NONE', #7549, .T. ) ;
#23775=CYLINDRICAL_SURFACE ( 'NONE', #90446, 0.1000000000000013933 ) ;
#23777=CARTESIAN_POINT ( 'NONE',  ( -21.59142135623730852, 21.63386431479164784, -232.5973262981661094 ) ) ;
#23784=EDGE_LOOP ( 'NONE', ( #231979, #24575, #160742, #180064 ) ) ;
#23811=AXIS2_PLACEMENT_3D ( 'NONE', #14722, #12152, #91662 ) ;
#23820=VERTEX_POINT ( 'NONE', #149102 ) ;
#23844=AXIS2_PLACEMENT_3D ( 'NONE', #177713, #219362, #78568 ) ;
#23845=EDGE_CURVE ( 'NONE', #88893, #65641, #91765, .T. ) ;
#23863=FACE_OUTER_BOUND ( 'NONE', #251869, .T. ) ;
#23880=CARTESIAN_POINT ( 'NONE',  ( -20.94999999999999929, 16.44800918141279666, -240.8068063186265135 ) ) ;
#23882=FACE_OUTER_BOUND ( 'NONE', #182960, .T. ) ;
#23895=AXIS2_PLACEMENT_3D ( 'NONE', #6703, #221874, #2834 ) ;
#23901=ORIENTED_EDGE ( 'NONE', *, *, #93525, .T. ) ;
#23929=FACE_OUTER_BOUND ( 'NONE', #19716, .T. ) ;
#23931=CIRCLE ( 'NONE', #173806, 0.1000000000000013933 ) ;
#23933=DIRECTION ( 'NONE',  ( 0.000000000000000000, 0.8814952561688430555, -0.4721928772777346239 ) ) ;
#23964=CARTESIAN_POINT ( 'NONE',  ( -18.50000000000000000, 19.02280865327213277, -233.3540837620168986 ) ) ;
#23971=ORIENTED_EDGE ( 'NONE', *, *, #15570, .T. ) ;
#23975=DIRECTION ( 'NONE',  ( 0.000000000000000000, -0.4721928772777346239, -0.8814952561688430555 ) ) ;
#23990=EDGE_CURVE ( 'NONE', #157381, #77718, #66824, .T. ) ;
#23991=DIRECTION ( 'NONE',  ( 1.000000000000000000, 0.000000000000000000, 0.000000000000000000 ) ) ;
#23994=CARTESIAN_POINT ( 'NONE',  ( 21.00000000000000000, 30.46448808713892831, -235.1722212069449256 ) ) ;
#24006=CIRCLE ( 'NONE', #119876, 0.09999999999999986677 ) ;
#24007=CARTESIAN_POINT ( 'NONE',  ( 18.59999999999999076, 30.68102565639535939, -234.7679863078877531 ) ) ;
#24009=AXIS2_PLACEMENT_3D ( 'NONE', #248333, #8447, #185791 ) ;
#24018=DIRECTION ( 'NONE',  ( 0.000000000000000000, 0.9371753822965315228, -0.3488585713686133682 ) ) ;
#24033=TOROIDAL_SURFACE ( 'NONE', #236398, 0.2000000000000000111, 0.1000000000000000056 ) ;
#24049=VERTEX_POINT ( 'NONE', #6786 ) ;
#24057=DIRECTION ( 'NONE',  ( -3.469446951953352918E-14, 0.4721928772776973204, 0.8814952561688629284 ) ) ;
#24069=CARTESIAN_POINT ( 'NONE',  ( -18.59999999999999787, 30.27561093622783517, -235.5248193094124645 ) ) ;
#24070=AXIS2_PLACEMENT_3D ( 'NONE', #230438, #51777, #12702 ) ;
#24075=ORIENTED_EDGE ( 'NONE', *, *, #61602, .T. ) ;
#24099=CARTESIAN_POINT ( 'NONE',  ( 21.05000000000000071, 36.65892442174935439, -249.5511627012433848 ) ) ;
#24162=ORIENTED_EDGE ( 'NONE', *, *, #13681, .T. ) ;
#24222=AXIS2_PLACEMENT_3D ( 'NONE', #214241, #238940, #55124 ) ;
#24245=ORIENTED_EDGE ( 'NONE', *, *, #36135, .F. ) ;
#24256=CARTESIAN_POINT ( 'NONE',  ( -20.94999999999999929, 43.35377423437995503, -245.1717807829448930 ) ) ;
#24272=VECTOR ( 'NONE', #189395, 1000.000000000000000 ) ;
#24298=EDGE_CURVE ( 'NONE', #153949, #57412, #158606, .T. ) ;
#24302=DIRECTION ( 'NONE',  ( 0.000000000000000000, 0.8814952561688430555, -0.4721928772777346239 ) ) ;
#24332=CIRCLE ( 'NONE', #115306, 0.09999999999999939493 ) ;
#24366=DIRECTION ( 'NONE',  ( -0.000000000000000000, 0.4721928772777345684, 0.8814952561688429444 ) ) ;
#24419=ORIENTED_EDGE ( 'NONE', *, *, #206019, .F. ) ;
#24445=CARTESIAN_POINT ( 'NONE',  ( 22.39999999999999503, 12.58895012248959944, -223.3279127647275857 ) ) ;
#24448=DIRECTION ( 'NONE',  ( 1.000000000000000000, 0.000000000000000000, 0.000000000000000000 ) ) ;
#24451=CARTESIAN_POINT ( 'NONE',  ( 23.14999999999999858, 34.81737220036618652, -252.9889942003018461 ) ) ;
#24478=VERTEX_POINT ( 'NONE', #112021 ) ;
#24498=CARTESIAN_POINT ( 'NONE',  ( 19.75857864376268935, 34.53503747617446606, -235.1972745784239578 ) ) ;
#24501=ORIENTED_EDGE ( 'NONE', *, *, #152657, .F. ) ;
#24520=EDGE_CURVE ( 'NONE', #5002, #18671, #28669, .T. ) ;
#24537=AXIS2_PLACEMENT_3D ( 'NONE', #175326, #77447, #233974 ) ;
#24545=EDGE_CURVE ( 'NONE', #42982, #186477, #187997, .T. ) ;
#24557=DIRECTION ( 'NONE',  ( 1.000000000000000000, 0.000000000000000000, 0.000000000000000000 ) ) ;
#24558=ORIENTED_EDGE ( 'NONE', *, *, #40442, .T. ) ;
#24575=ORIENTED_EDGE ( 'NONE', *, *, #196421, .T. ) ;
#24582=CARTESIAN_POINT ( 'NONE',  ( 21.05000000000000071, 18.65488991999774271, -228.0822300706204544 ) ) ;
#24591=CYLINDRICAL_SURFACE ( 'NONE', #131538, 0.09999999999999939493 ) ;
#24600=EDGE_CURVE ( 'NONE', #138276, #192532, #96391, .T. ) ;
#24601=ADVANCED_FACE ( 'NONE', ( #16772 ), #195417, .T. ) ;
#24645=DIRECTION ( 'NONE',  ( 1.000000000000000000, 0.000000000000000000, 0.000000000000000000 ) ) ;
#24651=CARTESIAN_POINT ( 'NONE',  ( 20.94999999999999929, 42.88650567345842290, -254.4176359484683871 ) ) ;
#24674=ORIENTED_EDGE ( 'NONE', *, *, #151628, .F. ) ;
#24713=ADVANCED_FACE ( 'NONE', ( #79266 ), #184618, .F. ) ;
#24723=FACE_OUTER_BOUND ( 'NONE', #244364, .T. ) ;
#24739=EDGE_LOOP ( 'NONE', ( #50791, #35786, #182866, #219446 ) ) ;
#24765=CARTESIAN_POINT ( 'NONE',  ( 18.47688499308725341, 38.09689311189373484, -261.0587169989327663 ) ) ;
#24770=EDGE_LOOP ( 'NONE', ( #249025, #22485, #152576, #53106 ) ) ;
#24778=ORIENTED_EDGE ( 'NONE', *, *, #146667, .T. ) ;
#24787=CARTESIAN_POINT ( 'NONE',  ( 23.14999999999999503, 2.319530388122574394, -217.8268657444419887 ) ) ;
#24824=DIRECTION ( 'NONE',  ( 0.000000000000000000, 0.8814952561694257005, -0.4721928772766468829 ) ) ;
#24836=ADVANCED_FACE ( 'NONE', ( #220089 ), #201193, .T. ) ;
#24845=ORIENTED_EDGE ( 'NONE', *, *, #187643, .T. ) ;
#24863=EDGE_CURVE ( 'NONE', #218506, #176897, #185656, .T. ) ;
#24893=EDGE_LOOP ( 'NONE', ( #100243, #234357, #70137, #172000 ) ) ;
#24928=ORIENTED_EDGE ( 'NONE', *, *, #138984, .F. ) ;
#24932=FACE_OUTER_BOUND ( 'NONE', #182929, .T. ) ;
#24940=LINE ( 'NONE', #44493, #94140 ) ;
#24953=AXIS2_PLACEMENT_3D ( 'NONE', #70575, #1252, #116098 ) ;
#24980=CIRCLE ( 'NONE', #178930, 0.1000000000000108025 ) ;
#25008=CARTESIAN_POINT ( 'NONE',  ( -22.59999999999999787, 12.61936297652653316, -223.3443501630868298 ) ) ;
#25010=LINE ( 'NONE', #124102, #218943 ) ;
#25036=ORIENTED_EDGE ( 'NONE', *, *, #22759, .F. ) ;
#25054=ORIENTED_EDGE ( 'NONE', *, *, #183512, .T. ) ;
#25057=EDGE_LOOP ( 'NONE', ( #229854, #5160, #239264, #128705 ) ) ;
#25077=CIRCLE ( 'NONE', #66749, 4.050000000000003375 ) ;
#25091=AXIS2_PLACEMENT_3D ( 'NONE', #135177, #204136, #105001 ) ;
#25117=CARTESIAN_POINT ( 'NONE',  ( -20.64999999999999858, 20.06933876993645782, -235.7297789824848451 ) ) ;
#25124=CIRCLE ( 'NONE', #58217, 7.791421356237317575 ) ;
#25129=DIRECTION ( 'NONE',  ( 1.000000000000000000, 0.000000000000000000, 0.000000000000000000 ) ) ;
#25156=FACE_OUTER_BOUND ( 'NONE', #153148, .T. ) ;
#25160=DIRECTION ( 'NONE',  ( 0.000000000000000000, -0.6410630849193120762, 0.7674881895858300940 ) ) ;
#25171=DIRECTION ( 'NONE',  ( -1.000000000000000000, 0.000000000000000000, 0.000000000000000000 ) ) ;
#25184=EDGE_LOOP ( 'NONE', ( #234187, #81864, #42268, #175693, #4708, #230029, #158670, #130065 ) ) ;
#25201=DIRECTION ( 'NONE',  ( 0.000000000000000000, -0.8814952561688430555, 0.4721928772777346239 ) ) ;
#25207=ORIENTED_EDGE ( 'NONE', *, *, #15947, .F. ) ;
#25224=ORIENTED_EDGE ( 'NONE', *, *, #240691, .T. ) ;
#25255=FACE_OUTER_BOUND ( 'NONE', #76323, .T. ) ;
#25297=EDGE_CURVE ( 'NONE', #170273, #231806, #64014, .T. ) ;
#25298=SPHERICAL_SURFACE ( 'NONE', #35956, 0.1000000000000000056 ) ;
#25316=CARTESIAN_POINT ( 'NONE',  ( 18.49999999999999289, 2.319530388122574394, -217.8268657444419887 ) ) ;
#25333=ORIENTED_EDGE ( 'NONE', *, *, #161069, .F. ) ;
#25364=EDGE_LOOP ( 'NONE', ( #111507, #126472, #244930, #190723, #91811, #153143, #255414, #194345, #40492, #114627, #184096, #221703, #33288, #56259, #191304, #90518 ) ) ;
#25374=DIRECTION ( 'NONE',  ( -0.000000000000000000, 0.8496786552930076786, 0.5273008465188218086 ) ) ;
#25382=EDGE_LOOP ( 'NONE', ( #153236, #114768, #238855, #253472 ) ) ;
#25392=ORIENTED_EDGE ( 'NONE', *, *, #75402, .T. ) ;
#25443=VERTEX_POINT ( 'NONE', #165204 ) ;
#25480=DIRECTION ( 'NONE',  ( 1.000000000000000000, 0.000000000000000000, 0.000000000000000000 ) ) ;
#25537=ORIENTED_EDGE ( 'NONE', *, *, #189107, .F. ) ;
#25546=ORIENTED_EDGE ( 'NONE', *, *, #181391, .T. ) ;
#25583=FACE_OUTER_BOUND ( 'NONE', #103893, .T. ) ;
#25592=ORIENTED_EDGE ( 'NONE', *, *, #24545, .F. ) ;
#25611=DIRECTION ( 'NONE',  ( 1.000000000000000000, 8.855395344894292773E-17, 1.653135691717061729E-16 ) ) ;
#25614=DIRECTION ( 'NONE',  ( 1.000000000000000000, 0.000000000000000000, 0.000000000000000000 ) ) ;
#25672=EDGE_CURVE ( 'NONE', #167145, #72511, #4411, .T. ) ;
#25676=CIRCLE ( 'NONE', #183892, 0.5000000000000147660 ) ;
#25698=ORIENTED_EDGE ( 'NONE', *, *, #8298, .T. ) ;
#25704=DIRECTION ( 'NONE',  ( -1.000000000000000000, 0.000000000000000000, 0.000000000000000000 ) ) ;
#25725=ORIENTED_EDGE ( 'NONE', *, *, #219455, .T. ) ;
#25733=CIRCLE ( 'NONE', #88240, 0.1000000000000013933 ) ;
#25756=DIRECTION ( 'NONE',  ( -0.000000000000000000, 0.4721928772777345684, 0.8814952561688429444 ) ) ;
#25761=CARTESIAN_POINT ( 'NONE',  ( 21.04999999999999716, 36.17635217701701578, -235.9630383263116187 ) ) ;
#25825=EDGE_LOOP ( 'NONE', ( #157068, #67976, #250781, #127409 ) ) ;
#25858=( BOUNDED_CURVE ( )  B_SPLINE_CURVE ( 3, ( #174866, #254326, #112288, #114838 ),
 .UNSPECIFIED., .F., .F. ) 
 B_SPLINE_CURVE_WITH_KNOTS ( ( 4, 4 ),
 ( 3.141592653589793116, 4.712388980384689674 ),
 .UNSPECIFIED. ) 
 CURVE ( )  GEOMETRIC_REPRESENTATION_ITEM ( )  RATIONAL_B_SPLINE_CURVE ( ( 1.000000000000000000, 0.8047378541243649375, 0.8047378541243649375, 1.000000000000000000 ) ) 
 REPRESENTATION_ITEM ( '' )  );
#25894=ORIENTED_EDGE ( 'NONE', *, *, #103570, .T. ) ;
#25899=DIRECTION ( 'NONE',  ( 0.000000000000000000, -0.4721928772777346239, -0.8814952561688430555 ) ) ;
#25909=LINE ( 'NONE', #10200, #59087 ) ;
#25953=DIRECTION ( 'NONE',  ( 0.000000000000000000, 0.8814952561688437216, -0.4721928772777334582 ) ) ;
#25958=CARTESIAN_POINT ( 'NONE',  ( -20.94999999999999929, 16.44800918141279666, -240.8068063186265135 ) ) ;
#25964=CIRCLE ( 'NONE', #229968, 0.1000000000000013933 ) ;
#25977=CARTESIAN_POINT ( 'NONE',  ( 23.14999999999999858, 38.42191493408704872, -250.4955484557988541 ) ) ;
#26024=CARTESIAN_POINT ( 'NONE',  ( -21.98333005346336932, 0.6286209188979320350, -230.2507154655492627 ) ) ;
#26038=EDGE_CURVE ( 'NONE', #198003, #28211, #160658, .T. ) ;
#26044=AXIS2_PLACEMENT_3D ( 'NONE', #129828, #211961, #33351 ) ;
#26050=DIRECTION ( 'NONE',  ( 1.000000000000000000, 0.000000000000000000, 0.000000000000000000 ) ) ;
#26083=VERTEX_POINT ( 'NONE', #159360 ) ;
#26095=ORIENTED_EDGE ( 'NONE', *, *, #228834, .T. ) ;
#26118=VERTEX_POINT ( 'NONE', #252664 ) ;
#26121=ADVANCED_FACE ( 'NONE', ( #54472 ), #146187, .T. ) ;
#26147=CARTESIAN_POINT ( 'NONE',  ( -20.94999999999999929, 40.27305497204160645, -251.4871534980821082 ) ) ;
#26167=ADVANCED_FACE ( 'NONE', ( #231854 ), #126352, .F. ) ;
#26170=CARTESIAN_POINT ( 'NONE',  ( 18.59999999999999076, 46.02130280899747561, -256.6489974955837852 ) ) ;
#26177=CARTESIAN_POINT ( 'NONE',  ( -21.14999999999999858, -3.187427350888460076, -228.3200064793908837 ) ) ;
#26187=CARTESIAN_POINT ( 'NONE',  ( -21.05000000000000071, 16.44800918141279311, -240.8068063186265135 ) ) ;
#26196=VECTOR ( 'NONE', #230883, 1000.000000000000000 ) ;
#26234=AXIS2_PLACEMENT_3D ( 'NONE', #215274, #92743, #114891 ) ;
#26265=VERTEX_POINT ( 'NONE', #80417 ) ;
#26279=AXIS2_PLACEMENT_3D ( 'NONE', #130830, #168726, #129558 ) ;
#26298=ADVANCED_FACE ( 'NONE', ( #115739 ), #2186, .T. ) ;
#26346=ORIENTED_EDGE ( 'NONE', *, *, #141038, .F. ) ;
#26393=DIRECTION ( 'NONE',  ( -1.000000000000000000, 0.000000000000000000, 0.000000000000000000 ) ) ;
#26435=DIRECTION ( 'NONE',  ( 0.000000000000000000, 0.8814952561688438326, -0.4721928772777331806 ) ) ;
#26459=VECTOR ( 'NONE', #93063, 1000.000000000000227 ) ;
#26490=ORIENTED_EDGE ( 'NONE', *, *, #161803, .F. ) ;
#26534=ADVANCED_FACE ( 'NONE', ( #71187, #54161 ), #51564, .F. ) ;
#26536=DIRECTION ( 'NONE',  ( 0.000000000000000000, 0.8814952561688476074, -0.4721928772777262417 ) ) ;
#26542=ADVANCED_FACE ( 'NONE', ( #210674 ), #218354, .T. ) ;
#26583=CARTESIAN_POINT ( 'NONE',  ( 21.14999999999999858, 12.71802988599559470, -223.5105008658000258 ) ) ;
#26593=( BOUNDED_SURFACE ( )  B_SPLINE_SURFACE ( 3, 2, ( 
 ( #238103, #119467, #101112 ),
 ( #21646, #217245, #102419 ),
 ( #240679, #256322, #56874 ),
 ( #37367, #62060, #201548 ) ),
 .UNSPECIFIED., .F., .F., .F. ) 
 B_SPLINE_SURFACE_WITH_KNOTS ( ( 4, 4 ),
 ( 3, 3 ),
 ( -2.087089182034596035E-18, 0.0003124336600439759455 ),
 ( 0.000000000000000000, 1.000000000000000000 ),
 .UNSPECIFIED. ) 
 GEOMETRIC_REPRESENTATION_ITEM ( )  RATIONAL_B_SPLINE_SURFACE ( (
 ( 1.000000000000000000, 0.7071067811865205943, 1.000000000000000000),
 ( 1.000000000000000000, 0.7089187706049330240, 1.000000000000000000),
 ( 1.000000000000000000, 0.7039288185051130187, 1.000000000000000000),
 ( 1.000000000000000000, 0.7040654476016154906, 1.000000000000000000) ) ) 
 REPRESENTATION_ITEM ( '' )  SURFACE ( )  );
#26599=CARTESIAN_POINT ( 'NONE',  ( 21.07928932188134397, 10.02993822722304351, -228.1074463178677263 ) ) ;
#26635=FACE_OUTER_BOUND ( 'NONE', #176204, .T. ) ;
#26643=ORIENTED_EDGE ( 'NONE', *, *, #254348, .F. ) ;
#26645=CARTESIAN_POINT ( 'NONE',  ( -23.25000000000000000, 7.128833340093095217, -233.7327013124392749 ) ) ;
#26651=EDGE_LOOP ( 'NONE', ( #186739, #200918, #169687 ) ) ;
#26690=CIRCLE ( 'NONE', #64081, 0.09999999999999939493 ) ;
#26751=AXIS2_PLACEMENT_3D ( 'NONE', #214857, #117051, #234412 ) ;
#26752=DIRECTION ( 'NONE',  ( 1.000000000000000000, 0.000000000000000000, 0.000000000000000000 ) ) ;
#26776=ORIENTED_EDGE ( 'NONE', *, *, #151865, .F. ) ;
#26792=DIRECTION ( 'NONE',  ( 1.000000000000000000, 0.000000000000000000, 0.000000000000000000 ) ) ;
#26793=DIRECTION ( 'NONE',  ( -0.000000000000000000, 0.4721928772777346239, 0.8814952561688430555 ) ) ;
#26796=DIRECTION ( 'NONE',  ( 1.000000000000000000, 0.000000000000000000, 0.000000000000000000 ) ) ;
#26801=DIRECTION ( 'NONE',  ( 0.000000000000000000, -0.5826443254699606999, -0.8127272543711416830 ) ) ;
#26814=ORIENTED_EDGE ( 'NONE', *, *, #163057, .T. ) ;
#26830=DIRECTION ( 'NONE',  ( 0.000000000000000000, 0.4721928772777344019, 0.8814952561688432775 ) ) ;
#26879=FACE_OUTER_BOUND ( 'NONE', #240717, .T. ) ;
#26993=CARTESIAN_POINT ( 'NONE',  ( -21.05000000000000071, 40.18490544642472884, -251.4399342103543233 ) ) ;
#27000=EDGE_CURVE ( 'NONE', #227815, #67400, #51865, .T. ) ;
#27003=EDGE_LOOP ( 'NONE', ( #137174, #36550, #169492, #149323, #42560, #206822, #25224, #22020, #175978, #204501, #112490, #31720, #177135, #24778 ) ) ;
#27008=EDGE_CURVE ( 'NONE', #26118, #30618, #22690, .T. ) ;
#27023=CYLINDRICAL_SURFACE ( 'NONE', #160672, 0.09999999999999939493 ) ;
#27032=TOROIDAL_SURFACE ( 'NONE', #22745, 1.900000000000002576, 0.1000000000000000056 ) ;
#27045=CYLINDRICAL_SURFACE ( 'NONE', #107337, 0.1000000000000013933 ) ;
#27081=AXIS2_PLACEMENT_3D ( 'NONE', #215306, #37984, #18390 ) ;
#27106=CARTESIAN_POINT ( 'NONE',  ( 20.90851465518106167, 46.44433919924416898, -243.0795225066946159 ) ) ;
#27153=EDGE_CURVE ( 'NONE', #179129, #155241, #197616, .T. ) ;
#27163=CARTESIAN_POINT ( 'NONE',  ( -20.15000000000000568, 22.40264273797979655, -231.3739394982302429 ) ) ;
#27177=EDGE_CURVE ( 'NONE', #105430, #231806, #204915, .T. ) ;
#27185=CARTESIAN_POINT ( 'NONE',  ( -20.64999999999999858, 25.94586868676353575, -241.5435999122864530 ) ) ;
#27189=FACE_OUTER_BOUND ( 'NONE', #184696, .T. ) ;
#27201=FACE_OUTER_BOUND ( 'NONE', #175977, .T. ) ;
#27238=ADVANCED_FACE ( 'NONE', ( #201078, #22468, #23760 ), #103240, .F. ) ;
#27246=DIRECTION ( 'NONE',  ( 1.000000000000000000, 0.000000000000000000, 0.000000000000000000 ) ) ;
#27248=AXIS2_PLACEMENT_3D ( 'NONE', #182174, #237012, #196584 ) ;
#27303=CIRCLE ( 'NONE', #256319, 0.1999999999999997335 ) ;
#27334=EDGE_CURVE ( 'NONE', #48376, #79572, #177003, .T. ) ;
#27344=CARTESIAN_POINT ( 'NONE',  ( 21.00000000000000000, 22.53103078161933936, -230.9224853114453140 ) ) ;
#27348=CARTESIAN_POINT ( 'NONE',  ( -18.50000000000000000, 9.122720154857367092, -245.4644708025848558 ) ) ;
#27363=CARTESIAN_POINT ( 'NONE',  ( -21.05000000000000071, 1.627596811821301115, -230.7476853162787052 ) ) ;
#27422=ORIENTED_EDGE ( 'NONE', *, *, #44279, .F. ) ;
#27445=CIRCLE ( 'NONE', #156439, 0.09999999999999939493 ) ;
#27490=DIRECTION ( 'NONE',  ( 0.000000000000000000, -0.8814952561688476074, 0.4721928772777262417 ) ) ;
#27507=CARTESIAN_POINT ( 'NONE',  ( -20.00857864376270001, 30.27561093622783517, -235.5248193094124645 ) ) ;
#27524=DIRECTION ( 'NONE',  ( 0.000000000000000000, -0.8814952561688430555, 0.4721928772777346239 ) ) ;
#27573=CARTESIAN_POINT ( 'NONE',  ( -21.05000000000000071, 36.65892442174935439, -249.5511627012433848 ) ) ;
#27591=CARTESIAN_POINT ( 'NONE',  ( 21.05000000000000071, 4.136903274969363942, -245.4596299165286268 ) ) ;
#27627=FACE_OUTER_BOUND ( 'NONE', #79774, .T. ) ;
#27636=ORIENTED_EDGE ( 'NONE', *, *, #89843, .T. ) ;
#27658=ORIENTED_EDGE ( 'NONE', *, *, #245555, .F. ) ;
#27667=EDGE_CURVE ( 'NONE', #207366, #2694, #44921, .T. ) ;
#27674=CYLINDRICAL_SURFACE ( 'NONE', #48891, 4.049999999999997158 ) ;
#27680=AXIS2_PLACEMENT_3D ( 'NONE', #35455, #229763, #51092 ) ;
#27690=VECTOR ( 'NONE', #244559, 1000.000000000000000 ) ;
#27709=ORIENTED_EDGE ( 'NONE', *, *, #254894, .F. ) ;
#27722=ORIENTED_EDGE ( 'NONE', *, *, #27334, .T. ) ;
#27777=CARTESIAN_POINT ( 'NONE',  ( -22.47071067811865319, 10.68684811775433374, -226.8807012965928038 ) ) ;
#27779=DIRECTION ( 'NONE',  ( -4.408576920032446739E-17, 0.9371753822965314118, -0.3488585713686133682 ) ) ;
#27831=CARTESIAN_POINT ( 'NONE',  ( 18.49999999999999645, 19.02280865327213277, -233.3540837620168986 ) ) ;
#27833=EDGE_LOOP ( 'NONE', ( #48482, #143697, #230816, #233926 ) ) ;
#27834=EDGE_CURVE ( 'NONE', #4561, #199335, #2162, .T. ) ;
#27847=AXIS2_PLACEMENT_3D ( 'NONE', #162077, #159506, #43394 ) ;
#27852=CARTESIAN_POINT ( 'NONE',  ( 18.49999999999999645, 18.37021030142088662, -237.6367305148568221 ) ) ;
#27887=DIRECTION ( 'NONE',  ( 0.000000000000000000, -0.4721928772777351790, -0.8814952561688427224 ) ) ;
#27890=CARTESIAN_POINT ( 'NONE',  ( 23.14999999999999147, 7.128833340093095217, -233.7327013124392749 ) ) ;
#27894=ORIENTED_EDGE ( 'NONE', *, *, #213724, .F. ) ;
#27899=DIRECTION ( 'NONE',  ( -3.265361837132812107E-16, 0.4721928772777345684, 0.8814952561688429444 ) ) ;
#27952=ORIENTED_EDGE ( 'NONE', *, *, #205604, .T. ) ;
#27956=CIRCLE ( 'NONE', #32039, 0.09999999999999986677 ) ;
#27967=AXIS2_PLACEMENT_3D ( 'NONE', #234350, #150979, #89698 ) ;
#27981=DIRECTION ( 'NONE',  ( 0.000000000000000000, -0.8814952561688476074, 0.4721928772777262417 ) ) ;
#28014=EDGE_LOOP ( 'NONE', ( #85192, #44487, #90079, #126315 ) ) ;
#28026=ADVANCED_FACE ( 'NONE', ( #59002 ), #18627, .T. ) ;
#28040=AXIS2_PLACEMENT_3D ( 'NONE', #66044, #243398, #123462 ) ;
#28047=ORIENTED_EDGE ( 'NONE', *, *, #214186, .T. ) ;
#28059=CARTESIAN_POINT ( 'NONE',  ( 18.39999999999999858, -7.667348966301519297, -236.4704904124130280 ) ) ;
#28070=DIRECTION ( 'NONE',  ( 0.000000000000000000, -0.8814952561688437216, 0.4721928772777334582 ) ) ;
#28071=EDGE_CURVE ( 'NONE', #182938, #20946, #102280, .T. ) ;
#28074=LINE ( 'NONE', #68463, #34392 ) ;
#28096=ORIENTED_EDGE ( 'NONE', *, *, #179557, .T. ) ;
#28116=DIRECTION ( 'NONE',  ( 0.000000000000000000, 0.8814952561688476074, -0.4721928772777262417 ) ) ;
#28136=ORIENTED_EDGE ( 'NONE', *, *, #113859, .T. ) ;
#28149=DIRECTION ( 'NONE',  ( 1.000000000000000000, 0.000000000000000000, 0.000000000000000000 ) ) ;
#28157=ADVANCED_FACE ( 'NONE', ( #156885 ), #116452, .T. ) ;
#28199=AXIS2_PLACEMENT_3D ( 'NONE', #72333, #35780, #133570 ) ;
#28211=VERTEX_POINT ( 'NONE', #81146 ) ;
#28218=TOROIDAL_SURFACE ( 'NONE', #120367, 0.2000000000000000111, 0.1000000000000000056 ) ;
#28291=CARTESIAN_POINT ( 'NONE',  ( -18.59999999999999787, 43.35377423437995503, -245.1717807829448930 ) ) ;
#28299=AXIS2_PLACEMENT_3D ( 'NONE', #79710, #75878, #39351 ) ;
#28337=CIRCLE ( 'NONE', #215720, 0.09999999999999939493 ) ;
#28340=CARTESIAN_POINT ( 'NONE',  ( 18.49999999999998934, 46.33035574435032800, -243.0552603638194284 ) ) ;
#28348=ORIENTED_EDGE ( 'NONE', *, *, #47014, .T. ) ;
#28353=DIRECTION ( 'NONE',  ( 0.000000000000000000, 0.8814952561688429444, -0.4721928772777345684 ) ) ;
#28356=ORIENTED_EDGE ( 'NONE', *, *, #2647, .T. ) ;
#28387=ORIENTED_EDGE ( 'NONE', *, *, #167127, .T. ) ;
#28389=AXIS2_PLACEMENT_3D ( 'NONE', #87001, #144405, #44055 ) ;
#28403=DIRECTION ( 'NONE',  ( 0.000000000000000000, 0.8814952561688437216, -0.4721928772777334582 ) ) ;
#28417=EDGE_CURVE ( 'NONE', #54485, #208784, #185882, .T. ) ;
#28426=VERTEX_POINT ( 'NONE', #56137 ) ;
#28438=ORIENTED_EDGE ( 'NONE', *, *, #213625, .T. ) ;
#28454=ORIENTED_EDGE ( 'NONE', *, *, #242764, .F. ) ;
#28529=EDGE_CURVE ( 'NONE', #138960, #171330, #20969, .T. ) ;
#28536=ORIENTED_EDGE ( 'NONE', *, *, #58658, .T. ) ;
#28555=AXIS2_PLACEMENT_3D ( 'NONE', #185836, #26796, #159880 ) ;
#28585=DIRECTION ( 'NONE',  ( 0.000000000000000000, 0.8814952561688359500, -0.4721928772777478911 ) ) ;
#28587=DIRECTION ( 'NONE',  ( 0.000000000000000000, -0.8814952561688476074, 0.4721928772777262417 ) ) ;
#28648=CIRCLE ( 'NONE', #257653, 0.1000000000000075273 ) ;
#28657=CARTESIAN_POINT ( 'NONE',  ( -21.05000000000000071, 1.316055977212913009, -230.7323992127457473 ) ) ;
#28661=CIRCLE ( 'NONE', #86843, 0.09999999999999983902 ) ;
#28669=LINE ( 'NONE', #230680, #146284 ) ;
#28678=CARTESIAN_POINT ( 'NONE',  ( -21.14999999999999858, 1.316055977212913009, -230.7323992127457473 ) ) ;
#28716=ORIENTED_EDGE ( 'NONE', *, *, #48346, .T. ) ;
#28726=ORIENTED_EDGE ( 'NONE', *, *, #45600, .F. ) ;
#28740=LINE ( 'NONE', #209911, #56222 ) ;
#28764=EDGE_CURVE ( 'NONE', #167398, #246715, #48512, .T. ) ;
#28828=DIRECTION ( 'NONE',  ( 0.000000000000000000, -0.4721928772776973204, -0.8814952561688629284 ) ) ;
#28855=PLANE ( 'NONE',  #138417 ) ;
#28902=CARTESIAN_POINT ( 'NONE',  ( 22.59999985501178799, 12.61921324905061326, -223.3442716046673127 ) ) ;
#28905=CIRCLE ( 'NONE', #228768, 0.09999999999999939493 ) ;
#28958=( BOUNDED_CURVE ( )  B_SPLINE_CURVE ( 3, ( #139684, #91900, #99276, #60155 ),
 .UNSPECIFIED., .F., .F. ) 
 B_SPLINE_CURVE_WITH_KNOTS ( ( 4, 4 ),
 ( 3.141592653589719397, 4.712388980384693227 ),
 .UNSPECIFIED. ) 
 CURVE ( )  GEOMETRIC_REPRESENTATION_ITEM ( )  RATIONAL_B_SPLINE_CURVE ( ( 1.000000000000000000, 0.8047378541243468408, 0.8047378541243468408, 1.000000000000000000 ) ) 
 REPRESENTATION_ITEM ( '' )  );
#28965=CARTESIAN_POINT ( 'NONE',  ( -23.25000000000000000, 7.128833340093095217, -233.7327013124392749 ) ) ;
#28968=AXIS2_PLACEMENT_3D ( 'NONE', #100719, #179051, #141177 ) ;
#28978=CARTESIAN_POINT ( 'NONE',  ( 21.14999999999999503, 12.71802988599559647, -223.5105008658000258 ) ) ;
#28992=CARTESIAN_POINT ( 'NONE',  ( 19.97071067811865674, 34.39212750349580006, -235.0405048756463486 ) ) ;
#28995=AXIS2_PLACEMENT_3D ( 'NONE', #161005, #606, #239255 ) ;
#29008=CARTESIAN_POINT ( 'NONE',  ( 18.59999999999999787, 7.128833340093095217, -233.7327013124392749 ) ) ;
#29034=FACE_OUTER_BOUND ( 'NONE', #87645, .T. ) ;
#29058=TOROIDAL_SURFACE ( 'NONE', #8180, 11.65000000000000036, 0.1000000000000000056 ) ;
#29059=ORIENTED_EDGE ( 'NONE', *, *, #239166, .T. ) ;
#29076=CARTESIAN_POINT ( 'NONE',  ( 18.49999999999999645, 38.22609996598573190, -261.0782621420140117 ) ) ;
#29150=CARTESIAN_POINT ( 'NONE',  ( 18.59999999999999432, 14.72981487416292623, -236.4853282537515895 ) ) ;
#29219=CARTESIAN_POINT ( 'NONE',  ( 20.94999999999999929, 11.41170713998153019, -246.6906184681487275 ) ) ;
#29233=LINE ( 'NONE', #7047, #65435 ) ;
#29239=VERTEX_POINT ( 'NONE', #81182 ) ;
#29252=ORIENTED_EDGE ( 'NONE', *, *, #139782, .T. ) ;
#29345=ORIENTED_EDGE ( 'NONE', *, *, #29543, .T. ) ;
#29373=CARTESIAN_POINT ( 'NONE',  ( 22.39999999999999503, 12.62988036037871176, -223.4632815780722410 ) ) ;
#29384=ORIENTED_EDGE ( 'NONE', *, *, #118918, .F. ) ;
#29391=EDGE_LOOP ( 'NONE', ( #151145, #106236, #164933, #206851, #140465 ) ) ;
#29414=LINE ( 'NONE', #9807, #173452 ) ;
#29428=DIRECTION ( 'NONE',  ( 0.000000000000000000, -0.8814952561687088295, 0.4721928772779852013 ) ) ;
#29434=AXIS2_PLACEMENT_3D ( 'NONE', #141763, #98757, #122221 ) ;
#29479=CIRCLE ( 'NONE', #95877, 0.1000000000000013933 ) ;
#29496=FACE_OUTER_BOUND ( 'NONE', #82063, .T. ) ;
#29508=ORIENTED_EDGE ( 'NONE', *, *, #55006, .F. ) ;
#29528=CARTESIAN_POINT ( 'NONE',  ( 23.14999999999999858, 35.71453866719386383, -251.3141532135810792 ) ) ;
#29541=DIRECTION ( 'NONE',  ( 0.000000000000000000, -0.4721928772777346794, -0.8814952561688431665 ) ) ;
#29543=EDGE_CURVE ( 'NONE', #256947, #50959, #89215, .T. ) ;
#29560=CARTESIAN_POINT ( 'NONE',  ( -21.55000000000000071, 29.23678660621682113, -237.4641088729839282 ) ) ;
#29567=DIRECTION ( 'NONE',  ( -1.000000000000000000, 0.000000000000000000, 0.000000000000000000 ) ) ;
#29580=ADVANCED_BREP_SHAPE_REPRESENTATION ( '', ( #107142, #2425 ), #110949 ) ;
#29616=CARTESIAN_POINT ( 'NONE',  ( 18.55807992284871233, 46.45729338110134421, -243.0823073233429170 ) ) ;
#29637=ORIENTED_EDGE ( 'NONE', *, *, #246368, .T. ) ;
#29638=FACE_OUTER_BOUND ( 'NONE', #61369, .T. ) ;
#29654=CARTESIAN_POINT ( 'NONE',  ( 23.25000000000000000, 28.42524210734032408, -258.3567845160494585 ) ) ;
#29656=VERTEX_POINT ( 'NONE', #19656 ) ;
#29661=CARTESIAN_POINT ( 'NONE',  ( -22.59999999999999787, 12.58798907299599179, -223.3278890275437050 ) ) ;
#29672=DIRECTION ( 'NONE',  ( 0.000000000000000000, 0.8814952561688476074, -0.4721928772777262417 ) ) ;
#29675=DIRECTION ( 'NONE',  ( 1.000000000000000000, 0.000000000000000000, 0.000000000000000000 ) ) ;
#29682=CARTESIAN_POINT ( 'NONE',  ( -18.39999999999999858, 38.03205796367813463, -261.1772988674111957 ) ) ;
#29717=CARTESIAN_POINT ( 'NONE',  ( -20.94999999999999929, 18.71344899777637494, -226.7788045585494388 ) ) ;
#29721=CIRCLE ( 'NONE', #113078, 0.09999999999999986677 ) ;
#29733=DIRECTION ( 'NONE',  ( -0.7071067811865708874, 0.3338907855511046296, 0.6233112732207185536 ) ) ;
#29749=EDGE_LOOP ( 'NONE', ( #178144, #1013, #256263, #165819 ) ) ;
#29795=CARTESIAN_POINT ( 'NONE',  ( 20.85000000000000142, 28.60154115857409352, -258.4512230915049713 ) ) ;
#29797=DIRECTION ( 'NONE',  ( 0.000000000000000000, -0.8814952561688476074, 0.4721928772777262417 ) ) ;
#29798=AXIS2_PLACEMENT_3D ( 'NONE', #10344, #151134, #173306 ) ;
#29802=EDGE_CURVE ( 'NONE', #135829, #175441, #243156, .T. ) ;
#29833=CARTESIAN_POINT ( 'NONE',  ( -21.14999999999999858, 10.21728496540352182, -227.9671432372868765 ) ) ;
#29844=DIRECTION ( 'NONE',  ( 0.000000000000000000, 0.4721928772778128947, 0.8814952561688012000 ) ) ;
#29857=ORIENTED_EDGE ( 'NONE', *, *, #100672, .T. ) ;
#29870=ORIENTED_EDGE ( 'NONE', *, *, #146724, .T. ) ;
#29875=DIRECTION ( 'NONE',  ( 0.000000000000000000, -0.8496786552930076786, -0.5273008465188220306 ) ) ;
#29886=LINE ( 'NONE', #125123, #160868 ) ;
#29888=ORIENTED_EDGE ( 'NONE', *, *, #189380, .F. ) ;
#29904=ORIENTED_EDGE ( 'NONE', *, *, #7528, .T. ) ;
#29924=DIRECTION ( 'NONE',  ( -1.000000000000000000, 0.000000000000000000, -0.000000000000000000 ) ) ;
#29932=LINE ( 'NONE', #248968, #17829 ) ;
#29948=AXIS2_PLACEMENT_3D ( 'NONE', #142317, #202308, #198448 ) ;
#29951=ADVANCED_FACE ( 'NONE', ( #97547 ), #152454, .F. ) ;
#29955=ORIENTED_EDGE ( 'NONE', *, *, #68430, .F. ) ;
#29985=DIRECTION ( 'NONE',  ( -1.000000000000000000, 0.000000000000000000, 0.000000000000000000 ) ) ;
#29988=AXIS2_PLACEMENT_3D ( 'NONE', #209658, #12765, #53146 ) ;
#30016=CARTESIAN_POINT ( 'NONE',  ( -20.64999999999999858, 24.07562609839690992, -252.7152152143214892 ) ) ;
#30021=EDGE_CURVE ( 'NONE', #105632, #240452, #222221, .T. ) ;
#30042=CARTESIAN_POINT ( 'NONE',  ( 21.14999999999999858, 1.316055977212909456, -230.7323992127457473 ) ) ;
#30051=ADVANCED_FACE ( 'NONE', ( #44027 ), #161429, .T. ) ;
#30061=CARTESIAN_POINT ( 'NONE',  ( 18.59999999999999076, 19.02280865327213277, -233.3540837620168986 ) ) ;
#30072=EDGE_LOOP ( 'NONE', ( #50689, #101298, #77671, #226157 ) ) ;
#30099=VECTOR ( 'NONE', #99396, 1000.000000000000000 ) ;
#30157=CARTESIAN_POINT ( 'NONE',  ( 22.49999999999999645, 12.58798907299599534, -223.3278890275437050 ) ) ;
#30199=EDGE_CURVE ( 'NONE', #69221, #59204, #66155, .T. ) ;
#30202=VECTOR ( 'NONE', #9895, 1000.000000000000000 ) ;
#30221=CARTESIAN_POINT ( 'NONE',  ( -20.64999999999999858, 20.06933876993645782, -235.7297789824848451 ) ) ;
#30256=ORIENTED_EDGE ( 'NONE', *, *, #70087, .T. ) ;
#30261=CARTESIAN_POINT ( 'NONE',  ( -20.54999999999999716, 29.28400589394459530, -237.3759593473670293 ) ) ;
#30262=ORIENTED_EDGE ( 'NONE', *, *, #182989, .F. ) ;
#30264=ORIENTED_EDGE ( 'NONE', *, *, #100477, .F. ) ;
#30283=CARTESIAN_POINT ( 'NONE',  ( -21.44999999999999929, 29.33122518167236237, -237.2878098217501588 ) ) ;
#30317=ORIENTED_EDGE ( 'NONE', *, *, #116711, .T. ) ;
#30328=FACE_OUTER_BOUND ( 'NONE', #115944, .T. ) ;
#30351=ORIENTED_EDGE ( 'NONE', *, *, #93247, .T. ) ;
#30356=DIRECTION ( 'NONE',  ( 0.000000000000000000, 0.8814952561688437216, -0.4721928772777334582 ) ) ;
#30367=DIRECTION ( 'NONE',  ( 0.000000000000000000, -0.8814952561688430555, 0.4721928772777346239 ) ) ;
#30375=DIRECTION ( 'NONE',  ( 0.000000000000000000, 0.8814952561688476074, -0.4721928772777262417 ) ) ;
#30417=( NAMED_UNIT ( * ) SI_UNIT ( $, .STERADIAN. ) SOLID_ANGLE_UNIT ( ) );
#30426=DIRECTION ( 'NONE',  ( 0.000000000000000000, -0.8096735173027155286, 0.5868805631290314739 ) ) ;
#30503=ORIENTED_EDGE ( 'NONE', *, *, #143698, .F. ) ;
#30522=DIRECTION ( 'NONE',  ( 0.000000000000000000, 0.8814952561688437216, -0.4721928772777334582 ) ) ;
#30532=ORIENTED_EDGE ( 'NONE', *, *, #194300, .T. ) ;
#30554=CARTESIAN_POINT ( 'NONE',  ( -23.25000000000000000, 26.42645436459467589, -241.9028176822583589 ) ) ;
#30581=ORIENTED_EDGE ( 'NONE', *, *, #123043, .F. ) ;
#30592=SPHERICAL_SURFACE ( 'NONE', #20184, 0.1000000000000000056 ) ;
#30600=ORIENTED_EDGE ( 'NONE', *, *, #85777, .T. ) ;
#30609=VERTEX_POINT ( 'NONE', #135760 ) ;
#30610=CARTESIAN_POINT ( 'NONE',  ( 21.05000000000000071, 7.216982865709976380, -233.7799206001670598 ) ) ;
#30618=VERTEX_POINT ( 'NONE', #101 ) ;
#30651=ADVANCED_FACE ( 'NONE', ( #77077 ), #177507, .F. ) ;
#30676=CARTESIAN_POINT ( 'NONE',  ( 20.94999999999999574, 7.128833340093095217, -233.7327013124392749 ) ) ;
#30679=CYLINDRICAL_SURFACE ( 'NONE', #33473, 0.1000000000000013933 ) ;
#30761=FACE_OUTER_BOUND ( 'NONE', #111176, .T. ) ;
#30781=ORIENTED_EDGE ( 'NONE', *, *, #212501, .T. ) ;
#30797=VERTEX_POINT ( 'NONE', #161781 ) ;
#30805=CARTESIAN_POINT ( 'NONE',  ( 21.05995757104869526, 22.02226065213599782, -231.7555846603365808 ) ) ;
#30823=CARTESIAN_POINT ( 'NONE',  ( -20.94999999999999929, 33.04479387145709524, -247.6151719044046899 ) ) ;
#30855=ORIENTED_EDGE ( 'NONE', *, *, #49569, .T. ) ;
#30862=CARTESIAN_POINT ( 'NONE',  ( -22.00356870069710524, 0.7342531110970158537, -230.3072997392041259 ) ) ;
#30867=DIRECTION ( 'NONE',  ( 0.000000000000000000, 0.8814952561688437216, -0.4721928772777334582 ) ) ;
#30881=DIRECTION ( 'NONE',  ( 0.000000000000000000, -0.8814952561688431665, 0.4721928772777344574 ) ) ;
#30903=CARTESIAN_POINT ( 'NONE',  ( 18.59117750673696179, 46.46967969402478360, -243.0849751855955674 ) ) ;
#30928=CIRCLE ( 'NONE', #176662, 12.87500000000000000 ) ;
#30935=CARTESIAN_POINT ( 'NONE',  ( -20.85000000000000142, 36.22724532936083364, -235.9903003947922002 ) ) ;
#30989=AXIS2_PLACEMENT_3D ( 'NONE', #216234, #217511, #61014 ) ;
#31043=CARTESIAN_POINT ( 'NONE',  ( -22.47007471830798764, 10.77449791745511476, -226.9269314985138237 ) ) ;
#31053=DIRECTION ( 'NONE',  ( -1.000000000000000000, 0.000000000000000000, 0.000000000000000000 ) ) ;
#31076=DIRECTION ( 'NONE',  ( 1.000000000000000000, 1.541880601228652843E-16, 2.878400969107353907E-16 ) ) ;
#31093=ORIENTED_EDGE ( 'NONE', *, *, #241636, .F. ) ;
#31109=DIRECTION ( 'NONE',  ( 1.000000000000000000, 0.000000000000000000, 0.000000000000000000 ) ) ;
#31130=DIRECTION ( 'NONE',  ( 0.000000000000000000, -0.8814952561688428334, 0.4721928772777350680 ) ) ;
#31139=DIRECTION ( 'NONE',  ( 1.000000000000000000, 8.674042436075353235E-17, 1.619280515896125144E-16 ) ) ;
#31147=CIRCLE ( 'NONE', #226912, 0.5000000000000069944 ) ;
#31151=CARTESIAN_POINT ( 'NONE',  ( -18.59999999999999787, 18.81339837015603322, -226.7756228984618190 ) ) ;
#31164=ADVANCED_FACE ( 'NONE', ( #125393 ), #145408, .T. ) ;
#31192=CIRCLE ( 'NONE', #85278, 0.5999999999999962030 ) ;
#31211=CARTESIAN_POINT ( 'NONE',  ( -20.64999999999999858, 24.12844930803500887, -253.0488546976795021 ) ) ;
#31213=EDGE_CURVE ( 'NONE', #155399, #238367, #110955, .T. ) ;
#31215=ORIENTED_EDGE ( 'NONE', *, *, #88512, .F. ) ;
#31247=EDGE_LOOP ( 'NONE', ( #167002, #187940, #2970, #121405 ) ) ;
#31296=DIRECTION ( 'NONE',  ( -1.000000000000000000, 0.000000000000000000, 0.000000000000000000 ) ) ;
#31322=AXIS2_PLACEMENT_3D ( 'NONE', #65315, #27524, #183982 ) ;
#31362=ORIENTED_EDGE ( 'NONE', *, *, #187321, .T. ) ;
#31372=CIRCLE ( 'NONE', #143744, 0.5000000000000008882 ) ;
#31397=ADVANCED_FACE ( 'NONE', ( #24723, #142059, #1254 ), #102920, .F. ) ;
#31410=CYLINDRICAL_SURFACE ( 'NONE', #109004, 0.1000000000000013933 ) ;
#31448=DIRECTION ( 'NONE',  ( 5.421010862427553724E-16, -0.4721928772777317374, -0.8814952561688446098 ) ) ;
#31456=CARTESIAN_POINT ( 'NONE',  ( 22.50014994444026328, 12.60373254347212679, -223.3361492492176126 ) ) ;
#31537=EDGE_CURVE ( 'NONE', #167022, #109890, #14411, .T. ) ;
#31565=CARTESIAN_POINT ( 'NONE',  ( 20.13684514580103269, 18.79075242197309947, -229.2072313918904456 ) ) ;
#31578=VERTEX_POINT ( 'NONE', #212333 ) ;
#31604=ORIENTED_EDGE ( 'NONE', *, *, #113268, .T. ) ;
#31605=DIRECTION ( 'NONE',  ( 0.000000000000000000, -0.8814952561688437216, 0.4721928772777334582 ) ) ;
#31611=DIRECTION ( 'NONE',  ( 2.465190328815661345E-32, -0.8814952561688430555, 0.4721928772777344574 ) ) ;
#31623=EDGE_CURVE ( 'NONE', #98621, #251099, #214299, .T. ) ;
#31626=ORIENTED_EDGE ( 'NONE', *, *, #244847, .T. ) ;
#31636=CARTESIAN_POINT ( 'NONE',  ( -20.85000000000000142, 46.01276039807270024, -256.6622985126337539 ) ) ;
#31642=VERTEX_POINT ( 'NONE', #173236 ) ;
#31645=ADVANCED_FACE ( 'NONE', ( #113208 ), #235711, .F. ) ;
#31648=CARTESIAN_POINT ( 'NONE',  ( -20.85000000000000142, 45.93315328338058379, -256.6017782078560003 ) ) ;
#31655=EDGE_CURVE ( 'NONE', #225564, #139998, #222640, .T. ) ;
#31672=CARTESIAN_POINT ( 'NONE',  ( -18.59999999999999787, 18.24178995542692050, -237.7003448530951459 ) ) ;
#31691=EDGE_CURVE ( 'NONE', #83686, #248838, #190196, .T. ) ;
#31693=CARTESIAN_POINT ( 'NONE',  ( 20.99999999999997868, 7.128833340093095217, -233.7327013124392749 ) ) ;
#31705=CYLINDRICAL_SURFACE ( 'NONE', #99915, 11.74999999999999112 ) ;
#31709=ORIENTED_EDGE ( 'NONE', *, *, #3338, .T. ) ;
#31720=ORIENTED_EDGE ( 'NONE', *, *, #100390, .T. ) ;
#31724=CARTESIAN_POINT ( 'NONE',  ( 21.05000000000000071, 30.48950451747912993, -239.6099224343151946 ) ) ;
#31734=AXIS2_PLACEMENT_3D ( 'NONE', #10050, #89577, #187422 ) ;
#31749=DIRECTION ( 'NONE',  ( 1.000000000000000000, 0.000000000000000000, 0.000000000000000000 ) ) ;
#31766=AXIS2_PLACEMENT_3D ( 'NONE', #42844, #201920, #59808 ) ;
#31782=CARTESIAN_POINT ( 'NONE',  ( 21.05000000000000071, 14.64166534854604507, -236.4381089660238331 ) ) ;
#31833=DIRECTION ( 'NONE',  ( 1.000000000000000000, 1.541880601228652843E-16, 2.878400969107353907E-16 ) ) ;
#31861=ORIENTED_EDGE ( 'NONE', *, *, #121046, .F. ) ;
#31869=ORIENTED_EDGE ( 'NONE', *, *, #179326, .F. ) ;
#31881=DIRECTION ( 'NONE',  ( -0.000000000000000000, 0.4721928772777345684, 0.8814952561688429444 ) ) ;
#31893=DIRECTION ( 'NONE',  ( 0.000000000000000000, 0.8814952561688434995, -0.4721928772777337913 ) ) ;
#31915=TOROIDAL_SURFACE ( 'NONE', #210965, 11.65000000000000036, 0.1000000000000000056 ) ;
#31932=VECTOR ( 'NONE', #30367, 1000.000000000000000 ) ;
#31935=DIRECTION ( 'NONE',  ( 0.000000000000000000, 0.8814952561688430555, -0.4721928772777346239 ) ) ;
#31944=CIRCLE ( 'NONE', #77686, 0.09999999999999939493 ) ;
#31963=FACE_BOUND ( 'NONE', #91277, .T. ) ;
#31966=CARTESIAN_POINT ( 'NONE',  ( 20.94999999999999929, 14.88773611405353314, -236.3451124650200370 ) ) ;
#31984=DIRECTION ( 'NONE',  ( 0.000000000000000000, 0.9994937237965569876, 0.03181660087583042945 ) ) ;
#32023=EDGE_CURVE ( 'NONE', #56882, #76756, #252069, .T. ) ;
#32039=AXIS2_PLACEMENT_3D ( 'NONE', #41579, #39001, #194236 ) ;
#32050=CARTESIAN_POINT ( 'NONE',  ( 20.04142135623730070, 2.272311100394801109, -217.9150152700588592 ) ) ;
#32073=AXIS2_PLACEMENT_3D ( 'NONE', #31648, #115002, #150295 ) ;
#32079=ORIENTED_EDGE ( 'NONE', *, *, #187682, .T. ) ;
#32112=CIRCLE ( 'NONE', #227706, 0.1000000000000031558 ) ;
#32113=EDGE_LOOP ( 'NONE', ( #170956, #45449, #51204, #34552, #228519 ) ) ;
#32134=ORIENTED_EDGE ( 'NONE', *, *, #133135, .F. ) ;
#32156=VECTOR ( 'NONE', #27246, 1000.000000000000000 ) ;
#32157=AXIS2_PLACEMENT_3D ( 'NONE', #256421, #101218, #97380 ) ;
#32175=VECTOR ( 'NONE', #67749, 1000.000000000000000 ) ;
#32196=ORIENTED_EDGE ( 'NONE', *, *, #224251, .T. ) ;
#32200=ORIENTED_EDGE ( 'NONE', *, *, #200216, .F. ) ;
#32201=B_SPLINE_CURVE_WITH_KNOTS ( 'NONE', 3,
 ( #217506, #173325, #237097, #58427, #153765, #113294, #74211, #192847, #21902, #220099, #239663, #240948, #122285, #199260, #41481, #44024 ),
 .UNSPECIFIED., .F., .F.,
 ( 4, 3, 3, 3, 3, 4 ),
 ( 0.000000000000000000, 2.209075297431637548E-05, 5.594258369011413288E-05, 8.979524372343752631E-05, 0.0001236472815274714237, 0.0001574990747609671831 ),
 .UNSPECIFIED. ) ;
#32209=CARTESIAN_POINT ( 'NONE',  ( -21.04386569057572487, 36.16263438457815482, -235.9556900804354314 ) ) ;
#32214=EDGE_LOOP ( 'NONE', ( #44184, #68320, #220279, #58988 ) ) ;
#32219=CARTESIAN_POINT ( 'NONE',  ( 20.85000000000000142, 42.15997144203495139, -239.2817429668763793 ) ) ;
#32223=CIRCLE ( 'NONE', #132169, 0.1000000000000013933 ) ;
#32251=CIRCLE ( 'NONE', #223748, 0.09999999999999939493 ) ;
#32261=ORIENTED_EDGE ( 'NONE', *, *, #42912, .T. ) ;
#32358=CIRCLE ( 'NONE', #32157, 7.799999999999993605 ) ;
#32365=ORIENTED_EDGE ( 'NONE', *, *, #237263, .F. ) ;
#32413=FACE_OUTER_BOUND ( 'NONE', #237501, .T. ) ;
#32414=CARTESIAN_POINT ( 'NONE',  ( 21.05000000000000071, 21.98309897467605722, -231.7335930323676791 ) ) ;
#32420=EDGE_CURVE ( 'NONE', #155020, #30797, #158836, .T. ) ;
#32438=AXIS2_PLACEMENT_3D ( 'NONE', #247565, #185023, #6383 ) ;
#32449=CARTESIAN_POINT ( 'NONE',  ( -20.85000000000000142, 36.46860332481993794, -249.8166405164294588 ) ) ;
#32471=DIRECTION ( 'NONE',  ( 1.000000000000000000, 0.000000000000000000, 0.000000000000000000 ) ) ;
#32473=EDGE_CURVE ( 'NONE', #112914, #183016, #198090, .T. ) ;
#32500=FACE_OUTER_BOUND ( 'NONE', #38791, .T. ) ;
#32541=EDGE_CURVE ( 'NONE', #217845, #173295, #27445, .T. ) ;
#32586=VERTEX_POINT ( 'NONE', #246348 ) ;
#32641=AXIS2_PLACEMENT_3D ( 'NONE', #33230, #127152, #107577 ) ;
#32648=ORIENTED_EDGE ( 'NONE', *, *, #27000, .F. ) ;
#32673=DIRECTION ( 'NONE',  ( 0.000000000000000000, 0.8814952561688430555, -0.4721928772777346239 ) ) ;
#32684=AXIS2_PLACEMENT_3D ( 'NONE', #26177, #206089, #87407 ) ;
#32749=VECTOR ( 'NONE', #146243, 1000.000000000000000 ) ;
#32754=DIRECTION ( 'NONE',  ( 0.000000000000000000, -0.8814952561688431665, 0.4721928772777346794 ) ) ;
#32766=VECTOR ( 'NONE', #183362, 1000.000000000000000 ) ;
#32798=CARTESIAN_POINT ( 'NONE',  ( -20.54999999999999716, 23.68770167995059595, -252.8127582590406348 ) ) ;
#32829=CARTESIAN_POINT ( 'NONE',  ( -23.15000000000000213, 25.30967299857550401, -243.4716794062925374 ) ) ;
#32840=DIRECTION ( 'NONE',  ( -0.000000000000000000, 0.8096735173027124199, -0.5868805631290358038 ) ) ;
#32885=AXIS2_PLACEMENT_3D ( 'NONE', #233205, #36283, #51946 ) ;
#32900=ORIENTED_EDGE ( 'NONE', *, *, #9740, .T. ) ;
#32913=CIRCLE ( 'NONE', #99473, 11.65000000000000391 ) ;
#32919=ORIENTED_EDGE ( 'NONE', *, *, #200593, .T. ) ;
#32924=CARTESIAN_POINT ( 'NONE',  ( 23.14999999999999503, 21.06094381221970124, -233.8786389445302518 ) ) ;
#32927=CARTESIAN_POINT ( 'NONE',  ( 18.50000000000000711, 33.85801315034685643, -236.2828094960805174 ) ) ;
#32933=CARTESIAN_POINT ( 'NONE',  ( 22.14074124539698829, 10.53106080608756479, -227.1716106721344772 ) ) ;
#32934=CARTESIAN_POINT ( 'NONE',  ( 18.58725287972280071, 38.15563695641856157, -261.2056371150309246 ) ) ;
#32941=ORIENTED_EDGE ( 'NONE', *, *, #138707, .F. ) ;
#32947=EDGE_LOOP ( 'NONE', ( #118277, #236000, #159644, #30351 ) ) ;
#32955=EDGE_LOOP ( 'NONE', ( #213981, #1304, #96230, #175713 ) ) ;
#32985=ADVANCED_FACE ( 'NONE', ( #158822 ), #101330, .F. ) ;
#33008=EDGE_CURVE ( 'NONE', #144717, #72511, #152517, .T. ) ;
#33014=LINE ( 'NONE', #112512, #108613 ) ;
#33048=CARTESIAN_POINT ( 'NONE',  ( -22.50000000000000000, 7.128833340093095217, -233.7327013124392749 ) ) ;
#33080=DIRECTION ( 'NONE',  ( -1.000000000000000000, 0.000000000000000000, 0.000000000000000000 ) ) ;
#33084=EDGE_LOOP ( 'NONE', ( #90185, #187812, #224196, #19368 ) ) ;
#33097=ORIENTED_EDGE ( 'NONE', *, *, #54504, .T. ) ;
#33117=LINE ( 'NONE', #153065, #205210 ) ;
#33157=CARTESIAN_POINT ( 'NONE',  ( 20.94999999999999929, 34.89593390941166007, -248.6067769466879156 ) ) ;
#33222=CARTESIAN_POINT ( 'NONE',  ( -23.15000000000000213, 7.128833340093095217, -233.7327013124392749 ) ) ;
#33230=CARTESIAN_POINT ( 'NONE',  ( -18.59999999999999787, 43.08613539620618837, -254.3146655184800409 ) ) ;
#33239=DIRECTION ( 'NONE',  ( 0.000000000000000000, 0.4721928772777346239, 0.8814952561688430555 ) ) ;
#33257=CARTESIAN_POINT ( 'NONE',  ( -18.59999999999999787, 43.18640298906419162, -245.2812653309023574 ) ) ;
#33271=AXIS2_PLACEMENT_3D ( 'NONE', #172156, #249100, #93850 ) ;
#33274=CARTESIAN_POINT ( 'NONE',  ( 21.07928932188134397, 1.596973512267586326, -230.6572452218016167 ) ) ;
#33276=EDGE_LOOP ( 'NONE', ( #239988, #61031, #154126, #55367 ) ) ;
#33288=ORIENTED_EDGE ( 'NONE', *, *, #6833, .T. ) ;
#33303=PRESENTATION_STYLE_ASSIGNMENT (( #238850 ) ) ;
#33339=ORIENTED_EDGE ( 'NONE', *, *, #147185, .F. ) ;
#33351=DIRECTION ( 'NONE',  ( 6.938893903907131190E-14, -0.8814952561688476074, 0.4721928772777262417 ) ) ;
#33362=AXIS2_PLACEMENT_3D ( 'NONE', #220561, #64051, #83578 ) ;
#33408=ORIENTED_EDGE ( 'NONE', *, *, #230075, .F. ) ;
#33410=DIRECTION ( 'NONE',  ( 0.000000000000000000, 0.8814952561688438326, -0.4721928772777334582 ) ) ;
#33422=ORIENTED_EDGE ( 'NONE', *, *, #144397, .T. ) ;
#33427=DIRECTION ( 'NONE',  ( 1.000000000000000000, 0.000000000000000000, 0.000000000000000000 ) ) ;
#33473=AXIS2_PLACEMENT_3D ( 'NONE', #110177, #26830, #188432 ) ;
#33520=CARTESIAN_POINT ( 'NONE',  ( -22.39999999999999858, -3.140208063160689012, -228.2318569537739847 ) ) ;
#33523=CARTESIAN_POINT ( 'NONE',  ( 21.05000000000000426, 1.434708683019007225, -230.7796371565282527 ) ) ;
#33538=CARTESIAN_POINT ( 'NONE',  ( 21.05000000000000071, 14.81796439977981272, -236.5325475414793743 ) ) ;
#33551=CIRCLE ( 'NONE', #158439, 11.70000000000000639 ) ;
#33552=ORIENTED_EDGE ( 'NONE', *, *, #227696, .F. ) ;
#33556=VERTEX_POINT ( 'NONE', #30554 ) ;
#33558=ORIENTED_EDGE ( 'NONE', *, *, #155932, .F. ) ;
#33565=ORIENTED_EDGE ( 'NONE', *, *, #191890, .F. ) ;
#33597=EDGE_CURVE ( 'NONE', #63208, #224437, #182081, .T. ) ;
#33606=CARTESIAN_POINT ( 'NONE',  ( 20.94999999999999574, 13.66123737402873495, -238.6633470470287648 ) ) ;
#33609=EDGE_LOOP ( 'NONE', ( #39952, #176135, #11143, #211476 ) ) ;
#33623=CARTESIAN_POINT ( 'NONE',  ( -21.53699400380515527, 10.33394250185281926, -227.7493655664984828 ) ) ;
#33627=CARTESIAN_POINT ( 'NONE',  ( -21.22070241538126112, 10.09669923035030692, -227.9827655035915654 ) ) ;
#33629=CARTESIAN_POINT ( 'NONE',  ( 21.05000000000000071, 34.98408343502854478, -248.6539962344157004 ) ) ;
#33704=CARTESIAN_POINT ( 'NONE',  ( -20.64999999999999858, 21.30332930069722863, -233.2143729774842882 ) ) ;
#33745=FACE_OUTER_BOUND ( 'NONE', #181305, .T. ) ;
#33758=ORIENTED_EDGE ( 'NONE', *, *, #198870, .T. ) ;
#33768=EDGE_CURVE ( 'NONE', #53873, #140884, #163021, .T. ) ;
#33769=CARTESIAN_POINT ( 'NONE',  ( -18.50000000000000000, 22.25400410509136151, -231.2278641261850680 ) ) ;
#33775=DIRECTION ( 'NONE',  ( -1.000000000000000000, 0.000000000000000000, 0.000000000000000000 ) ) ;
#33807=EDGE_CURVE ( 'NONE', #44944, #92704, #32251, .T. ) ;
#33856=DIRECTION ( 'NONE',  ( 0.000000000000000000, 0.8814952561688438326, -0.4721928772777330696 ) ) ;
#33869=AXIS2_PLACEMENT_3D ( 'NONE', #217044, #197494, #141375 ) ;
#33901=FACE_OUTER_BOUND ( 'NONE', #123526, .T. ) ;
#33941=EDGE_LOOP ( 'NONE', ( #210489, #145709, #139073, #158829 ) ) ;
#33942=EDGE_LOOP ( 'NONE', ( #188891, #34792, #94287, #26490 ) ) ;
#33977=DIRECTION ( 'NONE',  ( 0.000000000000000000, 0.8814952561688449428, -0.4721928772777310157 ) ) ;
#33988=ADVANCED_FACE ( 'NONE', ( #35084 ), #75482, .F. ) ;
#33991=CARTESIAN_POINT ( 'NONE',  ( -20.94999999999999929, 13.59055429284667404, -238.6121134008722038 ) ) ;
#33997=DIRECTION ( 'NONE',  ( 0.000000000000000000, 0.8814952561688430555, -0.4721928772777346239 ) ) ;
#34023=CARTESIAN_POINT ( 'NONE',  ( 20.94999999999999574, 18.52348994230296242, -223.9544021632493127 ) ) ;
#34051=CARTESIAN_POINT ( 'NONE',  ( 18.59999999999998366, 36.65892442174935439, -249.5511627012433848 ) ) ;
#34057=AXIS2_PLACEMENT_3D ( 'NONE', #5357, #150060, #84882 ) ;
#34076=CIRCLE ( 'NONE', #71647, 0.1000000000000035444 ) ;
#34092=CARTESIAN_POINT ( 'NONE',  ( 21.13461538461538680, 23.02743022372037274, -230.2075788195831478 ) ) ;
#34107=CARTESIAN_POINT ( 'NONE',  ( 20.94999999999999929, 38.33376540847015690, -250.4483291680710693 ) ) ;
#34120=ORIENTED_EDGE ( 'NONE', *, *, #246368, .F. ) ;
#34148=VERTEX_POINT ( 'NONE', #51691 ) ;
#34151=ORIENTED_EDGE ( 'NONE', *, *, #201408, .T. ) ;
#34199=CARTESIAN_POINT ( 'NONE',  ( 18.53691006697088284, 33.76830691225385550, -236.3156058738864544 ) ) ;
#34202=DIRECTION ( 'NONE',  ( -0.000000000000000000, -0.4721928772777346239, -0.8814952561688430555 ) ) ;
#34212=EDGE_LOOP ( 'NONE', ( #135068, #39582, #131284, #95043 ) ) ;
#34249=CIRCLE ( 'NONE', #100802, 0.1999999999999987899 ) ;
#34289=DIRECTION ( 'NONE',  ( -1.000000000000000000, -1.541880601228652843E-16, -2.878400969107353907E-16 ) ) ;
#34296=ORIENTED_EDGE ( 'NONE', *, *, #210020, .F. ) ;
#34315=DIRECTION ( 'NONE',  ( 1.000000000000000000, 0.000000000000000000, 0.000000000000000000 ) ) ;
#34338=EDGE_CURVE ( 'NONE', #242741, #65949, #115795, .T. ) ;
#34371=CARTESIAN_POINT ( 'NONE',  ( -21.14999999999999858, 1.658775325997247752, -230.6916041481598540 ) ) ;
#34385=CIRCLE ( 'NONE', #88492, 0.09999999999999986677 ) ;
#34390=DIRECTION ( 'NONE',  ( 0.000000000000000000, -0.4721928772777346239, -0.8814952561688430555 ) ) ;
#34392=VECTOR ( 'NONE', #226201, 1000.000000000000000 ) ;
#34395=CARTESIAN_POINT ( 'NONE',  ( 23.14999999999998437, 10.69888912757691202, -235.6450824654141059 ) ) ;
#34427=DIRECTION ( 'NONE',  ( 1.000000000000000000, 1.541880601228652843E-16, 2.878400969107353907E-16 ) ) ;
#34429=ADVANCED_FACE ( 'NONE', ( #1996 ), #217192, .F. ) ;
#34448=ORIENTED_EDGE ( 'NONE', *, *, #154099, .T. ) ;
#34468=CARTESIAN_POINT ( 'NONE',  ( -18.59999999999999787, 38.30077178631846380, -261.1858881914067751 ) ) ;
#34520=TOROIDAL_SURFACE ( 'NONE', #138534, 7.800000000000000711, 0.1000000000000000056 ) ;
#34521=CARTESIAN_POINT ( 'NONE',  ( -21.08479644141223375, 10.07329993697807069, -228.1119308447289598 ) ) ;
#34522=DIRECTION ( 'NONE',  ( -1.000000000000000000, -0.000000000000000000, -0.000000000000000000 ) ) ;
#34536=CARTESIAN_POINT ( 'NONE',  ( 18.41356215285961895, 8.841736820195405855, -245.4273993276876524 ) ) ;
#34537=DIRECTION ( 'NONE',  ( 2.840903330521631775E-16, -0.8454177738465993297, -0.5341055959866553016 ) ) ;
#34540=CARTESIAN_POINT ( 'NONE',  ( 20.94999999999999929, 36.65892442174935439, -249.5511627012433848 ) ) ;
#34543=VERTEX_POINT ( 'NONE', #134648 ) ;
#34551=EDGE_CURVE ( 'NONE', #134482, #24049, #61824, .T. ) ;
#34552=ORIENTED_EDGE ( 'NONE', *, *, #37696, .F. ) ;
#34565=( NAMED_UNIT ( * ) SI_UNIT ( $, .STERADIAN. ) SOLID_ANGLE_UNIT ( ) );
#34599=B_SPLINE_CURVE_WITH_KNOTS ( 'NONE', 3,
 ( #1126, #80666, #201927, #42850, #122391, #23315, #102789 ),
 .UNSPECIFIED., .F., .F.,
 ( 4, 3, 4 ),
 ( 0.000000000000000000, 0.0009834301579440011751, 0.001767853679402673663 ),
 .UNSPECIFIED. ) ;
#34617=VERTEX_POINT ( 'NONE', #42015 ) ;
#34638=EDGE_CURVE ( 'NONE', #34148, #157381, #249274, .T. ) ;
#34652=ORIENTED_EDGE ( 'NONE', *, *, #149586, .T. ) ;
#34653=EDGE_CURVE ( 'NONE', #24049, #188383, #228433, .T. ) ;
#34655=CARTESIAN_POINT ( 'NONE',  ( 21.08832698747859169, 22.05205433789857850, -231.7715725143952170 ) ) ;
#34677=EDGE_CURVE ( 'NONE', #17591, #229996, #240882, .T. ) ;
#34701=CARTESIAN_POINT ( 'NONE',  ( -21.44999999999999929, 29.23678660621682113, -237.4641088729839282 ) ) ;
#34705=EDGE_CURVE ( 'NONE', #248947, #111286, #11961, .T. ) ;
#34716=EDGE_CURVE ( 'NONE', #128122, #21732, #222362, .T. ) ;
#34720=VECTOR ( 'NONE', #202640, 1000.000000000000000 ) ;
#34728=EDGE_CURVE ( 'NONE', #79572, #103016, #5898, .T. ) ;
#34753=EDGE_CURVE ( 'NONE', #236113, #184466, #186740, .T. ) ;
#34767=AXIS2_PLACEMENT_3D ( 'NONE', #231392, #252210, #211827 ) ;
#34792=ORIENTED_EDGE ( 'NONE', *, *, #103249, .F. ) ;
#34794=AXIS2_PLACEMENT_3D ( 'NONE', #72630, #214675, #232989 ) ;
#34799=DIRECTION ( 'NONE',  ( -0.7071067811865473507, -0.3338907855510733769, -0.6233112732207618523 ) ) ;
#34827=ORIENTED_EDGE ( 'NONE', *, *, #122966, .T. ) ;
#34849=EDGE_CURVE ( 'NONE', #74203, #101747, #74331, .T. ) ;
#34865=DIRECTION ( 'NONE',  ( 1.000000000000000000, -0.000000000000000000, -0.000000000000000000 ) ) ;
#34878=ORIENTED_EDGE ( 'NONE', *, *, #240733, .F. ) ;
#34913=ORIENTED_EDGE ( 'NONE', *, *, #34753, .T. ) ;
#34988=CARTESIAN_POINT ( 'NONE',  ( 21.14999999999999858, 22.07612373182271881, -231.7717111801312342 ) ) ;
#35062=VERTEX_POINT ( 'NONE', #236513 ) ;
#35066=DIRECTION ( 'NONE',  ( 0.000000000000000000, 0.4721928772776973204, 0.8814952561688629284 ) ) ;
#35084=FACE_OUTER_BOUND ( 'NONE', #212036, .T. ) ;
#35103=EDGE_CURVE ( 'NONE', #69221, #50036, #240382, .T. ) ;
#35113=VERTEX_POINT ( 'NONE', #22634 ) ;
#35133=EDGE_LOOP ( 'NONE', ( #232350, #61830, #222119 ) ) ;
#35144=CARTESIAN_POINT ( 'NONE',  ( 23.24999999999999289, 29.04162040546706436, -238.0402253144129929 ) ) ;
#35160=ORIENTED_EDGE ( 'NONE', *, *, #57117, .T. ) ;
#35229=CARTESIAN_POINT ( 'NONE',  ( 18.59999999999999076, 28.90625159212240547, -238.0811555523021070 ) ) ;
#35238=AXIS2_PLACEMENT_3D ( 'NONE', #126715, #162016, #186707 ) ;
#35255=EDGE_CURVE ( 'NONE', #184383, #224941, #78725, .T. ) ;
#35279=DIRECTION ( 'NONE',  ( -1.000000000000000000, 3.469446951953635015E-14, 0.000000000000000000 ) ) ;
#35285=DIRECTION ( 'NONE',  ( 0.000000000000000000, -0.8814952561688437216, 0.4721928772777334582 ) ) ;
#35306=DIRECTION ( 'NONE',  ( 1.000000000000000000, 0.000000000000000000, 0.000000000000000000 ) ) ;
#35337=SPHERICAL_SURFACE ( 'NONE', #99313, 0.1000000000000000056 ) ;
#35419=CARTESIAN_POINT ( 'NONE',  ( 20.74625933824019697, 18.86462450770046928, -229.9421460041290004 ) ) ;
#35420=EDGE_LOOP ( 'NONE', ( #245849, #194838, #206574, #74006 ) ) ;
#35434=CIRCLE ( 'NONE', #151943, 0.09999999999999997780 ) ;
#35454=DIRECTION ( 'NONE',  ( -1.000000000000000000, 0.000000000000000000, 0.000000000000000000 ) ) ;
#35455=CARTESIAN_POINT ( 'NONE',  ( 20.85000000000000142, 45.93315328338058379, -256.6017782078560003 ) ) ;
#35521=CARTESIAN_POINT ( 'NONE',  ( 18.39999999999999858, 8.780520186313291120, -245.4165333277510115 ) ) ;
#35532=CARTESIAN_POINT ( 'NONE',  ( -23.25000000000000000, 31.49702336731127872, -233.4564499823349877 ) ) ;
#35535=CARTESIAN_POINT ( 'NONE',  ( -23.25000000000000000, 36.65892442174935439, -249.5511627012433848 ) ) ;
#35547=ORIENTED_EDGE ( 'NONE', *, *, #236977, .F. ) ;
#35554=EDGE_CURVE ( 'NONE', #162422, #254810, #220420, .T. ) ;
#35576=LINE ( 'NONE', #236308, #240901 ) ;
#35579=VERTEX_POINT ( 'NONE', #64953 ) ;
#35609=DIRECTION ( 'NONE',  ( 1.000000000000000000, -0.000000000000000000, -0.000000000000000000 ) ) ;
#35612=CARTESIAN_POINT ( 'NONE',  ( -20.94999999999999929, 42.15997144203495139, -239.2817429668763793 ) ) ;
#35613=CARTESIAN_POINT ( 'NONE',  ( 23.25000000000000000, 11.60058429089262333, -246.3380203656811887 ) ) ;
#35638=LINE ( 'NONE', #115140, #241240 ) ;
#35657=VERTEX_POINT ( 'NONE', #191361 ) ;
#35696=CIRCLE ( 'NONE', #248040, 0.5999999999999992006 ) ;
#35704=CARTESIAN_POINT ( 'NONE',  ( -21.55000000000000426, 29.50054346320101928, -236.9717244483098568 ) ) ;
#35713=ORIENTED_EDGE ( 'NONE', *, *, #93472, .T. ) ;
#35716=FACE_OUTER_BOUND ( 'NONE', #32214, .T. ) ;
#35718=ORIENTED_EDGE ( 'NONE', *, *, #77294, .F. ) ;
#35733=EDGE_LOOP ( 'NONE', ( #43743, #67980, #127891, #121743 ) ) ;
#35740=PLANE ( 'NONE',  #249377 ) ;
#35744=CARTESIAN_POINT ( 'NONE',  ( 20.94999999999999929, 38.42191493408704872, -250.4955484557988541 ) ) ;
#35751=ORIENTED_EDGE ( 'NONE', *, *, #34638, .T. ) ;
#35771=EDGE_CURVE ( 'NONE', #63208, #180293, #45798, .T. ) ;
#35772=DIRECTION ( 'NONE',  ( 0.000000000000000000, -0.8814952561688430555, 0.4721928772777346239 ) ) ;
#35780=DIRECTION ( 'NONE',  ( 0.000000000000000000, 0.03181660087582099256, -0.9994937237965573207 ) ) ;
#35786=ORIENTED_EDGE ( 'NONE', *, *, #62120, .F. ) ;
#35795=ORIENTED_EDGE ( 'NONE', *, *, #242813, .T. ) ;
#35817=CARTESIAN_POINT ( 'NONE',  ( 18.50000000000000000, 9.122720154857379526, -245.4644708025848558 ) ) ;
#35834=DIRECTION ( 'NONE',  ( 0.000000000000000000, 0.4721928772777551075, 0.8814952561688320642 ) ) ;
#35882=EDGE_CURVE ( 'NONE', #74336, #222562, #137356, .T. ) ;
#35904=EDGE_CURVE ( 'NONE', #208784, #62371, #24980, .T. ) ;
#35925=ORIENTED_EDGE ( 'NONE', *, *, #8072, .T. ) ;
#35945=VERTEX_POINT ( 'NONE', #65939 ) ;
#35956=AXIS2_PLACEMENT_3D ( 'NONE', #26583, #220894, #44844 ) ;
#35985=AXIS2_PLACEMENT_3D ( 'NONE', #193607, #13676, #94490 ) ;
#36006=ORIENTED_EDGE ( 'NONE', *, *, #248484, .F. ) ;
#36007=CARTESIAN_POINT ( 'NONE',  ( 20.85000000000000142, 45.93315328338058379, -256.6017782078560003 ) ) ;
#36035=CARTESIAN_POINT ( 'NONE',  ( -18.59999999999999787, 14.72981487416292623, -236.4853282537515895 ) ) ;
#36055=CARTESIAN_POINT ( 'NONE',  ( -22.50000000000094147, -3.092988775432980564, -228.1437074281571995 ) ) ;
#36082=ORIENTED_EDGE ( 'NONE', *, *, #142953, .F. ) ;
#36084=CARTESIAN_POINT ( 'NONE',  ( 21.05000000000000071, 28.08470566095357057, -239.2860081655328770 ) ) ;
#36088=EDGE_CURVE ( 'NONE', #159861, #135978, #136144, .T. ) ;
#36090=CARTESIAN_POINT ( 'NONE',  ( -20.94999999999999929, 13.71992543034163958, -238.5823796952984992 ) ) ;
#36097=ORIENTED_EDGE ( 'NONE', *, *, #191264, .T. ) ;
#36099=ORIENTED_EDGE ( 'NONE', *, *, #215598, .F. ) ;
#36107=EDGE_CURVE ( 'NONE', #218506, #82377, #95747, .T. ) ;
#36129=FACE_OUTER_BOUND ( 'NONE', #163566, .T. ) ;
#36134=DIRECTION ( 'NONE',  ( 0.000000000000000000, 0.8814952561688430555, -0.4721928772777346239 ) ) ;
#36135=EDGE_CURVE ( 'NONE', #240452, #251749, #199374, .T. ) ;
#36163=AXIS2_PLACEMENT_3D ( 'NONE', #215667, #218229, #158320 ) ;
#36167=DIRECTION ( 'NONE',  ( 0.000000000000000000, 0.8814952561688476074, -0.4721928772777262417 ) ) ;
#36176=ORIENTED_EDGE ( 'NONE', *, *, #133454, .T. ) ;
#36178=DIRECTION ( 'NONE',  ( 0.000000000000000000, 0.8814952561688430555, -0.4721928772777346239 ) ) ;
#36200=CARTESIAN_POINT ( 'NONE',  ( -18.59999999999999787, 43.17747518314618560, -245.0773422074893233 ) ) ;
#36213=CARTESIAN_POINT ( 'NONE',  ( 22.00356870141288823, 10.55423491370503797, -227.3381210828028713 ) ) ;
#36241=ORIENTED_EDGE ( 'NONE', *, *, #166195, .F. ) ;
#36252=EDGE_CURVE ( 'NONE', #246715, #186847, #166064, .T. ) ;
#36257=CIRCLE ( 'NONE', #69563, 0.1000000000000013933 ) ;
#36272=DIRECTION ( 'NONE',  ( 0.000000000000000000, -0.4721928772777383987, -0.8814952561688410571 ) ) ;
#36283=DIRECTION ( 'NONE',  ( -1.000000000000000000, -1.541880601228652843E-16, -2.878400969107353907E-16 ) ) ;
#36287=CYLINDRICAL_SURFACE ( 'NONE', #195560, 0.09999999999999986677 ) ;
#36290=EDGE_LOOP ( 'NONE', ( #116524, #177793, #197525, #226464 ) ) ;
#36323=CARTESIAN_POINT ( 'NONE',  ( 19.97071067811863898, 34.44376430008541945, -235.0681652939917115 ) ) ;
#36352=CARTESIAN_POINT ( 'NONE',  ( -20.94999999999999929, 13.71992543034163958, -238.5823796952984992 ) ) ;
#36366=CARTESIAN_POINT ( 'NONE',  ( 23.14999999999999858, 28.46934351190515855, -239.7465010792843714 ) ) ;
#36369=DIRECTION ( 'NONE',  ( -0.000000000000000000, 0.4721928772777345684, 0.8814952561688429444 ) ) ;
#36377=ORIENTED_EDGE ( 'NONE', *, *, #96784, .T. ) ;
#36394=AXIS2_PLACEMENT_3D ( 'NONE', #125922, #242030, #165067 ) ;
#36397=CARTESIAN_POINT ( 'NONE',  ( -20.07928932188135107, 30.12641191371051264, -235.5915679455963812 ) ) ;
#36413=ORIENTED_EDGE ( 'NONE', *, *, #126857, .T. ) ;
#36421=VECTOR ( 'NONE', #87848, 1000.000000000000000 ) ;
#36426=ORIENTED_EDGE ( 'NONE', *, *, #208627, .F. ) ;
#36442=DIRECTION ( 'NONE',  ( -1.000000000000000000, -0.000000000000000000, -0.000000000000000000 ) ) ;
#36462=PLANE ( 'NONE',  #241354 ) ;
#36465=CARTESIAN_POINT ( 'NONE',  ( -18.50000000000000000, 42.15997144203495139, -239.2817429668763793 ) ) ;
#36521=ADVANCED_FACE ( 'NONE', ( #98008 ), #232437, .T. ) ;
#36550=ORIENTED_EDGE ( 'NONE', *, *, #66638, .T. ) ;
#36558=CARTESIAN_POINT ( 'NONE',  ( 21.05000000000000071, 23.45160524131172153, -253.2535058871250726 ) ) ;
#36598=ORIENTED_EDGE ( 'NONE', *, *, #149687, .T. ) ;
#36607=DIRECTION ( 'NONE',  ( 0.000000000000000000, -0.8814952561688430555, 0.4721928772777346239 ) ) ;
#36668=ORIENTED_EDGE ( 'NONE', *, *, #254579, .F. ) ;
#36669=EDGE_CURVE ( 'NONE', #148687, #164610, #95477, .T. ) ;
#36697=ORIENTED_EDGE ( 'NONE', *, *, #176052, .T. ) ;
#36699=CARTESIAN_POINT ( 'NONE',  ( 20.72390388899194136, 18.75055638538003322, -227.9445042245518209 ) ) ;
#36718=EDGE_CURVE ( 'NONE', #53624, #2075, #49699, .T. ) ;
#36735=EDGE_CURVE ( 'NONE', #56714, #250188, #116349, .T. ) ;
#36764=EDGE_LOOP ( 'NONE', ( #255086, #245446, #231726, #198254 ) ) ;
#36767=ORIENTED_EDGE ( 'NONE', *, *, #237163, .F. ) ;
#36847=CARTESIAN_POINT ( 'NONE',  ( 18.50000000000000000, 38.28679861725831302, -261.0868692510649680 ) ) ;
#36861=EDGE_LOOP ( 'NONE', ( #43131, #159615, #112666, #154852 ) ) ;
#36883=DIRECTION ( 'NONE',  ( 0.000000000000000000, 0.8814952561688476074, -0.4721928772777262417 ) ) ;
#36899=CARTESIAN_POINT ( 'NONE',  ( 21.14999999999999858, -3.187427350888460076, -228.3200064793908837 ) ) ;
#36957=VECTOR ( 'NONE', #182699, 1000.000000000000000 ) ;
#36967=DIRECTION ( 'NONE',  ( -1.000000000000000000, -0.000000000000000000, -0.000000000000000000 ) ) ;
#36977=CARTESIAN_POINT ( 'NONE',  ( 23.14999999999999858, 28.36802138732021206, -238.7571110118315971 ) ) ;
#37009=FACE_OUTER_BOUND ( 'NONE', #237681, .T. ) ;
#37015=ADVANCED_FACE ( 'NONE', ( #213830 ), #196824, .T. ) ;
#37027=CARTESIAN_POINT ( 'NONE',  ( -18.50000000000000000, 38.28679861725832012, -261.0868692510649680 ) ) ;
#37035=EDGE_CURVE ( 'NONE', #45747, #181045, #255470, .T. ) ;
#37074=CARTESIAN_POINT ( 'NONE',  ( 23.14999999999999858, 36.65892442174935439, -249.5511627012433848 ) ) ;
#37077=CIRCLE ( 'NONE', #91034, 0.1000000000000013933 ) ;
#37117=ORIENTED_EDGE ( 'NONE', *, *, #250407, .F. ) ;
#37118=ADVANCED_FACE ( 'NONE', ( #222797 ), #249966, .F. ) ;
#37128=AXIS2_PLACEMENT_3D ( 'NONE', #28978, #150178, #65478 ) ;
#37137=DIRECTION ( 'NONE',  ( 0.000000000000000000, 0.1397316906016290161, -0.9901894034181595305 ) ) ;
#37138=ORIENTED_EDGE ( 'NONE', *, *, #30199, .T. ) ;
#37145=ORIENTED_EDGE ( 'NONE', *, *, #50828, .F. ) ;
#37162=AXIS2_PLACEMENT_3D ( 'NONE', #51922, #252700, #214866 ) ;
#37195=DIRECTION ( 'NONE',  ( -7.304098846217608103E-16, 0.4721928772776973204, 0.8814952561688629284 ) ) ;
#37200=DIRECTION ( 'NONE',  ( -0.000000000000000000, 0.8814952561688430555, -0.4721928772777346239 ) ) ;
#37244=AXIS2_PLACEMENT_3D ( 'NONE', #150732, #186004, #89457 ) ;
#37246=AXIS2_PLACEMENT_3D ( 'NONE', #67522, #229180, #8842 ) ;
#37254=CARTESIAN_POINT ( 'NONE',  ( -20.94999999999999929, 14.81796439977981272, -236.5325475414793743 ) ) ;
#37293=DIRECTION ( 'NONE',  ( 0.000000000000000000, 0.8814952561688448318, -0.4721928772777310157 ) ) ;
#37297=CIRCLE ( 'NONE', #166489, 0.1999999999999987899 ) ;
#37335=CARTESIAN_POINT ( 'NONE',  ( -18.50000000000000711, 9.064267525453134411, -245.4573321305639126 ) ) ;
#37367=CARTESIAN_POINT ( 'NONE',  ( 22.40000000000010516, -3.140208063161409324, -228.2318569537746953 ) ) ;
#37376=ORIENTED_EDGE ( 'NONE', *, *, #114140, .F. ) ;
#37442=FACE_OUTER_BOUND ( 'NONE', #169529, .T. ) ;
#37464=CARTESIAN_POINT ( 'NONE',  ( 23.14999999999999858, 21.15538238767524604, -233.7023398932965108 ) ) ;
#37472=ADVANCED_FACE ( 'NONE', ( #57950 ), #158394, .F. ) ;
#37478=CARTESIAN_POINT ( 'NONE',  ( 20.95512820512820440, 18.86447962780959386, -229.9497396848627204 ) ) ;
#37489=DIRECTION ( 'NONE',  ( -2.578261006436898806E-14, 0.9371753822965325220, -0.3488585713686107592 ) ) ;
#37511=B_SPLINE_CURVE_WITH_KNOTS ( 'NONE', 3,
 ( #73331, #211528, #154163, #54989, #32933, #152872, #228533, #13331, #90268, #207688 ),
 .UNSPECIFIED., .F., .F.,
 ( 4, 3, 3, 4 ),
 ( 0.000000000000000000, 0.0002000000000002886513, 0.001000000000045113023, 0.001967863649472102652 ),
 .UNSPECIFIED. ) ;
#37520=CARTESIAN_POINT ( 'NONE',  ( 21.05000000000254090, 18.87203871602090643, -227.9647184347600160 ) ) ;
#37526=CARTESIAN_POINT ( 'NONE',  ( 21.06277459767462545, 22.07630317885907800, -231.6739566574008506 ) ) ;
#37542=CARTESIAN_POINT ( 'NONE',  ( -22.39999999999999858, 12.76524917372336709, -223.4223513401831553 ) ) ;
#37566=FACE_OUTER_BOUND ( 'NONE', #44314, .T. ) ;
#37579=CARTESIAN_POINT ( 'NONE',  ( -20.94999999999999929, 4.436385504674529301, -245.3241086753762659 ) ) ;
#37591=CIRCLE ( 'NONE', #212379, 0.1000000000000013933 ) ;
#37596=FACE_OUTER_BOUND ( 'NONE', #237241, .T. ) ;
#37646=DIRECTION ( 'NONE',  ( 3.469446951953634384E-14, -0.8814952561688430555, 0.4721928772777346239 ) ) ;
#37664=ORIENTED_EDGE ( 'NONE', *, *, #79637, .F. ) ;
#37672=AXIS2_PLACEMENT_3D ( 'NONE', #173059, #252533, #73945 ) ;
#37683=CARTESIAN_POINT ( 'NONE',  ( -23.25000000000000000, 25.94586868676353575, -241.5435999122864530 ) ) ;
#37685=AXIS2_PLACEMENT_3D ( 'NONE', #36084, #19067, #215969 ) ;
#37692=LINE ( 'NONE', #195486, #171583 ) ;
#37696=EDGE_CURVE ( 'NONE', #134779, #126467, #94214, .T. ) ;
#37741=LINE ( 'NONE', #23314, #58144 ) ;
#37822=ADVANCED_FACE ( 'NONE', ( #135898 ), #217998, .T. ) ;
#37873=FACE_OUTER_BOUND ( 'NONE', #150366, .T. ) ;
#37877=CARTESIAN_POINT ( 'NONE',  ( -18.59999999999999787, 16.60731133254646963, -240.9277311905271688 ) ) ;
#37879=ADVANCED_FACE ( 'NONE', ( #41975 ), #8551, .F. ) ;
#37887=CARTESIAN_POINT ( 'NONE',  ( -18.58735405345343850, 38.15589195147379087, -261.2056054829760683 ) ) ;
#37895=CARTESIAN_POINT ( 'NONE',  ( -18.59999999999999787, 43.21392023178790964, -245.1418509714632421 ) ) ;
#37896=ADVANCED_FACE ( 'NONE', ( #125349 ), #22414, .T. ) ;
#37928=DIRECTION ( 'NONE',  ( 1.000000000000000000, 0.000000000000000000, 0.000000000000000000 ) ) ;
#37933=ORIENTED_EDGE ( 'NONE', *, *, #238606, .T. ) ;
#37953=LINE ( 'NONE', #99160, #201277 ) ;
#37980=ORIENTED_EDGE ( 'NONE', *, *, #52829, .F. ) ;
#37984=DIRECTION ( 'NONE',  ( -0.000000000000000000, 0.4721928772777345684, 0.8814952561688429444 ) ) ;
#38082=FACE_OUTER_BOUND ( 'NONE', #231524, .T. ) ;
#38167=CARTESIAN_POINT ( 'NONE',  ( 20.94999999999999574, 18.24178995542692050, -237.7003448530951459 ) ) ;
#38170=CARTESIAN_POINT ( 'NONE',  ( -20.94788355080264353, 46.36250628750308778, -243.0620573837410063 ) ) ;
#38175=DIRECTION ( 'NONE',  ( 0.000000000000000000, 0.8814952561688437216, -0.4721928772777334582 ) ) ;
#38193=ORIENTED_EDGE ( 'NONE', *, *, #227439, .T. ) ;
#38217=EDGE_CURVE ( 'NONE', #104319, #144042, #187448, .T. ) ;
#38234=DIRECTION ( 'NONE',  ( -1.000000000000000000, -8.674042436075348305E-17, -1.619280515896124405E-16 ) ) ;
#38262=VERTEX_POINT ( 'NONE', #213397 ) ;
#38264=DIRECTION ( 'NONE',  ( 0.000000000000000000, 0.8814952561688429444, -0.4721928772777349570 ) ) ;
#38273=DIRECTION ( 'NONE',  ( 0.000000000000000000, -0.4721928772776973204, -0.8814952561688629284 ) ) ;
#38287=CARTESIAN_POINT ( 'NONE',  ( -20.94999999999999929, 13.60254931771583387, -238.7443143987590304 ) ) ;
#38293=CARTESIAN_POINT ( 'NONE',  ( -18.48408745364643835, 37.98660231122499908, -261.2259190080672511 ) ) ;
#38305=ORIENTED_EDGE ( 'NONE', *, *, #231116, .F. ) ;
#38316=AXIS2_PLACEMENT_3D ( 'NONE', #54101, #131075, #37137 ) ;
#38323=CARTESIAN_POINT ( 'NONE',  ( -20.94999999999999929, 28.50120599808395028, -258.2149742250584268 ) ) ;
#38339=DIRECTION ( 'NONE',  ( 0.000000000000000000, -0.8814952561688476074, 0.4721928772777262417 ) ) ;
#38364=DIRECTION ( 'NONE',  ( 1.000000000000000000, 0.000000000000000000, 0.000000000000000000 ) ) ;
#38368=CARTESIAN_POINT ( 'NONE',  ( 18.46858270002953972, 8.915580963857621555, -245.4376901980162131 ) ) ;
#38377=DIRECTION ( 'NONE',  ( 1.000000000000000000, 0.000000000000000000, 0.000000000000000000 ) ) ;
#38406=CARTESIAN_POINT ( 'NONE',  ( -18.50000000000000000, 9.122720154857367092, -245.4644708025848558 ) ) ;
#38413=DIRECTION ( 'NONE',  ( -0.7071067811865474617, -0.3338907855510734324, -0.6233112732207618523 ) ) ;
#38415=ORIENTED_EDGE ( 'NONE', *, *, #58195, .T. ) ;
#38423=CARTESIAN_POINT ( 'NONE',  ( -20.85000000000000142, 43.35377423437995503, -245.1717807829448930 ) ) ;
#38492=AXIS2_PLACEMENT_3D ( 'NONE', #144880, #84880, #47060 ) ;
#38496=DIRECTION ( 'NONE',  ( 0.000000000000000000, -0.8814952561688431665, 0.4721928772777346794 ) ) ;
#38523=ORIENTED_EDGE ( 'NONE', *, *, #31691, .F. ) ;
#38540=AXIS2_PLACEMENT_3D ( 'NONE', #199, #233993, #99285 ) ;
#38547=CARTESIAN_POINT ( 'NONE',  ( -18.59999999999999787, 42.94477010600543565, -254.3363632230312703 ) ) ;
#38558=ADVANCED_FACE ( 'NONE', ( #157114 ), #180271, .F. ) ;
#38568=VERTEX_POINT ( 'NONE', #72442 ) ;
#38573=DIRECTION ( 'NONE',  ( 0.000000000000000000, 0.8814952561688437216, -0.4721928772777334582 ) ) ;
#38597=ORIENTED_EDGE ( 'NONE', *, *, #156278, .T. ) ;
#38636=B_SPLINE_CURVE_WITH_KNOTS ( 'NONE', 3,
 ( #17322, #138503, #55114, #115126, #197220, #38170, #154301, #77265, #233800, #16052, #173867, #95553, #176403, #253338, #60272, #19892, #99385, #156850, #98089 ),
 .UNSPECIFIED., .F., .F.,
 ( 4, 3, 3, 3, 3, 3, 4 ),
 ( -2.000416914651719952E-06, 0.000000000000000000, 4.714008503744950701E-05, 9.979203887777911156E-05, 0.0001372215519229559935, 0.0001635031576221014160, 0.0001900083748504201547 ),
 .UNSPECIFIED. ) ;
#38650=AXIS2_PLACEMENT_3D ( 'NONE', #129062, #252843, #33856 ) ;
#38653=ORIENTED_EDGE ( 'NONE', *, *, #86413, .F. ) ;
#38667=CARTESIAN_POINT ( 'NONE',  ( 20.94999999999999574, 18.90448995781211750, -232.7802074516171444 ) ) ;
#38689=CARTESIAN_POINT ( 'NONE',  ( 21.00000000000000000, 22.53103078161933936, -230.9224853114453140 ) ) ;
#38710=DIRECTION ( 'NONE',  ( 0.000000000000000000, 0.8814952561688476074, -0.4721928772777262417 ) ) ;
#38713=EDGE_CURVE ( 'NONE', #249890, #118730, #226189, .T. ) ;
#38737=CARTESIAN_POINT ( 'NONE',  ( 23.14999999999999503, 31.44980407958351876, -233.5445995079518582 ) ) ;
#38765=CARTESIAN_POINT ( 'NONE',  ( 23.14999999999999503, 21.10816309994747186, -233.7904894189133813 ) ) ;
#38777=ORIENTED_EDGE ( 'NONE', *, *, #80620, .F. ) ;
#38785=DIRECTION ( 'NONE',  ( 1.000000000000000000, 0.000000000000000000, 0.000000000000000000 ) ) ;
#38786=EDGE_CURVE ( 'NONE', #194489, #34148, #147117, .T. ) ;
#38791=EDGE_LOOP ( 'NONE', ( #1317, #162971, #157222, #90027 ) ) ;
#38823=FACE_OUTER_BOUND ( 'NONE', #153184, .T. ) ;
#38834=AXIS2_PLACEMENT_3D ( 'NONE', #32924, #154154, #54981 ) ;
#38837=CARTESIAN_POINT ( 'NONE',  ( -23.15000000000000213, 23.68770167995059595, -252.8127582590406348 ) ) ;
#38845=CARTESIAN_POINT ( 'NONE',  ( -21.05000000000000071, 8.780520186313289344, -245.4165333277510115 ) ) ;
#38865=DIRECTION ( 'NONE',  ( 0.000000000000000000, -0.4721928772777346239, -0.8814952561688430555 ) ) ;
#38919=LINE ( 'NONE', #101389, #148008 ) ;
#38946=DIRECTION ( 'NONE',  ( 4.377807931758638000E-15, -0.7280513885558889120, 0.6855225566105335178 ) ) ;
#38974=CIRCLE ( 'NONE', #142981, 0.1000000000000013933 ) ;
#39001=DIRECTION ( 'NONE',  ( 0.000000000000000000, 0.4721928772777346239, 0.8814952561688430555 ) ) ;
#39002=EDGE_CURVE ( 'NONE', #48376, #85650, #252034, .T. ) ;
#39021=EDGE_CURVE ( 'NONE', #93118, #176327, #176188, .T. ) ;
#39040=ADVANCED_FACE ( 'NONE', ( #154275 ), #254576, .T. ) ;
#39060=ADVANCED_FACE ( 'NONE', ( #161948 ), #221869, .F. ) ;
#39067=CARTESIAN_POINT ( 'NONE',  ( 20.94999999999999929, 19.00443933019177223, -232.7770257915295531 ) ) ;
#39070=CIRCLE ( 'NONE', #22501, 0.09999999999999939493 ) ;
#39088=DIRECTION ( 'NONE',  ( 0.000000000000000000, -0.8814952561688430555, 0.4721928772777346239 ) ) ;
#39122=FACE_OUTER_BOUND ( 'NONE', #44431, .T. ) ;
#39152=AXIS2_PLACEMENT_3D ( 'NONE', #233126, #174460, #115719 ) ;
#39155=AXIS2_PLACEMENT_3D ( 'NONE', #168205, #246417, #109450 ) ;
#39158=CARTESIAN_POINT ( 'NONE',  ( -20.64999999999999858, 11.46684968301824448, -245.9610388612851750 ) ) ;
#39162=DIRECTION ( 'NONE',  ( 0.000000000000000000, 0.6046243595031880469, 0.7965107556683460599 ) ) ;
#39180=CARTESIAN_POINT ( 'NONE',  ( -20.54999999999999716, 26.18196512540240661, -241.1028522842020152 ) ) ;
#39193=CARTESIAN_POINT ( 'NONE',  ( -18.59117750673697245, 46.46967969402478360, -243.0849751855955674 ) ) ;
#39196=VERTEX_POINT ( 'NONE', #126651 ) ;
#39200=CARTESIAN_POINT ( 'NONE',  ( 18.39999999999999858, 8.841736820195473356, -245.4273993276876240 ) ) ;
#39207=VECTOR ( 'NONE', #176314, 1000.000000000000000 ) ;
#39209=LINE ( 'NONE', #101687, #146081 ) ;
#39217=ORIENTED_EDGE ( 'NONE', *, *, #118881, .T. ) ;
#39302=CARTESIAN_POINT ( 'NONE',  ( 20.95392731769792150, 18.83565523496773864, -229.9264601087687652 ) ) ;
#39320=VERTEX_POINT ( 'NONE', #232194 ) ;
#39325=ORIENTED_EDGE ( 'NONE', *, *, #89388, .F. ) ;
#39335=DIRECTION ( 'NONE',  ( 0.000000000000000000, 0.8814952561688388366, -0.4721928772777424510 ) ) ;
#39351=DIRECTION ( 'NONE',  ( 0.7071359030028089299, 0.6232856014206507034, -0.3338770338704052376 ) ) ;
#39359=AXIS2_PLACEMENT_3D ( 'NONE', #178044, #636, #116761 ) ;
#39363=VERTEX_POINT ( 'NONE', #150091 ) ;
#39422=AXIS2_PLACEMENT_3D ( 'NONE', #197431, #134868, #214424 ) ;
#39437=CIRCLE ( 'NONE', #193540, 0.09999999999999939493 ) ;
#39449=AXIS2_PLACEMENT_3D ( 'NONE', #39951, #195177, #116895 ) ;
#39461=CARTESIAN_POINT ( 'NONE',  ( -23.15000000000000213, 19.73066058418984170, -238.2142830767208466 ) ) ;
#39476=ADVANCED_FACE ( 'NONE', ( #119962 ), #200751, .F. ) ;
#39490=CARTESIAN_POINT ( 'NONE',  ( 22.49806830649814060, 12.56154382881637943, -223.4268007483960616 ) ) ;
#39519=DIRECTION ( 'NONE',  ( 0.000000000000000000, -0.4834676483507011624, -0.8753622295931228203 ) ) ;
#39526=CIRCLE ( 'NONE', #185243, 0.1000000000000013933 ) ;
#39552=AXIS2_PLACEMENT_3D ( 'NONE', #17243, #231160, #250686 ) ;
#39582=ORIENTED_EDGE ( 'NONE', *, *, #101289, .T. ) ;
#39632=EDGE_CURVE ( 'NONE', #203844, #103016, #161347, .T. ) ;
#39648=EDGE_CURVE ( 'NONE', #172354, #134581, #47770, .T. ) ;
#39677=CARTESIAN_POINT ( 'NONE',  ( -18.59999999999999787, 9.122720154857397290, -245.4644708025847990 ) ) ;
#39720=CIRCLE ( 'NONE', #85429, 0.09999999999999983902 ) ;
#39723=ADVANCED_FACE ( 'NONE', ( #190183 ), #208474, .T. ) ;
#39734=CARTESIAN_POINT ( 'NONE',  ( -20.94999999999999929, 18.92285928089247804, -233.3572654221044900 ) ) ;
#39789=CARTESIAN_POINT ( 'NONE',  ( 18.49999999999998934, 28.86532135423329493, -237.9457867389574517 ) ) ;
#39817=CARTESIAN_POINT ( 'NONE',  ( -20.94999999999999929, 36.02918351690955490, -236.0543695120161374 ) ) ;
#39854=ORIENTED_EDGE ( 'NONE', *, *, #123221, .F. ) ;
#39862=AXIS2_PLACEMENT_3D ( 'NONE', #217023, #21437, #61828 ) ;
#39875=VERTEX_POINT ( 'NONE', #24069 ) ;
#39898=VERTEX_POINT ( 'NONE', #175763 ) ;
#39936=CARTESIAN_POINT ( 'NONE',  ( -21.14999999999999858, 1.580567032079710055, -244.0902705724231794 ) ) ;
#39941=CARTESIAN_POINT ( 'NONE',  ( 20.85000000000000142, 36.65892442174935439, -249.5511627012433848 ) ) ;
#39946=EDGE_CURVE ( 'NONE', #104599, #157387, #57445, .T. ) ;
#39951=CARTESIAN_POINT ( 'NONE',  ( -20.85000000000000142, 43.08613539620618837, -254.3146655184800409 ) ) ;
#39952=ORIENTED_EDGE ( 'NONE', *, *, #203819, .F. ) ;
#40022=CARTESIAN_POINT ( 'NONE',  ( 23.14999999999999503, 20.97908333644147660, -233.6079013178409411 ) ) ;
#40052=LINE ( 'NONE', #99962, #16698 ) ;
#40060=EDGE_CURVE ( 'NONE', #253940, #38262, #244897, .T. ) ;
#40065=CARTESIAN_POINT ( 'NONE',  ( 20.12500000000000000, 18.88320179786139619, -228.9684431863134932 ) ) ;
#40066=CARTESIAN_POINT ( 'NONE',  ( -22.50000000000000000, 12.55148283907650608, -223.4215551264213104 ) ) ;
#40103=TOROIDAL_SURFACE ( 'NONE', #131651, 7.800000000000000711, 0.1000000000000000056 ) ;
#40115=AXIS2_PLACEMENT_3D ( 'NONE', #58796, #112391, #236173 ) ;
#40135=CIRCLE ( 'NONE', #27680, 0.09999999999998464284 ) ;
#40153=CARTESIAN_POINT ( 'NONE',  ( 18.43709777086140988, 37.95493834378066822, -261.2294694241335264 ) ) ;
#40160=DIRECTION ( 'NONE',  ( 0.000000000000000000, 0.4721928772776973204, 0.8814952561688629284 ) ) ;
#40168=VERTEX_POINT ( 'NONE', #23777 ) ;
#40181=CARTESIAN_POINT ( 'NONE',  ( -20.15000000000000568, 30.15980099226561606, -235.5292368182743132 ) ) ;
#40207=CARTESIAN_POINT ( 'NONE',  ( -18.46902351632712325, 8.797055283856513697, -245.4142078959211517 ) ) ;
#40248=CARTESIAN_POINT ( 'NONE',  ( 20.88420186297724257, 46.46179379974390855, -243.0832762246653260 ) ) ;
#40274=TOROIDAL_SURFACE ( 'NONE', #36163, 7.791421356237316687, 0.1000000000000000056 ) ;
#40307=EDGE_CURVE ( 'NONE', #114431, #212495, #47129, .T. ) ;
#40328=AXIS2_PLACEMENT_3D ( 'NONE', #62955, #257249, #220748 ) ;
#40329=EDGE_CURVE ( 'NONE', #78910, #121993, #187960, .T. ) ;
#40352=CARTESIAN_POINT ( 'NONE',  ( 21.97500000000000497, 30.37633856152204359, -235.1250019192171408 ) ) ;
#40388=EDGE_LOOP ( 'NONE', ( #157794, #73391, #225708, #117784, #123962 ) ) ;
#40394=AXIS2_PLACEMENT_3D ( 'NONE', #72131, #166117, #188210 ) ;
#40399=CARTESIAN_POINT ( 'NONE',  ( -21.29999999999995808, 3.558777552609279304, -231.8203201594644725 ) ) ;
#40427=CARTESIAN_POINT ( 'NONE',  ( 23.14999999999999858, 34.89593390941166007, -248.6067769466879156 ) ) ;
#40442=EDGE_CURVE ( 'NONE', #231084, #13871, #66021, .T. ) ;
#40464=CARTESIAN_POINT ( 'NONE',  ( -18.50000000000000000, 38.31554990269469840, -261.1022705275898943 ) ) ;
#40492=ORIENTED_EDGE ( 'NONE', *, *, #116935, .F. ) ;
#40502=ADVANCED_FACE ( 'NONE', ( #135660 ), #35337, .T. ) ;
#40516=EDGE_LOOP ( 'NONE', ( #243557, #99012, #150302, #211466 ) ) ;
#40533=VECTOR ( 'NONE', #212516, 1000.000000000000000 ) ;
#40545=DIRECTION ( 'NONE',  ( 0.000000000000000000, -0.5954378521545836689, -0.8034013718071036925 ) ) ;
#40552=EDGE_CURVE ( 'NONE', #184383, #213072, #19122, .T. ) ;
#40574=CIRCLE ( 'NONE', #132289, 0.1000000000000013933 ) ;
#40575=CARTESIAN_POINT ( 'NONE',  ( 20.94999999999999929, 28.60154115857409352, -258.4512230915049713 ) ) ;
#40578=DIRECTION ( 'NONE',  ( 0.000000000000000000, -0.03181660087581233282, 0.9994937237965575427 ) ) ;
#40586=DIRECTION ( 'NONE',  ( 2.952720810173288619E-16, -0.4721928772777346239, -0.8814952561688430555 ) ) ;
#40613=TOROIDAL_SURFACE ( 'NONE', #207182, 4.099999999999999645, 0.1000000000000000056 ) ;
#40652=AXIS2_PLACEMENT_3D ( 'NONE', #234517, #55854, #96277 ) ;
#40668=ORIENTED_EDGE ( 'NONE', *, *, #214068, .F. ) ;
#40673=ORIENTED_EDGE ( 'NONE', *, *, #47951, .F. ) ;
#40708=LINE ( 'NONE', #99328, #112608 ) ;
#40720=FACE_OUTER_BOUND ( 'NONE', #8562, .T. ) ;
#40738=ORIENTED_EDGE ( 'NONE', *, *, #192441, .T. ) ;
#40754=ORIENTED_EDGE ( 'NONE', *, *, #71512, .T. ) ;
#40770=CARTESIAN_POINT ( 'NONE',  ( 22.50000000000000000, 12.54152817314149715, -223.4164406214577241 ) ) ;
#40802=CARTESIAN_POINT ( 'NONE',  ( -21.05000000000000071, 18.60982576078065165, -226.6665746245395496 ) ) ;
#40837=EDGE_CURVE ( 'NONE', #211434, #157387, #72865, .T. ) ;
#40850=DIRECTION ( 'NONE',  ( 0.000000000000000000, 0.8814952561688428334, -0.4721928772777350125 ) ) ;
#40876=SPHERICAL_SURFACE ( 'NONE', #224069, 0.1000000000000000056 ) ;
#40890=ORIENTED_EDGE ( 'NONE', *, *, #120897, .T. ) ;
#40958=DIRECTION ( 'NONE',  ( 0.000000000000000000, 0.8814952561688437216, -0.4721928772777334582 ) ) ;
#40981=EDGE_CURVE ( 'NONE', #231084, #149228, #214939, .T. ) ;
#40992=DIRECTION ( 'NONE',  ( -0.000000000000000000, 0.8814952561688430555, -0.4721928772777346239 ) ) ;
#41070=VERTEX_POINT ( 'NONE', #23149 ) ;
#41097=CARTESIAN_POINT ( 'NONE',  ( -20.07928932188135107, 30.21456143932739380, -235.6387872333241660 ) ) ;
#41122=DIRECTION ( 'NONE',  ( 0.000000000000000000, -0.8814952561688476074, 0.4721928772777262417 ) ) ;
#41126=TOROIDAL_SURFACE ( 'NONE', #232657, 0.4000000000000005773, 0.1000000000000000056 ) ;
#41157=AXIS2_PLACEMENT_3D ( 'NONE', #229301, #173221, #175757 ) ;
#41179=ORIENTED_EDGE ( 'NONE', *, *, #58053, .T. ) ;
#41187=DIRECTION ( 'NONE',  ( -0.000000000000000000, 0.2438576117979275315, -0.9698110461157942730 ) ) ;
#41189=DIRECTION ( 'NONE',  ( 1.000000000000000000, 3.448943450116727512E-16, 6.438528483529605672E-16 ) ) ;
#41196=VERTEX_POINT ( 'NONE', #75118 ) ;
#41211=ORIENTED_EDGE ( 'NONE', *, *, #6774, .T. ) ;
#41238=CARTESIAN_POINT ( 'NONE',  ( 21.14999999999999858, -3.140208063160686791, -228.2318569537739847 ) ) ;
#41248=VERTEX_POINT ( 'NONE', #34701 ) ;
#41254=VERTEX_POINT ( 'NONE', #98453 ) ;
#41260=DIRECTION ( 'NONE',  ( 0.000000000000000000, -0.8814952561688429444, 0.4721928772777350680 ) ) ;
#41264=ORIENTED_EDGE ( 'NONE', *, *, #116481, .T. ) ;
#41278=CARTESIAN_POINT ( 'NONE',  ( 20.94999999999999574, 14.64166534854604507, -236.4381089660238331 ) ) ;
#41294=ORIENTED_EDGE ( 'NONE', *, *, #99618, .T. ) ;
#41326=DIRECTION ( 'NONE',  ( 0.000000000000000000, -0.4721928772776973204, -0.8814952561688629284 ) ) ;
#41351=DIRECTION ( 'NONE',  ( 0.000000000000000000, -0.8814952561688429444, 0.4721928772777349570 ) ) ;
#41370=DIRECTION ( 'NONE',  ( 1.000000000000000000, 3.448943450116723568E-16, 6.438528483529607644E-16 ) ) ;
#41413=DIRECTION ( 'NONE',  ( 0.000000000000000000, -0.8814952561688439436, 0.4721928772777329586 ) ) ;
#41442=AXIS2_PLACEMENT_3D ( 'NONE', #42337, #63164, #183142 ) ;
#41468=CARTESIAN_POINT ( 'NONE',  ( -23.25000000000000000, 11.31726856452598184, -246.8669175193824969 ) ) ;
#41481=CARTESIAN_POINT ( 'NONE',  ( -22.41119224318417125, -3.140208063160686791, -228.2318569537739847 ) ) ;
#41489=AXIS2_PLACEMENT_3D ( 'NONE', #208502, #174543, #110659 ) ;
#41517=ADVANCED_FACE ( 'NONE', ( #135701 ), #66587, .F. ) ;
#41527=CARTESIAN_POINT ( 'NONE',  ( 20.94983749550516450, 46.34703458179515678, -243.0587802416264651 ) ) ;
#41528=DIRECTION ( 'NONE',  ( -1.000000000000000000, 0.000000000000000000, -0.000000000000000000 ) ) ;
#41542=CARTESIAN_POINT ( 'NONE',  ( 21.14999999999999503, 1.619487989037824871, -230.7814958294534335 ) ) ;
#41556=VERTEX_POINT ( 'NONE', #215258 ) ;
#41579=CARTESIAN_POINT ( 'NONE',  ( 20.94999999999999929, 13.54362637910787370, -238.4879411198429580 ) ) ;
#41587=CYLINDRICAL_SURFACE ( 'NONE', #114003, 3.999999999999994671 ) ;
#41594=TOROIDAL_SURFACE ( 'NONE', #170793, 11.90000000000000391, 0.1000000000000000056 ) ;
#41624=DIRECTION ( 'NONE',  ( -1.000000000000000000, -1.541880601228652843E-16, -2.878400969107353907E-16 ) ) ;
#41628=ORIENTED_EDGE ( 'NONE', *, *, #256019, .F. ) ;
#41639=ADVANCED_FACE ( 'NONE', ( #75758 ), #10634, .F. ) ;
#41642=DIRECTION ( 'NONE',  ( 1.000000000000000000, 0.000000000000000000, 0.000000000000000000 ) ) ;
#41644=TOROIDAL_SURFACE ( 'NONE', #174947, 0.6000000000000006439, 0.1000000000000000056 ) ;
#41664=VERTEX_POINT ( 'NONE', #3915 ) ;
#41685=CARTESIAN_POINT ( 'NONE',  ( 22.39999999999999503, -3.275978944802467652, -228.2735455795363748 ) ) ;
#41688=CARTESIAN_POINT ( 'NONE',  ( -20.64999999999999858, 19.98118924431957311, -235.6825596947570602 ) ) ;
#41708=ORIENTED_EDGE ( 'NONE', *, *, #191441, .F. ) ;
#41739=CARTESIAN_POINT ( 'NONE',  ( -21.64999999999999858, 29.28400589394459175, -237.3759593473670293 ) ) ;
#41760=EDGE_LOOP ( 'NONE', ( #30262, #52266, #219377, #184826 ) ) ;
#41762=ADVANCED_FACE ( 'NONE', ( #89855 ), #258065, .T. ) ;
#41770=DIRECTION ( 'NONE',  ( 1.000000000000000000, 0.000000000000000000, 0.000000000000000000 ) ) ;
#41793=DIRECTION ( 'NONE',  ( 0.000000000000000000, 0.8814952561688428334, -0.4721928772777349570 ) ) ;
#41816=DIRECTION ( 'NONE',  ( 1.000000000000000000, 0.000000000000000000, 0.000000000000000000 ) ) ;
#41941=CARTESIAN_POINT ( 'NONE',  ( 18.60000000000000142, 9.122720154857409725, -245.4644708025847990 ) ) ;
#41949=ORIENTED_EDGE ( 'NONE', *, *, #239089, .T. ) ;
#41953=FILL_AREA_STYLE_COLOUR ( '', #195254 ) ;
#41965=DIRECTION ( 'NONE',  ( -1.000000000000000000, -0.000000000000000000, -0.000000000000000000 ) ) ;
#41972=DIRECTION ( 'NONE',  ( -0.000000000000000000, -0.8814952561688430555, 0.4721928772777346239 ) ) ;
#41975=FACE_OUTER_BOUND ( 'NONE', #96161, .T. ) ;
#41997=TOROIDAL_SURFACE ( 'NONE', #116994, 11.70000000000000462, 0.1000000000000000056 ) ;
#42015=CARTESIAN_POINT ( 'NONE',  ( -21.05000000000000071, 28.58935552370083144, -258.2621935127861548 ) ) ;
#42065=ADVANCED_FACE ( 'NONE', ( #132637 ), #104154, .T. ) ;
#42072=TOROIDAL_SURFACE ( 'NONE', #71286, 11.65000000000000036, 0.1000000000000000056 ) ;
#42083=DIRECTION ( 'NONE',  ( 0.000000000000000000, -0.8814952561688430555, 0.4721928772777346239 ) ) ;
#42119=EDGE_CURVE ( 'NONE', #179081, #196849, #32913, .T. ) ;
#42125=CARTESIAN_POINT ( 'NONE',  ( -21.14999999999999858, 7.128833340093095217, -233.7327013124392749 ) ) ;
#42126=ORIENTED_EDGE ( 'NONE', *, *, #128289, .F. ) ;
#42162=CARTESIAN_POINT ( 'NONE',  ( -18.59999999999999787, 16.44800918141279311, -240.8068063186265135 ) ) ;
#42168=ADVANCED_FACE ( 'NONE', ( #48919 ), #30679, .T. ) ;
#42176=EDGE_LOOP ( 'NONE', ( #143607, #114057, #257289, #238476 ) ) ;
#42202=CIRCLE ( 'NONE', #4750, 11.70000000000000639 ) ;
#42218=EDGE_LOOP ( 'NONE', ( #54624, #128151, #210083, #70341 ) ) ;
#42230=CARTESIAN_POINT ( 'NONE',  ( 21.07928932188134397, 10.02993822722304351, -228.1074463178677263 ) ) ;
#42256=PLANE ( 'NONE',  #12674 ) ;
#42268=ORIENTED_EDGE ( 'NONE', *, *, #187879, .T. ) ;
#42269=DIRECTION ( 'NONE',  ( 0.000000000000000000, -0.8814952561688430555, 0.4721928772777346239 ) ) ;
#42277=CARTESIAN_POINT ( 'NONE',  ( -20.94999999999999929, 14.81796439977981272, -236.5325475414793743 ) ) ;
#42317=CARTESIAN_POINT ( 'NONE',  ( -20.85000000000000142, 31.11065811373596190, -259.9087319612273177 ) ) ;
#42323=EDGE_CURVE ( 'NONE', #1463, #41556, #28958, .T. ) ;
#42336=CARTESIAN_POINT ( 'NONE',  ( 20.94999999999999929, 33.04479387145709524, -247.6151719044046899 ) ) ;
#42337=CARTESIAN_POINT ( 'NONE',  ( -20.85000000000000142, 31.15787740146373608, -259.8205824356103903 ) ) ;
#42354=DIRECTION ( 'NONE',  ( 1.000000000000000000, 0.000000000000000000, 0.000000000000000000 ) ) ;
#42374=DIRECTION ( 'NONE',  ( 0.000000000000000000, 0.8814952561688444987, -0.4721928772777320149 ) ) ;
#42384=ORIENTED_EDGE ( 'NONE', *, *, #217492, .F. ) ;
#42391=CARTESIAN_POINT ( 'NONE',  ( -21.05000000000000071, 10.91926294161908295, -235.7631306847335395 ) ) ;
#42419=AXIS2_PLACEMENT_3D ( 'NONE', #47468, #210436, #87873 ) ;
#42450=DIRECTION ( 'NONE',  ( -4.801466763864312543E-15, 0.7280513885558889120, -0.6855225566105335178 ) ) ;
#42547=DIRECTION ( 'NONE',  ( 0.000000000000000000, 0.8814952561688430555, -0.4721928772777346239 ) ) ;
#42560=ORIENTED_EDGE ( 'NONE', *, *, #31691, .T. ) ;
#42580=CIRCLE ( 'NONE', #188322, 2.099999999999989875 ) ;
#42594=EDGE_CURVE ( 'NONE', #34617, #156004, #195581, .T. ) ;
#42607=EDGE_CURVE ( 'NONE', #118204, #249188, #158189, .T. ) ;
#42632=CARTESIAN_POINT ( 'NONE',  ( -21.07954640115394085, 10.05929242768339371, -228.1222958643088248 ) ) ;
#42649=ADVANCED_FACE ( 'NONE', ( #207405 ), #108076, .F. ) ;
#42665=DIRECTION ( 'NONE',  ( 0.000000000000000000, -0.8814952561688413901, 0.4721928772777376215 ) ) ;
#42692=DIRECTION ( 'NONE',  ( 7.304098846218132695E-16, -0.4721928772777346794, -0.8814952561688431665 ) ) ;
#42706=CARTESIAN_POINT ( 'NONE',  ( 20.85000000000000142, 45.93315328338058379, -256.6017782078560003 ) ) ;
#42719=DIRECTION ( 'NONE',  ( 0.000000000000000000, -0.8814952561688430555, 0.4721928772777346239 ) ) ;
#42720=DIRECTION ( 'NONE',  ( 0.000000000000000000, 0.8814952561688437216, -0.4721928772777334582 ) ) ;
#42754=DIRECTION ( 'NONE',  ( -1.000000000000000000, 0.000000000000000000, 0.000000000000000000 ) ) ;
#42844=CARTESIAN_POINT ( 'NONE',  ( -21.14999999999999858, -3.187427350888460076, -228.3200064793908837 ) ) ;
#42850=CARTESIAN_POINT ( 'NONE',  ( -21.70464131381649509, 10.47921085838517463, -227.4781768778995570 ) ) ;
#42860=ORIENTED_EDGE ( 'NONE', *, *, #151865, .T. ) ;
#42861=ORIENTED_EDGE ( 'NONE', *, *, #145301, .T. ) ;
#42865=CARTESIAN_POINT ( 'NONE',  ( 21.05000000000000071, -3.187427350888460076, -228.3200064793908837 ) ) ;
#42869=EDGE_CURVE ( 'NONE', #86057, #222451, #258049, .T. ) ;
#42882=EDGE_CURVE ( 'NONE', #240363, #170273, #99235, .T. ) ;
#42904=VECTOR ( 'NONE', #171792, 1000.000000000000000 ) ;
#42912=EDGE_CURVE ( 'NONE', #135120, #18374, #166359, .T. ) ;
#42953=VECTOR ( 'NONE', #158513, 1000.000000000000114 ) ;
#42982=VERTEX_POINT ( 'NONE', #68871 ) ;
#43001=EDGE_CURVE ( 'NONE', #205178, #241214, #25077, .T. ) ;
#43009=CYLINDRICAL_SURFACE ( 'NONE', #60197, 0.09999999999999986677 ) ;
#43029=DIRECTION ( 'NONE',  ( 1.000000000000000000, -3.448943450116727019E-16, -6.438528483529604686E-16 ) ) ;
#43042=DIRECTION ( 'NONE',  ( 0.000000000000000000, 0.8814952561688430555, -0.4721928772777346239 ) ) ;
#43061=DIRECTION ( 'NONE',  ( 0.000000000000000000, 0.4721928772777330696, 0.8814952561688438326 ) ) ;
#43094=ORIENTED_EDGE ( 'NONE', *, *, #103082, .F. ) ;
#43108=AXIS2_PLACEMENT_3D ( 'NONE', #60412, #155705, #219484 ) ;
#43112=FACE_OUTER_BOUND ( 'NONE', #156040, .T. ) ;
#43119=AXIS2_PLACEMENT_3D ( 'NONE', #106739, #88444, #130158 ) ;
#43131=ORIENTED_EDGE ( 'NONE', *, *, #254095, .F. ) ;
#43140=DIRECTION ( 'NONE',  ( 1.734723475976817192E-14, 0.8814952561688430555, -0.4721928772777346239 ) ) ;
#43219=ORIENTED_EDGE ( 'NONE', *, *, #209126, .T. ) ;
#43232=CIRCLE ( 'NONE', #39155, 0.09999999999999630018 ) ;
#43240=ORIENTED_EDGE ( 'NONE', *, *, #32420, .T. ) ;
#43248=DIRECTION ( 'NONE',  ( 0.000000000000000000, 0.4721928772777343464, 0.8814952561688431665 ) ) ;
#43290=CIRCLE ( 'NONE', #147324, 4.049999999999994493 ) ;
#43298=EDGE_CURVE ( 'NONE', #83188, #238889, #233177, .T. ) ;
#43302=ORIENTED_EDGE ( 'NONE', *, *, #62490, .T. ) ;
#43327=ORIENTED_EDGE ( 'NONE', *, *, #254991, .T. ) ;
#43331=EDGE_LOOP ( 'NONE', ( #179017, #50843, #238934, #157987 ) ) ;
#43353=DIRECTION ( 'NONE',  ( 1.000000000000000000, 0.000000000000000000, 0.000000000000000000 ) ) ;
#43381=EDGE_LOOP ( 'NONE', ( #136192, #130700, #206779, #184489 ) ) ;
#43394=DIRECTION ( 'NONE',  ( 1.000000000000000000, 0.000000000000000000, 0.000000000000000000 ) ) ;
#43424=CARTESIAN_POINT ( 'NONE',  ( -23.25000000000000000, 23.40438595358395091, -253.3416554127419431 ) ) ;
#43451=PLANE ( 'NONE',  #16820 ) ;
#43464=CARTESIAN_POINT ( 'NONE',  ( -22.39999999999999858, 7.040683814476209612, -233.6854820247115185 ) ) ;
#43480=EDGE_CURVE ( 'NONE', #178121, #22846, #250092, .T. ) ;
#43495=CARTESIAN_POINT ( 'NONE',  ( 21.05000000000000071, 16.50669723772569952, -240.7258389668962479 ) ) ;
#43496=VERTEX_POINT ( 'NONE', #175375 ) ;
#43502=SPHERICAL_SURFACE ( 'NONE', #154172, 0.1000000000000000056 ) ;
#43506=AXIS2_PLACEMENT_3D ( 'NONE', #202835, #224950, #124599 ) ;
#43529=EDGE_CURVE ( 'NONE', #239691, #121353, #100892, .T. ) ;
#43534=PLANE ( 'NONE',  #125237 ) ;
#43543=FACE_OUTER_BOUND ( 'NONE', #151226, .T. ) ;
#43563=DIRECTION ( 'NONE',  ( 0.000000000000000000, -0.3488585713686133682, -0.9371753822965315228 ) ) ;
#43586=DIRECTION ( 'NONE',  ( 0.000000000000000000, 0.4721928772776973204, 0.8814952561688629284 ) ) ;
#43635=CARTESIAN_POINT ( 'NONE',  ( -20.64999999999999858, 26.34635675162282098, -241.8429480539297174 ) ) ;
#43662=FACE_OUTER_BOUND ( 'NONE', #166540, .T. ) ;
#43684=CYLINDRICAL_SURFACE ( 'NONE', #14803, 0.1000000000000013933 ) ;
#43721=CARTESIAN_POINT ( 'NONE',  ( -21.05000000000000071, 13.63177590472475487, -238.5351604075707144 ) ) ;
#43725=ORIENTED_EDGE ( 'NONE', *, *, #39946, .T. ) ;
#43740=EDGE_CURVE ( 'NONE', #184576, #93118, #33014, .T. ) ;
#43743=ORIENTED_EDGE ( 'NONE', *, *, #152411, .F. ) ;
#43762=CARTESIAN_POINT ( 'NONE',  ( -20.00857864376270001, 30.18746141061095045, -235.4776000216846796 ) ) ;
#43770=CIRCLE ( 'NONE', #160511, 11.65000000000000746 ) ;
#43771=VERTEX_POINT ( 'NONE', #132061 ) ;
#43783=ADVANCED_FACE ( 'NONE', ( #113773 ), #41997, .F. ) ;
#43794=ORIENTED_EDGE ( 'NONE', *, *, #143561, .T. ) ;
#43811=CARTESIAN_POINT ( 'NONE',  ( 21.05000000000000071, 28.63831050940605394, -258.0693639473472558 ) ) ;
#43844=CARTESIAN_POINT ( 'NONE',  ( 20.85000000000000142, 45.93315328338058379, -256.6017782078560003 ) ) ;
#43887=CARTESIAN_POINT ( 'NONE',  ( 22.39999999999999503, 10.80758397488569500, -226.8651660546161395 ) ) ;
#43902=AXIS2_PLACEMENT_3D ( 'NONE', #59925, #179919, #143331 ) ;
#43925=LINE ( 'NONE', #140447, #97853 ) ;
#43953=DIRECTION ( 'NONE',  ( 0.000000000000000000, 0.9994937237965558774, 0.03181660087586650476 ) ) ;
#43961=AXIS2_PLACEMENT_3D ( 'NONE', #107255, #205052, #102094 ) ;
#43977=AXIS2_PLACEMENT_3D ( 'NONE', #86356, #44710, #25160 ) ;
#43984=DIRECTION ( 'NONE',  ( 1.000000000000000000, 0.000000000000000000, 0.000000000000000000 ) ) ;
#43995=CARTESIAN_POINT ( 'NONE',  ( 18.49999999999999645, 42.92545512184477730, -254.1955779480491344 ) ) ;
#44024=CARTESIAN_POINT ( 'NONE',  ( -22.39999999999999858, -3.140208063160686791, -228.2318569537739847 ) ) ;
#44025=CIRCLE ( 'NONE', #189776, 0.1000000000000013933 ) ;
#44027=FACE_OUTER_BOUND ( 'NONE', #181000, .T. ) ;
#44034=DIRECTION ( 'NONE',  ( 1.000000000000000000, -0.000000000000000000, -0.000000000000000000 ) ) ;
#44038=CARTESIAN_POINT ( 'NONE',  ( -21.05000000000000426, 18.71344899777637494, -226.7788045585494103 ) ) ;
#44055=DIRECTION ( 'NONE',  ( 1.000000000000000000, 0.000000000000000000, 0.000000000000000000 ) ) ;
#44081=ORIENTED_EDGE ( 'NONE', *, *, #159042, .T. ) ;
#44093=DIRECTION ( 'NONE',  ( -1.000000000000000000, 0.000000000000000000, 0.000000000000000000 ) ) ;
#44098=ORIENTED_EDGE ( 'NONE', *, *, #196337, .T. ) ;
#44117=FACE_OUTER_BOUND ( 'NONE', #46023, .T. ) ;
#44119=ADVANCED_FACE ( 'NONE', ( #206161 ), #210973, .T. ) ;
#44124=TOROIDAL_SURFACE ( 'NONE', #152477, 11.70000000000000107, 0.1000000000000000056 ) ;
#44128=CARTESIAN_POINT ( 'NONE',  ( 21.05000000000000071, 18.94908112497232011, -227.8991131484155517 ) ) ;
#44142=DIRECTION ( 'NONE',  ( -1.000000000000000000, -1.394253735153569469E-16, -2.602809386958778209E-16 ) ) ;
#44145=ORIENTED_EDGE ( 'NONE', *, *, #136173, .T. ) ;
#44171=EDGE_CURVE ( 'NONE', #135978, #161523, #129640, .T. ) ;
#44184=ORIENTED_EDGE ( 'NONE', *, *, #257553, .F. ) ;
#44216=ADVANCED_FACE ( 'NONE', ( #256439 ), #236948, .F. ) ;
#44268=ORIENTED_EDGE ( 'NONE', *, *, #172451, .F. ) ;
#44279=EDGE_CURVE ( 'NONE', #64541, #98189, #29721, .T. ) ;
#44292=LINE ( 'NONE', #123825, #99634 ) ;
#44305=VERTEX_POINT ( 'NONE', #124710 ) ;
#44310=CARTESIAN_POINT ( 'NONE',  ( -18.50000324121759476, 46.33100819526732295, -243.0553980158188381 ) ) ;
#44314=EDGE_LOOP ( 'NONE', ( #238617, #220179, #105225, #232367 ) ) ;
#44320=LINE ( 'NONE', #221636, #21681 ) ;
#44402=PLANE ( 'NONE',  #95550 ) ;
#44431=EDGE_LOOP ( 'NONE', ( #156692, #168723, #5693, #97116 ) ) ;
#44463=AXIS2_PLACEMENT_3D ( 'NONE', #125166, #79582, #23524 ) ;
#44487=ORIENTED_EDGE ( 'NONE', *, *, #39021, .T. ) ;
#44493=CARTESIAN_POINT ( 'NONE',  ( -23.25000000000000000, -3.275978944802464099, -228.2735455795363748 ) ) ;
#44524=DIRECTION ( 'NONE',  ( -1.000000000000000000, 0.000000000000000000, 0.000000000000000000 ) ) ;
#44541=AXIS2_PLACEMENT_3D ( 'NONE', #225964, #23975, #26536 ) ;
#44568=DIRECTION ( 'NONE',  ( 0.000000000000000000, -0.3350715337780675318, -0.9421926911474177713 ) ) ;
#44571=EDGE_LOOP ( 'NONE', ( #186626, #80373, #13654 ) ) ;
#44582=DIRECTION ( 'NONE',  ( 1.000000000000000000, 0.000000000000000000, 0.000000000000000000 ) ) ;
#44592=CARTESIAN_POINT ( 'NONE',  ( 18.59999999999998721, 18.51212680383529374, -217.3114114048737520 ) ) ;
#44593=DIRECTION ( 'NONE',  ( 1.000000000000000000, -0.000000000000000000, 0.000000000000000000 ) ) ;
#44634=DIRECTION ( 'NONE',  ( 1.000000000000000000, 0.000000000000000000, 0.000000000000000000 ) ) ;
#44710=DIRECTION ( 'NONE',  ( 0.000000000000000000, 0.7674881895858254310, 0.6410630849193176273 ) ) ;
#44729=VERTEX_POINT ( 'NONE', #145231 ) ;
#44764=ORIENTED_EDGE ( 'NONE', *, *, #35255, .T. ) ;
#44810=DIRECTION ( 'NONE',  ( 0.000000000000000000, 0.4721928772777343464, 0.8814952561688431665 ) ) ;
#44844=DIRECTION ( 'NONE',  ( 1.000000000000000000, 0.000000000000000000, 0.000000000000000000 ) ) ;
#44921=LINE ( 'NONE', #222235, #47959 ) ;
#44927=CARTESIAN_POINT ( 'NONE',  ( -22.59999999999999787, -3.180729737797944434, -228.0957332317254895 ) ) ;
#44931=CIRCLE ( 'NONE', #115662, 11.64999999999999503 ) ;
#44936=EDGE_LOOP ( 'NONE', ( #89272, #197628, #256942, #162082 ) ) ;
#44944=VERTEX_POINT ( 'NONE', #215489 ) ;
#44958=DIRECTION ( 'NONE',  ( -1.000000000000000000, 0.000000000000000000, 0.000000000000000000 ) ) ;
#44978=EDGE_CURVE ( 'NONE', #35579, #216812, #175819, .T. ) ;
#44996=EDGE_LOOP ( 'NONE', ( #120232, #58011, #195421, #139897 ) ) ;
#45017=DIRECTION ( 'NONE',  ( -0.000000000000000000, 0.8814952561688430555, -0.4721928772777346239 ) ) ;
#45030=CIRCLE ( 'NONE', #157303, 0.09999999999999986677 ) ;
#45063=EDGE_CURVE ( 'NONE', #9735, #192243, #218034, .T. ) ;
#45071=CARTESIAN_POINT ( 'NONE',  ( -18.59999999999999787, 18.81339837015603322, -226.7756228984618190 ) ) ;
#45101=ORIENTED_EDGE ( 'NONE', *, *, #62654, .T. ) ;
#45181=CARTESIAN_POINT ( 'NONE',  ( 22.39999999999999503, -3.140208063160686791, -228.2318569537739847 ) ) ;
#45199=CARTESIAN_POINT ( 'NONE',  ( -21.04999999999897398, 10.05835145952827503, -228.1548128398107451 ) ) ;
#45210=AXIS2_PLACEMENT_3D ( 'NONE', #203435, #224265, #24824 ) ;
#45230=ORIENTED_EDGE ( 'NONE', *, *, #34705, .F. ) ;
#45249=DIRECTION ( 'NONE',  ( -1.000000000000000000, 0.000000000000000000, 0.000000000000000000 ) ) ;
#45252=ORIENTED_EDGE ( 'NONE', *, *, #120119, .T. ) ;
#45285=ORIENTED_EDGE ( 'NONE', *, *, #138970, .F. ) ;
#45293=DIRECTION ( 'NONE',  ( 1.000000000000000000, 0.000000000000000000, 0.000000000000000000 ) ) ;
#45301=DIRECTION ( 'NONE',  ( 1.000000000000000000, -3.448943450116721596E-16, -6.438528483529603700E-16 ) ) ;
#45313=DIRECTION ( 'NONE',  ( 0.000000000000000000, 0.8814952561688476074, -0.4721928772777262417 ) ) ;
#45324=CARTESIAN_POINT ( 'NONE',  ( 20.84999999999998721, 42.20719072976272912, -239.1935934412594804 ) ) ;
#45328=CARTESIAN_POINT ( 'NONE',  ( 22.50000000000000000, 10.71943444926881561, -226.8179467668883547 ) ) ;
#45358=AXIS2_PLACEMENT_3D ( 'NONE', #30676, #231433, #148033 ) ;
#45363=DIRECTION ( 'NONE',  ( 0.000000000000000000, 0.8814952561688441657, -0.4721928772777325145 ) ) ;
#45383=ORIENTED_EDGE ( 'NONE', *, *, #190761, .F. ) ;
#45397=CIRCLE ( 'NONE', #191168, 11.80000000000000959 ) ;
#45400=DIRECTION ( 'NONE',  ( -1.000000000000000000, 0.000000000000000000, 0.000000000000000000 ) ) ;
#45403=ORIENTED_EDGE ( 'NONE', *, *, #203792, .T. ) ;
#45431=DIRECTION ( 'NONE',  ( 0.000000000000000000, 0.8814952561688430555, -0.4721928772777346239 ) ) ;
#45449=ORIENTED_EDGE ( 'NONE', *, *, #184069, .F. ) ;
#45466=VECTOR ( 'NONE', #139151, 1000.000000000000000 ) ;
#45469=EDGE_CURVE ( 'NONE', #218153, #35062, #92207, .T. ) ;
#45509=EDGE_LOOP ( 'NONE', ( #210578, #142761, #60880, #213064 ) ) ;
#45529=VERTEX_POINT ( 'NONE', #106621 ) ;
#45532=DIRECTION ( 'NONE',  ( 0.000000000000000000, 0.8814952561688429444, -0.4721928772777349015 ) ) ;
#45545=CARTESIAN_POINT ( 'NONE',  ( -20.94999999999999929, 4.384524567800934136, -245.2091454203640239 ) ) ;
#45550=DIRECTION ( 'NONE',  ( 0.000000000000000000, -0.4721928772777258532, -0.8814952561688478294 ) ) ;
#45588=AXIS2_PLACEMENT_3D ( 'NONE', #194935, #115371, #218302 ) ;
#45600=EDGE_CURVE ( 'NONE', #52358, #82377, #180276, .T. ) ;
#45603=EDGE_LOOP ( 'NONE', ( #248362, #105788 ) ) ;
#45618=VECTOR ( 'NONE', #69843, 1000.000000000000000 ) ;
#45664=DIRECTION ( 'NONE',  ( -0.000000000000000000, -0.4721928772777346239, -0.8814952561688430555 ) ) ;
#45747=VERTEX_POINT ( 'NONE', #254853 ) ;
#45748=AXIS2_PLACEMENT_3D ( 'NONE', #242149, #127345, #102611 ) ;
#45793=CYLINDRICAL_SURFACE ( 'NONE', #53713, 0.09999999999999986677 ) ;
#45796=DIRECTION ( 'NONE',  ( 0.000000000000000000, -0.8814952561688476074, 0.4721928772777262417 ) ) ;
#45798=CIRCLE ( 'NONE', #70771, 0.1000000000000013933 ) ;
#45839=CARTESIAN_POINT ( 'NONE',  ( -23.15000000000000213, 28.58935552370083144, -258.2621935127861548 ) ) ;
#45912=EDGE_CURVE ( 'NONE', #246412, #182351, #123120, .T. ) ;
#45923=CARTESIAN_POINT ( 'NONE',  ( -23.15000000000000213, 27.82649702422227733, -239.8850763025288870 ) ) ;
#45939=CARTESIAN_POINT ( 'NONE',  ( 19.75857864376269291, 34.49410723828536618, -235.0619057650792740 ) ) ;
#45970=AXIS2_PLACEMENT_3D ( 'NONE', #213138, #175331, #38364 ) ;
#46023=EDGE_LOOP ( 'NONE', ( #22885, #75430, #227917, #145468 ) ) ;
#46035=ORIENTED_EDGE ( 'NONE', *, *, #28071, .T. ) ;
#46063=VECTOR ( 'NONE', #99624, 1000.000000000000000 ) ;
#46069=CIRCLE ( 'NONE', #191862, 0.09999999999998916700 ) ;
#46117=CARTESIAN_POINT ( 'NONE',  ( -21.05000000000000071, 18.24178995542692050, -237.7003448530951459 ) ) ;
#46118=FACE_OUTER_BOUND ( 'NONE', #115902, .T. ) ;
#46148=DIRECTION ( 'NONE',  ( 0.000000000000000000, 0.8814952561688476074, -0.4721928772777262417 ) ) ;
#46171=ORIENTED_EDGE ( 'NONE', *, *, #42607, .T. ) ;
#46197=EDGE_CURVE ( 'NONE', #220389, #11913, #105582, .T. ) ;
#46219=FACE_OUTER_BOUND ( 'NONE', #93541, .T. ) ;
#46228=CARTESIAN_POINT ( 'NONE',  ( -21.55000000000000071, 21.43869811404188752, -233.1734427395952025 ) ) ;
#46235=ADVANCED_FACE ( 'NONE', ( #46775 ), #14058, .T. ) ;
#46249=CARTESIAN_POINT ( 'NONE',  ( 20.84999999999998721, 46.46967969402478360, -243.0849751855955674 ) ) ;
#46297=DIRECTION ( 'NONE',  ( 0.7071067811865476838, -0.3338907855510733769, -0.6233112732207617412 ) ) ;
#46314=DIRECTION ( 'NONE',  ( 6.938893903907220489E-15, -0.4721928772777346239, -0.8814952561688430555 ) ) ;
#46384=PLANE ( 'NONE',  #248764 ) ;
#46397=ORIENTED_EDGE ( 'NONE', *, *, #168069, .F. ) ;
#46403=DIRECTION ( 'NONE',  ( 0.000000000000000000, 0.3280696808754309246, 0.9446535261619960488 ) ) ;
#46404=EDGE_CURVE ( 'NONE', #89936, #9735, #72494, .T. ) ;
#46429=ORIENTED_EDGE ( 'NONE', *, *, #136672, .T. ) ;
#46450=DIRECTION ( 'NONE',  ( 0.000000000000000000, -0.8814952561688476074, 0.4721928772777262417 ) ) ;
#46452=CARTESIAN_POINT ( 'NONE',  ( -18.59999999999999787, 7.128833340093095217, -233.7327013124392749 ) ) ;
#46463=VECTOR ( 'NONE', #39088, 1000.000000000000000 ) ;
#46480=CIRCLE ( 'NONE', #179794, 0.1999999999999997335 ) ;
#46495=CARTESIAN_POINT ( 'NONE',  ( -23.25000000000000000, 31.44980407958350455, -233.5445995079518866 ) ) ;
#46504=DIRECTION ( 'NONE',  ( -1.000000000000000000, -3.448943450116723568E-16, -6.438528483529607644E-16 ) ) ;
#46536=CARTESIAN_POINT ( 'NONE',  ( 21.05000000000000071, 24.12844930803501242, -253.0488546976795021 ) ) ;
#46538=ORIENTED_EDGE ( 'NONE', *, *, #214186, .F. ) ;
#46567=CARTESIAN_POINT ( 'NONE',  ( -21.05000000000000071, 4.481636728799211156, -245.1292951062512770 ) ) ;
#46570=EDGE_CURVE ( 'NONE', #16895, #71383, #86866, .T. ) ;
#46583=CARTESIAN_POINT ( 'NONE',  ( -18.59999999999999787, 46.46967969402478360, -243.0849751855955674 ) ) ;
#46609=EDGE_CURVE ( 'NONE', #166239, #92704, #83004, .T. ) ;
#46612=CARTESIAN_POINT ( 'NONE',  ( 20.94999675878240808, 46.33100819526731584, -243.0553980158188381 ) ) ;
#46653=ORIENTED_EDGE ( 'NONE', *, *, #243669, .F. ) ;
#46660=DIRECTION ( 'NONE',  ( 0.000000000000000000, 0.8814952561688437216, -0.4721928772777334582 ) ) ;
#46674=CARTESIAN_POINT ( 'NONE',  ( -20.12071067811865888, 22.41647294715246375, -231.3481210999354403 ) ) ;
#46699=CYLINDRICAL_SURFACE ( 'NONE', #223597, 0.09999999999999939493 ) ;
#46707=ADVANCED_FACE ( 'NONE', ( #231551 ), #72484, .F. ) ;
#46711=FACE_OUTER_BOUND ( 'NONE', #181529, .T. ) ;
#46723=CARTESIAN_POINT ( 'NONE',  ( 18.49999999999999645, -3.616484641954614165, -226.0163245033746477 ) ) ;
#46754=EDGE_CURVE ( 'NONE', #23820, #142016, #72114, .T. ) ;
#46755=CIRCLE ( 'NONE', #209253, 0.1000000000000013933 ) ;
#46775=FACE_OUTER_BOUND ( 'NONE', #57775, .T. ) ;
#46786=DIRECTION ( 'NONE',  ( 0.000000000000000000, 0.8814952561688430555, -0.4721928772777346239 ) ) ;
#46823=DIRECTION ( 'NONE',  ( 0.000000000000000000, 0.8814952561688476074, -0.4721928772777262417 ) ) ;
#46830=DIRECTION ( 'NONE',  ( 1.000000000000000000, 0.000000000000000000, 0.000000000000000000 ) ) ;
#46846=VERTEX_POINT ( 'NONE', #157169 ) ;
#46906=DIRECTION ( 'NONE',  ( -0.000000000000000000, 0.4721928772777345684, 0.8814952561688429444 ) ) ;
#46946=DIRECTION ( 'NONE',  ( 0.000000000000000000, -0.8814952561688438326, 0.4721928772777334582 ) ) ;
#46953=VERTEX_POINT ( 'NONE', #42336 ) ;
#46956=DIRECTION ( 'NONE',  ( 0.000000000000000000, 0.8814952561688437216, -0.4721928772777331806 ) ) ;
#46961=LINE ( 'NONE', #163099, #107225 ) ;
#46988=ADVANCED_FACE ( 'NONE', ( #100966 ), #223518, .T. ) ;
#46998=FACE_OUTER_BOUND ( 'NONE', #215751, .T. ) ;
#47014=EDGE_CURVE ( 'NONE', #205943, #221081, #180427, .T. ) ;
#47045=LINE ( 'NONE', #107023, #20945 ) ;
#47060=DIRECTION ( 'NONE',  ( 0.000000000000000000, 0.5341055959866798375, -0.8454177738465836756 ) ) ;
#47086=DIRECTION ( 'NONE',  ( 1.000000000000000000, -0.000000000000000000, -0.000000000000000000 ) ) ;
#47099=ORIENTED_EDGE ( 'NONE', *, *, #97856, .T. ) ;
#47121=CIRCLE ( 'NONE', #55298, 0.1000000000000019901 ) ;
#47129=LINE ( 'NONE', #144954, #32749 ) ;
#47151=CARTESIAN_POINT ( 'NONE',  ( -18.50000000000000000, 42.96960653111219131, -254.4772109693542745 ) ) ;
#47152=ORIENTED_EDGE ( 'NONE', *, *, #239956, .T. ) ;
#47168=DIRECTION ( 'NONE',  ( 0.000000000000000000, 0.4583618696494374256, 0.8887656589064814039 ) ) ;
#47210=DIRECTION ( 'NONE',  ( 0.000000000000000000, -0.8814952561688441657, 0.4721928772777327366 ) ) ;
#47243=DIRECTION ( 'NONE',  ( 1.000000000000000000, 0.000000000000000000, 0.000000000000000000 ) ) ;
#47247=ORIENTED_EDGE ( 'NONE', *, *, #208484, .T. ) ;
#47248=EDGE_CURVE ( 'NONE', #121353, #100546, #38974, .T. ) ;
#47268=AXIS2_PLACEMENT_3D ( 'NONE', #119700, #47508, #199233 ) ;
#47269=ORIENTED_EDGE ( 'NONE', *, *, #229809, .F. ) ;
#47272=DIRECTION ( 'NONE',  ( -0.000000000000000000, 0.4721928772777347350, 0.8814952561688429444 ) ) ;
#47285=CARTESIAN_POINT ( 'NONE',  ( 18.37172112093865195, 38.14850358416990872, -261.2067334498989339 ) ) ;
#47291=CIRCLE ( 'NONE', #22398, 0.09999999999999834022 ) ;
#47301=AXIS2_PLACEMENT_3D ( 'NONE', #255099, #97328, #113084 ) ;
#47306=VECTOR ( 'NONE', #204937, 999.9999999999998863 ) ;
#47315=EDGE_CURVE ( 'NONE', #162422, #63327, #125430, .T. ) ;
#47379=AXIS2_PLACEMENT_3D ( 'NONE', #74104, #72816, #153666 ) ;
#47433=ORIENTED_EDGE ( 'NONE', *, *, #211360, .F. ) ;
#47447=DIRECTION ( 'NONE',  ( -1.000000000000000000, -0.000000000000000000, -0.000000000000000000 ) ) ;
#47468=CARTESIAN_POINT ( 'NONE',  ( 20.94999999999999574, 13.71992543034163958, -238.5823796952984992 ) ) ;
#47473=CIRCLE ( 'NONE', #193256, 0.1000000000000013933 ) ;
#47490=DIRECTION ( 'NONE',  ( 0.000000000000000000, -0.8814952561688476074, 0.4721928772777262417 ) ) ;
#47495=CIRCLE ( 'NONE', #226549, 0.1000000000000009354 ) ;
#47508=DIRECTION ( 'NONE',  ( 1.000000000000000000, 1.394253735153569469E-16, 2.602809386958778209E-16 ) ) ;
#47512=EDGE_CURVE ( 'NONE', #138960, #193873, #232245, .T. ) ;
#47537=ORIENTED_EDGE ( 'NONE', *, *, #236442, .F. ) ;
#47541=CARTESIAN_POINT ( 'NONE',  ( -18.49513951962169145, 38.17733670730264350, -261.0710301328860510 ) ) ;
#47556=ORIENTED_EDGE ( 'NONE', *, *, #45063, .F. ) ;
#47557=DIRECTION ( 'NONE',  ( 0.000000000000000000, 0.8814952561688429444, -0.4721928772777345684 ) ) ;
#47573=DIRECTION ( 'NONE',  ( 0.000000000000000000, -0.8814952561688430555, 0.4721928772777346239 ) ) ;
#47575=EDGE_LOOP ( 'NONE', ( #13801, #128302, #245357, #83041, #251564, #77260 ) ) ;
#47576=AXIS2_PLACEMENT_3D ( 'NONE', #188408, #31935, #148006 ) ;
#47583=AXIS2_PLACEMENT_3D ( 'NONE', #158153, #155574, #38175 ) ;
#47597=DIRECTION ( 'NONE',  ( 1.000000000000000000, 0.000000000000000000, 0.000000000000000000 ) ) ;
#47617=ORIENTED_EDGE ( 'NONE', *, *, #5730, .T. ) ;
#47652=SURFACE_SIDE_STYLE ('',( #226287 ) ) ;
#47653=TOROIDAL_SURFACE ( 'NONE', #56030, 3.899999999999999467, 0.1000000000000000056 ) ;
#47718=CARTESIAN_POINT ( 'NONE',  ( 22.16821283564876666, 10.69812671114205394, -227.0695021710343156 ) ) ;
#47749=VECTOR ( 'NONE', #233778, 1000.000000000000000 ) ;
#47751=DIRECTION ( 'NONE',  ( 1.000000000000000000, 0.000000000000000000, 0.000000000000000000 ) ) ;
#47770=B_SPLINE_CURVE_WITH_KNOTS ( 'NONE', 3,
 ( #108077, #8966, #3834, #88475, #168087, #83332, #242430, #222869, #92347, #10262, #71534, #171935, #211023, #113200, #70259, #75387, #169367, #191490, #170665, #174522, #94907, #253981 ),
 .UNSPECIFIED., .F., .F.,
 ( 4, 3, 3, 3, 3, 3, 3, 4 ),
 ( 0.000000000000000000, 7.307836821075256540E-06, 4.161455748546809275E-05, 7.576591810647573624E-05, 0.0001098090429817548115, 0.0001438003617351177430, 0.0001777914035423749776, 0.0002117966137403039836 ),
 .UNSPECIFIED. ) ;
#47777=CARTESIAN_POINT ( 'NONE',  ( 23.24999999999999289, 23.38726701055792745, -229.1122755113798348 ) ) ;
#47783=DIRECTION ( 'NONE',  ( 0.000000000000000000, 0.03181660087583042945, -0.9994937237965569876 ) ) ;
#47792=DIRECTION ( 'NONE',  ( 0.000000000000000000, -0.8814952561688430555, 0.4721928772777346239 ) ) ;
#47821=DIRECTION ( 'NONE',  ( 0.000000000000000000, -0.03181660087581233282, 0.9994937237965575427 ) ) ;
#47832=CARTESIAN_POINT ( 'NONE',  ( 18.46082813848001436, 8.896929522169481075, -245.4351262571402970 ) ) ;
#47847=EDGE_CURVE ( 'NONE', #154949, #102316, #239237, .T. ) ;
#47870=AXIS2_PLACEMENT_3D ( 'NONE', #101065, #67129, #245774 ) ;
#47909=CARTESIAN_POINT ( 'NONE',  ( 23.15000000000000213, 28.06530170954950165, -259.0287255139427884 ) ) ;
#47916=AXIS2_PLACEMENT_3D ( 'NONE', #12417, #89344, #29428 ) ;
#47932=DIRECTION ( 'NONE',  ( 0.000000000000000000, 0.4721928772778128947, 0.8814952561688012000 ) ) ;
#47951=EDGE_CURVE ( 'NONE', #192532, #21708, #189179, .T. ) ;
#47959=VECTOR ( 'NONE', #25374, 1000.000000000000114 ) ;
#48019=VERTEX_POINT ( 'NONE', #214570 ) ;
#48032=ORIENTED_EDGE ( 'NONE', *, *, #193726, .T. ) ;
#48043=EDGE_CURVE ( 'NONE', #209230, #86653, #226758, .T. ) ;
#48095=CARTESIAN_POINT ( 'NONE',  ( -20.54999999999999716, 36.65892442174935439, -249.5511627012433848 ) ) ;
#48131=LINE ( 'NONE', #243773, #99095 ) ;
#48137=CIRCLE ( 'NONE', #135611, 12.97499999999999076 ) ;
#48140=CARTESIAN_POINT ( 'NONE',  ( 23.24999999999999645, 28.08470566095357057, -239.2860081655328770 ) ) ;
#48143=DIRECTION ( 'NONE',  ( 0.000000000000000000, 0.8814952561688429444, -0.4721928772777347350 ) ) ;
#48178=DIRECTION ( 'NONE',  ( 0.000000000000000000, 0.8814952561688476074, -0.4721928772777262417 ) ) ;
#48205=SPHERICAL_SURFACE ( 'NONE', #227171, 0.1000000000000000056 ) ;
#48207=EDGE_CURVE ( 'NONE', #194489, #77718, #10304, .T. ) ;
#48226=CARTESIAN_POINT ( 'NONE',  ( 21.08489247129321598, 22.20727474569241977, -231.7386547802595373 ) ) ;
#48252=ORIENTED_EDGE ( 'NONE', *, *, #178726, .F. ) ;
#48259=CARTESIAN_POINT ( 'NONE',  ( -20.94999999999999929, 18.86061765788380740, -226.6874733728449485 ) ) ;
#48335=EDGE_CURVE ( 'NONE', #149025, #102673, #79875, .T. ) ;
#48346=EDGE_CURVE ( 'NONE', #227874, #30797, #97739, .T. ) ;
#48349=EDGE_CURVE ( 'NONE', #226515, #173747, #85261, .T. ) ;
#48350=AXIS2_PLACEMENT_3D ( 'NONE', #194301, #162541, #57304 ) ;
#48351=CARTESIAN_POINT ( 'NONE',  ( -23.15000000000000213, 20.06933876993645782, -235.7297789824848451 ) ) ;
#48361=ORIENTED_EDGE ( 'NONE', *, *, #125775, .F. ) ;
#48376=VERTEX_POINT ( 'NONE', #233852 ) ;
#48400=CARTESIAN_POINT ( 'NONE',  ( 21.05000000000000071, 18.94908112497232366, -227.8991131484155517 ) ) ;
#48410=FACE_OUTER_BOUND ( 'NONE', #43331, .T. ) ;
#48438=CIRCLE ( 'NONE', #35985, 0.09999999999999779898 ) ;
#48459=VERTEX_POINT ( 'NONE', #182885 ) ;
#48482=ORIENTED_EDGE ( 'NONE', *, *, #79285, .T. ) ;
#48512=CIRCLE ( 'NONE', #148488, 0.1000000000000013933 ) ;
#48547=CARTESIAN_POINT ( 'NONE',  ( 19.75857864376268935, 34.58225676390223668, -235.1091250528070589 ) ) ;
#48556=AXIS2_PLACEMENT_3D ( 'NONE', #181069, #2388, #81907 ) ;
#48560=CARTESIAN_POINT ( 'NONE',  ( -20.64999999999999858, 23.49882452903949925, -253.1653563615082305 ) ) ;
#48586=CARTESIAN_POINT ( 'NONE',  ( -18.39999999999999858, 37.94390843806124280, -261.1300795796834109 ) ) ;
#48588=CARTESIAN_POINT ( 'NONE',  ( 18.31572054635746838, 38.18894743439052064, -261.2028889386127730 ) ) ;
#48650=DIRECTION ( 'NONE',  ( 0.000000000000000000, 0.8814952561688432775, -0.4721928772777344019 ) ) ;
#48651=VERTEX_POINT ( 'NONE', #70654 ) ;
#48656=CARTESIAN_POINT ( 'NONE',  ( -21.11927991906891222, 1.448806495452435117, -230.6797615723483261 ) ) ;
#48661=CARTESIAN_POINT ( 'NONE',  ( -20.15000000000000568, 22.31449321236291183, -231.3267202105024580 ) ) ;
#48666=ORIENTED_EDGE ( 'NONE', *, *, #121730, .F. ) ;
#48707=ADVANCED_FACE ( 'NONE', ( #60 ), #173630, .T. ) ;
#48710=CARTESIAN_POINT ( 'NONE',  ( -23.15000000000000213, 31.49702336731127872, -233.4564499823349877 ) ) ;
#48714=EDGE_CURVE ( 'NONE', #30797, #94319, #216546, .T. ) ;
#48717=CIRCLE ( 'NONE', #227775, 0.09999999999999986677 ) ;
#48768=DIRECTION ( 'NONE',  ( 1.000000000000000000, 0.000000000000000000, 0.000000000000000000 ) ) ;
#48773=ORIENTED_EDGE ( 'NONE', *, *, #244847, .F. ) ;
#48801=DIRECTION ( 'NONE',  ( 1.000000000000000000, 0.000000000000000000, 0.000000000000000000 ) ) ;
#48816=EDGE_CURVE ( 'NONE', #201516, #168277, #227592, .T. ) ;
#48869=ORIENTED_EDGE ( 'NONE', *, *, #43298, .F. ) ;
#48870=CYLINDRICAL_SURFACE ( 'NONE', #218726, 0.09999999999999939493 ) ;
#48872=EDGE_CURVE ( 'NONE', #104063, #250188, #169390, .T. ) ;
#48875=DIRECTION ( 'NONE',  ( 0.000000000000000000, 0.8814952561688444987, -0.4721928772777320149 ) ) ;
#48886=ORIENTED_EDGE ( 'NONE', *, *, #56690, .F. ) ;
#48888=CARTESIAN_POINT ( 'NONE',  ( -22.48660254037843487, 12.58580559757028183, -223.4396719342083770 ) ) ;
#48891=AXIS2_PLACEMENT_3D ( 'NONE', #28965, #208836, #107158 ) ;
#48897=ADVANCED_FACE ( 'NONE', ( #61331 ), #220415, .T. ) ;
#48907=DIRECTION ( 'NONE',  ( -0.000000000000000000, 0.8814952561688430555, -0.4721928772777346239 ) ) ;
#48919=FACE_OUTER_BOUND ( 'NONE', #226416, .T. ) ;
#48947=ADVANCED_FACE ( 'NONE', ( #105549 ), #244345, .T. ) ;
#48957=AXIS2_PLACEMENT_3D ( 'NONE', #225589, #243892, #245191 ) ;
#48973=EDGE_CURVE ( 'NONE', #105209, #218153, #209833, .T. ) ;
#48994=EDGE_CURVE ( 'NONE', #97016, #102393, #223669, .T. ) ;
#49022=DIRECTION ( 'NONE',  ( -0.000000000000000000, -0.8814952561688430555, 0.4721928772777346239 ) ) ;
#49032=DIRECTION ( 'NONE',  ( 0.000000000000000000, -0.8814952561688431665, 0.4721928772777346794 ) ) ;
#49038=CARTESIAN_POINT ( 'NONE',  ( -20.54999999999999716, 19.91953773510093839, -237.8616849742533077 ) ) ;
#49049=CARTESIAN_POINT ( 'NONE',  ( 21.06600267594171783, 22.03040400259985176, -231.7602000086088765 ) ) ;
#49051=CARTESIAN_POINT ( 'NONE',  ( -21.44999999999999929, 21.30332930069722863, -233.2143729774842882 ) ) ;
#49085=CARTESIAN_POINT ( 'NONE',  ( -20.94999999999999929, 4.184122562697133674, -245.3714803909117279 ) ) ;
#49105=ADVANCED_FACE ( 'NONE', ( #124708 ), #204229, .F. ) ;
#49115=TOROIDAL_SURFACE ( 'NONE', #103274, 0.6000000000000017542, 0.1000000000000000056 ) ;
#49137=EDGE_LOOP ( 'NONE', ( #110780, #186774, #95827, #124245, #238414 ) ) ;
#49139=CARTESIAN_POINT ( 'NONE',  ( 18.50596464788227280, 46.37740828070798216, -243.0652246697500800 ) ) ;
#49141=EDGE_CURVE ( 'NONE', #207603, #130702, #173683, .T. ) ;
#49177=CARTESIAN_POINT ( 'NONE',  ( -20.94999999999999929, 28.51339163295720169, -258.4040038037771865 ) ) ;
#49180=EDGE_CURVE ( 'NONE', #116426, #152553, #48717, .T. ) ;
#49203=CARTESIAN_POINT ( 'NONE',  ( -23.25000000000000000, 7.128833340093095217, -233.7327013124392749 ) ) ;
#49213=DIRECTION ( 'NONE',  ( 0.000000000000000000, 0.8814952561688476074, -0.4721928772777262417 ) ) ;
#49223=ORIENTED_EDGE ( 'NONE', *, *, #49394, .F. ) ;
#49240=FACE_OUTER_BOUND ( 'NONE', #13249, .T. ) ;
#49250=CARTESIAN_POINT ( 'NONE',  ( 20.94999999999999929, 28.43730376342110944, -239.4748853164439879 ) ) ;
#49255=FACE_OUTER_BOUND ( 'NONE', #15127, .T. ) ;
#49264=AXIS2_PLACEMENT_3D ( 'NONE', #27890, #184346, #4424 ) ;
#49273=DIRECTION ( 'NONE',  ( 1.000000000000000000, 0.000000000000000000, 0.000000000000000000 ) ) ;
#49274=CARTESIAN_POINT ( 'NONE',  ( -23.15000000000000213, 31.44980407958351165, -233.5445995079518866 ) ) ;
#49275=DIRECTION ( 'NONE',  ( -1.000000000000000000, 0.000000000000000000, 0.000000000000000000 ) ) ;
#49293=AXIS2_PLACEMENT_3D ( 'NONE', #10410, #9121, #226872 ) ;
#49315=CIRCLE ( 'NONE', #215699, 0.8750000000000007772 ) ;
#49321=CARTESIAN_POINT ( 'NONE',  ( 23.14999999999999147, 9.088433780795693195, -230.0744959993385805 ) ) ;
#49377=DIRECTION ( 'NONE',  ( 0.000000000000000000, -0.5826443254700256480, -0.8127272543710952757 ) ) ;
#49382=LINE ( 'NONE', #209739, #163020 ) ;
#49394=EDGE_CURVE ( 'NONE', #54600, #140913, #184045, .T. ) ;
#49435=ORIENTED_EDGE ( 'NONE', *, *, #227212, .F. ) ;
#49438=CARTESIAN_POINT ( 'NONE',  ( -21.55000000000000071, 29.24307565605548120, -237.2405905340223455 ) ) ;
#49471=ORIENTED_EDGE ( 'NONE', *, *, #116741, .F. ) ;
#49501=DIRECTION ( 'NONE',  ( 1.000000000000000000, 0.000000000000000000, 0.000000000000000000 ) ) ;
#49569=EDGE_CURVE ( 'NONE', #100199, #71987, #86706, .T. ) ;
#49586=CIRCLE ( 'NONE', #57756, 0.09999999999999939493 ) ;
#49598=EDGE_LOOP ( 'NONE', ( #136639, #192983, #238778, #10896, #176252 ) ) ;
#49599=CARTESIAN_POINT ( 'NONE',  ( -20.54999999999999716, 26.29846678923107817, -241.7324770631975639 ) ) ;
#49617=CARTESIAN_POINT ( 'NONE',  ( -20.94999999999999929, 36.65892442174935439, -249.5511627012433848 ) ) ;
#49630=AXIS2_PLACEMENT_3D ( 'NONE', #203584, #41965, #164470 ) ;
#49632=AXIS2_PLACEMENT_3D ( 'NONE', #64901, #242254, #165296 ) ;
#49658=EDGE_CURVE ( 'NONE', #41070, #60897, #95123, .T. ) ;
#49674=DIRECTION ( 'NONE',  ( -1.000000000000000000, -1.541880601228652843E-16, -2.878400969107353907E-16 ) ) ;
#49699=CIRCLE ( 'NONE', #195463, 0.1000000000000134115 ) ;
#49739=ADVANCED_FACE ( 'NONE', ( #156518 ), #92642, .T. ) ;
#49754=CARTESIAN_POINT ( 'NONE',  ( 21.00000000000000000, 30.46448808713892831, -235.1722212069449256 ) ) ;
#49811=ORIENTED_EDGE ( 'NONE', *, *, #15256, .T. ) ;
#49842=ORIENTED_EDGE ( 'NONE', *, *, #129144, .F. ) ;
#49846=DIRECTION ( 'NONE',  ( 1.000000000000000000, 0.000000000000000000, 0.000000000000000000 ) ) ;
#49854=AXIS2_PLACEMENT_3D ( 'NONE', #223182, #86223, #241482 ) ;
#49864=CARTESIAN_POINT ( 'NONE',  ( 23.14999999999999858, 36.65892442174935439, -249.5511627012433848 ) ) ;
#49878=AXIS2_PLACEMENT_3D ( 'NONE', #90652, #231478, #8570 ) ;
#49880=CIRCLE ( 'NONE', #120641, 0.4000000000000086264 ) ;
#49890=CARTESIAN_POINT ( 'NONE',  ( 21.14999999999999858, 1.363275264940682741, -230.6442496871288483 ) ) ;
#49943=DIRECTION ( 'NONE',  ( 0.000000000000000000, -0.5826443254699743557, -0.8127272543711318020 ) ) ;
#49955=ORIENTED_EDGE ( 'NONE', *, *, #86201, .F. ) ;
#49995=EDGE_CURVE ( 'NONE', #171330, #73607, #182816, .T. ) ;
#50012=DIRECTION ( 'NONE',  ( 0.000000000000000000, 0.8814952561688429444, -0.4721928772777348460 ) ) ;
#50015=DIRECTION ( 'NONE',  ( 1.000000000000000000, 0.000000000000000000, 0.000000000000000000 ) ) ;
#50036=VERTEX_POINT ( 'NONE', #93629 ) ;
#50078=LINE ( 'NONE', #8401, #201547 ) ;
#50101=ORIENTED_EDGE ( 'NONE', *, *, #212169, .T. ) ;
#50106=VERTEX_POINT ( 'NONE', #252686 ) ;
#50120=CARTESIAN_POINT ( 'NONE',  ( 20.85000000000000142, 42.15997144203495139, -239.2817429668763793 ) ) ;
#50149=AXIS2_PLACEMENT_3D ( 'NONE', #86907, #167785, #127344 ) ;
#50181=DIRECTION ( 'NONE',  ( 0.000000000000000000, -0.3488585713686311318, -0.9371753822965249725 ) ) ;
#50195=EDGE_LOOP ( 'NONE', ( #29904, #82099, #12766, #146319 ) ) ;
#50234=CARTESIAN_POINT ( 'NONE',  ( 21.14999999999999858, 22.98593783141595992, -230.0732594427593938 ) ) ;
#50259=EDGE_CURVE ( 'NONE', #15820, #203639, #12298, .T. ) ;
#50261=CARTESIAN_POINT ( 'NONE',  ( -20.85000000000000142, 43.02787096365918984, -254.3959382439171577 ) ) ;
#50274=TOROIDAL_SURFACE ( 'NONE', #21109, 0.2000000000000000111, 0.1000000000000000056 ) ;
#50369=DIRECTION ( 'NONE',  ( 1.000000000000000000, 0.000000000000000000, 0.000000000000000000 ) ) ;
#50373=DIRECTION ( 'NONE',  ( 0.000000000000000000, 0.8814952561688438326, -0.4721928772777330696 ) ) ;
#50388=EDGE_CURVE ( 'NONE', #82237, #59204, #252372, .T. ) ;
#50403=CARTESIAN_POINT ( 'NONE',  ( 18.50211644919735221, 46.36250628750310909, -243.0620573837409779 ) ) ;
#50408=CIRCLE ( 'NONE', #21420, 11.69999999999999396 ) ;
#50414=CARTESIAN_POINT ( 'NONE',  ( 21.05000000000000071, 18.81018314204461817, -229.8995852278561642 ) ) ;
#50424=ORIENTED_EDGE ( 'NONE', *, *, #99782, .F. ) ;
#50454=DIRECTION ( 'NONE',  ( -1.000000000000000000, -0.000000000000000000, -0.000000000000000000 ) ) ;
#50470=ORIENTED_EDGE ( 'NONE', *, *, #117106, .F. ) ;
#50475=ADVANCED_FACE ( 'NONE', ( #77580 ), #161990, .T. ) ;
#50477=EDGE_LOOP ( 'NONE', ( #52053, #20018, #185270, #21315 ) ) ;
#50486=EDGE_CURVE ( 'NONE', #63323, #162761, #28905, .T. ) ;
#50520=ORIENTED_EDGE ( 'NONE', *, *, #112739, .F. ) ;
#50538=CARTESIAN_POINT ( 'NONE',  ( -21.46681500593518876, 10.36690126540584700, -227.6878377563191691 ) ) ;
#50542=CARTESIAN_POINT ( 'NONE',  ( -21.07928932188134041, 10.02993822722303818, -228.1074463178677263 ) ) ;
#50543=ORIENTED_EDGE ( 'NONE', *, *, #68219, .T. ) ;
#50548=CIRCLE ( 'NONE', #33869, 11.89999999999998970 ) ;
#50576=CARTESIAN_POINT ( 'NONE',  ( -20.54999999999999716, 7.128833340093095217, -233.7327013124392749 ) ) ;
#50595=LINE ( 'NONE', #207134, #204959 ) ;
#50638=CARTESIAN_POINT ( 'NONE',  ( -23.25000000000000000, 28.42524210734032053, -258.3567845160494585 ) ) ;
#50647=ADVANCED_FACE ( 'NONE', ( #27627 ), #69298, .T. ) ;
#50689=ORIENTED_EDGE ( 'NONE', *, *, #316, .T. ) ;
#50704=CYLINDRICAL_SURFACE ( 'NONE', #131305, 0.09999999999999939493 ) ;
#50713=CARTESIAN_POINT ( 'NONE',  ( -21.07928932188134041, 7.128833340093095217, -233.7327013124392749 ) ) ;
#50738=ORIENTED_EDGE ( 'NONE', *, *, #177442, .T. ) ;
#50742=DIRECTION ( 'NONE',  ( 0.000000000000000000, 0.8814952561688476074, -0.4721928772777262417 ) ) ;
#50748=VERTEX_POINT ( 'NONE', #116122 ) ;
#50770=TOROIDAL_SURFACE ( 'NONE', #42419, 0.2000000000000000111, 0.1000000000000000056 ) ;
#50791=ORIENTED_EDGE ( 'NONE', *, *, #32473, .T. ) ;
#50798=LINE ( 'NONE', #213746, #153058 ) ;
#50828=EDGE_CURVE ( 'NONE', #222562, #159519, #203353, .T. ) ;
#50843=ORIENTED_EDGE ( 'NONE', *, *, #168311, .T. ) ;
#50850=ORIENTED_EDGE ( 'NONE', *, *, #49180, .T. ) ;
#50882=ADVANCED_FACE ( 'NONE', ( #199519 ), #242460, .F. ) ;
#50902=ORIENTED_EDGE ( 'NONE', *, *, #121224, .F. ) ;
#50954=CARTESIAN_POINT ( 'NONE',  ( 22.48660254037844552, 12.58580559757025696, -223.4396719342083770 ) ) ;
#50959=VERTEX_POINT ( 'NONE', #219044 ) ;
#50988=CARTESIAN_POINT ( 'NONE',  ( -20.64999999999999858, 27.82649702422227733, -239.8850763025288870 ) ) ;
#51015=VERTEX_POINT ( 'NONE', #128954 ) ;
#51019=EDGE_CURVE ( 'NONE', #48019, #62589, #169400, .T. ) ;
#51034=CARTESIAN_POINT ( 'NONE',  ( -21.29999999999995808, 7.128833340093095217, -233.7327013124392749 ) ) ;
#51040=ORIENTED_EDGE ( 'NONE', *, *, #37035, .T. ) ;
#51051=CARTESIAN_POINT ( 'NONE',  ( 20.52683494730124991, 18.86671595410186697, -229.8325257532585795 ) ) ;
#51058=CARTESIAN_POINT ( 'NONE',  ( -23.15000000000000213, 36.02367271998545561, -235.8812521208699309 ) ) ;
#51086=ADVANCED_FACE ( 'NONE', ( #33745 ), #12875, .T. ) ;
#51092=DIRECTION ( 'NONE',  ( 0.000000000000000000, -0.7960711469212456981, 0.6052030477777622375 ) ) ;
#51101=CARTESIAN_POINT ( 'NONE',  ( -18.50000000000000000, 22.43030315632513094, -231.3223027016406093 ) ) ;
#51129=EDGE_CURVE ( 'NONE', #32586, #5211, #75203, .T. ) ;
#51143=ORIENTED_EDGE ( 'NONE', *, *, #43298, .T. ) ;
#51154=ORIENTED_EDGE ( 'NONE', *, *, #36669, .T. ) ;
#51158=CARTESIAN_POINT ( 'NONE',  ( 18.52130828395271678, 8.843855271129630324, -245.4074285112719451 ) ) ;
#51165=DIRECTION ( 'NONE',  ( 1.000000000000000000, 0.000000000000000000, 0.000000000000000000 ) ) ;
#51173=DIRECTION ( 'NONE',  ( 0.1538461538461670663, 0.4665713331246195694, 0.8710008909599673554 ) ) ;
#51201=DIRECTION ( 'NONE',  ( 0.000000000000000000, 0.8814952561688437216, -0.4721928772777331806 ) ) ;
#51204=ORIENTED_EDGE ( 'NONE', *, *, #62490, .F. ) ;
#51205=DIRECTION ( 'NONE',  ( -0.000000000000000000, -0.03181660087581238833, 0.9994937237965575427 ) ) ;
#51253=ADVANCED_FACE ( 'NONE', ( #118377 ), #141809, .F. ) ;
#51277=DIRECTION ( 'NONE',  ( 0.000000000000000000, 0.6855225566104508061, 0.7280513885559666276 ) ) ;
#51309=CARTESIAN_POINT ( 'NONE',  ( -22.39999999999999858, 0.3085173699977072914, -229.9658011520297691 ) ) ;
#51332=CARTESIAN_POINT ( 'NONE',  ( -18.50000000000000000, 30.22839164850006455, -235.6129688350293350 ) ) ;
#51333=DIRECTION ( 'NONE',  ( 1.000000000000000000, 3.448943450116723568E-16, 6.438528483529607644E-16 ) ) ;
#51347=ORIENTED_EDGE ( 'NONE', *, *, #82859, .T. ) ;
#51356=DIRECTION ( 'NONE',  ( 2.952720810173290098E-16, -0.4721928772777345129, -0.8814952561688431665 ) ) ;
#51378=CARTESIAN_POINT ( 'NONE',  ( -18.47690164073606667, 38.09692775460474223, -261.0587226095922802 ) ) ;
#51394=B_SPLINE_CURVE_WITH_KNOTS ( 'NONE', 3,
 ( #196141, #197416, #34521, #96997, #193580, #14952, #94460, #18777 ),
 .UNSPECIFIED., .F., .F.,
 ( 4, 2, 2, 4 ),
 ( 0.000000000000000000, 6.534141206310459531E-05, 0.0001306828241262091906, 0.0002613656482524183812 ),
 .UNSPECIFIED. ) ;
#51398=ORIENTED_EDGE ( 'NONE', *, *, #40837, .T. ) ;
#51400=EDGE_CURVE ( 'NONE', #191683, #216206, #8731, .T. ) ;
#51402=DIRECTION ( 'NONE',  ( -1.000000000000000000, 0.000000000000000000, 0.000000000000000000 ) ) ;
#51405=ORIENTED_EDGE ( 'NONE', *, *, #60144, .F. ) ;
#51415=ADVANCED_FACE ( 'NONE', ( #84308 ), #121199, .T. ) ;
#51433=CARTESIAN_POINT ( 'NONE',  ( -23.15000000000000213, 11.36448785225375602, -246.7787679937655980 ) ) ;
#51441=AXIS2_PLACEMENT_3D ( 'NONE', #191873, #52304, #172328 ) ;
#51466=VECTOR ( 'NONE', #172214, 1000.000000000000000 ) ;
#51489=DIRECTION ( 'NONE',  ( 0.000000000000000000, -0.03181660087583042251, 0.9994937237965568766 ) ) ;
#51524=LINE ( 'NONE', #88086, #228472 ) ;
#51558=AXIS2_PLACEMENT_3D ( 'NONE', #36200, #74057, #14066 ) ;
#51564=PLANE ( 'NONE',  #76638 ) ;
#51568=CARTESIAN_POINT ( 'NONE',  ( -23.25000000000000000, 11.60058429089262333, -246.3380203656811887 ) ) ;
#51573=VECTOR ( 'NONE', #114840, 1000.000000000000000 ) ;
#51576=CARTESIAN_POINT ( 'NONE',  ( -21.14999999999999858, 12.67709964810648238, -223.3751320524553705 ) ) ;
#51661=FACE_OUTER_BOUND ( 'NONE', #68273, .T. ) ;
#51677=CARTESIAN_POINT ( 'NONE',  ( 18.59999994388910238, 9.037544858871804365, -245.3775128972792174 ) ) ;
#51682=CARTESIAN_POINT ( 'NONE',  ( 18.51697539158856998, 46.41023286455060770, -243.0722154975327385 ) ) ;
#51691=CARTESIAN_POINT ( 'NONE',  ( -20.54999999999999716, 19.35378350773087419, -238.0802544632095987 ) ) ;
#51704=CARTESIAN_POINT ( 'NONE',  ( 23.14999999999999503, 36.02367271998545561, -235.8812521208699309 ) ) ;
#51730=AXIS2_PLACEMENT_3D ( 'NONE', #41278, #119513, #158655 ) ;
#51744=CARTESIAN_POINT ( 'NONE',  ( 21.14999999999999858, 1.658775325997237315, -230.6916041481598540 ) ) ;
#51761=EDGE_CURVE ( 'NONE', #177294, #16167, #117068, .T. ) ;
#51777=DIRECTION ( 'NONE',  ( 0.000000000000000000, 0.8814952561688430555, -0.4721928772777346239 ) ) ;
#51808=CARTESIAN_POINT ( 'NONE',  ( 20.85000000000000142, 43.53458741986632674, -253.2342671440096922 ) ) ;
#51829=CARTESIAN_POINT ( 'NONE',  ( -22.01447462590973103, 10.47144741134476931, -227.2829313272817444 ) ) ;
#51845=ORIENTED_EDGE ( 'NONE', *, *, #88560, .F. ) ;
#51857=CARTESIAN_POINT ( 'NONE',  ( -21.29999999999995808, 7.128833340093095217, -233.7327013124392749 ) ) ;
#51865=CIRCLE ( 'NONE', #255846, 0.09999999999999711897 ) ;
#51878=CARTESIAN_POINT ( 'NONE',  ( 22.47071067811865674, 10.68684811775432841, -226.8807012965928607 ) ) ;
#51920=DIRECTION ( 'NONE',  ( 1.000000000000000000, 3.448943450116723568E-16, 6.438528483529607644E-16 ) ) ;
#51922=CARTESIAN_POINT ( 'NONE',  ( -18.59999999999999787, 30.09302283515540211, -235.6538990729184491 ) ) ;
#51946=DIRECTION ( 'NONE',  ( 0.000000000000000000, 0.4721928772777242433, 0.8814952561688484955 ) ) ;
#51955=DIRECTION ( 'NONE',  ( 0.000000000000000000, -0.4721928772776973204, -0.8814952561688629284 ) ) ;
#51984=ORIENTED_EDGE ( 'NONE', *, *, #231288, .F. ) ;
#52035=ORIENTED_EDGE ( 'NONE', *, *, #251691, .T. ) ;
#52053=ORIENTED_EDGE ( 'NONE', *, *, #168311, .F. ) ;
#52073=ORIENTED_EDGE ( 'NONE', *, *, #242103, .T. ) ;
#52105=EDGE_CURVE ( 'NONE', #41556, #198415, #122909, .T. ) ;
#52112=VECTOR ( 'NONE', #137063, 1000.000000000000000 ) ;
#52114=LINE ( 'NONE', #211206, #171757 ) ;
#52150=TOROIDAL_SURFACE ( 'NONE', #168741, 11.89999999999999858, 0.1000000000000000056 ) ;
#52174=DIRECTION ( 'NONE',  ( 2.952720810173288126E-16, -0.4721928772777346794, -0.8814952561688429444 ) ) ;
#52195=AXIS2_PLACEMENT_3D ( 'NONE', #168206, #250266, #49501 ) ;
#52197=EDGE_CURVE ( 'NONE', #43496, #71417, #224553, .T. ) ;
#52240=DIRECTION ( 'NONE',  ( 0.000000000000000000, 0.03181660087583042945, -0.9994937237965569876 ) ) ;
#52253=VECTOR ( 'NONE', #106436, 1000.000000000000000 ) ;
#52266=ORIENTED_EDGE ( 'NONE', *, *, #257553, .T. ) ;
#52272=ORIENTED_EDGE ( 'NONE', *, *, #242883, .T. ) ;
#52287=CIRCLE ( 'NONE', #247935, 0.1000000000000013933 ) ;
#52304=DIRECTION ( 'NONE',  ( -1.000000000000000000, -0.000000000000000000, -0.000000000000000000 ) ) ;
#52316=DIRECTION ( 'NONE',  ( 1.000000000000000000, -0.000000000000000000, -0.000000000000000000 ) ) ;
#52351=CARTESIAN_POINT ( 'NONE',  ( 20.30531438145591139, 18.76867081783750635, -228.5135550048062782 ) ) ;
#52358=VERTEX_POINT ( 'NONE', #20613 ) ;
#52382=ORIENTED_EDGE ( 'NONE', *, *, #139807, .F. ) ;
#52384=VECTOR ( 'NONE', #180114, 1000.000000000000000 ) ;
#52393=ORIENTED_EDGE ( 'NONE', *, *, #130909, .T. ) ;
#52398=CYLINDRICAL_SURFACE ( 'NONE', #186136, 0.09999999999999939493 ) ;
#52430=CARTESIAN_POINT ( 'NONE',  ( 18.54271179734066521, 38.05662890930041442, -261.2177829373591180 ) ) ;
#52442=DIRECTION ( 'NONE',  ( 0.000000000000000000, -0.5826443254699606999, -0.8127272543711416830 ) ) ;
#52463=VERTEX_POINT ( 'NONE', #137952 ) ;
#52521=VECTOR ( 'NONE', #243228, 1000.000000000000000 ) ;
#52542=ORIENTED_EDGE ( 'NONE', *, *, #36669, .F. ) ;
#52557=CARTESIAN_POINT ( 'NONE',  ( -23.15000000000000213, 19.97490019448090948, -235.9060780337186145 ) ) ;
#52650=ORIENTED_EDGE ( 'NONE', *, *, #20814, .T. ) ;
#52681=VECTOR ( 'NONE', #176496, 1000.000000000000000 ) ;
#52689=EDGE_LOOP ( 'NONE', ( #109804, #171911, #131763, #19039 ) ) ;
#52695=ORIENTED_EDGE ( 'NONE', *, *, #213625, .F. ) ;
#52697=EDGE_CURVE ( 'NONE', #50748, #104681, #121831, .T. ) ;
#52723=ORIENTED_EDGE ( 'NONE', *, *, #8096, .F. ) ;
#52725=CARTESIAN_POINT ( 'NONE',  ( 20.85000000000000142, 43.30036367478129478, -245.0872390055602352 ) ) ;
#52765=DIRECTION ( 'NONE',  ( -1.000000000000000000, -1.394253735153568729E-16, -2.602809386958776729E-16 ) ) ;
#52775=DIRECTION ( 'NONE',  ( 0.000000000000000000, 0.8814952561688444987, -0.4721928772777320149 ) ) ;
#52779=CARTESIAN_POINT ( 'NONE',  ( 21.05000000000000071, 1.542939424703665630, -230.7237943920232226 ) ) ;
#52781=AXIS2_PLACEMENT_3D ( 'NONE', #143592, #223119, #35834 ) ;
#52790=DIRECTION ( 'NONE',  ( 0.000000000000000000, -0.4721928772777346239, -0.8814952561688430555 ) ) ;
#52829=EDGE_CURVE ( 'NONE', #217322, #63208, #176908, .T. ) ;
#52842=AXIS2_PLACEMENT_3D ( 'NONE', #257841, #216185, #76681 ) ;
#52850=AXIS2_PLACEMENT_3D ( 'NONE', #95394, #73297, #253175 ) ;
#52865=AXIS2_PLACEMENT_3D ( 'NONE', #5378, #21151, #181498 ) ;
#52878=VECTOR ( 'NONE', #43061, 1000.000000000000000 ) ;
#52881=CIRCLE ( 'NONE', #32073, 0.1000000000000066391 ) ;
#52902=ORIENTED_EDGE ( 'NONE', *, *, #118066, .T. ) ;
#52905=DIRECTION ( 'NONE',  ( 1.000000000000000000, 0.000000000000000000, 0.000000000000000000 ) ) ;
#52909=EDGE_CURVE ( 'NONE', #138714, #19770, #102438, .T. ) ;
#52935=ORIENTED_EDGE ( 'NONE', *, *, #71494, .F. ) ;
#52958=LINE ( 'NONE', #38547, #235509 ) ;
#52980=CARTESIAN_POINT ( 'NONE',  ( 18.58703555225010717, 8.967833031541422528, -245.3886906379661923 ) ) ;
#53001=CARTESIAN_POINT ( 'NONE',  ( -20.54999999999999716, 11.60058429089262333, -246.3380203656811887 ) ) ;
#53017=LINE ( 'NONE', #11337, #67042 ) ;
#53034=EDGE_CURVE ( 'NONE', #63323, #26083, #68494, .T. ) ;
#53066=ORIENTED_EDGE ( 'NONE', *, *, #55506, .F. ) ;
#53097=CARTESIAN_POINT ( 'NONE',  ( 21.05000000000000071, 18.18127959618848877, -237.5711165786817389 ) ) ;
#53106=ORIENTED_EDGE ( 'NONE', *, *, #157809, .T. ) ;
#53108=EDGE_CURVE ( 'NONE', #164610, #176897, #177877, .T. ) ;
#53110=CIRCLE ( 'NONE', #144683, 0.1000000000000013933 ) ;
#53121=ORIENTED_EDGE ( 'NONE', *, *, #160337, .F. ) ;
#53130=FACE_OUTER_BOUND ( 'NONE', #58301, .T. ) ;
#53140=CARTESIAN_POINT ( 'NONE',  ( -20.64999999999999858, 24.04029978241813126, -253.0016354099517457 ) ) ;
#53142=DIRECTION ( 'NONE',  ( 1.000000000000000000, 0.000000000000000000, 0.000000000000000000 ) ) ;
#53146=DIRECTION ( 'NONE',  ( 0.000000000000000000, 0.8814952561688418342, -0.4721928772777367889 ) ) ;
#53195=CARTESIAN_POINT ( 'NONE',  ( -23.25000000000000000, 7.128833340093095217, -233.7327013124392749 ) ) ;
#53196=DIRECTION ( 'NONE',  ( -3.469446951953352918E-14, 0.4721928772776973204, 0.8814952561688629284 ) ) ;
#53210=ORIENTED_EDGE ( 'NONE', *, *, #242514, .T. ) ;
#53227=CARTESIAN_POINT ( 'NONE',  ( 20.97462148592293829, 22.12183205585962043, -231.6962180060701542 ) ) ;
#53245=SPHERICAL_SURFACE ( 'NONE', #151429, 0.1000000000000000056 ) ;
#53247=DIRECTION ( 'NONE',  ( -1.000000000000000000, -1.394253735153569469E-16, -2.602809386958778209E-16 ) ) ;
#53287=DIRECTION ( 'NONE',  ( -1.000000000000000000, -8.674042436075348305E-17, -1.619280515896124405E-16 ) ) ;
#53295=FACE_OUTER_BOUND ( 'NONE', #244275, .T. ) ;
#53299=FACE_OUTER_BOUND ( 'NONE', #90661, .T. ) ;
#53302=FACE_OUTER_BOUND ( 'NONE', #156942, .T. ) ;
#53304=TOROIDAL_SURFACE ( 'NONE', #199051, 0.4000000000000017431, 0.1000000000000000056 ) ;
#53326=EDGE_LOOP ( 'NONE', ( #119090, #146361, #120659, #169657 ) ) ;
#53388=AXIS2_PLACEMENT_3D ( 'NONE', #224606, #65532, #169824 ) ;
#53390=ORIENTED_EDGE ( 'NONE', *, *, #235520, .F. ) ;
#53411=CARTESIAN_POINT ( 'NONE',  ( -21.05000000000000071, 18.18127959618848877, -237.5711165786817389 ) ) ;
#53412=VECTOR ( 'NONE', #43042, 1000.000000000000000 ) ;
#53485=VECTOR ( 'NONE', #187827, 1000.000000000000000 ) ;
#53511=PRODUCT_CONTEXT ( 'NONE', #182240, 'mechanical' ) ;
#53529=AXIS2_PLACEMENT_3D ( 'NONE', #154930, #191494, #71537 ) ;
#53530=AXIS2_PLACEMENT_3D ( 'NONE', #205377, #26792, #245816 ) ;
#53557=VECTOR ( 'NONE', #86255, 1000.000000000000000 ) ;
#53619=FACE_OUTER_BOUND ( 'NONE', #136863, .T. ) ;
#53624=VERTEX_POINT ( 'NONE', #220233 ) ;
#53640=EDGE_LOOP ( 'NONE', ( #31362, #21296, #93363, #192791 ) ) ;
#53648=CARTESIAN_POINT ( 'NONE',  ( 21.00000000000000000, 30.37633856152204359, -235.1250019192171408 ) ) ;
#53702=CARTESIAN_POINT ( 'NONE',  ( -23.25000000000000000, 36.65892442174935439, -249.5511627012433848 ) ) ;
#53713=AXIS2_PLACEMENT_3D ( 'NONE', #163187, #199759, #160638 ) ;
#53751=DIRECTION ( 'NONE',  ( 0.000000000000000000, 0.4721928772776973204, 0.8814952561688629284 ) ) ;
#53759=CARTESIAN_POINT ( 'NONE',  ( 18.54116936837188234, 8.873462500583581658, -245.4030598191407648 ) ) ;
#53791=VERTEX_POINT ( 'NONE', #242341 ) ;
#53822=ORIENTED_EDGE ( 'NONE', *, *, #117153, .T. ) ;
#53847=CARTESIAN_POINT ( 'NONE',  ( -20.94999999999999929, 36.65892442174935439, -249.5511627012433848 ) ) ;
#53852=DIRECTION ( 'NONE',  ( 0.000000000000000000, -0.8814952561688430555, 0.4721928772777346239 ) ) ;
#53862=ORIENTED_EDGE ( 'NONE', *, *, #240250, .T. ) ;
#53872=ADVANCED_FACE ( 'NONE', ( #231782 ), #74017, .F. ) ;
#53873=VERTEX_POINT ( 'NONE', #149690 ) ;
#53890=EDGE_LOOP ( 'NONE', ( #64918, #207864, #218478, #142595 ) ) ;
#53898=B_SPLINE_CURVE_WITH_KNOTS ( 'NONE', 3,
 ( #205639, #126101, #203082, #6155 ),
 .UNSPECIFIED., .F., .F.,
 ( 4, 4 ),
 ( 0.000000000000000000, 0.0002118541922231917721 ),
 .UNSPECIFIED. ) ;
#53909=AXIS2_PLACEMENT_3D ( 'NONE', #113113, #207086, #229221 ) ;
#53917=DIRECTION ( 'NONE',  ( -0.000000000000000000, -0.8814952561688430555, 0.4721928772777346239 ) ) ;
#53927=( BOUNDED_SURFACE ( )  B_SPLINE_SURFACE ( 3, 2, ( 
 ( #48400, #105784, #185355 ),
 ( #217407, #37520, #161320 ),
 ( #257778, #100009, #81726 ),
 ( #58322, #97446, #137868 ),
 ( #76625, #118340, #62208 ),
 ( #117049, #238262, #197853 ) ),
 .UNSPECIFIED., .F., .F., .F. ) 
 B_SPLINE_SURFACE_WITH_KNOTS ( ( 4, 2, 4 ),
 ( 3, 3 ),
 ( 6.719893378900011955E-05, 0.0002757154632485553998, 0.0004842319927081106530 ),
 ( 0.000000000000000000, 1.000000000000000000 ),
 .UNSPECIFIED. ) 
 GEOMETRIC_REPRESENTATION_ITEM ( )  RATIONAL_B_SPLINE_SURFACE ( (
 ( 1.000000000000000000, 0.7250110520820690629, 1.000000000000000000),
 ( 1.000000000000000000, 0.7277932058357374778, 1.000000000000000000),
 ( 1.000000000000000000, 0.7278452872618936809, 1.000000000000000000),
 ( 1.000000000000000000, 0.7221445671547916945, 1.000000000000000000),
 ( 1.000000000000000000, 0.7163662143780868963, 1.000000000000000000),
 ( 1.000000000000000000, 0.7071067811865475727, 1.000000000000000000) ) ) 
 REPRESENTATION_ITEM ( '' )  SURFACE ( )  );
#53948=VERTEX_POINT ( 'NONE', #79086 ) ;
#53974=VECTOR ( 'NONE', #42547, 1000.000000000000000 ) ;
#53986=EDGE_CURVE ( 'NONE', #186652, #79572, #96714, .T. ) ;
#53992=CARTESIAN_POINT ( 'NONE',  ( -18.41817142474017999, 37.99506873957891884, -261.0425698592600270 ) ) ;
#54005=CARTESIAN_POINT ( 'NONE',  ( -18.50000000000000000, 43.24695311518262741, -245.0026972281755775 ) ) ;
#54026=CARTESIAN_POINT ( 'NONE',  ( -22.59999985501179154, 12.61921324905064701, -223.3442716046673411 ) ) ;
#54029=CARTESIAN_POINT ( 'NONE',  ( 18.49999999999999645, 45.93315328338058379, -256.6017782078560003 ) ) ;
#54033=FACE_OUTER_BOUND ( 'NONE', #42176, .T. ) ;
#54050=EDGE_CURVE ( 'NONE', #58384, #39320, #42580, .T. ) ;
#54056=CARTESIAN_POINT ( 'NONE',  ( -20.54999999999999716, 25.94586868676353575, -241.5435999122864530 ) ) ;
#54061=CARTESIAN_POINT ( 'NONE',  ( -21.05000000000000071, 10.23283250993384641, -228.1194284103923451 ) ) ;
#54101=CARTESIAN_POINT ( 'NONE',  ( -18.59999999999999787, 38.28679861725830591, -261.0868692510649680 ) ) ;
#54125=DIRECTION ( 'NONE',  ( -1.000000000000000000, 0.000000000000000000, 0.000000000000000000 ) ) ;
#54161=FACE_BOUND ( 'NONE', #199596, .T. ) ;
#54181=DIRECTION ( 'NONE',  ( -2.342056488767300981E-15, -0.9371753822965326330, 0.3488585713686107592 ) ) ;
#54190=EDGE_CURVE ( 'NONE', #109684, #122934, #208064, .T. ) ;
#54239=CARTESIAN_POINT ( 'NONE',  ( 18.59999999999999432, 14.81796439977981272, -236.5325475414793743 ) ) ;
#54261=CARTESIAN_POINT ( 'NONE',  ( 18.40000000000000213, 8.841736820195471580, -245.4273993276876240 ) ) ;
#54327=VECTOR ( 'NONE', #253927, 1000.000000000000000 ) ;
#54331=ORIENTED_EDGE ( 'NONE', *, *, #64293, .T. ) ;
#54352=ORIENTED_EDGE ( 'NONE', *, *, #236977, .T. ) ;
#54359=FACE_OUTER_BOUND ( 'NONE', #252308, .T. ) ;
#54365=DIRECTION ( 'NONE',  ( 0.000000000000000000, 0.8814952561688434995, -0.4721928772777335137 ) ) ;
#54385=DIRECTION ( 'NONE',  ( 0.000000000000000000, -0.5826443254700256480, -0.8127272543710952757 ) ) ;
#54387=ORIENTED_EDGE ( 'NONE', *, *, #235407, .T. ) ;
#54425=CARTESIAN_POINT ( 'NONE',  ( 21.14999999999999858, 20.97908333644147660, -233.6079013178409411 ) ) ;
#54428=EDGE_LOOP ( 'NONE', ( #210028, #240753, #112102, #201577, #147230 ) ) ;
#54472=FACE_OUTER_BOUND ( 'NONE', #23211, .T. ) ;
#54485=VERTEX_POINT ( 'NONE', #102177 ) ;
#54493=CARTESIAN_POINT ( 'NONE',  ( -20.85000000000000142, 36.65892442174935439, -249.5511627012433848 ) ) ;
#54504=EDGE_CURVE ( 'NONE', #182052, #39363, #220868, .T. ) ;
#54536=DIRECTION ( 'NONE',  ( 0.000000000000000000, -0.8814952561688476074, 0.4721928772777262417 ) ) ;
#54561=ORIENTED_EDGE ( 'NONE', *, *, #194767, .F. ) ;
#54580=CYLINDRICAL_SURFACE ( 'NONE', #146268, 0.1000000000000075273 ) ;
#54588=CARTESIAN_POINT ( 'NONE',  ( -18.59999999999999787, 18.18127959618848166, -237.5711165786817389 ) ) ;
#54594=VERTEX_POINT ( 'NONE', #87768 ) ;
#54600=VERTEX_POINT ( 'NONE', #29150 ) ;
#54624=ORIENTED_EDGE ( 'NONE', *, *, #150379, .T. ) ;
#54645=( BOUNDED_SURFACE ( )  B_SPLINE_SURFACE ( 3, 2, ( 
 ( #110433, #135114, #30935 ),
 ( #189979, #132575, #73912 ),
 ( #11340, #75188, #71334 ),
 ( #90865, #32209, #251213 ),
 ( #154728, #153467, #150845 ),
 ( #113009, #95990, #114285 ) ),
 .UNSPECIFIED., .F., .F., .F. ) 
 B_SPLINE_SURFACE_WITH_KNOTS ( ( 4, 2, 4 ),
 ( 3, 3 ),
 ( 1.570796326794897668, 2.356194490192346169, 3.141592653589794448 ),
 ( 0.000000000000000000, 1.000000000000000000 ),
 .UNSPECIFIED. ) 
 GEOMETRIC_REPRESENTATION_ITEM ( )  RATIONAL_B_SPLINE_SURFACE ( (
 ( 1.000000000000000000, 0.7071067811864732988, 1.000000000000000000),
 ( 1.000000000000000000, 0.6611148371780445343, 1.000000000000000000),
 ( 1.000000000000000000, 0.6092287576693995454, 1.000000000000000000),
 ( 1.000000000000000000, 0.5278258667060209408, 1.000000000000000000),
 ( 1.000000000000000000, 0.4993418825331956135, 1.000000000000000000),
 ( 1.000000000000000000, 0.4999999999999739098, 1.000000000000000000) ) ) 
 REPRESENTATION_ITEM ( '' )  SURFACE ( )  );
#54673=EDGE_LOOP ( 'NONE', ( #38193, #143543, #143554, #242988 ) ) ;
#54681=ORIENTED_EDGE ( 'NONE', *, *, #251919, .T. ) ;
#54685=CARTESIAN_POINT ( 'NONE',  ( 20.94999999999999929, 28.63831050940605394, -258.0693639473472558 ) ) ;
#54717=ORIENTED_EDGE ( 'NONE', *, *, #202684, .T. ) ;
#54724=CARTESIAN_POINT ( 'NONE',  ( -21.05000000000000071, 26.34542992457388522, -244.0265060370938954 ) ) ;
#54779=LINE ( 'NONE', #33991, #213603 ) ;
#54787=DIRECTION ( 'NONE',  ( 0.000000000000000000, 0.4721928772777352346, 0.8814952561688428334 ) ) ;
#54792=CARTESIAN_POINT ( 'NONE',  ( 23.14999999999998437, 1.580567032079710055, -244.0902705724231794 ) ) ;
#54815=ORIENTED_EDGE ( 'NONE', *, *, #133059, .T. ) ;
#54828=CIRCLE ( 'NONE', #200589, 0.1999999999999987899 ) ;
#54830=DIRECTION ( 'NONE',  ( 0.000000000000000000, -0.7965107556683636014, 0.6046243595031649543 ) ) ;
#54860=DIRECTION ( 'NONE',  ( 1.000000000000000000, -0.000000000000000000, -0.000000000000000000 ) ) ;
#54866=CARTESIAN_POINT ( 'NONE',  ( 22.60000000000000142, 12.58798907299599179, -223.3278890275437050 ) ) ;
#54900=DIRECTION ( 'NONE',  ( 0.000000000000000000, -0.8814952561688513821, 0.4721928772777189698 ) ) ;
#54910=CARTESIAN_POINT ( 'NONE',  ( -23.15000000000000213, 19.73066058418984170, -238.2142830767208466 ) ) ;
#54931=ADVANCED_FACE ( 'NONE', ( #184010 ), #234674, .T. ) ;
#54981=DIRECTION ( 'NONE',  ( 1.000000000000000000, 0.000000000000000000, 0.000000000000000000 ) ) ;
#54984=CARTESIAN_POINT ( 'NONE',  ( 18.50000000000000711, 33.77764400792123212, -236.3455570846021203 ) ) ;
#54986=DIRECTION ( 'NONE',  ( -4.408576920032446739E-17, -0.8096735173027155286, 0.5868805631290315850 ) ) ;
#54989=CARTESIAN_POINT ( 'NONE',  ( 22.32929514600007792, 10.62008199960298427, -227.0053766058674967 ) ) ;
#55006=EDGE_CURVE ( 'NONE', #210749, #39196, #68260, .T. ) ;
#55022=CARTESIAN_POINT ( 'NONE',  ( -21.14999999999999858, 18.60982576078065520, -226.6665746245395496 ) ) ;
#55055=CIRCLE ( 'NONE', #13400, 0.1000000000000058481 ) ;
#55075=ORIENTED_EDGE ( 'NONE', *, *, #36718, .T. ) ;
#55078=DIRECTION ( 'NONE',  ( 0.000000000000000000, -0.8814952561688430555, 0.4721928772777346239 ) ) ;
#55114=CARTESIAN_POINT ( 'NONE',  ( -20.94999675878240808, 46.33100819526731584, -243.0553980158188381 ) ) ;
#55124=DIRECTION ( 'NONE',  ( 1.000000000000000000, 0.000000000000000000, 0.000000000000000000 ) ) ;
#55127=CIRCLE ( 'NONE', #21843, 0.1000000000000053763 ) ;
#55137=DIRECTION ( 'NONE',  ( -0.000000000000000000, 0.4721928772777347905, 0.8814952561688430555 ) ) ;
#55146=CARTESIAN_POINT ( 'NONE',  ( -20.94999999999999929, 36.65892442174935439, -249.5511627012433848 ) ) ;
#55181=EDGE_CURVE ( 'NONE', #28211, #223089, #56031, .T. ) ;
#55195=AXIS2_PLACEMENT_3D ( 'NONE', #116957, #94817, #38710 ) ;
#55225=ORIENTED_EDGE ( 'NONE', *, *, #257731, .F. ) ;
#55230=AXIS2_PLACEMENT_3D ( 'NONE', #55146, #134699, #135982 ) ;
#55277=DIRECTION ( 'NONE',  ( 0.000000000000000000, -0.8814952561688425003, 0.4721928772777359007 ) ) ;
#55286=EDGE_CURVE ( 'NONE', #89573, #70952, #188879, .T. ) ;
#55289=VECTOR ( 'NONE', #161230, 1000.000000000000000 ) ;
#55298=AXIS2_PLACEMENT_3D ( 'NONE', #104680, #182987, #102118 ) ;
#55311=EDGE_LOOP ( 'NONE', ( #8328, #236907, #220483, #170788 ) ) ;
#55312=AXIS2_PLACEMENT_3D ( 'NONE', #239197, #83922, #140076 ) ;
#55314=CIRCLE ( 'NONE', #238708, 0.1000000000000009354 ) ;
#55321=DIRECTION ( 'NONE',  ( -0.000000000000000000, -0.4721928772777351790, -0.8814952561688427224 ) ) ;
#55350=FACE_OUTER_BOUND ( 'NONE', #147836, .T. ) ;
#55367=ORIENTED_EDGE ( 'NONE', *, *, #6833, .F. ) ;
#55370=CYLINDRICAL_SURFACE ( 'NONE', #111744, 3.999999999999994671 ) ;
#55381=VECTOR ( 'NONE', #230367, 1000.000000000000000 ) ;
#55382=DIRECTION ( 'NONE',  ( -0.000000000000000000, -0.8814952561688430555, 0.4721928772777346239 ) ) ;
#55483=ORIENTED_EDGE ( 'NONE', *, *, #35554, .T. ) ;
#55488=EDGE_LOOP ( 'NONE', ( #134650, #222400, #9984, #104769 ) ) ;
#55506=EDGE_CURVE ( 'NONE', #199581, #104599, #218329, .T. ) ;
#55510=EDGE_CURVE ( 'NONE', #84289, #227126, #176602, .T. ) ;
#55526=ORIENTED_EDGE ( 'NONE', *, *, #77388, .T. ) ;
#55532=SPHERICAL_SURFACE ( 'NONE', #210042, 0.1000000000000000056 ) ;
#55539=VECTOR ( 'NONE', #81877, 1000.000000000000114 ) ;
#55558=CARTESIAN_POINT ( 'NONE',  ( 21.05000000000000071, 38.33376540847015690, -250.4483291680710693 ) ) ;
#55567=CARTESIAN_POINT ( 'NONE',  ( 21.05000000000046256, 10.18588724833545989, -228.0632827051668414 ) ) ;
#55623=DIRECTION ( 'NONE',  ( 1.000000000000000000, 0.000000000000000000, 0.000000000000000000 ) ) ;
#55641=ORIENTED_EDGE ( 'NONE', *, *, #184198, .T. ) ;
#55643=DIRECTION ( 'NONE',  ( -1.000000000000000000, -0.000000000000000000, -0.000000000000000000 ) ) ;
#55677=LINE ( 'NONE', #216064, #61676 ) ;
#55694=CARTESIAN_POINT ( 'NONE',  ( 23.14999999999999503, 36.06460295787456261, -236.0166209342146146 ) ) ;
#55715=AXIS2_PLACEMENT_3D ( 'NONE', #143718, #163301, #47168 ) ;
#55735=CIRCLE ( 'NONE', #234850, 0.5000000000000008882 ) ;
#55764=CARTESIAN_POINT ( 'NONE',  ( 20.94999999999999929, 46.41626913442612334, -243.0004334082109096 ) ) ;
#55814=EDGE_CURVE ( 'NONE', #136089, #149361, #134639, .T. ) ;
#55836=DIRECTION ( 'NONE',  ( 0.000000000000000000, -0.4721928772776935457, -0.8814952561688651489 ) ) ;
#55852=AXIS2_PLACEMENT_3D ( 'NONE', #39461, #64124, #241480 ) ;
#55854=DIRECTION ( 'NONE',  ( 1.000000000000000000, 0.000000000000000000, 0.000000000000000000 ) ) ;
#55856=DIRECTION ( 'NONE',  ( -1.000000000000000000, 0.000000000000000000, 0.000000000000000000 ) ) ;
#55870=DIRECTION ( 'NONE',  ( 0.000000000000000000, -0.6410630849193120762, 0.7674881895858300940 ) ) ;
#55875=CARTESIAN_POINT ( 'NONE',  ( 21.14261333020286671, 22.98702397223716076, -230.0712318222100805 ) ) ;
#55889=LINE ( 'NONE', #114611, #133321 ) ;
#55903=CARTESIAN_POINT ( 'NONE',  ( -21.14999999999999858, 4.184122562697131897, -245.3714803909117279 ) ) ;
#55931=ORIENTED_EDGE ( 'NONE', *, *, #192513, .T. ) ;
#55939=DIRECTION ( 'NONE',  ( -1.000000000000000000, -0.000000000000000000, -0.000000000000000000 ) ) ;
#55968=CARTESIAN_POINT ( 'NONE',  ( -23.15000000000000213, 33.13294339707397285, -247.6623911921324463 ) ) ;
#55976=ORIENTED_EDGE ( 'NONE', *, *, #133206, .F. ) ;
#55989=ORIENTED_EDGE ( 'NONE', *, *, #138085, .T. ) ;
#56006=LINE ( 'NONE', #216388, #166049 ) ;
#56015=AXIS2_PLACEMENT_3D ( 'NONE', #237375, #54860, #14500 ) ;
#56030=AXIS2_PLACEMENT_3D ( 'NONE', #84471, #165349, #46660 ) ;
#56031=LINE ( 'NONE', #92602, #51466 ) ;
#56084=FACE_OUTER_BOUND ( 'NONE', #199415, .T. ) ;
#56095=AXIS2_PLACEMENT_3D ( 'NONE', #144028, #223560, #124493 ) ;
#56120=CARTESIAN_POINT ( 'NONE',  ( -23.25000000000000000, 42.20719072976272912, -239.1935934412594804 ) ) ;
#56137=CARTESIAN_POINT ( 'NONE',  ( 22.48660254037844197, 12.58580559757026940, -223.4396719342083486 ) ) ;
#56163=CARTESIAN_POINT ( 'NONE',  ( 20.97468175916186439, 22.94852194069405371, -230.1531915370501906 ) ) ;
#56200=AXIS2_PLACEMENT_3D ( 'NONE', #238654, #43029, #182551 ) ;
#56205=CARTESIAN_POINT ( 'NONE',  ( 20.19326291203161716, 18.76649736222367437, -228.4452775901896473 ) ) ;
#56208=ORIENTED_EDGE ( 'NONE', *, *, #161393, .F. ) ;
#56222=VECTOR ( 'NONE', #31296, 1000.000000000000000 ) ;
#56224=AXIS2_PLACEMENT_3D ( 'NONE', #208163, #29541, #89465 ) ;
#56259=ORIENTED_EDGE ( 'NONE', *, *, #42119, .T. ) ;
#56283=DIRECTION ( 'NONE',  ( -1.000000000000000000, -1.394253735153569469E-16, -2.602809386958778209E-16 ) ) ;
#56343=AXIS2_PLACEMENT_3D ( 'NONE', #250963, #52765, #112761 ) ;
#56419=AXIS2_PLACEMENT_3D ( 'NONE', #215802, #213245, #232842 ) ;
#56477=PLANE ( 'NONE',  #181127 ) ;
#56484=LINE ( 'NONE', #90484, #219580 ) ;
#56497=LINE ( 'NONE', #61660, #68780 ) ;
#56498=EDGE_CURVE ( 'NONE', #233103, #81229, #48137, .T. ) ;
#56525=ORIENTED_EDGE ( 'NONE', *, *, #39648, .F. ) ;
#56558=CARTESIAN_POINT ( 'NONE',  ( -18.39999999999999858, 37.95493834378066111, -261.2294694241335264 ) ) ;
#56562=DIRECTION ( 'NONE',  ( 0.000000000000000000, 0.8814952561688432775, -0.4721928772777342354 ) ) ;
#56644=CARTESIAN_POINT ( 'NONE',  ( -18.46856557590794168, 8.915543251359052235, -245.4376850085415356 ) ) ;
#56681=ORIENTED_EDGE ( 'NONE', *, *, #32420, .F. ) ;
#56690=EDGE_CURVE ( 'NONE', #160449, #62992, #10398, .T. ) ;
#56697=CIRCLE ( 'NONE', #90043, 1.899999999999996136 ) ;
#56707=EDGE_CURVE ( 'NONE', #151273, #59542, #243854, .T. ) ;
#56714=VERTEX_POINT ( 'NONE', #164340 ) ;
#56748=CIRCLE ( 'NONE', #115236, 11.75000000000000533 ) ;
#56766=DIRECTION ( 'NONE',  ( 0.000000000000000000, -0.8496786552930224445, -0.5273008465187981608 ) ) ;
#56836=LINE ( 'NONE', #176844, #101720 ) ;
#56838=CIRCLE ( 'NONE', #140061, 0.1000000000000013933 ) ;
#56863=DIRECTION ( 'NONE',  ( 0.000000000000000000, -0.8814952561688430555, 0.4721928772777346239 ) ) ;
#56871=AXIS2_PLACEMENT_3D ( 'NONE', #143427, #164293, #80869 ) ;
#56874=CARTESIAN_POINT ( 'NONE',  ( 22.50927854361890113, -3.275978807471259913, -228.2735453177909335 ) ) ;
#56882=VERTEX_POINT ( 'NONE', #239709 ) ;
#56901=CARTESIAN_POINT ( 'NONE',  ( -21.14999999999999858, 1.627786319807485116, -244.0021210468063089 ) ) ;
#56921=ORIENTED_EDGE ( 'NONE', *, *, #232590, .F. ) ;
#56930=ORIENTED_EDGE ( 'NONE', *, *, #139206, .F. ) ;
#56945=DIRECTION ( 'NONE',  ( 0.000000000000000000, 0.8814952561688476074, -0.4721928772777262417 ) ) ;
#56981=CYLINDRICAL_SURFACE ( 'NONE', #88503, 0.1000000000000013933 ) ;
#56997=CARTESIAN_POINT ( 'NONE',  ( -23.15000000000000213, 35.97645343225767789, -235.9694016464868298 ) ) ;
#56999=VECTOR ( 'NONE', #142793, 1000.000000000000000 ) ;
#57041=CARTESIAN_POINT ( 'NONE',  ( 21.04105312098486635, 22.18722240147778280, -231.7305707818096323 ) ) ;
#57061=CIRCLE ( 'NONE', #235578, 0.1000000000000026146 ) ;
#57117=EDGE_CURVE ( 'NONE', #167556, #11331, #206996, .T. ) ;
#57120=ORIENTED_EDGE ( 'NONE', *, *, #9755, .F. ) ;
#57129=DIRECTION ( 'NONE',  ( 0.000000000000000000, 0.8814952561688416122, -0.4721928772777371219 ) ) ;
#57183=DIRECTION ( 'NONE',  ( 0.000000000000000000, -0.6855225566104692358, -0.7280513885559494192 ) ) ;
#57186=CIRCLE ( 'NONE', #123868, 0.1000000000000013933 ) ;
#57188=CARTESIAN_POINT ( 'NONE',  ( 20.84999999999998721, 46.46967969402478360, -243.0849751855955674 ) ) ;
#57228=B_SPLINE_CURVE_WITH_KNOTS ( 'NONE', 3,
 ( #226772, #127690, #26024, #207232 ),
 .UNSPECIFIED., .F., .F.,
 ( 4, 4 ),
 ( 0.000000000000000000, 0.001767853679387128589 ),
 .UNSPECIFIED. ) ;
#57304=DIRECTION ( 'NONE',  ( 0.000000000000000000, 0.8814952561688476074, -0.4721928772777262417 ) ) ;
#57307=VERTEX_POINT ( 'NONE', #176875 ) ;
#57333=CARTESIAN_POINT ( 'NONE',  ( 21.08489834409762054, 23.03108543700951216, -230.2007552241209680 ) ) ;
#57343=LINE ( 'NONE', #113485, #117487 ) ;
#57344=CIRCLE ( 'NONE', #99029, 1.999999999999997335 ) ;
#57346=AXIS2_PLACEMENT_3D ( 'NONE', #204211, #245923, #105076 ) ;
#57348=EDGE_LOOP ( 'NONE', ( #134459, #253713, #20717, #228497 ) ) ;
#57354=AXIS2_PLACEMENT_3D ( 'NONE', #26187, #147407, #9179 ) ;
#57371=SPHERICAL_SURFACE ( 'NONE', #57782, 0.1000000000000000056 ) ;
#57393=ORIENTED_EDGE ( 'NONE', *, *, #23845, .T. ) ;
#57403=FACE_OUTER_BOUND ( 'NONE', #86454, .T. ) ;
#57406=CARTESIAN_POINT ( 'NONE',  ( -18.39999999999999858, 37.95493834378066111, -261.2294694241335264 ) ) ;
#57412=VERTEX_POINT ( 'NONE', #215957 ) ;
#57429=AXIS2_PLACEMENT_3D ( 'NONE', #42277, #142630, #81359 ) ;
#57445=CIRCLE ( 'NONE', #199117, 0.09999999999999939493 ) ;
#57452=DIRECTION ( 'NONE',  ( -1.000000000000000000, 0.000000000000000000, 0.000000000000000000 ) ) ;
#57455=ORIENTED_EDGE ( 'NONE', *, *, #149586, .F. ) ;
#57505=AXIS2_PLACEMENT_3D ( 'NONE', #42162, #139942, #121707 ) ;
#57581=EDGE_CURVE ( 'NONE', #86057, #125245, #56838, .T. ) ;
#57627=ADVANCED_FACE ( 'NONE', ( #13626 ), #18893, .T. ) ;
#57653=AXIS2_PLACEMENT_3D ( 'NONE', #148150, #192421, #247238 ) ;
#57678=VECTOR ( 'NONE', #80119, 1000.000000000000000 ) ;
#57690=ORIENTED_EDGE ( 'NONE', *, *, #9755, .T. ) ;
#57756=AXIS2_PLACEMENT_3D ( 'NONE', #252170, #214345, #211787 ) ;
#57775=EDGE_LOOP ( 'NONE', ( #131917, #202586, #35547, #69045 ) ) ;
#57782=AXIS2_PLACEMENT_3D ( 'NONE', #173545, #251742, #35306 ) ;
#57794=EDGE_CURVE ( 'NONE', #170273, #179549, #127238, .T. ) ;
#57843=CARTESIAN_POINT ( 'NONE',  ( -21.05000000000000071, 13.60254931771583387, -238.7443143987590304 ) ) ;
#57852=DIRECTION ( 'NONE',  ( -1.000000000000000000, 0.000000000000000000, 0.000000000000000000 ) ) ;
#57866=AXIS2_PLACEMENT_3D ( 'NONE', #228049, #211054, #166822 ) ;
#57911=CARTESIAN_POINT ( 'NONE',  ( 21.09316766718127667, 10.10216385852922194, -228.0989014875141265 ) ) ;
#57930=AXIS2_PLACEMENT_3D ( 'NONE', #45071, #124616, #185862 ) ;
#57931=VERTEX_POINT ( 'NONE', #129412 ) ;
#57941=DIRECTION ( 'NONE',  ( -1.000000000000000000, 0.000000000000000000, 0.000000000000000000 ) ) ;
#57950=FACE_OUTER_BOUND ( 'NONE', #162349, .T. ) ;
#57958=DIRECTION ( 'NONE',  ( 1.000000000000000000, 0.000000000000000000, 0.000000000000000000 ) ) ;
#57994=DIRECTION ( 'NONE',  ( 3.265361837132812600E-16, -0.4721928772777346239, -0.8814952561688430555 ) ) ;
#58003=CARTESIAN_POINT ( 'NONE',  ( 18.59999999999999787, 45.93315328338058379, -256.6017782078560003 ) ) ;
#58006=AXIS2_PLACEMENT_3D ( 'NONE', #38837, #21834, #119659 ) ;
#58011=ORIENTED_EDGE ( 'NONE', *, *, #90939, .T. ) ;
#58012=DIRECTION ( 'NONE',  ( 2.259780016855444047E-14, 0.6052030477779081208, 0.7960711469211347868 ) ) ;
#58024=ORIENTED_EDGE ( 'NONE', *, *, #122478, .F. ) ;
#58041=AXIS2_PLACEMENT_3D ( 'NONE', #35229, #156465, #78153 ) ;
#58045=ORIENTED_EDGE ( 'NONE', *, *, #165306, .T. ) ;
#58046=AXIS2_PLACEMENT_3D ( 'NONE', #147082, #67561, #184942 ) ;
#58053=EDGE_CURVE ( 'NONE', #177294, #145739, #81579, .T. ) ;
#58060=DIRECTION ( 'NONE',  ( 0.000000000000000000, 0.8814952561688429444, -0.4721928772777345684 ) ) ;
#58063=ORIENTED_EDGE ( 'NONE', *, *, #79868, .T. ) ;
#58069=ORIENTED_EDGE ( 'NONE', *, *, #93472, .F. ) ;
#58096=ORIENTED_EDGE ( 'NONE', *, *, #107757, .F. ) ;
#58097=AXIS2_PLACEMENT_3D ( 'NONE', #153639, #194012, #15375 ) ;
#58099=CARTESIAN_POINT ( 'NONE',  ( 18.40000000000000213, 8.812905490826908661, -245.4119551738195071 ) ) ;
#58139=CARTESIAN_POINT ( 'NONE',  ( 23.15000000000000213, 28.50120599808395028, -258.2149742250584268 ) ) ;
#58144=VECTOR ( 'NONE', #79388, 1000.000000000000000 ) ;
#58195=EDGE_CURVE ( 'NONE', #88325, #93493, #116289, .T. ) ;
#58217=AXIS2_PLACEMENT_3D ( 'NONE', #92376, #14162, #229346 ) ;
#58238=ORIENTED_EDGE ( 'NONE', *, *, #254840, .F. ) ;
#58250=VECTOR ( 'NONE', #254788, 1000.000000000000000 ) ;
#58252=LINE ( 'NONE', #74022, #236529 ) ;
#58256=CARTESIAN_POINT ( 'NONE',  ( 23.14999999999998437, 7.128833340093095217, -233.7327013124392749 ) ) ;
#58266=ORIENTED_EDGE ( 'NONE', *, *, #175392, .T. ) ;
#58273=DIRECTION ( 'NONE',  ( 2.952720810173290098E-16, -0.4721928772777359007, -0.8814952561688425003 ) ) ;
#58301=EDGE_LOOP ( 'NONE', ( #54717, #189372, #85805, #128461 ) ) ;
#58320=CARTESIAN_POINT ( 'NONE',  ( -20.64999999999999858, 21.39147882631411335, -233.2615922652120730 ) ) ;
#58322=CARTESIAN_POINT ( 'NONE',  ( 21.05000000000000071, 18.68960778496915509, -227.9427670361891956 ) ) ;
#58355=DIRECTION ( 'NONE',  ( -6.938893903907219700E-15, 0.4721928772777345684, 0.8814952561688429444 ) ) ;
#58358=DIRECTION ( 'NONE',  ( -1.000000000000000000, -0.000000000000000000, -0.000000000000000000 ) ) ;
#58363=CARTESIAN_POINT ( 'NONE',  ( 21.53752568622139307, 1.193029429790094298, -230.4407734565393469 ) ) ;
#58381=EDGE_CURVE ( 'NONE', #218153, #218718, #44025, .T. ) ;
#58384=VERTEX_POINT ( 'NONE', #189093 ) ;
#58415=ORIENTED_EDGE ( 'NONE', *, *, #8072, .F. ) ;
#58427=CARTESIAN_POINT ( 'NONE',  ( -22.49756042579671700, -3.103614433689099616, -228.1629205807172980 ) ) ;
#58428=CARTESIAN_POINT ( 'NONE',  ( -18.39999999999999858, 8.780520186313291120, -245.4165333277510115 ) ) ;
#58432=VECTOR ( 'NONE', #153823, 1000.000000000000000 ) ;
#58484=CARTESIAN_POINT ( 'NONE',  ( 23.24999999999999645, 7.128833340093095217, -233.7327013124392749 ) ) ;
#58516=ORIENTED_EDGE ( 'NONE', *, *, #100831, .F. ) ;
#58531=EDGE_LOOP ( 'NONE', ( #144779, #177939, #201186, #226738 ) ) ;
#58561=ORIENTED_EDGE ( 'NONE', *, *, #216838, .F. ) ;
#58563=ADVANCED_FACE ( 'NONE', ( #84152 ), #65936, .F. ) ;
#58619=ORIENTED_EDGE ( 'NONE', *, *, #154936, .T. ) ;
#58622=CARTESIAN_POINT ( 'NONE',  ( 20.85000000000000142, 36.65892442174935439, -249.5511627012433848 ) ) ;
#58655=CARTESIAN_POINT ( 'NONE',  ( 23.25000000000000000, -8.777002227904191045, -238.5420042644097975 ) ) ;
#58658=EDGE_CURVE ( 'NONE', #39875, #188830, #107620, .T. ) ;
#58663=AXIS2_PLACEMENT_3D ( 'NONE', #53140, #252615, #233093 ) ;
#58665=TOROIDAL_SURFACE ( 'NONE', #100162, 0.6000000000000013101, 0.1000000000000000056 ) ;
#58668=EDGE_CURVE ( 'NONE', #86653, #67751, #29414, .T. ) ;
#58686=ORIENTED_EDGE ( 'NONE', *, *, #69170, .F. ) ;
#58687=DIRECTION ( 'NONE',  ( -6.938893903907222856E-15, 0.4721928772777346239, 0.8814952561688430555 ) ) ;
#58700=CARTESIAN_POINT ( 'NONE',  ( -18.50016250449483124, 46.34703458179508573, -243.0587802416268346 ) ) ;
#58746=B_SPLINE_CURVE_WITH_KNOTS ( 'NONE', 3,
 ( #58808, #138348, #15893, #155411, #217886, #92817, #39302, #73300, #251898, #14605 ),
 .UNSPECIFIED., .F., .F.,
 ( 4, 3, 3, 4 ),
 ( 0.000000000000000000, 3.394313611811087942E-05, 6.779740500699110782E-05, 0.0001049857339142587780 ),
 .UNSPECIFIED. ) ;
#58754=CIRCLE ( 'NONE', #100264, 0.1000000000000076522 ) ;
#58796=CARTESIAN_POINT ( 'NONE',  ( -20.54999999999999361, 31.44980407958351165, -233.5445995079518866 ) ) ;
#58808=CARTESIAN_POINT ( 'NONE',  ( 20.94999999999999574, 18.81166555858608902, -229.8642012822692777 ) ) ;
#58824=CARTESIAN_POINT ( 'NONE',  ( 18.59999999999999076, 43.24695311518262031, -245.0026972281755491 ) ) ;
#58827=EDGE_LOOP ( 'NONE', ( #106461, #246756, #145868, #152654 ) ) ;
#58855=LINE ( 'NONE', #219229, #7092 ) ;
#58868=CARTESIAN_POINT ( 'NONE',  ( -18.59999999999999787, 23.38726701055792745, -229.1122755113798632 ) ) ;
#58890=DIRECTION ( 'NONE',  ( 1.000000000000000000, 0.000000000000000000, 0.000000000000000000 ) ) ;
#58916=DIRECTION ( 'NONE',  ( 0.000000000000000000, 0.8814952561688437216, -0.4721928772777334582 ) ) ;
#58937=DIRECTION ( 'NONE',  ( -1.000000000000000000, 0.000000000000000000, 0.000000000000000000 ) ) ;
#58967=ORIENTED_EDGE ( 'NONE', *, *, #118194, .F. ) ;
#58988=ORIENTED_EDGE ( 'NONE', *, *, #57581, .F. ) ;
#58989=ORIENTED_EDGE ( 'NONE', *, *, #201246, .F. ) ;
#59002=FACE_OUTER_BOUND ( 'NONE', #82920, .T. ) ;
#59021=DIRECTION ( 'NONE',  ( 0.000000000000000000, 0.8814952561688513821, -0.4721928772777189698 ) ) ;
#59026=CARTESIAN_POINT ( 'NONE',  ( 23.24999999999999289, 12.62988036037870998, -223.4632815780722410 ) ) ;
#59040=ADVANCED_FACE ( 'NONE', ( #10798 ), #190748, .F. ) ;
#59060=CARTESIAN_POINT ( 'NONE',  ( -23.15000000000000213, 20.02211948220868365, -235.8179285081017156 ) ) ;
#59073=ORIENTED_EDGE ( 'NONE', *, *, #10618, .T. ) ;
#59076=ORIENTED_EDGE ( 'NONE', *, *, #214510, .T. ) ;
#59077=CARTESIAN_POINT ( 'NONE',  ( -21.05000000000000071, 26.25728039895700761, -243.9792867493661106 ) ) ;
#59081=ORIENTED_EDGE ( 'NONE', *, *, #38786, .F. ) ;
#59087=VECTOR ( 'NONE', #88409, 1000.000000000000000 ) ;
#59090=CARTESIAN_POINT ( 'NONE',  ( -18.39999999999999858, 37.95493834378067532, -261.2294694241335264 ) ) ;
#59146=( NAMED_UNIT ( * ) SI_UNIT ( $, .STERADIAN. ) SOLID_ANGLE_UNIT ( ) );
#59166=CARTESIAN_POINT ( 'NONE',  ( 18.45068634130097607, 8.880467395992003077, -245.4328382399599491 ) ) ;
#59200=VERTEX_POINT ( 'NONE', #180156 ) ;
#59204=VERTEX_POINT ( 'NONE', #19802 ) ;
#59211=DIRECTION ( 'NONE',  ( 0.000000000000000000, -0.8814952561688444987, 0.4721928772777320149 ) ) ;
#59237=ORIENTED_EDGE ( 'NONE', *, *, #145049, .F. ) ;
#59261=EDGE_LOOP ( 'NONE', ( #43725, #111150, #62687, #79509 ) ) ;
#59269=AXIS2_PLACEMENT_3D ( 'NONE', #185976, #85549, #182135 ) ;
#59278=CARTESIAN_POINT ( 'NONE',  ( 21.14999999999999858, 23.34004772283015683, -229.2004250369967338 ) ) ;
#59320=DIRECTION ( 'NONE',  ( 0.000000000000000000, -0.8814952561688429444, 0.4721928772777345684 ) ) ;
#59368=EDGE_CURVE ( 'NONE', #148681, #195613, #33551, .T. ) ;
#59369=CARTESIAN_POINT ( 'NONE',  ( 18.43579564894475453, 8.780520514393622022, -245.4165332813718976 ) ) ;
#59382=EDGE_CURVE ( 'NONE', #70494, #53791, #83360, .T. ) ;
#59437=CARTESIAN_POINT ( 'NONE',  ( -18.50000000000000000, 43.35377423437995503, -245.1717807829448930 ) ) ;
#59449=AXIS2_PLACEMENT_3D ( 'NONE', #164056, #244856, #124929 ) ;
#59473=DIRECTION ( 'NONE',  ( 0.000000000000000000, 0.8814952561688494947, -0.4721928772777226890 ) ) ;
#59480=FACE_OUTER_BOUND ( 'NONE', #148368, .T. ) ;
#59542=VERTEX_POINT ( 'NONE', #156463 ) ;
#59552=ADVANCED_FACE ( 'NONE', ( #234677 ), #215111, .T. ) ;
#59595=DIRECTION ( 'NONE',  ( 1.000000000000000000, 0.000000000000000000, 0.000000000000000000 ) ) ;
#59621=DIRECTION ( 'NONE',  ( 1.000000000000000000, -0.000000000000000000, -0.000000000000000000 ) ) ;
#59630=CARTESIAN_POINT ( 'NONE',  ( -23.15000000000000213, 7.128833340093095217, -233.7327013124392749 ) ) ;
#59634=DIRECTION ( 'NONE',  ( 1.000000000000000000, 3.276496277610882853E-15, 6.116602059353118732E-15 ) ) ;
#59745=EDGE_LOOP ( 'NONE', ( #100890, #203058, #238108, #98433 ) ) ;
#59771=AXIS2_PLACEMENT_3D ( 'NONE', #203778, #79945, #25171 ) ;
#59772=ORIENTED_EDGE ( 'NONE', *, *, #161069, .T. ) ;
#59775=DIRECTION ( 'NONE',  ( -0.7071067811865474617, -0.3338907855510734324, -0.6233112732207618523 ) ) ;
#59808=DIRECTION ( 'NONE',  ( 0.000000000000000000, 0.8855159391400395652, -0.4646089985449416981 ) ) ;
#59851=EDGE_LOOP ( 'NONE', ( #100862, #150255, #148370, #157454 ) ) ;
#59861=DIRECTION ( 'NONE',  ( 0.000000000000000000, 0.5341055959867045955, -0.8454177738465681324 ) ) ;
#59925=CARTESIAN_POINT ( 'NONE',  ( -18.59999999999999787, 2.272311100394797556, -217.9150152700588876 ) ) ;
#59930=AXIS2_PLACEMENT_3D ( 'NONE', #87219, #247595, #190204 ) ;
#59969=CARTESIAN_POINT ( 'NONE',  ( -18.43707690579160641, 37.95493834378067532, -261.2294694241335833 ) ) ;
#60035=CIRCLE ( 'NONE', #147345, 0.6000000000000008660 ) ;
#60048=ORIENTED_EDGE ( 'NONE', *, *, #81559, .T. ) ;
#60083=DIRECTION ( 'NONE',  ( -1.000000000000000000, 0.000000000000000000, 0.000000000000000000 ) ) ;
#60097=CARTESIAN_POINT ( 'NONE',  ( -18.50000000000000000, 45.93315328338058379, -256.6017782078560003 ) ) ;
#60111=ADVANCED_FACE ( 'NONE', ( #32413 ), #196179, .T. ) ;
#60128=DIRECTION ( 'NONE',  ( 0.000000000000000000, -0.8814952561688430555, 0.4721928772777346239 ) ) ;
#60144=EDGE_CURVE ( 'NONE', #108480, #68656, #117080, .T. ) ;
#60155=CARTESIAN_POINT ( 'NONE',  ( 18.59999999999999076, 33.89981536720673461, -236.1713368690715527 ) ) ;
#60176=VECTOR ( 'NONE', #229089, 1000.000000000000000 ) ;
#60196=( NAMED_UNIT ( * ) PLANE_ANGLE_UNIT ( ) SI_UNIT ( $, .RADIAN. ) );
#60197=AXIS2_PLACEMENT_3D ( 'NONE', #221609, #162967, #101650 ) ;
#60210=DIRECTION ( 'NONE',  ( 1.000000000000000000, 0.000000000000000000, 0.000000000000000000 ) ) ;
#60264=DIRECTION ( 'NONE',  ( 0.000000000000000000, -0.8814952561688430555, 0.4721928772777346239 ) ) ;
#60271=ORIENTED_EDGE ( 'NONE', *, *, #113859, .F. ) ;
#60272=CARTESIAN_POINT ( 'NONE',  ( -20.88420186297724257, 46.46179379974390855, -243.0832762246653260 ) ) ;
#60306=DIRECTION ( 'NONE',  ( 1.000000000000000000, 0.000000000000000000, 0.000000000000000000 ) ) ;
#60338=CARTESIAN_POINT ( 'NONE',  ( 20.94999999999999929, 23.45160524131172153, -253.2535058871250726 ) ) ;
#60360=ORIENTED_EDGE ( 'NONE', *, *, #166781, .F. ) ;
#60388=VERTEX_POINT ( 'NONE', #124756 ) ;
#60412=CARTESIAN_POINT ( 'NONE',  ( -18.59999999999999787, 36.65892442174935439, -249.5511627012433848 ) ) ;
#60441=DIRECTION ( 'NONE',  ( 0.000000000000000000, 0.4721928772777352346, 0.8814952561688428334 ) ) ;
#60470=CYLINDRICAL_SURFACE ( 'NONE', #150052, 4.049999999999997158 ) ;
#60482=CARTESIAN_POINT ( 'NONE',  ( 21.08376601933332495, 10.06723741856825782, -228.1121902998345092 ) ) ;
#60486=DIRECTION ( 'NONE',  ( -0.000000000000000000, -0.8814952561688432775, 0.4721928772777344019 ) ) ;
#60498=DIRECTION ( 'NONE',  ( 0.000000000000000000, -0.8814952561688476074, 0.4721928772777262417 ) ) ;
#60587=DIRECTION ( 'NONE',  ( 0.000000000000000000, -0.9698110461157734008, -0.2438576117980102709 ) ) ;
#60598=CARTESIAN_POINT ( 'NONE',  ( -22.50000000000000000, 12.54152817314149715, -223.4164406214577241 ) ) ;
#60620=EDGE_CURVE ( 'NONE', #41664, #123927, #77583, .T. ) ;
#60644=CIRCLE ( 'NONE', #219056, 0.1000000000000013933 ) ;
#60688=DIRECTION ( 'NONE',  ( 0.000000000000000000, 0.8814952561688439436, -0.4721928772777328476 ) ) ;
#60692=CIRCLE ( 'NONE', #43961, 0.1000000000000013933 ) ;
#60710=CARTESIAN_POINT ( 'NONE',  ( -18.49346865148304886, 9.003597566524152995, -245.4495245630940587 ) ) ;
#60750=( BOUNDED_SURFACE ( )  B_SPLINE_SURFACE ( 3, 2, ( 
 ( #106625, #164071, #166663 ),
 ( #246166, #123660, #147046 ),
 ( #187496, #226582, #127503 ),
 ( #8840, #247443, #109205 ),
 ( #128796, #64948, #208345 ),
 ( #29717, #188751, #144471 ) ),
 .UNSPECIFIED., .F., .F., .F. ) 
 B_SPLINE_SURFACE_WITH_KNOTS ( ( 4, 2, 4 ),
 ( 3, 3 ),
 ( 1.570796326794895448, 2.356194490192343505, 3.141592653589791784 ),
 ( 0.000000000000000000, 1.000000000000000000 ),
 .UNSPECIFIED. ) 
 GEOMETRIC_REPRESENTATION_ITEM ( )  RATIONAL_B_SPLINE_SURFACE ( (
 ( 1.000000000000000000, 0.7071067811865475727, 1.000000000000000000),
 ( 1.000000000000000000, 0.6611148371771847776, 1.000000000000000000),
 ( 1.000000000000000000, 0.6092287576706065799, 1.000000000000000000),
 ( 1.000000000000000000, 0.5278258667047666108, 1.000000000000000000),
 ( 1.000000000000000000, 0.4993418825338903910, 1.000000000000000000),
 ( 1.000000000000000000, 0.5000000000000048850, 1.000000000000000000) ) ) 
 REPRESENTATION_ITEM ( '' )  SURFACE ( )  );
#60789=CIRCLE ( 'NONE', #206558, 0.5000000000000008882 ) ;
#60808=ORIENTED_EDGE ( 'NONE', *, *, #119706, .T. ) ;
#60816=FACE_OUTER_BOUND ( 'NONE', #248941, .T. ) ;
#60845=FACE_OUTER_BOUND ( 'NONE', #175638, .T. ) ;
#60848=DIRECTION ( 'NONE',  ( 0.000000000000000000, -0.8814952561688476074, 0.4721928772777262417 ) ) ;
#60880=ORIENTED_EDGE ( 'NONE', *, *, #94085, .F. ) ;
#60887=EDGE_CURVE ( 'NONE', #167022, #200406, #55055, .T. ) ;
#60894=CARTESIAN_POINT ( 'NONE',  ( -18.59999999999999787, 22.33586458086958615, -231.4986017528744071 ) ) ;
#60897=VERTEX_POINT ( 'NONE', #228702 ) ;
#60899=LINE ( 'NONE', #163869, #131833 ) ;
#60956=CARTESIAN_POINT ( 'NONE',  ( 18.59999999999999076, 38.22825984020919066, -261.1961207961828677 ) ) ;
#61014=DIRECTION ( 'NONE',  ( 0.000000000000000000, -0.4721928772777332917, -0.8814952561688437216 ) ) ;
#61031=ORIENTED_EDGE ( 'NONE', *, *, #37035, .F. ) ;
#61050=ADVANCED_FACE ( 'NONE', ( #233828 ), #111311, .F. ) ;
#61078=TOROIDAL_SURFACE ( 'NONE', #177647, 12.77499999999999858, 0.1000000000000000056 ) ;
#61101=ORIENTED_EDGE ( 'NONE', *, *, #82859, .F. ) ;
#61128=VECTOR ( 'NONE', #36134, 1000.000000000000000 ) ;
#61151=VECTOR ( 'NONE', #16036, 1000.000000000000000 ) ;
#61190=ADVANCED_FACE ( 'NONE', ( #98126 ), #119023, .T. ) ;
#61195=ADVANCED_FACE ( 'NONE', ( #179020 ), #332, .T. ) ;
#61212=DIRECTION ( 'NONE',  ( 1.000000000000000000, 0.000000000000000000, 0.000000000000000000 ) ) ;
#61255=CARTESIAN_POINT ( 'NONE',  ( -23.25000000000000000, 37.95493834378066111, -261.2294694241335264 ) ) ;
#61279=CARTESIAN_POINT ( 'NONE',  ( -18.60000000000000142, 38.22824641643772736, -261.1961226904935529 ) ) ;
#61284=TOROIDAL_SURFACE ( 'NONE', #132010, 7.800000000000000711, 0.1000000000000000056 ) ;
#61293=CARTESIAN_POINT ( 'NONE',  ( 18.45139536634706445, 38.03324368979225056, -261.0487010247114767 ) ) ;
#61295=CARTESIAN_POINT ( 'NONE',  ( -18.51024323315077069, 46.39397692848788779, -243.0687461883537708 ) ) ;
#61331=FACE_OUTER_BOUND ( 'NONE', #223603, .T. ) ;
#61359=ORIENTED_EDGE ( 'NONE', *, *, #158848, .T. ) ;
#61369=EDGE_LOOP ( 'NONE', ( #170454, #149947, #240223, #29059 ) ) ;
#61382=EDGE_CURVE ( 'NONE', #237152, #105632, #197894, .T. ) ;
#61444=ORIENTED_EDGE ( 'NONE', *, *, #229803, .F. ) ;
#61446=AXIS2_PLACEMENT_3D ( 'NONE', #249054, #55939, #15587 ) ;
#61480=ORIENTED_EDGE ( 'NONE', *, *, #47512, .T. ) ;
#61503=AXIS2_PLACEMENT_3D ( 'NONE', #69840, #231475, #191074 ) ;
#61515=FACE_OUTER_BOUND ( 'NONE', #117497, .T. ) ;
#61517=CARTESIAN_POINT ( 'NONE',  ( 20.04142135623730070, 31.49702336731128582, -233.4564499823349877 ) ) ;
#61519=CARTESIAN_POINT ( 'NONE',  ( -20.54999999999999716, 24.17260720300848931, -252.6908294531417027 ) ) ;
#61527=ORIENTED_EDGE ( 'NONE', *, *, #229803, .T. ) ;
#61537=ORIENTED_EDGE ( 'NONE', *, *, #104245, .F. ) ;
#61545=CARTESIAN_POINT ( 'NONE',  ( -18.59999999999999787, 2.272311100394797556, -217.9150152700588876 ) ) ;
#61578=( BOUNDED_SURFACE ( )  B_SPLINE_SURFACE ( 3, 2, ( 
 ( #187384, #249912, #150806 ),
 ( #230334, #152118, #51677 ),
 ( #111680, #93392, #52980 ),
 ( #192505, #13869, #172981 ),
 ( #47832, #8736, #88237 ),
 ( #167836, #68711, #148238 ),
 ( #227771, #128692, #59369 ),
 ( #54261, #58099, #76383 ) ),
 .UNSPECIFIED., .F., .F., .F. ) 
 B_SPLINE_SURFACE_WITH_KNOTS ( ( 4, 2, 2, 4 ),
 ( 3, 3 ),
 ( 0.0001704874539069848162, 0.0003809798300636535939, 0.0004862260181419879963, 0.0005914722062203223987 ),
 ( 0.000000000000000000, 1.000000000000000000 ),
 .UNSPECIFIED. ) 
 GEOMETRIC_REPRESENTATION_ITEM ( )  RATIONAL_B_SPLINE_SURFACE ( (
 ( 1.000000000000000000, 0.7071067811864538699, 1.000000000000000000),
 ( 1.000000000000000000, 0.7670648383549212301, 1.000000000000000000),
 ( 1.000000000000000000, 0.8204820770288628884, 1.000000000000000000),
 ( 1.000000000000000000, 0.8877218296095996664, 1.000000000000000000),
 ( 1.000000000000000000, 0.9080815932668204749, 1.000000000000000000),
 ( 1.000000000000000000, 0.9395541505859124065, 1.000000000000000000),
 ( 1.000000000000000000, 0.9506520335380942432, 1.000000000000000000),
 ( 1.000000000000000000, 0.9504532311154588742, 1.000000000000000000) ) ) 
 REPRESENTATION_ITEM ( '' )  SURFACE ( )  );
#61582=CARTESIAN_POINT ( 'NONE',  ( 21.05000000000000071, 33.13294339707397285, -247.6623911921324463 ) ) ;
#61591=VERTEX_POINT ( 'NONE', #242157 ) ;
#61602=EDGE_CURVE ( 'NONE', #89895, #245302, #230232, .T. ) ;
#61613=AXIS2_PLACEMENT_3D ( 'NONE', #88996, #128153, #227235 ) ;
#61645=VECTOR ( 'NONE', #188442, 1000.000000000000114 ) ;
#61660=CARTESIAN_POINT ( 'NONE',  ( 20.85000000000000142, 28.46617234522943463, -258.4921533293940570 ) ) ;
#61674=CYLINDRICAL_SURFACE ( 'NONE', #40328, 0.09999999999999939493 ) ;
#61676=VECTOR ( 'NONE', #114414, 1000.000000000000000 ) ;
#61692=EDGE_CURVE ( 'NONE', #132235, #41070, #128651, .T. ) ;
#61767=ORIENTED_EDGE ( 'NONE', *, *, #249816, .T. ) ;
#61772=EDGE_CURVE ( 'NONE', #116921, #83686, #113893, .T. ) ;
#61786=CARTESIAN_POINT ( 'NONE',  ( 21.07971444708685738, 10.04030013319147585, -228.1115500188630278 ) ) ;
#61795=ORIENTED_EDGE ( 'NONE', *, *, #144813, .T. ) ;
#61815=DIRECTION ( 'NONE',  ( -1.000000000000000000, 0.000000000000000000, 0.000000000000000000 ) ) ;
#61824=CIRCLE ( 'NONE', #215909, 0.5999999999999969802 ) ;
#61828=DIRECTION ( 'NONE',  ( 1.000000000000000000, 0.000000000000000000, 0.000000000000000000 ) ) ;
#61830=ORIENTED_EDGE ( 'NONE', *, *, #198988, .T. ) ;
#61841=DIRECTION ( 'NONE',  ( 0.000000000000000000, 0.8814952561688444987, -0.4721928772777320149 ) ) ;
#61892=ORIENTED_EDGE ( 'NONE', *, *, #193302, .T. ) ;
#61900=DIRECTION ( 'NONE',  ( -1.000000000000000000, -0.000000000000000000, -0.000000000000000000 ) ) ;
#61901=ORIENTED_EDGE ( 'NONE', *, *, #127434, .F. ) ;
#61981=SHAPE_REPRESENTATION ( 'Injection Molded Chain Links 8', ( #2425 ), #110949 ) ;
#61992=ORIENTED_EDGE ( 'NONE', *, *, #81559, .F. ) ;
#61999=CIRCLE ( 'NONE', #236969, 11.74999999999999112 ) ;
#62005=EDGE_CURVE ( 'NONE', #60897, #82258, #76461, .T. ) ;
#62029=ORIENTED_EDGE ( 'NONE', *, *, #193302, .F. ) ;
#62032=CARTESIAN_POINT ( 'NONE',  ( -20.00857864376270001, 22.38308386859736032, -231.4104522272575082 ) ) ;
#62046=ADVANCED_FACE ( 'NONE', ( #46219 ), #189608, .F. ) ;
#62047=CYLINDRICAL_SURFACE ( 'NONE', #10025, 0.1000000000000013933 ) ;
#62060=CARTESIAN_POINT ( 'NONE',  ( 22.40000000000010161, -3.229117512540232049, -228.1842305956910195 ) ) ;
#62116=ORIENTED_EDGE ( 'NONE', *, *, #201323, .T. ) ;
#62120=EDGE_CURVE ( 'NONE', #93493, #183016, #50078, .T. ) ;
#62168=ADVANCED_FACE ( 'NONE', ( #230002 ), #130900, .F. ) ;
#62205=CARTESIAN_POINT ( 'NONE',  ( -21.05000000000045546, 10.18563131712793357, -228.0635015899710254 ) ) ;
#62208=CARTESIAN_POINT ( 'NONE',  ( 20.95262331984796234, 18.75370877634653155, -228.0435341303648897 ) ) ;
#62265=CARTESIAN_POINT ( 'NONE',  ( -18.50000000000000000, 12.76524917372336532, -223.4223513401831553 ) ) ;
#62356=CARTESIAN_POINT ( 'NONE',  ( 20.93302460841142931, 46.41023286455059349, -243.0722154975327385 ) ) ;
#62371=VERTEX_POINT ( 'NONE', #180306 ) ;
#62405=LINE ( 'NONE', #79375, #92928 ) ;
#62415=FACE_OUTER_BOUND ( 'NONE', #220157, .T. ) ;
#62489=AXIS2_PLACEMENT_3D ( 'NONE', #14518, #37928, #207905 ) ;
#62490=EDGE_CURVE ( 'NONE', #126467, #124845, #63616, .T. ) ;
#62519=CARTESIAN_POINT ( 'NONE',  ( 22.60000000000000142, -3.180729737797944434, -228.0957332317254895 ) ) ;
#62532=CYLINDRICAL_SURFACE ( 'NONE', #229746, 12.87500000000000355 ) ;
#62548=AXIS2_PLACEMENT_3D ( 'NONE', #185611, #23991, #120529 ) ;
#62565=DIRECTION ( 'NONE',  ( -0.7071067811865795472, 0.3338907855511005218, 0.6233112732207110041 ) ) ;
#62572=ORIENTED_EDGE ( 'NONE', *, *, #123221, .T. ) ;
#62578=EDGE_CURVE ( 'NONE', #93118, #220499, #111036, .T. ) ;
#62589=VERTEX_POINT ( 'NONE', #109735 ) ;
#62594=CARTESIAN_POINT ( 'NONE',  ( -18.59999999999999787, 18.81339837015603322, -226.7756228984618190 ) ) ;
#62604=LINE ( 'NONE', #24787, #53412 ) ;
#62620=CARTESIAN_POINT ( 'NONE',  ( -21.14999999999999858, 7.128833340093095217, -233.7327013124392749 ) ) ;
#62654=EDGE_CURVE ( 'NONE', #218397, #227951, #139170, .T. ) ;
#62655=VERTEX_POINT ( 'NONE', #32829 ) ;
#62687=ORIENTED_EDGE ( 'NONE', *, *, #239385, .F. ) ;
#62689=AXIS2_PLACEMENT_3D ( 'NONE', #172647, #89192, #27981 ) ;
#62713=DIRECTION ( 'NONE',  ( -1.000000000000000000, 0.000000000000000000, 0.000000000000000000 ) ) ;
#62739=EDGE_LOOP ( 'NONE', ( #237463, #51398, #199847, #237970 ) ) ;
#62746=ORIENTED_EDGE ( 'NONE', *, *, #32541, .F. ) ;
#62840=CARTESIAN_POINT ( 'NONE',  ( 23.24999999999999645, 7.128833340093095217, -233.7327013124392749 ) ) ;
#62901=CARTESIAN_POINT ( 'NONE',  ( -23.15000000000000213, 30.38404434817536526, -239.4399867032565794 ) ) ;
#62905=DIRECTION ( 'NONE',  ( 0.000000000000000000, 0.8814952561688438326, -0.4721928772777331251 ) ) ;
#62906=AXIS2_PLACEMENT_3D ( 'NONE', #86188, #119257, #243996 ) ;
#62910=DIRECTION ( 'NONE',  ( 0.000000000000000000, 0.8814952561688359500, -0.4721928772777482242 ) ) ;
#62927=ORIENTED_EDGE ( 'NONE', *, *, #185527, .F. ) ;
#62955=CARTESIAN_POINT ( 'NONE',  ( 20.94999999999999929, 30.00470580581253799, -236.0305482155950472 ) ) ;
#62976=DIRECTION ( 'NONE',  ( 1.000000000000000000, 0.000000000000000000, 0.000000000000000000 ) ) ;
#62979=ORIENTED_EDGE ( 'NONE', *, *, #7199, .F. ) ;
#62992=VERTEX_POINT ( 'NONE', #238038 ) ;
#62998=ORIENTED_EDGE ( 'NONE', *, *, #24520, .T. ) ;
#63022=VECTOR ( 'NONE', #232193, 1000.000000000000000 ) ;
#63024=DIRECTION ( 'NONE',  ( 1.000000000000000000, 0.000000000000000000, 0.000000000000000000 ) ) ;
#63026=TOROIDAL_SURFACE ( 'NONE', #208798, 6.258578643762712446, 0.1000000000000000056 ) ;
#63043=DIRECTION ( 'NONE',  ( 1.000000000000000000, 0.000000000000000000, 0.000000000000000000 ) ) ;
#63053=CIRCLE ( 'NONE', #87979, 0.09999999999999986677 ) ;
#63057=AXIS2_PLACEMENT_3D ( 'NONE', #77987, #16765, #55836 ) ;
#63113=CIRCLE ( 'NONE', #146321, 0.1000000000000013933 ) ;
#63137=ORIENTED_EDGE ( 'NONE', *, *, #12986, .T. ) ;
#63152=CYLINDRICAL_SURFACE ( 'NONE', #161955, 0.1000000000000075273 ) ;
#63164=DIRECTION ( 'NONE',  ( 0.000000000000000000, 0.8814952561688430555, -0.4721928772777346239 ) ) ;
#63184=CARTESIAN_POINT ( 'NONE',  ( 23.15000000000000213, 28.42524210734032408, -258.3567845160494585 ) ) ;
#63208=VERTEX_POINT ( 'NONE', #162380 ) ;
#63253=AXIS2_PLACEMENT_3D ( 'NONE', #146568, #48768, #224830 ) ;
#63291=DIRECTION ( 'NONE',  ( 0.000000000000000000, -0.4721928772777346239, -0.8814952561688430555 ) ) ;
#63298=DIRECTION ( 'NONE',  ( 0.7071067811865473507, 0.3338907855510733769, 0.6233112732207618523 ) ) ;
#63323=VERTEX_POINT ( 'NONE', #228770 ) ;
#63327=VERTEX_POINT ( 'NONE', #146626 ) ;
#63348=EDGE_CURVE ( 'NONE', #31642, #221637, #226145, .T. ) ;
#63378=CARTESIAN_POINT ( 'NONE',  ( -23.25000000000000000, 23.38726701055792745, -229.1122755113798632 ) ) ;
#63389=CARTESIAN_POINT ( 'NONE',  ( 18.59999999999999076, 2.272311100394801109, -217.9150152700588592 ) ) ;
#63396=AXIS2_PLACEMENT_3D ( 'NONE', #11483, #195267, #16620 ) ;
#63456=DIRECTION ( 'NONE',  ( 0.000000000000000000, 0.5868805631290353597, 0.8096735173027127530 ) ) ;
#63469=CARTESIAN_POINT ( 'NONE',  ( -21.05000000000000071, 10.05599437547273389, -228.2004445046334240 ) ) ;
#63512=AXIS2_PLACEMENT_3D ( 'NONE', #129723, #71058, #150580 ) ;
#63515=FACE_OUTER_BOUND ( 'NONE', #175852, .T. ) ;
#63546=CARTESIAN_POINT ( 'NONE',  ( 21.05000000000000071, 18.47808476326694915, -239.8121846073901224 ) ) ;
#63564=DIRECTION ( 'NONE',  ( 1.000000000000000000, 0.000000000000000000, 0.000000000000000000 ) ) ;
#63565=ORIENTED_EDGE ( 'NONE', *, *, #34677, .F. ) ;
#63597=CARTESIAN_POINT ( 'NONE',  ( 20.94560253601876809, 36.04561250502854364, -235.8930046631029711 ) ) ;
#63609=CARTESIAN_POINT ( 'NONE',  ( 20.94999999999999929, 7.128833340093095217, -233.7327013124392749 ) ) ;
#63610=CARTESIAN_POINT ( 'NONE',  ( 20.94999999999999929, 43.18640298906419162, -245.2812653309023574 ) ) ;
#63616=CIRCLE ( 'NONE', #230212, 0.1000000000000013933 ) ;
#63633=AXIS2_PLACEMENT_3D ( 'NONE', #102622, #3542, #83048 ) ;
#63645=ORIENTED_EDGE ( 'NONE', *, *, #19678, .T. ) ;
#63664=ORIENTED_EDGE ( 'NONE', *, *, #252410, .F. ) ;
#63672=AXIS2_PLACEMENT_3D ( 'NONE', #8335, #89134, #171299 ) ;
#63716=VECTOR ( 'NONE', #65593, 1000.000000000000000 ) ;
#63758=DIRECTION ( 'NONE',  ( 0.000000000000000000, 0.8814952561688476074, -0.4721928772777262417 ) ) ;
#63771=CARTESIAN_POINT ( 'NONE',  ( -18.59999999999999787, 45.93315328338058379, -256.6017782078560003 ) ) ;
#63775=VERTEX_POINT ( 'NONE', #51058 ) ;
#63805=CYLINDRICAL_SURFACE ( 'NONE', #43902, 0.09999999999999939493 ) ;
#63814=DIRECTION ( 'NONE',  ( 0.000000000000000000, 0.8814952561688438326, -0.4721928772777331806 ) ) ;
#63816=CARTESIAN_POINT ( 'NONE',  ( 20.94999999999999929, 28.34113089492129589, -239.5930034413672161 ) ) ;
#63861=CARTESIAN_POINT ( 'NONE',  ( -18.57399277249657032, 46.46487552657983144, -243.0839400145317484 ) ) ;
#63869=AXIS2_PLACEMENT_3D ( 'NONE', #223192, #81110, #141115 ) ;
#63975=ORIENTED_EDGE ( 'NONE', *, *, #237801, .T. ) ;
#64002=DIRECTION ( 'NONE',  ( -3.265361837132814079E-16, 0.4721928772777338468, 0.8814952561688436106 ) ) ;
#64014=CIRCLE ( 'NONE', #209761, 0.1000000000000059591 ) ;
#64051=DIRECTION ( 'NONE',  ( -1.000000000000000000, -0.000000000000000000, -0.000000000000000000 ) ) ;
#64052=DIRECTION ( 'NONE',  ( 0.000000000000000000, -0.8814952561688398358, 0.4721928772777406746 ) ) ;
#64064=CIRCLE ( 'NONE', #151585, 0.09999999999999834022 ) ;
#64069=AXIS2_PLACEMENT_3D ( 'NONE', #63609, #84404, #240972 ) ;
#64081=AXIS2_PLACEMENT_3D ( 'NONE', #99896, #180763, #176932 ) ;
#64089=AXIS2_PLACEMENT_3D ( 'NONE', #227435, #48801, #128356 ) ;
#64111=DIRECTION ( 'NONE',  ( 0.000000000000000000, 0.8814952561688428334, -0.4721928772777350125 ) ) ;
#64112=CARTESIAN_POINT ( 'NONE',  ( -22.59080734064477980, 12.64999392629038155, -223.3606122593135979 ) ) ;
#64124=DIRECTION ( 'NONE',  ( -1.000000000000000000, -0.000000000000000000, -0.000000000000000000 ) ) ;
#64125=DIRECTION ( 'NONE',  ( 0.000000000000000000, 0.8814952561688430555, -0.4721928772777344019 ) ) ;
#64137=ORIENTED_EDGE ( 'NONE', *, *, #196605, .T. ) ;
#64224=ADVANCED_FACE ( 'NONE', ( #249991 ), #166637, .T. ) ;
#64234=ORIENTED_EDGE ( 'NONE', *, *, #178070, .F. ) ;
#64244=ORIENTED_EDGE ( 'NONE', *, *, #99341, .T. ) ;
#64273=ORIENTED_EDGE ( 'NONE', *, *, #126816, .T. ) ;
#64293=EDGE_CURVE ( 'NONE', #109178, #205457, #235056, .T. ) ;
#64311=CARTESIAN_POINT ( 'NONE',  ( 20.04142135623730070, 34.40595771266846725, -235.0146864773515176 ) ) ;
#64358=ADVANCED_FACE ( 'NONE', ( #218533 ), #135152, .T. ) ;
#64361=CARTESIAN_POINT ( 'NONE',  ( 21.14999999999999858, 12.76524917372336887, -223.4223513401831269 ) ) ;
#64386=CARTESIAN_POINT ( 'NONE',  ( -21.44999999999999929, 29.24307565605548120, -237.2405905340223455 ) ) ;
#64395=EDGE_CURVE ( 'NONE', #116921, #7289, #156049, .T. ) ;
#64452=DIRECTION ( 'NONE',  ( 1.000000000000000000, 3.403959061552269104E-14, 2.112458025737858499E-14 ) ) ;
#64509=CYLINDRICAL_SURFACE ( 'NONE', #56095, 0.09999999999999939493 ) ;
#64524=DIRECTION ( 'NONE',  ( 0.000000000000000000, 0.8814952561688476074, -0.4721928772777262417 ) ) ;
#64541=VERTEX_POINT ( 'NONE', #41238 ) ;
#64581=CARTESIAN_POINT ( 'NONE',  ( -20.54999999999999716, 11.46684968301824448, -245.9610388612851750 ) ) ;
#64626=DIRECTION ( 'NONE',  ( -0.000000000000000000, 0.8814952561688430555, -0.4721928772777346239 ) ) ;
#64654=( BOUNDED_CURVE ( )  B_SPLINE_CURVE ( 3, ( #117129, #36323, #196647, #140517 ),
 .UNSPECIFIED., .F., .F. ) 
 B_SPLINE_CURVE_WITH_KNOTS ( ( 4, 4 ),
 ( 4.790818349670541706E-14, 1.570796326794909881 ),
 .UNSPECIFIED. ) 
 CURVE ( )  GEOMETRIC_REPRESENTATION_ITEM ( )  RATIONAL_B_SPLINE_CURVE ( ( 1.000000000000000000, 0.8047378541243732641, 0.8047378541243732641, 1.000000000000000000 ) ) 
 REPRESENTATION_ITEM ( '' )  );
#64668=LINE ( 'NONE', #4674, #69568 ) ;
#64670=ORIENTED_EDGE ( 'NONE', *, *, #212169, .F. ) ;
#64731=DIRECTION ( 'NONE',  ( -1.000000000000000000, -0.000000000000000000, -0.000000000000000000 ) ) ;
#64734=AXIS2_PLACEMENT_3D ( 'NONE', #24256, #8526, #161186 ) ;
#64778=ADVANCED_FACE ( 'NONE', ( #186527 ), #105667, .F. ) ;
#64793=VECTOR ( 'NONE', #94285, 1000.000000000000000 ) ;
#64819=VECTOR ( 'NONE', #191806, 1000.000000000000000 ) ;
#64841=CARTESIAN_POINT ( 'NONE',  ( -20.64999999999999858, 26.13474583767463244, -241.1910018098189141 ) ) ;
#64849=CARTESIAN_POINT ( 'NONE',  ( -18.59999999999999787, 18.37021030142088662, -237.6367305148568221 ) ) ;
#64856=DIRECTION ( 'NONE',  ( 0.000000000000000000, -0.4721928772777346239, -0.8814952561688430555 ) ) ;
#64901=CARTESIAN_POINT ( 'NONE',  ( -18.59999999999999787, 30.18746141061095045, -235.4776000216846796 ) ) ;
#64918=ORIENTED_EDGE ( 'NONE', *, *, #199548, .T. ) ;
#64942=CARTESIAN_POINT ( 'NONE',  ( -20.94999999999999929, 36.18002604163306302, -236.0784499204090991 ) ) ;
#64948=CARTESIAN_POINT ( 'NONE',  ( -20.94684162748235678, 18.70797638544537733, -226.6057076234665999 ) ) ;
#64953=CARTESIAN_POINT ( 'NONE',  ( -18.50000000000000000, 43.17747518314619271, -245.0773422074893233 ) ) ;
#64955=CIRCLE ( 'NONE', #210710, 0.1000000000000013933 ) ;
#64959=ORIENTED_EDGE ( 'NONE', *, *, #124439, .F. ) ;
#64979=EDGE_LOOP ( 'NONE', ( #29888, #106297, #18206, #126290 ) ) ;
#64982=ORIENTED_EDGE ( 'NONE', *, *, #69333, .F. ) ;
#65013=LINE ( 'NONE', #5016, #73857 ) ;
#65020=DIRECTION ( 'NONE',  ( 0.000000000000000000, -0.8814952561688430555, 0.4721928772777346239 ) ) ;
#65024=AXIS2_PLACEMENT_3D ( 'NONE', #47909, #40586, #147004 ) ;
#65025=CARTESIAN_POINT ( 'NONE',  ( 21.05000000000000071, 28.42524210734032408, -258.3567845160494585 ) ) ;
#65056=FACE_OUTER_BOUND ( 'NONE', #27833, .T. ) ;
#65077=DIRECTION ( 'NONE',  ( -3.265361837132812600E-16, 0.4721928772777346239, 0.8814952561688430555 ) ) ;
#65094=CARTESIAN_POINT ( 'NONE',  ( -23.15000000000000213, 36.65892442174935439, -249.5511627012433848 ) ) ;
#65127=DIRECTION ( 'NONE',  ( 0.000000000000000000, 0.8814952561688444987, -0.4721928772777320149 ) ) ;
#65195=CARTESIAN_POINT ( 'NONE',  ( 21.05000000000000071, 18.81166555858609257, -229.8642012822692777 ) ) ;
#65200=ADVANCED_FACE ( 'NONE', ( #141938 ), #24591, .T. ) ;
#65210=ORIENTED_EDGE ( 'NONE', *, *, #250072, .T. ) ;
#65228=ORIENTED_EDGE ( 'NONE', *, *, #216873, .F. ) ;
#65258=DIRECTION ( 'NONE',  ( -0.000000000000000000, -0.8814952561688430555, 0.4721928772777346239 ) ) ;
#65262=ORIENTED_EDGE ( 'NONE', *, *, #726, .T. ) ;
#65288=DIRECTION ( 'NONE',  ( 1.000000000000000000, 0.000000000000000000, 0.000000000000000000 ) ) ;
#65315=CARTESIAN_POINT ( 'NONE',  ( 20.04142135623730070, 31.44980407958351165, -233.5445995079518866 ) ) ;
#65352=DIRECTION ( 'NONE',  ( 0.000000000000000000, 0.8814952561688438326, -0.4721928772777330696 ) ) ;
#65354=FACE_OUTER_BOUND ( 'NONE', #19290, .T. ) ;
#65374=AXIS2_PLACEMENT_3D ( 'NONE', #31693, #192040, #186903 ) ;
#65380=EDGE_CURVE ( 'NONE', #103462, #89253, #60789, .T. ) ;
#65384=CARTESIAN_POINT ( 'NONE',  ( 23.14999999999999858, 20.42498087366621817, -235.1829032864613396 ) ) ;
#65435=VECTOR ( 'NONE', #147864, 1000.000000000000000 ) ;
#65478=DIRECTION ( 'NONE',  ( -3.469446951953352918E-14, -0.4721928772776973204, -0.8814952561688629284 ) ) ;
#65479=ORIENTED_EDGE ( 'NONE', *, *, #68190, .T. ) ;
#65519=ORIENTED_EDGE ( 'NONE', *, *, #159720, .T. ) ;
#65532=DIRECTION ( 'NONE',  ( -1.000000000000000000, -0.000000000000000000, -0.000000000000000000 ) ) ;
#65581=FACE_OUTER_BOUND ( 'NONE', #193061, .T. ) ;
#65593=DIRECTION ( 'NONE',  ( 0.000000000000000000, -0.8814952561688430555, 0.4721928772777346239 ) ) ;
#65599=DIRECTION ( 'NONE',  ( -0.000000000000000000, 0.4721928772777346239, 0.8814952561688430555 ) ) ;
#65641=VERTEX_POINT ( 'NONE', #167640 ) ;
#65654=CARTESIAN_POINT ( 'NONE',  ( -21.08078803292166725, 1.583703513802046547, -230.6724956268899689 ) ) ;
#65655=FACE_OUTER_BOUND ( 'NONE', #25382, .T. ) ;
#65682=ADVANCED_FACE ( 'NONE', ( #110198 ), #168948, .F. ) ;
#65686=DIRECTION ( 'NONE',  ( 0.000000000000000000, 0.4721928772776973204, 0.8814952561688629284 ) ) ;
#65696=ORIENTED_EDGE ( 'NONE', *, *, #28071, .F. ) ;
#65726=DIRECTION ( 'NONE',  ( -1.000000000000000000, 0.000000000000000000, 0.000000000000000000 ) ) ;
#65747=CARTESIAN_POINT ( 'NONE',  ( -2.995603634470829482E-16, 23.39757462225858475, -255.7770442850471113 ) ) ;
#65755=CIRCLE ( 'NONE', #211505, 0.1000000000000022815 ) ;
#65814=LINE ( 'NONE', #245746, #130603 ) ;
#65836=CARTESIAN_POINT ( 'NONE',  ( -20.94999999999999929, 18.81339837015603322, -226.7756228984618190 ) ) ;
#65854=VECTOR ( 'NONE', #248855, 1000.000000000000000 ) ;
#65872=DIRECTION ( 'NONE',  ( 1.000000000000000000, 1.394253735153569469E-16, 2.602809386958778209E-16 ) ) ;
#65908=AXIS2_PLACEMENT_3D ( 'NONE', #43762, #180716, #104974 ) ;
#65936=CYLINDRICAL_SURFACE ( 'NONE', #140045, 0.1000000000000013933 ) ;
#65939=CARTESIAN_POINT ( 'NONE',  ( 21.05000000000000071, 10.30543449102040654, -228.0143625250146329 ) ) ;
#65946=ORIENTED_EDGE ( 'NONE', *, *, #135594, .T. ) ;
#65948=AXIS2_PLACEMENT_3D ( 'NONE', #114988, #56283, #164 ) ;
#65949=VERTEX_POINT ( 'NONE', #205132 ) ;
#65977=DIRECTION ( 'NONE',  ( 1.000000000000000000, 1.394253735153569469E-16, 2.602809386958778209E-16 ) ) ;
#65986=ORIENTED_EDGE ( 'NONE', *, *, #48349, .F. ) ;
#65999=TOROIDAL_SURFACE ( 'NONE', #211755, 2.100000000000002309, 0.1000000000000000056 ) ;
#66021=CIRCLE ( 'NONE', #228349, 11.75000000000000000 ) ;
#66030=DIRECTION ( 'NONE',  ( -0.000000000000000000, 0.8814952561688430555, -0.4721928772777346239 ) ) ;
#66044=CARTESIAN_POINT ( 'NONE',  ( 21.05000000000000071, 28.08470566095357057, -239.2860081655328770 ) ) ;
#66053=CIRCLE ( 'NONE', #111871, 11.75000000000000178 ) ;
#66083=CARTESIAN_POINT ( 'NONE',  ( -18.50000000000000000, 23.42819724844703444, -229.2476443247244902 ) ) ;
#66106=CIRCLE ( 'NONE', #211869, 0.9750000000000036415 ) ;
#66115=AXIS2_PLACEMENT_3D ( 'NONE', #49754, #249251, #230985 ) ;
#66118=EDGE_LOOP ( 'NONE', ( #56921, #27658, #180810, #133286 ) ) ;
#66119=DIRECTION ( 'NONE',  ( 1.000000000000000000, 0.000000000000000000, 0.000000000000000000 ) ) ;
#66136=EDGE_CURVE ( 'NONE', #154949, #40168, #197137, .T. ) ;
#66144=CARTESIAN_POINT ( 'NONE',  ( 18.57399277249656322, 46.46487552657982434, -243.0839400145317200 ) ) ;
#66155=LINE ( 'NONE', #124853, #60176 ) ;
#66171=CARTESIAN_POINT ( 'NONE',  ( 21.05315837413339253, 36.17631400070159486, -235.9630178772347051 ) ) ;
#66173=ORIENTED_EDGE ( 'NONE', *, *, #176052, .F. ) ;
#66189=( BOUNDED_SURFACE ( )  B_SPLINE_SURFACE ( 3, 2, ( 
 ( #37027, #216908, #34468 ),
 ( #117816, #232655, #116545 ),
 ( #136071, #115252, #113960 ),
 ( #175268, #197348, #253465 ),
 ( #194819, #215624, #196081 ),
 ( #173995, #119116, #38293 ),
 ( #14891, #98214, #158276 ),
 ( #53992, #16179, #17433 ),
 ( #198638, #76121, #177825 ),
 ( #154422, #254714, #59090 ) ),
 .UNSPECIFIED., .F., .F., .F. ) 
 B_SPLINE_SURFACE_WITH_KNOTS ( ( 4, 2, 2, 2, 4 ),
 ( 3, 3 ),
 ( 0.0001836757140119120197, 0.0004000170051583426273, 0.0005081876507315579447, 0.0005622729735181655492, 0.0006163582963047732621 ),
 ( 0.000000000000000000, 1.000000000000000000 ),
 .UNSPECIFIED. ) 
 GEOMETRIC_REPRESENTATION_ITEM ( )  RATIONAL_B_SPLINE_SURFACE ( (
 ( 1.000000000000000000, 0.7071067811865543451, 1.000000000000000000),
 ( 1.000000000000000000, 0.6461995200018084695, 1.000000000000000000),
 ( 1.000000000000000000, 0.5776453529564903322, 1.000000000000000000),
 ( 1.000000000000000000, 0.4585233068343699259, 1.000000000000000000),
 ( 1.000000000000000000, 0.4154092989948574566, 1.000000000000000000),
 ( 1.000000000000000000, 0.3550093145831485497, 1.000000000000000000),
 ( 1.000000000000000000, 0.3354498651685384747, 1.000000000000000000),
 ( 1.000000000000000000, 0.3060347992258684036, 1.000000000000000000),
 ( 1.000000000000000000, 0.2963555829624233140, 1.000000000000000000),
 ( 1.000000000000000000, 0.2966190024561738969, 1.000000000000000000) ) ) 
 REPRESENTATION_ITEM ( '' )  SURFACE ( )  );
#66215=ADVANCED_FACE ( 'NONE', ( #233723 ), #236141, .T. ) ;
#66253=DIRECTION ( 'NONE',  ( 0.000000000000000000, -0.8814952561688476074, 0.4721928772777262417 ) ) ;
#66283=CARTESIAN_POINT ( 'NONE',  ( -21.05000000000000071, 28.56975825374500388, -258.1421690862028413 ) ) ;
#66290=LINE ( 'NONE', #166701, #10541 ) ;
#66293=ORIENTED_EDGE ( 'NONE', *, *, #198602, .T. ) ;
#66320=DIRECTION ( 'NONE',  ( 0.000000000000000000, 0.8814952561688438326, -0.4721928772777331806 ) ) ;
#66330=EDGE_CURVE ( 'NONE', #253481, #240913, #65013, .T. ) ;
#66339=CARTESIAN_POINT ( 'NONE',  ( -23.25000000000000000, 45.93315328338058379, -256.6017782078560003 ) ) ;
#66356=TOROIDAL_SURFACE ( 'NONE', #216374, 0.2000000000000000111, 0.1000000000000000056 ) ;
#66358=ORIENTED_EDGE ( 'NONE', *, *, #177723, .F. ) ;
#66378=ORIENTED_EDGE ( 'NONE', *, *, #191032, .F. ) ;
#66387=CARTESIAN_POINT ( 'NONE',  ( 18.59999999999999787, 16.44800918141279311, -240.8068063186265135 ) ) ;
#66412=CARTESIAN_POINT ( 'NONE',  ( 20.94999999999999929, 18.18127959618848877, -237.5711165786817389 ) ) ;
#66443=EDGE_CURVE ( 'NONE', #248870, #236989, #12773, .T. ) ;
#66501=EDGE_LOOP ( 'NONE', ( #161874, #55976, #226584, #44268 ) ) ;
#66584=AXIS2_PLACEMENT_3D ( 'NONE', #50576, #15346, #70193 ) ;
#66587=TOROIDAL_SURFACE ( 'NONE', #62489, 11.70000000000000639, 0.1000000000000000056 ) ;
#66610=ORIENTED_EDGE ( 'NONE', *, *, #208627, .T. ) ;
#66627=CIRCLE ( 'NONE', #199904, 0.1000000000000075273 ) ;
#66635=ADVANCED_FACE ( 'NONE', ( #235635 ), #111428, .T. ) ;
#66638=EDGE_CURVE ( 'NONE', #218497, #74755, #32358, .T. ) ;
#66661=DIRECTION ( 'NONE',  ( 1.000000000000000000, 0.000000000000000000, 0.000000000000000000 ) ) ;
#66668=DIRECTION ( 'NONE',  ( 0.000000000000000000, 0.8814952561688429444, -0.4721928772777348460 ) ) ;
#66693=ADVANCED_FACE ( 'NONE', ( #60845 ), #140381, .T. ) ;
#66710=CIRCLE ( 'NONE', #12550, 0.09999999999999939493 ) ;
#66749=AXIS2_PLACEMENT_3D ( 'NONE', #58256, #137790, #218607 ) ;
#66779=CARTESIAN_POINT ( 'NONE',  ( 21.05000000000000071, 35.97645343225767789, -235.9694016464868014 ) ) ;
#66791=CARTESIAN_POINT ( 'NONE',  ( 19.83283456528359423, 34.58225676339163357, -235.1091250525335568 ) ) ;
#66795=DIRECTION ( 'NONE',  ( -1.000000000000000000, 0.000000000000000000, 0.000000000000000000 ) ) ;
#66824=CIRCLE ( 'NONE', #112615, 12.87499999999999289 ) ;
#66833=CARTESIAN_POINT ( 'NONE',  ( 21.00000000000000000, 22.61918030723622408, -230.9697045991730988 ) ) ;
#66862=AXIS2_PLACEMENT_3D ( 'NONE', #195238, #96087, #191390 ) ;
#66869=FACE_OUTER_BOUND ( 'NONE', #122940, .T. ) ;
#66891=ORIENTED_EDGE ( 'NONE', *, *, #226178, .T. ) ;
#66927=SPHERICAL_SURFACE ( 'NONE', #177831, 0.1000000000000000056 ) ;
#66951=LINE ( 'NONE', #179545, #248063 ) ;
#66954=DIRECTION ( 'NONE',  ( -0.000000000000000000, 0.4721928772777345684, 0.8814952561688429444 ) ) ;
#66985=DIRECTION ( 'NONE',  ( 1.000000000000000000, 1.541880601228652350E-16, 2.878400969107352921E-16 ) ) ;
#67020=EDGE_CURVE ( 'NONE', #186223, #74336, #219740, .T. ) ;
#67042=VECTOR ( 'NONE', #171726, 999.9999999999998863 ) ;
#67052=VECTOR ( 'NONE', #139930, 1000.000000000000000 ) ;
#67063=EDGE_CURVE ( 'NONE', #12413, #153891, #24332, .T. ) ;
#67078=CARTESIAN_POINT ( 'NONE',  ( -20.94999999999999929, 43.35377423437995503, -245.1717807829448930 ) ) ;
#67115=ORIENTED_EDGE ( 'NONE', *, *, #177442, .F. ) ;
#67118=ORIENTED_EDGE ( 'NONE', *, *, #246282, .F. ) ;
#67125=AXIS2_PLACEMENT_3D ( 'NONE', #185031, #6392, #246298 ) ;
#67127=DIRECTION ( 'NONE',  ( 0.000000000000000000, 0.8814952561688476074, -0.4721928772777262417 ) ) ;
#67129=DIRECTION ( 'NONE',  ( 1.000000000000000000, 0.000000000000000000, 0.000000000000000000 ) ) ;
#67167=DIRECTION ( 'NONE',  ( 4.239556034732056127E-17, 0.8127272543710951647, -0.5826443254700257590 ) ) ;
#67190=ORIENTED_EDGE ( 'NONE', *, *, #90833, .T. ) ;
#67199=ORIENTED_EDGE ( 'NONE', *, *, #66443, .T. ) ;
#67256=DIRECTION ( 'NONE',  ( 0.000000000000000000, 0.8814952561688430555, -0.4721928772777346239 ) ) ;
#67345=ADVANCED_FACE ( 'NONE', ( #40720 ), #21146, .F. ) ;
#67371=VERTEX_POINT ( 'NONE', #163206 ) ;
#67373=LINE ( 'NONE', #29560, #120927 ) ;
#67380=DIRECTION ( 'NONE',  ( 0.000000000000000000, -0.8454177738465953329, -0.5341055959866617409 ) ) ;
#67397=CARTESIAN_POINT ( 'NONE',  ( 18.59999999999999432, 14.81796439977981272, -236.5325475414793743 ) ) ;
#67400=VERTEX_POINT ( 'NONE', #4113 ) ;
#67406=VECTOR ( 'NONE', #155219, 1000.000000000000114 ) ;
#67437=DIRECTION ( 'NONE',  ( 0.000000000000000000, -0.8814952561688388366, 0.4721928772777422845 ) ) ;
#67439=CARTESIAN_POINT ( 'NONE',  ( -22.50000000000000000, 1.619487989037824871, -230.7814958294534335 ) ) ;
#67442=SPHERICAL_SURFACE ( 'NONE', #96985, 0.1000000000000000056 ) ;
#67445=LINE ( 'NONE', #146970, #9595 ) ;
#67480=CYLINDRICAL_SURFACE ( 'NONE', #65024, 0.09999999999999939493 ) ;
#67520=TOROIDAL_SURFACE ( 'NONE', #13551, 11.65000000000000036, 0.1000000000000000056 ) ;
#67522=CARTESIAN_POINT ( 'NONE',  ( 21.05000000000000071, 11.60058429089262333, -246.3380203656811887 ) ) ;
#67550=VECTOR ( 'NONE', #130159, 1000.000000000000000 ) ;
#67552=AXIS2_PLACEMENT_3D ( 'NONE', #236917, #79106, #139064 ) ;
#67561=DIRECTION ( 'NONE',  ( -1.000000000000000000, -1.394253735153569469E-16, -2.602809386958778209E-16 ) ) ;
#67562=DIRECTION ( 'NONE',  ( -4.408576920032447355E-17, 0.9371753822965316338, -0.3488585713686134793 ) ) ;
#67576=CARTESIAN_POINT ( 'NONE',  ( -20.94999999999999929, 4.313202326203128933, -245.5540684919841681 ) ) ;
#67586=EDGE_CURVE ( 'NONE', #144717, #168277, #243091, .T. ) ;
#67590=ORIENTED_EDGE ( 'NONE', *, *, #10721, .T. ) ;
#67598=DIRECTION ( 'NONE',  ( 0.000000000000000000, -0.4721928772776973204, -0.8814952561688629284 ) ) ;
#67641=CARTESIAN_POINT ( 'NONE',  ( -23.15000000000000213, 36.17635217701699446, -235.9630383263116471 ) ) ;
#67652=DIRECTION ( 'NONE',  ( 1.000000000000000000, 0.000000000000000000, 0.000000000000000000 ) ) ;
#67655=ORIENTED_EDGE ( 'NONE', *, *, #52105, .F. ) ;
#67657=EDGE_CURVE ( 'NONE', #41196, #74683, #29233, .T. ) ;
#67671=ADVANCED_FACE ( 'NONE', ( #108725 ), #256923, .T. ) ;
#67690=VECTOR ( 'NONE', #113346, 1000.000000000000000 ) ;
#67699=ORIENTED_EDGE ( 'NONE', *, *, #71764, .F. ) ;
#67720=LINE ( 'NONE', #89836, #113444 ) ;
#67749=DIRECTION ( 'NONE',  ( 1.000000000000000000, 3.448943450116723568E-16, 6.438528483529607644E-16 ) ) ;
#67751=VERTEX_POINT ( 'NONE', #5742 ) ;
#67758=ORIENTED_EDGE ( 'NONE', *, *, #42882, .T. ) ;
#67764=DIRECTION ( 'NONE',  ( 1.000000000000000000, 0.000000000000000000, 0.000000000000000000 ) ) ;
#67775=AXIS2_PLACEMENT_3D ( 'NONE', #112569, #150419, #50012 ) ;
#67777=EDGE_LOOP ( 'NONE', ( #88601, #161828, #180079, #230320 ) ) ;
#67785=VERTEX_POINT ( 'NONE', #12218 ) ;
#67802=DIRECTION ( 'NONE',  ( 1.000000000000000000, 0.000000000000000000, 0.000000000000000000 ) ) ;
#67820=CARTESIAN_POINT ( 'NONE',  ( -18.59999999999999787, 16.56538529403860238, -240.6448716151659823 ) ) ;
#67832=EDGE_LOOP ( 'NONE', ( #124918, #108078, #5100, #184397, #98363, #169714, #211339, #121702 ) ) ;
#67833=AXIS2_PLACEMENT_3D ( 'NONE', #9882, #13741, #206810 ) ;
#67844=CARTESIAN_POINT ( 'NONE',  ( 23.14999999999999503, 35.97645343225767789, -235.9694016464868298 ) ) ;
#67860=ORIENTED_EDGE ( 'NONE', *, *, #95951, .T. ) ;
#67862=FACE_OUTER_BOUND ( 'NONE', #91892, .T. ) ;
#67918=VECTOR ( 'NONE', #47792, 1000.000000000000000 ) ;
#67968=DIRECTION ( 'NONE',  ( -0.000000000000000000, 0.8814952561688430555, -0.4721928772777346239 ) ) ;
#67976=ORIENTED_EDGE ( 'NONE', *, *, #35103, .T. ) ;
#67980=ORIENTED_EDGE ( 'NONE', *, *, #202167, .F. ) ;
#67999=AXIS2_PLACEMENT_3D ( 'NONE', #26645, #47447, #229958 ) ;
#68056=AXIS2_PLACEMENT_3D ( 'NONE', #258078, #22103, #217688 ) ;
#68072=CARTESIAN_POINT ( 'NONE',  ( 19.99999999737999090, 34.43872460993190288, -235.0322388072028161 ) ) ;
#68133=CYLINDRICAL_SURFACE ( 'NONE', #249089, 0.09999999999998304689 ) ;
#68152=DIRECTION ( 'NONE',  ( 1.000000000000000000, -3.448943450116721102E-16, -6.438528483529607644E-16 ) ) ;
#68190=EDGE_CURVE ( 'NONE', #167556, #136922, #25858, .T. ) ;
#68219=EDGE_CURVE ( 'NONE', #194531, #235463, #2209, .T. ) ;
#68231=CARTESIAN_POINT ( 'NONE',  ( -21.08884785362073089, 1.548504767058726417, -230.6869963227249229 ) ) ;
#68259=ORIENTED_EDGE ( 'NONE', *, *, #49658, .F. ) ;
#68260=CIRCLE ( 'NONE', #130612, 0.1000000000000012546 ) ;
#68273=EDGE_LOOP ( 'NONE', ( #170863, #224994, #194578, #88052 ) ) ;
#68320=ORIENTED_EDGE ( 'NONE', *, *, #99999, .T. ) ;
#68387=CARTESIAN_POINT ( 'NONE',  ( 21.05000000000000071, 10.30543449102040654, -228.0143625250146329 ) ) ;
#68412=ADVANCED_FACE ( 'NONE', ( #177412 ), #256859, .T. ) ;
#68430=EDGE_CURVE ( 'NONE', #241914, #21212, #48131, .T. ) ;
#68431=CARTESIAN_POINT ( 'NONE',  ( 21.00000000000000000, 22.61918030723622408, -230.9697045991730988 ) ) ;
#68441=CARTESIAN_POINT ( 'NONE',  ( -20.85000000000000142, 31.11065811373596190, -259.9087319612273177 ) ) ;
#68463=CARTESIAN_POINT ( 'NONE',  ( -23.25000000000000000, 46.01276039807270024, -256.6622985126337539 ) ) ;
#68481=ADVANCED_FACE ( 'NONE', ( #88522 ), #108118, .F. ) ;
#68494=LINE ( 'NONE', #72360, #21943 ) ;
#68502=PLANE ( 'NONE',  #56343 ) ;
#68542=CARTESIAN_POINT ( 'NONE',  ( 20.94999999999999929, 36.65892442174935439, -249.5511627012433848 ) ) ;
#68554=AXIS2_PLACEMENT_3D ( 'NONE', #134044, #192761, #213585 ) ;
#68567=DIRECTION ( 'NONE',  ( -0.000000000000000000, 0.4721928772777343464, 0.8814952561688431665 ) ) ;
#68573=AXIS2_PLACEMENT_3D ( 'NONE', #173600, #135678, #215238 ) ;
#68586=LINE ( 'NONE', #245940, #86951 ) ;
#68601=FACE_OUTER_BOUND ( 'NONE', #72058, .T. ) ;
#68634=AXIS2_PLACEMENT_3D ( 'NONE', #43464, #60441, #142547 ) ;
#68656=VERTEX_POINT ( 'NONE', #114533 ) ;
#68681=CARTESIAN_POINT ( 'NONE',  ( -22.47007471830799119, 0.3230635261676482739, -230.0870367350772483 ) ) ;
#68690=ORIENTED_EDGE ( 'NONE', *, *, #51129, .T. ) ;
#68697=FACE_OUTER_BOUND ( 'NONE', #123527, .T. ) ;
#68709=EDGE_CURVE ( 'NONE', #118204, #52463, #120975, .T. ) ;
#68711=CARTESIAN_POINT ( 'NONE',  ( 18.45036689428327747, 8.829294088443328192, -245.4095986352067484 ) ) ;
#68716=CARTESIAN_POINT ( 'NONE',  ( 18.50016250449482058, 46.34703458179488678, -243.0587802416278009 ) ) ;
#68753=DIRECTION ( 'NONE',  ( 2.952720810173288619E-16, -0.4721928772777346239, -0.8814952561688430555 ) ) ;
#68759=CARTESIAN_POINT ( 'NONE',  ( 21.05000000000000782, 1.643181256369374843, -230.7196533885927181 ) ) ;
#68780=VECTOR ( 'NONE', #79902, 1000.000000000000000 ) ;
#68809=ORIENTED_EDGE ( 'NONE', *, *, #254041, .T. ) ;
#68848=CARTESIAN_POINT ( 'NONE',  ( 23.14999999999999858, 20.42498087366621817, -235.1829032864613396 ) ) ;
#68867=CARTESIAN_POINT ( 'NONE',  ( -22.00411653962174441, 10.46655577783124969, -227.2920607449393344 ) ) ;
#68871=CARTESIAN_POINT ( 'NONE',  ( -18.59999999999999787, 18.14639373905162145, -237.6648341169113792 ) ) ;
#68884=ORIENTED_EDGE ( 'NONE', *, *, #179068, .T. ) ;
#68929=ORIENTED_EDGE ( 'NONE', *, *, #125382, .T. ) ;
#68938=AXIS2_PLACEMENT_3D ( 'NONE', #214260, #117717, #19925 ) ;
#68942=FACE_OUTER_BOUND ( 'NONE', #135182, .T. ) ;
#68977=ORIENTED_EDGE ( 'NONE', *, *, #191899, .F. ) ;
#68982=ADVANCED_FACE ( 'NONE', ( #153391 ), #132460, .F. ) ;
#69012=DIRECTION ( 'NONE',  ( -0.000000000000000000, -0.8814952561688432775, 0.4721928772777344019 ) ) ;
#69021=CARTESIAN_POINT ( 'NONE',  ( -21.05000000000000071, 30.43677443282725292, -239.5249545687858870 ) ) ;
#69024=AXIS2_PLACEMENT_3D ( 'NONE', #34371, #14810, #177734 ) ;
#69045=ORIENTED_EDGE ( 'NONE', *, *, #138085, .F. ) ;
#69065=CARTESIAN_POINT ( 'NONE',  ( -18.50000000000000000, -4.963776450181787148, -229.1688993039521449 ) ) ;
#69066=VECTOR ( 'NONE', #216755, 1000.000000000000000 ) ;
#69105=LINE ( 'NONE', #243863, #166026 ) ;
#69170=EDGE_CURVE ( 'NONE', #123093, #3876, #102317, .T. ) ;
#69195=CARTESIAN_POINT ( 'NONE',  ( -21.04999999999998295, 1.543325666084004677, -230.7238449902075956 ) ) ;
#69202=CARTESIAN_POINT ( 'NONE',  ( -22.37643362114956957, 0.4535211548021770844, -230.0445178328014606 ) ) ;
#69221=VERTEX_POINT ( 'NONE', #84025 ) ;
#69283=EDGE_CURVE ( 'NONE', #81676, #255363, #224860, .T. ) ;
#69287=ORIENTED_EDGE ( 'NONE', *, *, #100464, .T. ) ;
#69298=CYLINDRICAL_SURFACE ( 'NONE', #133269, 0.1000000000000013933 ) ;
#69304=DIRECTION ( 'NONE',  ( 0.000000000000000000, 0.4646089985449745052, 0.8855159391400224678 ) ) ;
#69319=CIRCLE ( 'NONE', #31734, 0.1999999999999987899 ) ;
#69333=EDGE_CURVE ( 'NONE', #123927, #181985, #197388, .T. ) ;
#69356=EDGE_CURVE ( 'NONE', #29239, #5002, #43290, .T. ) ;
#69392=ORIENTED_EDGE ( 'NONE', *, *, #156373, .F. ) ;
#69421=CARTESIAN_POINT ( 'NONE',  ( 18.49999999999999645, 18.11150788191476124, -237.7585516551410478 ) ) ;
#69460=LINE ( 'NONE', #70755, #106875 ) ;
#69464=CARTESIAN_POINT ( 'NONE',  ( 18.40916198585718888, 37.99112793787836750, -261.0419301676770374 ) ) ;
#69478=CARTESIAN_POINT ( 'NONE',  ( -20.85000000000000142, 42.96960653111219131, -254.4772109693542745 ) ) ;
#69563=AXIS2_PLACEMENT_3D ( 'NONE', #192052, #77203, #75938 ) ;
#69568=VECTOR ( 'NONE', #144188, 1000.000000000000000 ) ;
#69584=CARTESIAN_POINT ( 'NONE',  ( 18.49999999999999645, 43.08613539620618837, -254.3146655184800409 ) ) ;
#69591=DIRECTION ( 'NONE',  ( 0.000000000000000000, 0.8814952561688430555, -0.4721928772777346239 ) ) ;
#69631=TOROIDAL_SURFACE ( 'NONE', #240306, 0.2000000000000000111, 0.1000000000000000056 ) ;
#69652=VECTOR ( 'NONE', #9498, 1000.000000000000000 ) ;
#69673=CARTESIAN_POINT ( 'NONE',  ( 21.09793522318398828, 22.98180148693077740, -230.0583016547000739 ) ) ;
#69697=FACE_OUTER_BOUND ( 'NONE', #54428, .T. ) ;
#69703=CIRCLE ( 'NONE', #98870, 4.300000000000035350 ) ;
#69751=AXIS2_PLACEMENT_3D ( 'NONE', #65025, #10209, #29797 ) ;
#69773=ORIENTED_EDGE ( 'NONE', *, *, #80936, .T. ) ;
#69788=ORIENTED_EDGE ( 'NONE', *, *, #123269, .T. ) ;
#69802=DIRECTION ( 'NONE',  ( -1.000000000000000000, -0.000000000000000000, -0.000000000000000000 ) ) ;
#69840=CARTESIAN_POINT ( 'NONE',  ( 22.59999999999999432, -3.092988775432913506, -228.1437074281570858 ) ) ;
#69843=DIRECTION ( 'NONE',  ( -1.000000000000000000, -0.000000000000000000, -0.000000000000000000 ) ) ;
#69882=ORIENTED_EDGE ( 'NONE', *, *, #218124, .F. ) ;
#69884=DIRECTION ( 'NONE',  ( -1.000000000000000000, -0.000000000000000000, -0.000000000000000000 ) ) ;
#69953=ORIENTED_EDGE ( 'NONE', *, *, #153141, .F. ) ;
#70020=CARTESIAN_POINT ( 'NONE',  ( 18.58222699835054570, 46.46797214202639026, -243.0846070113367432 ) ) ;
#70087=EDGE_CURVE ( 'NONE', #226630, #20661, #53898, .T. ) ;
#70108=EDGE_LOOP ( 'NONE', ( #120378, #142118, #150522, #168990 ) ) ;
#70137=ORIENTED_EDGE ( 'NONE', *, *, #48714, .F. ) ;
#70148=ORIENTED_EDGE ( 'NONE', *, *, #202262, .T. ) ;
#70193=DIRECTION ( 'NONE',  ( 0.000000000000000000, 0.8814952561688428334, -0.4721928772777348460 ) ) ;
#70205=DIRECTION ( 'NONE',  ( 0.000000000000000000, 0.03181660087583048496, -0.9994937237965570986 ) ) ;
#70233=CARTESIAN_POINT ( 'NONE',  ( -23.25000000000000000, -3.275978944802464099, -228.2735455795363748 ) ) ;
#70247=DIRECTION ( 'NONE',  ( -1.000000000000000000, -0.000000000000000000, -0.000000000000000000 ) ) ;
#70259=CARTESIAN_POINT ( 'NONE',  ( 20.95561247346651967, 18.82560383811837568, -227.9789827151014947 ) ) ;
#70260=EDGE_LOOP ( 'NONE', ( #32196, #231480, #200876, #161073 ) ) ;
#70263=LINE ( 'NONE', #148491, #228642 ) ;
#70273=AXIS2_PLACEMENT_3D ( 'NONE', #110260, #114108, #172862 ) ;
#70287=VECTOR ( 'NONE', #204300, 1000.000000000000000 ) ;
#70300=ADVANCED_FACE ( 'NONE', ( #214626 ), #196353, .F. ) ;
#70319=EDGE_CURVE ( 'NONE', #192243, #158502, #193855, .T. ) ;
#70324=ORIENTED_EDGE ( 'NONE', *, *, #236536, .T. ) ;
#70341=ORIENTED_EDGE ( 'NONE', *, *, #43529, .F. ) ;
#70348=CIRCLE ( 'NONE', #45358, 11.80000000000000782 ) ;
#70350=DIRECTION ( 'NONE',  ( 0.000000000000000000, 0.8814952561688428334, -0.4721928772777350125 ) ) ;
#70353=DIRECTION ( 'NONE',  ( -0.000000000000000000, 0.4721928772777345684, 0.8814952561688429444 ) ) ;
#70426=VERTEX_POINT ( 'NONE', #226151 ) ;
#70450=EDGE_CURVE ( 'NONE', #193873, #149301, #73092, .T. ) ;
#70464=DIRECTION ( 'NONE',  ( 1.000000000000000000, 0.000000000000000000, 0.000000000000000000 ) ) ;
#70490=CARTESIAN_POINT ( 'NONE',  ( -21.05000000000000071, 1.371682548295136472, -230.7621968047018584 ) ) ;
#70494=VERTEX_POINT ( 'NONE', #207938 ) ;
#70525=CIRCLE ( 'NONE', #249569, 0.09999999999999939493 ) ;
#70543=DIRECTION ( 'NONE',  ( 1.000000000000000000, -0.000000000000000000, -0.000000000000000000 ) ) ;
#70562=DIRECTION ( 'NONE',  ( 0.000000000000000000, -0.8814952561688438326, 0.4721928772777334582 ) ) ;
#70575=CARTESIAN_POINT ( 'NONE',  ( 23.14999999999999503, 35.97645343225767789, -235.9694016464868298 ) ) ;
#70602=VERTEX_POINT ( 'NONE', #134773 ) ;
#70629=CIRCLE ( 'NONE', #187137, 0.09999999999999939493 ) ;
#70654=CARTESIAN_POINT ( 'NONE',  ( -21.05000000000000071, 36.02367271998545561, -235.8812521208699309 ) ) ;
#70671=CARTESIAN_POINT ( 'NONE',  ( 20.95512820512820440, 18.90192396791320562, -227.9871466877642661 ) ) ;
#70674=CIRCLE ( 'NONE', #28995, 0.09999999999999986677 ) ;
#70685=CARTESIAN_POINT ( 'NONE',  ( 20.11144452914042091, 18.77466987908303508, -228.7020108391373014 ) ) ;
#70718=ORIENTED_EDGE ( 'NONE', *, *, #174064, .T. ) ;
#70721=CIRCLE ( 'NONE', #166403, 0.09999999999999939493 ) ;
#70743=DIRECTION ( 'NONE',  ( 0.000000000000000000, -0.8814952561688476074, 0.4721928772777262417 ) ) ;
#70755=CARTESIAN_POINT ( 'NONE',  ( 18.49999999999999645, -2.275048162540885155, -230.1697641654749305 ) ) ;
#70757=DIRECTION ( 'NONE',  ( 1.000000000000000000, -0.000000000000000000, -0.000000000000000000 ) ) ;
#70759=CARTESIAN_POINT ( 'NONE',  ( 18.33683296300444709, 38.25517547545369723, -261.1960221343530293 ) ) ;
#70771=AXIS2_PLACEMENT_3D ( 'NONE', #135188, #234295, #236865 ) ;
#70798=LINE ( 'NONE', #231154, #7631 ) ;
#70817=CIRCLE ( 'NONE', #129051, 0.09999999999999742428 ) ;
#70819=VECTOR ( 'NONE', #113351, 1000.000000000000114 ) ;
#70821=EDGE_CURVE ( 'NONE', #239499, #15247, #88930, .T. ) ;
#70830=FACE_OUTER_BOUND ( 'NONE', #123890, .T. ) ;
#70842=ORIENTED_EDGE ( 'NONE', *, *, #211172, .T. ) ;
#70860=CIRCLE ( 'NONE', #220684, 0.1000000000000013933 ) ;
#70864=AXIS2_PLACEMENT_3D ( 'NONE', #7593, #89679, #88387 ) ;
#70915=DIRECTION ( 'NONE',  ( 1.000000000000000000, 1.541880601228652843E-16, 2.878400969107353907E-16 ) ) ;
#70926=EDGE_LOOP ( 'NONE', ( #72670, #181058, #181268, #70324 ) ) ;
#70946=DIRECTION ( 'NONE',  ( -1.000000000000000000, -0.000000000000000000, -0.000000000000000000 ) ) ;
#70952=VERTEX_POINT ( 'NONE', #25977 ) ;
#70955=AXIS2_PLACEMENT_3D ( 'NONE', #249124, #71772, #191732 ) ;
#70986=DIRECTION ( 'NONE',  ( 1.000000000000000000, 0.000000000000000000, 0.000000000000000000 ) ) ;
#70995=ORIENTED_EDGE ( 'NONE', *, *, #227537, .T. ) ;
#71009=CARTESIAN_POINT ( 'NONE',  ( -18.42637059832564361, 38.00040471499162464, -261.0434343050587813 ) ) ;
#71039=VERTEX_POINT ( 'NONE', #85905 ) ;
#71058=DIRECTION ( 'NONE',  ( 1.000000000000000000, 1.541880601228652843E-16, 2.878400969107353907E-16 ) ) ;
#71086=CARTESIAN_POINT ( 'NONE',  ( 23.14999999999999858, 36.65892442174935439, -249.5511627012433848 ) ) ;
#71094=CARTESIAN_POINT ( 'NONE',  ( 21.05000000000000071, 1.434803724213256082, -230.7796651547878355 ) ) ;
#71141=AXIS2_PLACEMENT_3D ( 'NONE', #95072, #234581, #252855 ) ;
#71187=FACE_OUTER_BOUND ( 'NONE', #176195, .T. ) ;
#71200=EDGE_CURVE ( 'NONE', #1255, #235463, #81748, .T. ) ;
#71201=EDGE_CURVE ( 'NONE', #199913, #45747, #177506, .T. ) ;
#71206=CARTESIAN_POINT ( 'NONE',  ( -22.45305610364635385, -3.275978944802467652, -228.2735455795363748 ) ) ;
#71230=AXIS2_PLACEMENT_3D ( 'NONE', #246279, #169347, #25953 ) ;
#71233=CARTESIAN_POINT ( 'NONE',  ( -20.00857864376270001, 22.34215363070824623, -231.2750834139128528 ) ) ;
#71254=DIRECTION ( 'NONE',  ( 0.000000000000000000, 0.5341055959866798375, -0.8454177738465836756 ) ) ;
#71258=ORIENTED_EDGE ( 'NONE', *, *, #24298, .F. ) ;
#71286=AXIS2_PLACEMENT_3D ( 'NONE', #58622, #2500, #82018 ) ;
#71314=CARTESIAN_POINT ( 'NONE',  ( 21.04999999999913030, 18.82942951893005201, -229.9355821828612534 ) ) ;
#71334=CARTESIAN_POINT ( 'NONE',  ( -20.87155475150660777, 36.12098300858677646, -235.9333785785471775 ) ) ;
#71359=ADVANCED_FACE ( 'NONE', ( #235491 ), #6952, .T. ) ;
#71363=CIRCLE ( 'NONE', #125510, 0.09999999999998464284 ) ;
#71375=ORIENTED_EDGE ( 'NONE', *, *, #102918, .F. ) ;
#71383=VERTEX_POINT ( 'NONE', #238058 ) ;
#71399=CARTESIAN_POINT ( 'NONE',  ( 20.85000000000000142, 45.93315328338058379, -256.6017782078560003 ) ) ;
#71410=ORIENTED_EDGE ( 'NONE', *, *, #11715, .T. ) ;
#71417=VERTEX_POINT ( 'NONE', #36035 ) ;
#71436=CARTESIAN_POINT ( 'NONE',  ( -22.47071067811866385, 10.68684811775433907, -226.8807012965928323 ) ) ;
#71447=FACE_OUTER_BOUND ( 'NONE', #87526, .T. ) ;
#71486=DIRECTION ( 'NONE',  ( -1.000000000000000000, -0.000000000000000000, -0.000000000000000000 ) ) ;
#71491=DIRECTION ( 'NONE',  ( 0.000000000000000000, -0.8814952561688513821, 0.4721928772777189698 ) ) ;
#71492=CARTESIAN_POINT ( 'NONE',  ( 21.46681500593592773, 10.36690126540559653, -227.6878377563196523 ) ) ;
#71494=EDGE_CURVE ( 'NONE', #126765, #166239, #219775, .T. ) ;
#71512=EDGE_CURVE ( 'NONE', #140913, #126382, #120716, .T. ) ;
#71530=DIRECTION ( 'NONE',  ( 0.000000000000000000, -0.8814952561688423893, 0.4721928772777359007 ) ) ;
#71534=CARTESIAN_POINT ( 'NONE',  ( 20.95462737510932882, 18.78654564892814349, -228.0014245997133742 ) ) ;
#71536=CARTESIAN_POINT ( 'NONE',  ( 18.49999999999998934, 33.69766839675186532, -236.3369293616048026 ) ) ;
#71537=DIRECTION ( 'NONE',  ( 0.000000000000000000, -0.03181660087583042251, 0.9994937237965568766 ) ) ;
#71561=CARTESIAN_POINT ( 'NONE',  ( -23.25000000000000000, 36.65892442174935439, -249.5511627012433848 ) ) ;
#71601=CARTESIAN_POINT ( 'NONE',  ( -21.05000000000000071, 36.65892442174935439, -249.5511627012433848 ) ) ;
#71627=ORIENTED_EDGE ( 'NONE', *, *, #171013, .F. ) ;
#71629=LINE ( 'NONE', #69065, #168620 ) ;
#71630=CARTESIAN_POINT ( 'NONE',  ( -23.15000000000000213, 35.97645343225767789, -235.9694016464868298 ) ) ;
#71647=AXIS2_PLACEMENT_3D ( 'NONE', #153423, #188647, #132533 ) ;
#71658=EDGE_CURVE ( 'NONE', #158295, #156870, #227700, .T. ) ;
#71666=VECTOR ( 'NONE', #1918, 1000.000000000000000 ) ;
#71680=CARTESIAN_POINT ( 'NONE',  ( 23.14999999999999503, 2.272311100394802885, -217.9150152700588592 ) ) ;
#71698=CARTESIAN_POINT ( 'NONE',  ( 20.94999999999999929, 36.65892442174935439, -249.5511627012433848 ) ) ;
#71733=VECTOR ( 'NONE', #252084, 1000.000000000000000 ) ;
#71742=ADVANCED_FACE ( 'NONE', ( #74880 ), #66189, .T. ) ;
#71764=EDGE_CURVE ( 'NONE', #65641, #117652, #133532, .T. ) ;
#71772=DIRECTION ( 'NONE',  ( 0.000000000000000000, -0.8814952561688430555, 0.4721928772777346239 ) ) ;
#71792=CARTESIAN_POINT ( 'NONE',  ( -20.54999999999999716, 38.42191493408704872, -250.4955484557988541 ) ) ;
#71895=VECTOR ( 'NONE', #57994, 1000.000000000000000 ) ;
#71896=EDGE_LOOP ( 'NONE', ( #92362, #32079, #170504, #80104 ) ) ;
#71910=DIRECTION ( 'NONE',  ( 1.000000000000000000, 0.000000000000000000, 0.000000000000000000 ) ) ;
#71933=VERTEX_POINT ( 'NONE', #159531 ) ;
#71938=CARTESIAN_POINT ( 'NONE',  ( 20.12499999999999645, 18.89374182079812314, -228.4160025464828152 ) ) ;
#71949=CARTESIAN_POINT ( 'NONE',  ( 20.77766267348356166, 18.75573362213343387, -228.1071430829227324 ) ) ;
#71962=ORIENTED_EDGE ( 'NONE', *, *, #203732, .F. ) ;
#71975=CARTESIAN_POINT ( 'NONE',  ( -20.54999999999999716, 26.13474583767463244, -241.1910018098189141 ) ) ;
#71976=EDGE_LOOP ( 'NONE', ( #59073, #2635, #241097, #40754 ) ) ;
#71987=VERTEX_POINT ( 'NONE', #69421 ) ;
#72003=ORIENTED_EDGE ( 'NONE', *, *, #17983, .T. ) ;
#72026=CARTESIAN_POINT ( 'NONE',  ( 18.48413544395656416, 37.98663424106526065, -261.2259154368716736 ) ) ;
#72058=EDGE_LOOP ( 'NONE', ( #189544, #142035, #29508 ) ) ;
#72067=ADVANCED_FACE ( 'NONE', ( #75822 ), #237464, .T. ) ;
#72114=CIRCLE ( 'NONE', #130341, 0.09999999999999939493 ) ;
#72131=CARTESIAN_POINT ( 'NONE',  ( -23.15000000000000213, 33.22109292269086467, -247.7096104798602312 ) ) ;
#72144=DIRECTION ( 'NONE',  ( -1.000000000000000000, -1.394253735153569469E-16, -2.602809386958778209E-16 ) ) ;
#72151=ORIENTED_EDGE ( 'NONE', *, *, #205081, .T. ) ;
#72153=CARTESIAN_POINT ( 'NONE',  ( 21.05000000000000071, 24.17260720300848575, -252.6908294531417027 ) ) ;
#72175=CIRCLE ( 'NONE', #34767, 0.1000000000000009354 ) ;
#72233=DIRECTION ( 'NONE',  ( -1.000000000000000000, 0.000000000000000000, 0.000000000000000000 ) ) ;
#72248=ADVANCED_FACE ( 'NONE', ( #246130 ), #67480, .T. ) ;
#72277=DIRECTION ( 'NONE',  ( -1.000000000000000000, -0.000000000000000000, -0.000000000000000000 ) ) ;
#72296=LINE ( 'NONE', #30610, #164935 ) ;
#72313=CIRCLE ( 'NONE', #222101, 0.1000000000000013933 ) ;
#72333=CARTESIAN_POINT ( 'NONE',  ( -18.59999999999999787, 19.02280865327213277, -233.3540837620168986 ) ) ;
#72339=VERTEX_POINT ( 'NONE', #72644 ) ;
#72346=CARTESIAN_POINT ( 'NONE',  ( -23.15000000000000213, 40.18490544642472884, -251.4399342103543233 ) ) ;
#72356=EDGE_LOOP ( 'NONE', ( #33422, #244447, #45383, #194394 ) ) ;
#72360=CARTESIAN_POINT ( 'NONE',  ( 22.50000000000000000, -3.181516632163039482, -228.0962854788089942 ) ) ;
#72362=ADVANCED_FACE ( 'NONE', ( #131306 ), #132604, .F. ) ;
#72368=DIRECTION ( 'NONE',  ( 1.713247197920696300E-14, 0.6046243595031879359, 0.7965107556683461709 ) ) ;
#72379=CARTESIAN_POINT ( 'NONE',  ( 21.05000000000000071, 1.316055977212907901, -230.7323992127457473 ) ) ;
#72439=ADVANCED_FACE ( 'NONE', ( #96018 ), #31915, .T. ) ;
#72442=CARTESIAN_POINT ( 'NONE',  ( 23.14999999999999503, 31.49702336731128582, -233.4564499823349877 ) ) ;
#72484=CYLINDRICAL_SURFACE ( 'NONE', #230301, 0.5000000000000008882 ) ;
#72493=ORIENTED_EDGE ( 'NONE', *, *, #148438, .F. ) ;
#72494=CIRCLE ( 'NONE', #147491, 0.4000000000000010214 ) ;
#72511=VERTEX_POINT ( 'NONE', #120764 ) ;
#72535=CIRCLE ( 'NONE', #26751, 0.09999999999998304689 ) ;
#72545=CARTESIAN_POINT ( 'NONE',  ( -21.00023020733502221, 1.495312417593689602, -230.7149783752102508 ) ) ;
#72550=LINE ( 'NONE', #42391, #42953 ) ;
#72557=DIRECTION ( 'NONE',  ( 1.000000000000000000, 1.394253735153569469E-16, 2.602809386958778209E-16 ) ) ;
#72562=CIRCLE ( 'NONE', #230788, 4.099999999999996980 ) ;
#72578=CARTESIAN_POINT ( 'NONE',  ( -20.85000000000000142, 36.22724532936083364, -235.9903003947922286 ) ) ;
#72605=VERTEX_POINT ( 'NONE', #101109 ) ;
#72630=CARTESIAN_POINT ( 'NONE',  ( -20.64999999999999858, 19.91953773510093839, -237.8616849742533077 ) ) ;
#72631=EDGE_CURVE ( 'NONE', #167145, #238889, #221103, .T. ) ;
#72641=DIRECTION ( 'NONE',  ( 1.000000000000000000, 0.000000000000000000, 0.000000000000000000 ) ) ;
#72644=CARTESIAN_POINT ( 'NONE',  ( -23.15000000000000213, 10.69888912757691024, -235.6450824654141059 ) ) ;
#72668=ORIENTED_EDGE ( 'NONE', *, *, #88881, .F. ) ;
#72670=ORIENTED_EDGE ( 'NONE', *, *, #122468, .F. ) ;
#72721=ORIENTED_EDGE ( 'NONE', *, *, #20814, .F. ) ;
#72749=CARTESIAN_POINT ( 'NONE',  ( 23.15000000000000213, 23.45160524131172153, -253.2535058871250726 ) ) ;
#72784=CARTESIAN_POINT ( 'NONE',  ( 20.94999999999999574, 18.18127959618848521, -237.5711165786817389 ) ) ;
#72792=FACE_OUTER_BOUND ( 'NONE', #192560, .T. ) ;
#72800=ORIENTED_EDGE ( 'NONE', *, *, #7528, .F. ) ;
#72810=CARTESIAN_POINT ( 'NONE',  ( -21.44999999999999929, 29.28400589394459530, -237.3759593473670293 ) ) ;
#72816=DIRECTION ( 'NONE',  ( 2.879366945564059217E-14, -0.6052030477779082318, -0.7960711469211348978 ) ) ;
#72830=CIRCLE ( 'NONE', #147818, 0.09999999999999939493 ) ;
#72832=DIRECTION ( 'NONE',  ( 1.000000000000000000, 0.000000000000000000, 0.000000000000000000 ) ) ;
#72865=LINE ( 'NONE', #12884, #145296 ) ;
#72923=DIRECTION ( 'NONE',  ( 0.000000000000000000, 0.8814952561688430555, -0.4721928772777346239 ) ) ;
#72924=ORIENTED_EDGE ( 'NONE', *, *, #107757, .T. ) ;
#72959=VERTEX_POINT ( 'NONE', #96969 ) ;
#72963=ORIENTED_EDGE ( 'NONE', *, *, #13854, .F. ) ;
#72976=ORIENTED_EDGE ( 'NONE', *, *, #33807, .T. ) ;
#73042=ORIENTED_EDGE ( 'NONE', *, *, #12503, .T. ) ;
#73092=CIRCLE ( 'NONE', #218775, 0.09999999999999031886 ) ;
#73095=CARTESIAN_POINT ( 'NONE',  ( -21.14999999999999858, 4.136903274969358613, -245.4596299165286268 ) ) ;
#73105=VERTEX_POINT ( 'NONE', #31636 ) ;
#73106=DIRECTION ( 'NONE',  ( 1.000000000000000000, -0.000000000000000000, -0.000000000000000000 ) ) ;
#73112=SHAPE_DEFINITION_REPRESENTATION ( #226236, #61981 ) ;
#73148=ORIENTED_EDGE ( 'NONE', *, *, #239166, .F. ) ;
#73150=ADVANCED_FACE ( 'NONE', ( #171164 ), #236026, .T. ) ;
#73210=AXIS2_PLACEMENT_3D ( 'NONE', #78968, #41187, #215923 ) ;
#73257=CARTESIAN_POINT ( 'NONE',  ( 20.12518398540832365, 18.88802431391419034, -228.7156777160730030 ) ) ;
#73282=ORIENTED_EDGE ( 'NONE', *, *, #82021, .T. ) ;
#73297=DIRECTION ( 'NONE',  ( 1.000000000000000000, 0.000000000000000000, 0.000000000000000000 ) ) ;
#73300=CARTESIAN_POINT ( 'NONE',  ( 20.95443524775735256, 18.84365912742161697, -229.9358607224024524 ) ) ;
#73315=AXIS2_PLACEMENT_3D ( 'NONE', #194636, #135889, #191699 ) ;
#73331=CARTESIAN_POINT ( 'NONE',  ( 22.47071067811865319, 10.68684811775432664, -226.8807012965928323 ) ) ;
#73332=CARTESIAN_POINT ( 'NONE',  ( 18.39999999999999858, 37.99112772578903474, -261.0419300540665404 ) ) ;
#73375=EDGE_CURVE ( 'NONE', #1130, #35113, #78030, .T. ) ;
#73380=ORIENTED_EDGE ( 'NONE', *, *, #124571, .T. ) ;
#73391=ORIENTED_EDGE ( 'NONE', *, *, #103570, .F. ) ;
#73400=CARTESIAN_POINT ( 'NONE',  ( 23.24999999999999645, 20.70829660003285611, -234.6540061327600597 ) ) ;
#73422=EDGE_LOOP ( 'NONE', ( #200388, #83075, #8885, #19682, #113186, #107848 ) ) ;
#73436=CARTESIAN_POINT ( 'NONE',  ( 23.25000000000000000, -8.729782940176418649, -238.4538547387928986 ) ) ;
#73442=DIRECTION ( 'NONE',  ( -1.000000000000000000, -0.000000000000000000, -0.000000000000000000 ) ) ;
#73443=ADVANCED_FACE ( 'NONE', ( #91285 ), #149993, .F. ) ;
#73483=EDGE_LOOP ( 'NONE', ( #121765, #169178, #18770, #256325 ) ) ;
#73506=CARTESIAN_POINT ( 'NONE',  ( 20.94999999999999929, 21.98309897467606433, -231.7335930323676791 ) ) ;
#73507=DIRECTION ( 'NONE',  ( 0.7071359030027126735, -0.6232856014206268336, 0.3338770338706537610 ) ) ;
#73508=ORIENTED_EDGE ( 'NONE', *, *, #205604, .F. ) ;
#73510=CARTESIAN_POINT ( 'NONE',  ( 18.59999999999999432, 16.50669723772569952, -240.7258389668962479 ) ) ;
#73515=AXIS2_PLACEMENT_3D ( 'NONE', #15816, #94020, #18350 ) ;
#73593=B_SPLINE_CURVE_WITH_KNOTS ( 'NONE', 3,
 ( #19184, #196529, #257734, #218651, #80398, #40066, #239523 ),
 .UNSPECIFIED., .F., .F.,
 ( 4, 3, 4 ),
 ( 0.000000000000000000, 1.860045280645939271E-05, 5.251155757305736512E-05 ),
 .UNSPECIFIED. ) ;
#73603=ORIENTED_EDGE ( 'NONE', *, *, #79417, .F. ) ;
#73607=VERTEX_POINT ( 'NONE', #36465 ) ;
#73625=CARTESIAN_POINT ( 'NONE',  ( -22.59999999999999787, 12.58798907299599001, -223.3278890275437050 ) ) ;
#73626=CARTESIAN_POINT ( 'NONE',  ( -18.59999999999999787, 43.08613539620618837, -254.3146655184800409 ) ) ;
#73630=CIRCLE ( 'NONE', #77666, 11.75000000000000355 ) ;
#73649=DIRECTION ( 'NONE',  ( 0.000000000000000000, 0.8496786552930157832, 0.5273008465188090410 ) ) ;
#73662=CARTESIAN_POINT ( 'NONE',  ( -21.04999999999999716, 10.27539803298866516, -228.0704349406337030 ) ) ;
#73686=EDGE_LOOP ( 'NONE', ( #3452, #86524, #67860, #109998 ) ) ;
#73701=DIRECTION ( 'NONE',  ( 1.000000000000000000, 0.000000000000000000, 0.000000000000000000 ) ) ;
#73740=CARTESIAN_POINT ( 'NONE',  ( 20.85000000000000142, 43.62273694548321856, -253.2814864317374770 ) ) ;
#73741=DIRECTION ( 'NONE',  ( 0.000000000000000000, 0.8814952561688432775, -0.4721928772777344019 ) ) ;
#73766=CYLINDRICAL_SURFACE ( 'NONE', #205582, 0.1000000000000053763 ) ;
#73786=CARTESIAN_POINT ( 'NONE',  ( 21.05095171578076574, 21.99704254906454537, -231.7411790891100907 ) ) ;
#73835=ORIENTED_EDGE ( 'NONE', *, *, #16202, .F. ) ;
#73857=VECTOR ( 'NONE', #183695, 1000.000000000000000 ) ;
#73861=TOROIDAL_SURFACE ( 'NONE', #244683, 0.2000000000000000111, 0.1000000000000000056 ) ;
#73892=CARTESIAN_POINT ( 'NONE',  ( 20.85000000000000142, 46.07463622722161745, -256.5801648492221148 ) ) ;
#73912=CARTESIAN_POINT ( 'NONE',  ( -20.85000000106542117, 36.17380055357438096, -235.9616714914856459 ) ) ;
#73921=AXIS2_PLACEMENT_3D ( 'NONE', #193766, #252437, #235440 ) ;
#73929=ORIENTED_EDGE ( 'NONE', *, *, #99429, .T. ) ;
#73945=DIRECTION ( 'NONE',  ( 0.000000000000000000, 0.8814952561688438326, -0.4721928772777331806 ) ) ;
#73959=ORIENTED_EDGE ( 'NONE', *, *, #102477, .T. ) ;
#73980=CARTESIAN_POINT ( 'NONE',  ( -21.05000000000000071, 18.27574494880468592, -237.6039235467692947 ) ) ;
#73990=FACE_OUTER_BOUND ( 'NONE', #130822, .T. ) ;
#74006=ORIENTED_EDGE ( 'NONE', *, *, #67020, .T. ) ;
#74017=CYLINDRICAL_SURFACE ( 'NONE', #221623, 0.1000000000000013933 ) ;
#74022=CARTESIAN_POINT ( 'NONE',  ( 18.49999999999999289, -0.1830918614494220220, -222.4987906021368360 ) ) ;
#74057=DIRECTION ( 'NONE',  ( -0.000000000000000000, -0.4721928772777346794, -0.8814952561688431665 ) ) ;
#74070=LINE ( 'NONE', #96143, #193403 ) ;
#74079=DIRECTION ( 'NONE',  ( 0.000000000000000000, 0.8814952561688428334, -0.4721928772777350125 ) ) ;
#74104=CARTESIAN_POINT ( 'NONE',  ( 18.59999999999999076, 45.93315328338058379, -256.6017782078560003 ) ) ;
#74203=VERTEX_POINT ( 'NONE', #204684 ) ;
#74211=CARTESIAN_POINT ( 'NONE',  ( -22.48479450179659977, -3.118395934723631413, -228.1902321699264746 ) ) ;
#74230=AXIS2_PLACEMENT_3D ( 'NONE', #116401, #73442, #96793 ) ;
#74278=CARTESIAN_POINT ( 'NONE',  ( -23.25000000000000000, 43.62273694548321146, -253.2814864317374770 ) ) ;
#74296=DIRECTION ( 'NONE',  ( 0.000000000000000000, -0.8814952561688430555, 0.4721928772777346239 ) ) ;
#74331=CIRCLE ( 'NONE', #32641, 0.1000000000000013933 ) ;
#74336=VERTEX_POINT ( 'NONE', #208577 ) ;
#74343=VECTOR ( 'NONE', #136702, 1000.000000000000114 ) ;
#74364=DIRECTION ( 'NONE',  ( 0.000000000000000000, -0.4721928772777342354, -0.8814952561688431665 ) ) ;
#74388=CARTESIAN_POINT ( 'NONE',  ( 21.30000000000002558, 3.558777552609279304, -231.8203201594644725 ) ) ;
#74396=CIRCLE ( 'NONE', #32885, 0.1000000000000091649 ) ;
#74449=CARTESIAN_POINT ( 'NONE',  ( -18.59999999999999787, 30.18746141061095045, -235.4776000216846796 ) ) ;
#74494=ADVANCED_FACE ( 'NONE', ( #20637 ), #19336, .T. ) ;
#74496=LINE ( 'NONE', #92718, #14938 ) ;
#74507=CARTESIAN_POINT ( 'NONE',  ( 21.06280952165538167, 22.90470512554973581, -230.1276019220326532 ) ) ;
#74538=EDGE_LOOP ( 'NONE', ( #168811, #34448, #236665, #134508 ) ) ;
#74554=ORIENTED_EDGE ( 'NONE', *, *, #173962, .F. ) ;
#74555=CARTESIAN_POINT ( 'NONE',  ( 20.97565083910961192, 18.75479403086622199, -228.0776265554289068 ) ) ;
#74567=ORIENTED_EDGE ( 'NONE', *, *, #400, .T. ) ;
#74602=CIRCLE ( 'NONE', #237059, 0.09999999999999939493 ) ;
#74623=CIRCLE ( 'NONE', #16342, 4.050000000000002487 ) ;
#74683=VERTEX_POINT ( 'NONE', #250516 ) ;
#74687=ADVANCED_FACE ( 'NONE', ( #11937 ), #171042, .T. ) ;
#74735=DIRECTION ( 'NONE',  ( 0.000000000000000000, 0.8814952561688476074, -0.4721928772777262417 ) ) ;
#74755=VERTEX_POINT ( 'NONE', #130565 ) ;
#74774=ORIENTED_EDGE ( 'NONE', *, *, #232288, .T. ) ;
#74798=ORIENTED_EDGE ( 'NONE', *, *, #49180, .F. ) ;
#74799=EDGE_LOOP ( 'NONE', ( #101655, #129389, #223077, #233829 ) ) ;
#74812=ORIENTED_EDGE ( 'NONE', *, *, #155310, .F. ) ;
#74880=FACE_OUTER_BOUND ( 'NONE', #175022, .T. ) ;
#74910=DIRECTION ( 'NONE',  ( -1.000000000000000000, 0.000000000000000000, 0.000000000000000000 ) ) ;
#74945=FACE_OUTER_BOUND ( 'NONE', #102831, .T. ) ;
#74949=ADVANCED_FACE ( 'NONE', ( #144681 ), #228812, .F. ) ;
#74972=CARTESIAN_POINT ( 'NONE',  ( -23.15000000000000213, 7.128833340093095217, -233.7327013124392749 ) ) ;
#74981=CARTESIAN_POINT ( 'NONE',  ( 21.05000000000000071, 7.128833340093095217, -233.7327013124392749 ) ) ;
#74991=DIRECTION ( 'NONE',  ( 1.000000000000000000, 1.541880601228652843E-16, 2.878400969107353907E-16 ) ) ;
#74992=EDGE_CURVE ( 'NONE', #35062, #68656, #93705, .T. ) ;
#74998=CIRCLE ( 'NONE', #45748, 0.09999999999999939493 ) ;
#75003=ADVANCED_FACE ( 'NONE', ( #53302 ), #162184, .F. ) ;
#75075=ORIENTED_EDGE ( 'NONE', *, *, #35904, .F. ) ;
#75093=AXIS2_PLACEMENT_3D ( 'NONE', #248224, #145248, #86542 ) ;
#75118=CARTESIAN_POINT ( 'NONE',  ( -23.25000000000000000, 26.22918441313017723, -241.0147027585851731 ) ) ;
#75126=B_SPLINE_CURVE_WITH_KNOTS ( 'NONE', 3,
 ( #84918, #25008, #64112, #139771 ),
 .UNSPECIFIED., .F., .F.,
 ( 4, 4 ),
 ( 0.000000000000000000, 0.0001048066582182494762 ),
 .UNSPECIFIED. ) ;
#75127=CARTESIAN_POINT ( 'NONE',  ( -20.94999999999999929, 14.64166534854604507, -236.4381089660238331 ) ) ;
#75184=CARTESIAN_POINT ( 'NONE',  ( -20.54999999999999716, 36.65892442174935439, -249.5511627012433848 ) ) ;
#75186=CARTESIAN_POINT ( 'NONE',  ( -18.49999999999997868, 9.105964803472803126, -245.3658845043482302 ) ) ;
#75188=CARTESIAN_POINT ( 'NONE',  ( -20.99551997958407057, 36.17041074700907899, -235.9598556649060015 ) ) ;
#75194=FACE_OUTER_BOUND ( 'NONE', #140250, .T. ) ;
#75199=DIRECTION ( 'NONE',  ( 0.000000000000000000, -0.9994937237965558774, -0.03181660087586650476 ) ) ;
#75203=CIRCLE ( 'NONE', #133453, 0.1000000000000013933 ) ;
#75206=EDGE_CURVE ( 'NONE', #173295, #198415, #64654, .T. ) ;
#75247=DIRECTION ( 'NONE',  ( 0.000000000000000000, -0.8814952561688428334, 0.4721928772777348460 ) ) ;
#75251=ORIENTED_EDGE ( 'NONE', *, *, #254095, .T. ) ;
#75284=VERTEX_POINT ( 'NONE', #43995 ) ;
#75375=LINE ( 'NONE', #157487, #174240 ) ;
#75387=CARTESIAN_POINT ( 'NONE',  ( 20.95568717954149562, 18.83659447889446170, -227.9769441489441704 ) ) ;
#75402=EDGE_CURVE ( 'NONE', #148418, #19570, #153094, .T. ) ;
#75416=FACE_OUTER_BOUND ( 'NONE', #3382, .T. ) ;
#75421=AXIS2_PLACEMENT_3D ( 'NONE', #179761, #117211, #139312 ) ;
#75430=ORIENTED_EDGE ( 'NONE', *, *, #223660, .F. ) ;
#75438=DIRECTION ( 'NONE',  ( 1.000000000000000000, 0.000000000000000000, 0.000000000000000000 ) ) ;
#75440=CYLINDRICAL_SURFACE ( 'NONE', #118709, 0.1000000000000013933 ) ;
#75461=ORIENTED_EDGE ( 'NONE', *, *, #182618, .T. ) ;
#75482=CYLINDRICAL_SURFACE ( 'NONE', #40652, 0.1000000000000013933 ) ;
#75542=DIRECTION ( 'NONE',  ( 1.000000000000000000, 0.000000000000000000, 0.000000000000000000 ) ) ;
#75568=DIRECTION ( 'NONE',  ( 0.000000000000000000, 0.8814952561688438326, -0.4721928772777334582 ) ) ;
#75603=DIRECTION ( 'NONE',  ( -0.000000000000000000, -0.4721928772777346239, -0.8814952561688430555 ) ) ;
#75620=DIRECTION ( 'NONE',  ( 1.000000000000000000, 0.000000000000000000, 0.000000000000000000 ) ) ;
#75684=LINE ( 'NONE', #119961, #200411 ) ;
#75690=CARTESIAN_POINT ( 'NONE',  ( -21.14999999999999858, 7.128833340093095217, -233.7327013124392749 ) ) ;
#75735=DIRECTION ( 'NONE',  ( 1.000000000000000000, 0.000000000000000000, 0.000000000000000000 ) ) ;
#75738=AXIS2_PLACEMENT_3D ( 'NONE', #231618, #50369, #30867 ) ;
#75744=VERTEX_POINT ( 'NONE', #4229 ) ;
#75745=DIRECTION ( 'NONE',  ( 1.000000000000000000, 0.000000000000000000, 0.000000000000000000 ) ) ;
#75758=FACE_OUTER_BOUND ( 'NONE', #80267, .T. ) ;
#75778=ORIENTED_EDGE ( 'NONE', *, *, #235520, .T. ) ;
#75782=ORIENTED_EDGE ( 'NONE', *, *, #8061, .T. ) ;
#75791=ADVANCED_FACE ( 'NONE', ( #190611 ), #133190, .F. ) ;
#75795=CARTESIAN_POINT ( 'NONE',  ( 20.30466543256790501, 18.79779222453387533, -229.4283813036538788 ) ) ;
#75796=ORIENTED_EDGE ( 'NONE', *, *, #156072, .T. ) ;
#75812=DIRECTION ( 'NONE',  ( 1.000000000000000000, 0.000000000000000000, 0.000000000000000000 ) ) ;
#75822=FACE_OUTER_BOUND ( 'NONE', #124973, .T. ) ;
#75848=DIRECTION ( 'NONE',  ( -1.000000000000000000, 0.000000000000000000, 0.000000000000000000 ) ) ;
#75859=CARTESIAN_POINT ( 'NONE',  ( 18.49999999999999289, 33.95290177507398255, -236.2840123990883114 ) ) ;
#75874=CARTESIAN_POINT ( 'NONE',  ( 20.94999999999999574, 13.53186623653377119, -238.6930807526024694 ) ) ;
#75878=DIRECTION ( 'NONE',  ( 0.7070776581708964059, -0.6233369439636241571, 0.3339045366652730884 ) ) ;
#75887=EDGE_CURVE ( 'NONE', #137538, #119326, #12714, .T. ) ;
#75894=CARTESIAN_POINT ( 'NONE',  ( 18.46921299892753865, 8.797208686344667683, -245.4141857684114427 ) ) ;
#75907=CYLINDRICAL_SURFACE ( 'NONE', #201672, 0.1000000000000013933 ) ;
#75928=CARTESIAN_POINT ( 'NONE',  ( -21.14999999999999858, 18.65704504850842582, -226.5784250989226507 ) ) ;
#75938=DIRECTION ( 'NONE',  ( 0.000000000000000000, -0.8814952561688476074, 0.4721928772777262417 ) ) ;
#75973=ORIENTED_EDGE ( 'NONE', *, *, #47248, .F. ) ;
#75994=CARTESIAN_POINT ( 'NONE',  ( -23.15000000000000213, 27.77927773649450316, -239.9732258281457860 ) ) ;
#76009=DIRECTION ( 'NONE',  ( 0.000000000000000000, 0.8814952561688430555, -0.4721928772777346239 ) ) ;
#76053=AXIS2_PLACEMENT_3D ( 'NONE', #236505, #35772, #154450 ) ;
#76059=DIRECTION ( 'NONE',  ( 0.000000000000000000, 0.8814952561688431665, -0.4721928772777344019 ) ) ;
#76105=VECTOR ( 'NONE', #114521, 1000.000000000000000 ) ;
#76121=CARTESIAN_POINT ( 'NONE',  ( -18.36527282682001427, 38.27493327899719588, -261.1939576002376953 ) ) ;
#76190=CARTESIAN_POINT ( 'NONE',  ( 18.49505832270841310, 9.017683668627247684, -245.4513460378304899 ) ) ;
#76212=EDGE_CURVE ( 'NONE', #123298, #93557, #200898, .T. ) ;
#76214=ORIENTED_EDGE ( 'NONE', *, *, #63348, .T. ) ;
#76224=FACE_OUTER_BOUND ( 'NONE', #235719, .T. ) ;
#76246=DIRECTION ( 'NONE',  ( 1.000000000000000000, 0.000000000000000000, 0.000000000000000000 ) ) ;
#76285=EDGE_LOOP ( 'NONE', ( #89590, #203962, #148670, #159261 ) ) ;
#76321=CARTESIAN_POINT ( 'NONE',  ( 23.14999999999999858, 35.66731937946610742, -251.4023027391979497 ) ) ;
#76323=EDGE_LOOP ( 'NONE', ( #202930, #74798, #174971 ) ) ;
#76333=FACE_OUTER_BOUND ( 'NONE', #215750, .T. ) ;
#76366=CIRCLE ( 'NONE', #1542, 0.1000000000000031558 ) ;
#76383=CARTESIAN_POINT ( 'NONE',  ( 18.40000000000000213, 8.780520186313284015, -245.4165333277510115 ) ) ;
#76391=AXIS2_PLACEMENT_3D ( 'NONE', #22477, #44593, #225766 ) ;
#76411=ORIENTED_EDGE ( 'NONE', *, *, #249926, .T. ) ;
#76431=CARTESIAN_POINT ( 'NONE',  ( -18.39999999999999858, 8.841736820195468027, -245.4273993276875956 ) ) ;
#76435=DIRECTION ( 'NONE',  ( 0.000000000000000000, 0.4721928772777351790, 0.8814952561688427224 ) ) ;
#76441=CARTESIAN_POINT ( 'NONE',  ( 21.05000000000000071, 10.05622153401856522, -228.2005611962535454 ) ) ;
#76460=CARTESIAN_POINT ( 'NONE',  ( -18.59999999999999787, 31.49702336731128582, -233.4564499823349877 ) ) ;
#76461=CIRCLE ( 'NONE', #226289, 12.87500000000000711 ) ;
#76498=EDGE_CURVE ( 'NONE', #214842, #109178, #53017, .T. ) ;
#76506=AXIS2_PLACEMENT_3D ( 'NONE', #252712, #94923, #177069 ) ;
#76536=DIRECTION ( 'NONE',  ( 0.000000000000000000, -0.4721928772777346239, -0.8814952561688430555 ) ) ;
#76540=FACE_OUTER_BOUND ( 'NONE', #186309, .T. ) ;
#76561=DIRECTION ( 'NONE',  ( -1.000000000000000000, 0.000000000000000000, 0.000000000000000000 ) ) ;
#76584=DIRECTION ( 'NONE',  ( 0.000000000000000000, -0.3488585713686311318, -0.9371753822965249725 ) ) ;
#76625=CARTESIAN_POINT ( 'NONE',  ( 21.05000000000000071, 18.65264105882984680, -228.0115894607347968 ) ) ;
#76631=CARTESIAN_POINT ( 'NONE',  ( 21.08804582317339893, 22.20750643078865139, -231.7382219064953404 ) ) ;
#76638=AXIS2_PLACEMENT_3D ( 'NONE', #193690, #149444, #131134 ) ;
#76641=CARTESIAN_POINT ( 'NONE',  ( 20.94999999999999929, 23.68770167995059239, -252.8127582590406348 ) ) ;
#76656=ADVANCED_FACE ( 'NONE', ( #214659 ), #197922, .T. ) ;
#76672=ORIENTED_EDGE ( 'NONE', *, *, #250111, .F. ) ;
#76681=DIRECTION ( 'NONE',  ( 0.000000000000000000, 0.8814952561688416122, -0.4721928772777371219 ) ) ;
#76740=DIRECTION ( 'NONE',  ( 6.484947573744953299E-15, 0.7674881895858254310, 0.6410630849193176273 ) ) ;
#76745=CARTESIAN_POINT ( 'NONE',  ( 21.09696443733127325, 22.97753277350960488, -230.0567122760072039 ) ) ;
#76756=VERTEX_POINT ( 'NONE', #223636 ) ;
#76774=DIRECTION ( 'NONE',  ( 0.000000000000000000, 0.8814952561688431665, -0.4721928772777346794 ) ) ;
#76848=CARTESIAN_POINT ( 'NONE',  ( -21.44999999999999929, 21.43869811404188752, -233.1734427395952025 ) ) ;
#76904=VERTEX_POINT ( 'NONE', #209225 ) ;
#76916=AXIS2_PLACEMENT_3D ( 'NONE', #226746, #145922, #105487 ) ;
#76924=AXIS2_PLACEMENT_3D ( 'NONE', #53001, #92135, #132556 ) ;
#76934=CARTESIAN_POINT ( 'NONE',  ( -20.54999999999999716, 19.73066058418984170, -238.2142830767208466 ) ) ;
#76950=DIRECTION ( 'NONE',  ( -3.265361837132813586E-16, 0.4721928772777346239, 0.8814952561688430555 ) ) ;
#77017=CARTESIAN_POINT ( 'NONE',  ( -21.37071067811865532, 29.58339010484111498, -236.6052874901905625 ) ) ;
#77019=AXIS2_PLACEMENT_3D ( 'NONE', #67844, #88668, #192610 ) ;
#77020=CARTESIAN_POINT ( 'NONE',  ( 20.95512820512820440, 22.85550638026972692, -230.1049725544161220 ) ) ;
#77023=FACE_OUTER_BOUND ( 'NONE', #84441, .T. ) ;
#77077=FACE_OUTER_BOUND ( 'NONE', #102464, .T. ) ;
#77111=FACE_OUTER_BOUND ( 'NONE', #188871, .T. ) ;
#77127=CARTESIAN_POINT ( 'NONE',  ( -23.15000000000000213, 28.50120599808395028, -258.2149742250584268 ) ) ;
#77168=EDGE_LOOP ( 'NONE', ( #147106, #78717, #150909, #239661 ) ) ;
#77174=CARTESIAN_POINT ( 'NONE',  ( 23.14999999999999858, 33.13294339707397285, -247.6623911921324463 ) ) ;
#77203=DIRECTION ( 'NONE',  ( -1.000000000000000000, 0.000000000000000000, 0.000000000000000000 ) ) ;
#77221=CIRCLE ( 'NONE', #198021, 0.1000000000000108025 ) ;
#77240=EDGE_LOOP ( 'NONE', ( #15339, #217903, #192812, #36426 ) ) ;
#77241=DIRECTION ( 'NONE',  ( 0.000000000000000000, 0.8814952561688430555, -0.4721928772777346239 ) ) ;
#77260=ORIENTED_EDGE ( 'NONE', *, *, #178726, .T. ) ;
#77265=CARTESIAN_POINT ( 'NONE',  ( -20.93975676684922504, 46.39397692848788068, -243.0687461883537424 ) ) ;
#77280=CARTESIAN_POINT ( 'NONE',  ( 23.15000000000000213, 11.31726856452598362, -246.8669175193824969 ) ) ;
#77292=AXIS2_PLACEMENT_3D ( 'NONE', #228487, #103364, #102434 ) ;
#77294=EDGE_CURVE ( 'NONE', #101453, #97478, #112092, .T. ) ;
#77312=EDGE_CURVE ( 'NONE', #245302, #109034, #91783, .T. ) ;
#77340=AXIS2_PLACEMENT_3D ( 'NONE', #90377, #168696, #246886 ) ;
#77377=EDGE_LOOP ( 'NONE', ( #45230, #22770, #197729, #183300 ) ) ;
#77388=EDGE_CURVE ( 'NONE', #60388, #137538, #167018, .T. ) ;
#77409=AXIS2_PLACEMENT_3D ( 'NONE', #225121, #127332, #223842 ) ;
#77447=DIRECTION ( 'NONE',  ( 0.000000000000000000, -0.4721928772777346239, -0.8814952561688430555 ) ) ;
#77449=ORIENTED_EDGE ( 'NONE', *, *, #176193, .F. ) ;
#77460=LINE ( 'NONE', #236551, #137046 ) ;
#77465=CARTESIAN_POINT ( 'NONE',  ( 21.08134388332232234, 10.05319037393296355, -228.1129092785580781 ) ) ;
#77467=CYLINDRICAL_SURFACE ( 'NONE', #151421, 11.80000000000000782 ) ;
#77513=LINE ( 'NONE', #179240, #119747 ) ;
#77525=CIRCLE ( 'NONE', #73315, 3.999999999999994671 ) ;
#77535=CARTESIAN_POINT ( 'NONE',  ( -21.44999999999999929, 29.24307565605548120, -237.2405905340223455 ) ) ;
#77562=DIRECTION ( 'NONE',  ( -1.000000000000000000, -5.641646265808601873E-14, 4.044497296483820071E-14 ) ) ;
#77569=ADVANCED_FACE ( 'NONE', ( #107905 ), #187467, .F. ) ;
#77580=FACE_OUTER_BOUND ( 'NONE', #159364, .T. ) ;
#77583=LINE ( 'NONE', #212004, #175731 ) ;
#77601=ORIENTED_EDGE ( 'NONE', *, *, #38713, .F. ) ;
#77641=CARTESIAN_POINT ( 'NONE',  ( 23.14999999999999858, 21.15538238767524604, -233.7023398932965108 ) ) ;
#77646=ADVANCED_FACE ( 'NONE', ( #132617 ), #150885, .F. ) ;
#77666=AXIS2_PLACEMENT_3D ( 'NONE', #245554, #123036, #162177 ) ;
#77671=ORIENTED_EDGE ( 'NONE', *, *, #224251, .F. ) ;
#77686=AXIS2_PLACEMENT_3D ( 'NONE', #248204, #189522, #254589 ) ;
#77705=CARTESIAN_POINT ( 'NONE',  ( -18.41799967126726756, 8.841737187388694963, -245.4273995243829347 ) ) ;
#77717=AXIS2_PLACEMENT_3D ( 'NONE', #128494, #31984, #51489 ) ;
#77718=VERTEX_POINT ( 'NONE', #196424 ) ;
#77749=( NAMED_UNIT ( * ) PLANE_ANGLE_UNIT ( ) SI_UNIT ( $, .RADIAN. ) );
#77797=EDGE_CURVE ( 'NONE', #202163, #253241, #34385, .T. ) ;
#77798=ORIENTED_EDGE ( 'NONE', *, *, #184198, .F. ) ;
#77800=VECTOR ( 'NONE', #182781, 1000.000000000000114 ) ;
#77848=CARTESIAN_POINT ( 'NONE',  ( 23.14999999999999503, 28.86532135423329493, -237.9457867389574517 ) ) ;
#77876=DIRECTION ( 'NONE',  ( 0.000000000000000000, -0.8814952561688430555, 0.4721928772777346239 ) ) ;
#77881=ORIENTED_EDGE ( 'NONE', *, *, #240250, .F. ) ;
#77886=EDGE_CURVE ( 'NONE', #97681, #126765, #33117, .T. ) ;
#77959=DIRECTION ( 'NONE',  ( 0.000000000000000000, 0.9994937237965558774, 0.03181660087586650476 ) ) ;
#77971=ORIENTED_EDGE ( 'NONE', *, *, #207808, .T. ) ;
#77987=CARTESIAN_POINT ( 'NONE',  ( 23.15000000000000213, 11.60058429089262333, -246.3380203656811887 ) ) ;
#78025=ADVANCED_FACE ( 'NONE', ( #255912 ), #18642, .T. ) ;
#78030=CIRCLE ( 'NONE', #19808, 0.5000000000000008882 ) ;
#78072=CARTESIAN_POINT ( 'NONE',  ( 18.57071067811864040, 30.75534497283957691, -234.8410239939103406 ) ) ;
#78074=ORIENTED_EDGE ( 'NONE', *, *, #3426, .T. ) ;
#78082=ORIENTED_EDGE ( 'NONE', *, *, #172499, .T. ) ;
#78153=DIRECTION ( 'NONE',  ( 1.000000000000000000, 0.000000000000000000, 0.000000000000000000 ) ) ;
#78173=LINE ( 'NONE', #252963, #46463 ) ;
#78221=CARTESIAN_POINT ( 'NONE',  ( 23.14999999999999503, 29.00069016757795026, -237.9048565010683376 ) ) ;
#78223=EDGE_CURVE ( 'NONE', #254810, #205457, #217853, .T. ) ;
#78231=CARTESIAN_POINT ( 'NONE',  ( 20.02499999999999858, 30.46448808713892831, -235.1722212069449256 ) ) ;
#78237=TOROIDAL_SURFACE ( 'NONE', #248949, 11.65000000000000036, 0.1000000000000000056 ) ;
#78301=ORIENTED_EDGE ( 'NONE', *, *, #112233, .T. ) ;
#78317=ORIENTED_EDGE ( 'NONE', *, *, #248168, .T. ) ;
#78368=CARTESIAN_POINT ( 'NONE',  ( 21.05000000000000071, 4.260086453440762533, -245.2296700999207246 ) ) ;
#78373=VECTOR ( 'NONE', #46314, 1000.000000000000000 ) ;
#78403=CIRCLE ( 'NONE', #32684, 0.1000000000000091649 ) ;
#78408=EDGE_CURVE ( 'NONE', #2075, #237152, #109656, .T. ) ;
#78427=AXIS2_PLACEMENT_3D ( 'NONE', #224897, #248330, #145370 ) ;
#78450=CYLINDRICAL_SURFACE ( 'NONE', #103772, 0.1000000000000076522 ) ;
#78466=CARTESIAN_POINT ( 'NONE',  ( 22.39999999999999858, 10.71943444926881561, -226.8179467668883547 ) ) ;
#78474=ADVANCED_FACE ( 'NONE', ( #17222 ), #113830, .T. ) ;
#78568=DIRECTION ( 'NONE',  ( 1.000000000000000000, 0.000000000000000000, 0.000000000000000000 ) ) ;
#78573=VERTEX_POINT ( 'NONE', #58868 ) ;
#78671=CARTESIAN_POINT ( 'NONE',  ( 18.39999999999999858, 38.03205796367814173, -261.1772988674111957 ) ) ;
#78681=AXIS2_PLACEMENT_3D ( 'NONE', #129256, #125410, #9300 ) ;
#78717=ORIENTED_EDGE ( 'NONE', *, *, #140223, .F. ) ;
#78719=VECTOR ( 'NONE', #127630, 1000.000000000000114 ) ;
#78725=CIRCLE ( 'NONE', #178558, 0.1000000000000013933 ) ;
#78776=CARTESIAN_POINT ( 'NONE',  ( -23.25000000000000000, 10.78703865319380206, -235.6923017531418623 ) ) ;
#78783=FACE_OUTER_BOUND ( 'NONE', #81451, .T. ) ;
#78809=CIRCLE ( 'NONE', #12233, 0.1000000000000013933 ) ;
#78884=DIRECTION ( 'NONE',  ( 0.000000000000000000, 0.8814952561688431665, -0.4721928772777346794 ) ) ;
#78905=FACE_OUTER_BOUND ( 'NONE', #175556, .T. ) ;
#78910=VERTEX_POINT ( 'NONE', #221175 ) ;
#78915=DIRECTION ( 'NONE',  ( 0.000000000000000000, 0.8814952561688437216, -0.4721928772777334582 ) ) ;
#78918=LINE ( 'NONE', #179355, #111486 ) ;
#78946=ADVANCED_FACE ( 'NONE', ( #60816 ), #84181, .T. ) ;
#78968=CARTESIAN_POINT ( 'NONE',  ( -23.15000000000000213, 24.26958830762006869, -252.6664436919618879 ) ) ;
#78974=CARTESIAN_POINT ( 'NONE',  ( -18.48550754432023169, 8.873758098311299136, -245.4030316389878124 ) ) ;
#78985=ORIENTED_EDGE ( 'NONE', *, *, #186901, .T. ) ;
#78988=DIRECTION ( 'NONE',  ( 0.000000000000000000, -0.8814952561688429444, 0.4721928772777345684 ) ) ;
#78999=CIRCLE ( 'NONE', #133040, 0.09999999999999939493 ) ;
#79046=DIRECTION ( 'NONE',  ( 0.000000000000000000, -0.3343365196859449662, 0.9424537609900497381 ) ) ;
#79055=FACE_OUTER_BOUND ( 'NONE', #184589, .T. ) ;
#79069=CYLINDRICAL_SURFACE ( 'NONE', #19215, 0.09999999999999939493 ) ;
#79086=CARTESIAN_POINT ( 'NONE',  ( -20.94999999999999929, 28.60154115857408641, -258.4512230915049713 ) ) ;
#79099=VERTEX_POINT ( 'NONE', #107655 ) ;
#79106=DIRECTION ( 'NONE',  ( 0.000000000000000000, -0.8814952561688430555, 0.4721928772777346239 ) ) ;
#79148=AXIS2_PLACEMENT_3D ( 'NONE', #152891, #233687, #53751 ) ;
#79222=CARTESIAN_POINT ( 'NONE',  ( 18.47149038651510722, 37.97416073834201455, -261.2273484851261856 ) ) ;
#79224=FACE_OUTER_BOUND ( 'NONE', #53640, .T. ) ;
#79228=EDGE_LOOP ( 'NONE', ( #93204, #188963, #121333 ) ) ;
#79266=FACE_OUTER_BOUND ( 'NONE', #156006, .T. ) ;
#79280=FACE_OUTER_BOUND ( 'NONE', #111875, .T. ) ;
#79285=EDGE_CURVE ( 'NONE', #98428, #54594, #248431, .T. ) ;
#79307=VECTOR ( 'NONE', #121187, 999.9999999999998863 ) ;
#79309=EDGE_CURVE ( 'NONE', #108480, #220499, #227573, .T. ) ;
#79316=EDGE_LOOP ( 'NONE', ( #248420, #98528, #107873, #802, #243806, #165060, #70995, #129712, #83970, #177240, #181090 ) ) ;
#79317=ORIENTED_EDGE ( 'NONE', *, *, #243765, .T. ) ;
#79322=CARTESIAN_POINT ( 'NONE',  ( 20.85882249326303040, 46.46967969402478360, -243.0849751855955674 ) ) ;
#79332=AXIS2_PLACEMENT_3D ( 'NONE', #59437, #5577, #96028 ) ;
#79375=CARTESIAN_POINT ( 'NONE',  ( -20.94999999999999929, 43.16050967218924939, -245.0573091940785844 ) ) ;
#79388=DIRECTION ( 'NONE',  ( 0.000000000000000000, -0.8814952561688430555, 0.4721928772777346239 ) ) ;
#79401=CARTESIAN_POINT ( 'NONE',  ( -21.65000000000000213, 21.56708615768143034, -232.7219885528102736 ) ) ;
#79417=EDGE_CURVE ( 'NONE', #182938, #92704, #114717, .T. ) ;
#79431=DIRECTION ( 'NONE',  ( 2.840903330521632762E-16, -0.8454177738465994407, -0.5341055959866553016 ) ) ;
#79441=ORIENTED_EDGE ( 'NONE', *, *, #209888, .F. ) ;
#79509=ORIENTED_EDGE ( 'NONE', *, *, #146724, .F. ) ;
#79520=DIRECTION ( 'NONE',  ( 0.000000000000000000, 0.8814952561688430555, -0.4721928772777346239 ) ) ;
#79550=AXIS2_PLACEMENT_3D ( 'NONE', #141462, #137591, #59320 ) ;
#79558=FACE_OUTER_BOUND ( 'NONE', #178516, .T. ) ;
#79571=DIRECTION ( 'NONE',  ( -0.7071067811865708874, 0.3338907855511046296, 0.6233112732207185536 ) ) ;
#79572=VERTEX_POINT ( 'NONE', #250709 ) ;
#79582=DIRECTION ( 'NONE',  ( -0.000000000000000000, 0.4721928772777345684, 0.8814952561688429444 ) ) ;
#79601=CIRCLE ( 'NONE', #175503, 0.1000000000000012546 ) ;
#79602=ORIENTED_EDGE ( 'NONE', *, *, #42869, .F. ) ;
#79616=CIRCLE ( 'NONE', #63057, 0.5000000000000048850 ) ;
#79637=EDGE_CURVE ( 'NONE', #205457, #137667, #36257, .T. ) ;
#79684=ORIENTED_EDGE ( 'NONE', *, *, #108378, .T. ) ;
#79686=DIRECTION ( 'NONE',  ( -1.000000000000000000, 0.000000000000000000, 0.000000000000000000 ) ) ;
#79687=FACE_OUTER_BOUND ( 'NONE', #123514, .T. ) ;
#79710=CARTESIAN_POINT ( 'NONE',  ( 22.39999999999999503, 0.3085173699977246109, -229.9658011520297975 ) ) ;
#79722=CARTESIAN_POINT ( 'NONE',  ( 18.59999999999999076, 43.30036367478129478, -245.0872390055602352 ) ) ;
#79766=DIRECTION ( 'NONE',  ( -1.000000000000000000, -7.166229603267618227E-16, -4.447280054184918885E-16 ) ) ;
#79774=EDGE_LOOP ( 'NONE', ( #221142, #212136, #161806, #212068 ) ) ;
#79831=FACE_OUTER_BOUND ( 'NONE', #97506, .T. ) ;
#79852=ORIENTED_EDGE ( 'NONE', *, *, #228413, .T. ) ;
#79868=EDGE_CURVE ( 'NONE', #135120, #246187, #104454, .T. ) ;
#79875=LINE ( 'NONE', #98147, #22962 ) ;
#79902=DIRECTION ( 'NONE',  ( -0.000000000000000000, -0.8814952561688430555, 0.4721928772777346239 ) ) ;
#79941=AXIS2_PLACEMENT_3D ( 'NONE', #18359, #196979, #96582 ) ;
#79945=DIRECTION ( 'NONE',  ( 0.000000000000000000, 0.8814952561688430555, -0.4721928772777346239 ) ) ;
#79960=CARTESIAN_POINT ( 'NONE',  ( -21.29999999999995808, 10.69888912757691024, -235.6450824654141059 ) ) ;
#80022=CARTESIAN_POINT ( 'NONE',  ( 23.14999999999999858, 36.65892442174935439, -249.5511627012433848 ) ) ;
#80039=ORIENTED_EDGE ( 'NONE', *, *, #48872, .F. ) ;
#80079=DIRECTION ( 'NONE',  ( 0.000000000000000000, -0.8814952561688428334, 0.4721928772777350680 ) ) ;
#80104=ORIENTED_EDGE ( 'NONE', *, *, #80202, .F. ) ;
#80119=DIRECTION ( 'NONE',  ( -1.000000000000000000, -0.000000000000000000, -0.000000000000000000 ) ) ;
#80123=CARTESIAN_POINT ( 'NONE',  ( 23.24999999999999645, 19.82851818057134707, -235.1178474969725016 ) ) ;
#80130=DIRECTION ( 'NONE',  ( 0.000000000000000000, 0.8814952561688430555, -0.4721928772777346239 ) ) ;
#80136=ORIENTED_EDGE ( 'NONE', *, *, #214614, .T. ) ;
#80192=CIRCLE ( 'NONE', #225940, 0.1000000000000013933 ) ;
#80201=CARTESIAN_POINT ( 'NONE',  ( -18.50000000000000000, -1.293555411365099994, -227.7000673772910204 ) ) ;
#80202=EDGE_CURVE ( 'NONE', #13871, #75744, #3798, .T. ) ;
#80214=EDGE_CURVE ( 'NONE', #226091, #62371, #186296, .T. ) ;
#80240=CARTESIAN_POINT ( 'NONE',  ( 21.40925344232283223, 1.306104126701115531, -230.5013720119504228 ) ) ;
#80260=LINE ( 'NONE', #175568, #106060 ) ;
#80267=EDGE_LOOP ( 'NONE', ( #124524, #196639, #150185, #220793 ) ) ;
#80317=CARTESIAN_POINT ( 'NONE',  ( -20.94999999999999929, 36.65892442174935439, -249.5511627012433848 ) ) ;
#80327=AXIS2_PLACEMENT_3D ( 'NONE', #67439, #227794, #127423 ) ;
#80330=DIRECTION ( 'NONE',  ( 0.000000000000000000, 0.9371753822965326330, -0.3488585713686107592 ) ) ;
#80373=ORIENTED_EDGE ( 'NONE', *, *, #239385, .T. ) ;
#80380=ORIENTED_EDGE ( 'NONE', *, *, #94470, .F. ) ;
#80398=CARTESIAN_POINT ( 'NONE',  ( -22.49806830649814415, 12.56154382881637943, -223.4268007483960616 ) ) ;
#80405=CARTESIAN_POINT ( 'NONE',  ( -20.54999999999999716, 21.39147882631411335, -233.2615922652120730 ) ) ;
#80417=CARTESIAN_POINT ( 'NONE',  ( -22.50000000000000000, -3.092988775432913506, -228.1437074281570858 ) ) ;
#80437=AXIS2_PLACEMENT_3D ( 'NONE', #145219, #244322, #128248 ) ;
#80449=DIRECTION ( 'NONE',  ( 0.000000000000000000, -0.8368562265788574983, -0.5474227397872651890 ) ) ;
#80494=ORIENTED_EDGE ( 'NONE', *, *, #152050, .T. ) ;
#80522=CARTESIAN_POINT ( 'NONE',  ( 20.94999999999999574, 7.128833340093095217, -233.7327013124392749 ) ) ;
#80546=ORIENTED_EDGE ( 'NONE', *, *, #97573, .T. ) ;
#80558=DIRECTION ( 'NONE',  ( 0.000000000000000000, 0.8814952561688430555, -0.4721928772777346239 ) ) ;
#80605=DIRECTION ( 'NONE',  ( 0.000000000000000000, 0.8814952561688476074, -0.4721928772777262417 ) ) ;
#80620=EDGE_CURVE ( 'NONE', #59200, #250188, #253250, .T. ) ;
#80621=AXIS2_PLACEMENT_3D ( 'NONE', #123356, #239452, #158654 ) ;
#80643=EDGE_LOOP ( 'NONE', ( #215360, #105686, #225130, #56930 ) ) ;
#80650=CARTESIAN_POINT ( 'NONE',  ( 20.85000000000000142, 46.02130280899747561, -256.6489974955837852 ) ) ;
#80666=CARTESIAN_POINT ( 'NONE',  ( -22.16821283564876666, 10.69812671114206282, -227.0695021710342871 ) ) ;
#80671=AXIS2_PLACEMENT_3D ( 'NONE', #116320, #173767, #91604 ) ;
#80840=DIRECTION ( 'NONE',  ( 0.000000000000000000, -0.9901894034181596416, -0.1397316906016281834 ) ) ;
#80868=AXIS2_PLACEMENT_3D ( 'NONE', #77017, #135699, #79571 ) ;
#80869=DIRECTION ( 'NONE',  ( -5.551115123125807946E-13, -0.4608403197577645716, -0.8874830700839093645 ) ) ;
#80901=AXIS2_PLACEMENT_3D ( 'NONE', #38323, #57852, #83503 ) ;
#80906=EDGE_CURVE ( 'NONE', #182351, #112914, #144919, .T. ) ;
#80928=DIRECTION ( 'NONE',  ( 0.000000000000000000, 0.8814952561688436106, -0.4721928772777334027 ) ) ;
#80936=EDGE_CURVE ( 'NONE', #7289, #176897, #146210, .T. ) ;
#80954=EDGE_LOOP ( 'NONE', ( #220887, #60271, #158317, #202469 ) ) ;
#80962=AXIS2_PLACEMENT_3D ( 'NONE', #116756, #13806, #33410 ) ;
#80992=CARTESIAN_POINT ( 'NONE',  ( 22.39999999999999503, 12.67709964810648238, -223.3751320524553705 ) ) ;
#81025=FACE_OUTER_BOUND ( 'NONE', #108968, .T. ) ;
#81035=DIRECTION ( 'NONE',  ( 6.938893903907222856E-15, -0.4721928772777343464, -0.8814952561688431665 ) ) ;
#81044=CIRCLE ( 'NONE', #47916, 0.1000000000000053346 ) ;
#81047=DIRECTION ( 'NONE',  ( -0.000000000000000000, -0.8814952561688430555, 0.4721928772777346239 ) ) ;
#81048=ORIENTED_EDGE ( 'NONE', *, *, #226216, .F. ) ;
#81049=CYLINDRICAL_SURFACE ( 'NONE', #29948, 12.87500000000000178 ) ;
#81060=ADVANCED_FACE ( 'NONE', ( #233487 ), #57371, .F. ) ;
#81110=DIRECTION ( 'NONE',  ( 1.224646799147353700E-16, 0.4721928772777346239, 0.8814952561688430555 ) ) ;
#81128=ORIENTED_EDGE ( 'NONE', *, *, #106119, .T. ) ;
#81131=ORIENTED_EDGE ( 'NONE', *, *, #133779, .F. ) ;
#81135=ORIENTED_EDGE ( 'NONE', *, *, #212258, .T. ) ;
#81146=CARTESIAN_POINT ( 'NONE',  ( 23.24999999999999289, 23.34004772283015683, -229.2004250369967338 ) ) ;
#81182=CARTESIAN_POINT ( 'NONE',  ( 21.30000000000002558, 10.69888912757691024, -235.6450824654141059 ) ) ;
#81229=VERTEX_POINT ( 'NONE', #63816 ) ;
#81278=AXIS2_PLACEMENT_3D ( 'NONE', #108073, #7696, #28585 ) ;
#81279=FACE_OUTER_BOUND ( 'NONE', #77240, .T. ) ;
#81287=VERTEX_POINT ( 'NONE', #126347 ) ;
#81337=ADVANCED_FACE ( 'NONE', ( #84609 ), #65999, .T. ) ;
#81359=DIRECTION ( 'NONE',  ( 0.000000000000000000, 0.8814952561688359500, -0.4721928772777478911 ) ) ;
#81379=EDGE_LOOP ( 'NONE', ( #126164, #234557, #74812, #39217 ) ) ;
#81396=ADVANCED_FACE ( 'NONE', ( #113204 ), #110638, .F. ) ;
#81409=AXIS2_PLACEMENT_3D ( 'NONE', #204544, #7641, #85851 ) ;
#81412=FACE_OUTER_BOUND ( 'NONE', #105489, .T. ) ;
#81415=EDGE_CURVE ( 'NONE', #140599, #72959, #228706, .T. ) ;
#81451=EDGE_LOOP ( 'NONE', ( #57393, #254939, #171228, #211165, #199702, #43794, #3490 ) ) ;
#81502=ORIENTED_EDGE ( 'NONE', *, *, #232590, .T. ) ;
#81506=CARTESIAN_POINT ( 'NONE',  ( 21.05000000000000071, 21.98309897467606433, -231.7335930323676791 ) ) ;
#81534=FACE_OUTER_BOUND ( 'NONE', #23195, .T. ) ;
#81559=EDGE_CURVE ( 'NONE', #178121, #217322, #128729, .T. ) ;
#81573=AXIS2_PLACEMENT_3D ( 'NONE', #2336, #242239, #121055 ) ;
#81576=EDGE_CURVE ( 'NONE', #22846, #137667, #86994, .T. ) ;
#81579=CIRCLE ( 'NONE', #2501, 0.1000000000000013933 ) ;
#81615=CARTESIAN_POINT ( 'NONE',  ( -20.94999999999999929, 36.18002604163306302, -236.0784499204090991 ) ) ;
#81625=DIRECTION ( 'NONE',  ( 0.000000000000000000, -0.8814952561688430555, 0.4721928772777346239 ) ) ;
#81676=VERTEX_POINT ( 'NONE', #143008 ) ;
#81716=ORIENTED_EDGE ( 'NONE', *, *, #126761, .F. ) ;
#81726=CARTESIAN_POINT ( 'NONE',  ( 20.95595012432476523, 18.83168586542424094, -227.9718358157221019 ) ) ;
#81744=DIRECTION ( 'NONE',  ( -0.000000000000000000, 0.8814952561688430555, -0.4721928772777346239 ) ) ;
#81748=CIRCLE ( 'NONE', #144118, 0.09999999999999022171 ) ;
#81786=CARTESIAN_POINT ( 'NONE',  ( -23.25000000000000000, 25.94586868676353575, -241.5435999122864530 ) ) ;
#81811=EDGE_CURVE ( 'NONE', #25443, #236903, #174755, .T. ) ;
#81827=CARTESIAN_POINT ( 'NONE',  ( -18.58671080940900566, 8.966855012152855409, -245.3888429975481813 ) ) ;
#81830=ORIENTED_EDGE ( 'NONE', *, *, #180699, .F. ) ;
#81847=DIRECTION ( 'NONE',  ( -0.000000000000000000, 0.4721928772777346239, 0.8814952561688430555 ) ) ;
#81864=ORIENTED_EDGE ( 'NONE', *, *, #215891, .T. ) ;
#81867=CARTESIAN_POINT ( 'NONE',  ( 20.94999999999999929, 28.58935552370083144, -258.2621935127861548 ) ) ;
#81877=DIRECTION ( 'NONE',  ( 2.557131231893036492E-16, -0.8496786552930076786, -0.5273008465188218086 ) ) ;
#81887=ADVANCED_FACE ( 'NONE', ( #110305 ), #237252, .T. ) ;
#81893=CARTESIAN_POINT ( 'NONE',  ( 20.04142135623730070, 31.44980407958351165, -233.5445995079518866 ) ) ;
#81907=DIRECTION ( 'NONE',  ( 0.000000000000000000, 0.8814952561688476074, -0.4721928772777262417 ) ) ;
#81917=DIRECTION ( 'NONE',  ( 0.000000000000000000, 0.4721928772777346239, 0.8814952561688430555 ) ) ;
#81919=CARTESIAN_POINT ( 'NONE',  ( -18.59999999999999787, 13.71992543034163958, -238.5823796952984992 ) ) ;
#82000=EDGE_CURVE ( 'NONE', #214701, #140884, #70674, .T. ) ;
#82004=CARTESIAN_POINT ( 'NONE',  ( 23.14999999999999858, 28.52545328903799415, -239.5221046041717443 ) ) ;
#82018=DIRECTION ( 'NONE',  ( 0.000000000000000000, 0.8814952561688437216, -0.4721928772777331806 ) ) ;
#82021=EDGE_CURVE ( 'NONE', #209722, #15820, #100967, .T. ) ;
#82063=EDGE_LOOP ( 'NONE', ( #21566, #108230, #164569, #104281 ) ) ;
#82099=ORIENTED_EDGE ( 'NONE', *, *, #162146, .F. ) ;
#82107=CARTESIAN_POINT ( 'NONE',  ( 18.46905048506369695, 38.07034010913391597, -261.0545764982895776 ) ) ;
#82119=CARTESIAN_POINT ( 'NONE',  ( -18.50000000000000000, 19.09764897702175546, -235.7051342141560042 ) ) ;
#82122=DIRECTION ( 'NONE',  ( 0.000000000000000000, -0.4721928772777344019, -0.8814952561688432775 ) ) ;
#82132=CARTESIAN_POINT ( 'NONE',  ( -21.65000000000000213, 21.67479455268075128, -232.7326951115107647 ) ) ;
#82170=FACE_OUTER_BOUND ( 'NONE', #35133, .T. ) ;
#82182=ADVANCED_FACE ( 'NONE', ( #107441 ), #187006, .T. ) ;
#82196=ORIENTED_EDGE ( 'NONE', *, *, #10092, .T. ) ;
#82216=DIRECTION ( 'NONE',  ( -0.000000000000000000, -0.4721928772777346794, -0.8814952561688431665 ) ) ;
#82237=VERTEX_POINT ( 'NONE', #249538 ) ;
#82258=VERTEX_POINT ( 'NONE', #252087 ) ;
#82292=CARTESIAN_POINT ( 'NONE',  ( 18.60000000000000497, 7.128833340093095217, -233.7327013124392749 ) ) ;
#82354=ORIENTED_EDGE ( 'NONE', *, *, #166282, .F. ) ;
#82377=VERTEX_POINT ( 'NONE', #158176 ) ;
#82424=ORIENTED_EDGE ( 'NONE', *, *, #146560, .F. ) ;
#82433=DIRECTION ( 'NONE',  ( -1.000000000000000000, -0.000000000000000000, -0.000000000000000000 ) ) ;
#82452=CARTESIAN_POINT ( 'NONE',  ( -1.820710678118657944, 24.25730123604973087, -254.1720964594295538 ) ) ;
#82473=AXIS2_PLACEMENT_3D ( 'NONE', #124293, #244206, #145110 ) ;
#82521=EDGE_LOOP ( 'NONE', ( #171071, #219368, #244495, #80380 ) ) ;
#82565=CARTESIAN_POINT ( 'NONE',  ( -23.15000000000000213, 27.91464654983916205, -239.9322955902566719 ) ) ;
#82581=CARTESIAN_POINT ( 'NONE',  ( -23.25000000000000000, 7.128833340093095217, -233.7327013124392749 ) ) ;
#82648=PLANE ( 'NONE',  #181698 ) ;
#82655=AXIS2_PLACEMENT_3D ( 'NONE', #120804, #142878, #21688 ) ;
#82725=LINE ( 'NONE', #41097, #71666 ) ;
#82740=CYLINDRICAL_SURFACE ( 'NONE', #132523, 0.1000000000000089151 ) ;
#82776=AXIS2_PLACEMENT_3D ( 'NONE', #39677, #236550, #158349 ) ;
#82786=AXIS2_PLACEMENT_3D ( 'NONE', #92557, #174730, #95140 ) ;
#82791=( BOUNDED_SURFACE ( )  B_SPLINE_SURFACE ( 3, 2, ( 
 ( #111436, #113991, #73625 ),
 ( #13625, #93145, #54026 ),
 ( #193552, #87993, #227521 ),
 ( #48888, #128434, #188401 ) ),
 .UNSPECIFIED., .F., .F., .F. ) 
 B_SPLINE_SURFACE_WITH_KNOTS ( ( 4, 4 ),
 ( 3, 3 ),
 ( 0.0006461284895273852530, 0.0007503702773986309620 ),
 ( 0.000000000000000000, 1.000000000000000000 ),
 .UNSPECIFIED. ) 
 GEOMETRIC_REPRESENTATION_ITEM ( )  RATIONAL_B_SPLINE_SURFACE ( (
 ( 1.000000000000000000, 0.7071067811865561215, 1.000000000000000000),
 ( 1.000000000000000000, 0.7076476444647564756, 1.000000000000000000),
 ( 1.000000000000000000, 0.7075727925193199264, 1.000000000000000000),
 ( 1.000000000000000000, 0.7071067811865359154, 1.000000000000000000) ) ) 
 REPRESENTATION_ITEM ( '' )  SURFACE ( )  );
#82824=FACE_OUTER_BOUND ( 'NONE', #134108, .T. ) ;
#82849=FACE_OUTER_BOUND ( 'NONE', #227619, .T. ) ;
#82852=ADVANCED_FACE ( 'NONE', ( #208183 ), #91857, .F. ) ;
#82859=EDGE_CURVE ( 'NONE', #76904, #205599, #124786, .T. ) ;
#82872=CARTESIAN_POINT ( 'NONE',  ( 20.94999999999999929, 30.43677443282724937, -239.5249545687858870 ) ) ;
#82897=EDGE_CURVE ( 'NONE', #18238, #41248, #67373, .T. ) ;
#82905=ADVANCED_FACE ( 'NONE', ( #146881 ), #226417, .F. ) ;
#82906=AXIS2_PLACEMENT_3D ( 'NONE', #120237, #243986, #65352 ) ;
#82920=EDGE_LOOP ( 'NONE', ( #132877, #115338, #54561 ) ) ;
#82928=DIRECTION ( 'NONE',  ( -0.000000000000000000, 0.4721928772777345684, 0.8814952561688429444 ) ) ;
#82949=AXIS2_PLACEMENT_3D ( 'NONE', #111461, #73649, #252241 ) ;
#82994=CARTESIAN_POINT ( 'NONE',  ( -18.59999999999999787, 31.44980407958351165, -233.5445995079518866 ) ) ;
#83004=LINE ( 'NONE', #162594, #184905 ) ;
#83041=ORIENTED_EDGE ( 'NONE', *, *, #244043, .T. ) ;
#83048=DIRECTION ( 'NONE',  ( 0.000000000000000000, 0.8814952561688438326, -0.4721928772777334582 ) ) ;
#83063=CARTESIAN_POINT ( 'NONE',  ( 21.05000000000000071, 28.32080209959243788, -238.8452605374484676 ) ) ;
#83075=ORIENTED_EDGE ( 'NONE', *, *, #23990, .T. ) ;
#83115=CIRCLE ( 'NONE', #58006, 0.4999999999999978351 ) ;
#83119=CARTESIAN_POINT ( 'NONE',  ( 18.39999999999999858, 8.780520186313291120, -245.4165333277510115 ) ) ;
#83122=CARTESIAN_POINT ( 'NONE',  ( 20.96077737575343747, 36.10128815642510602, -236.0658802525694568 ) ) ;
#83137=ORIENTED_EDGE ( 'NONE', *, *, #171033, .F. ) ;
#83147=ORIENTED_EDGE ( 'NONE', *, *, #19678, .F. ) ;
#83168=ADVANCED_FACE ( 'NONE', ( #76333 ), #237984, .F. ) ;
#83188=VERTEX_POINT ( 'NONE', #235413 ) ;
#83204=CARTESIAN_POINT ( 'NONE',  ( -20.94999999999999929, 4.272272088314018390, -245.4186996786394843 ) ) ;
#83234=( BOUNDED_CURVE ( )  B_SPLINE_CURVE ( 3, ( #106525, #21886, #201792, #72578 ),
 .UNSPECIFIED., .F., .T. ) 
 B_SPLINE_CURVE_WITH_KNOTS ( ( 4, 4 ),
 ( 3.141592653589791784, 4.712388980384688786 ),
 .UNSPECIFIED. ) 
 CURVE ( )  GEOMETRIC_REPRESENTATION_ITEM ( )  RATIONAL_B_SPLINE_CURVE ( ( 1.000000000000000000, 0.8047378541243649375, 0.8047378541243649375, 1.000000000000000000 ) ) 
 REPRESENTATION_ITEM ( '' )  );
#83238=ORIENTED_EDGE ( 'NONE', *, *, #133135, .T. ) ;
#83245=CARTESIAN_POINT ( 'NONE',  ( 22.41477678272288188, -3.139831800996500721, -228.2311238840898397 ) ) ;
#83253=ORIENTED_EDGE ( 'NONE', *, *, #257141, .F. ) ;
#83280=DIRECTION ( 'NONE',  ( 1.000000000000000000, 3.448943450116721596E-16, 6.438528483529603700E-16 ) ) ;
#83332=CARTESIAN_POINT ( 'NONE',  ( 20.95203847575071521, 18.75769682750340905, -228.0491834549998771 ) ) ;
#83352=LINE ( 'NONE', #45545, #247061 ) ;
#83360=CIRCLE ( 'NONE', #70955, 0.09999999999999939493 ) ;
#83365=DIRECTION ( 'NONE',  ( 1.000000000000000000, 0.000000000000000000, 0.000000000000000000 ) ) ;
#83460=ORIENTED_EDGE ( 'NONE', *, *, #55181, .T. ) ;
#83470=EDGE_LOOP ( 'NONE', ( #153588, #72924, #156300, #163076 ) ) ;
#83473=CARTESIAN_POINT ( 'NONE',  ( -20.94999999999999929, 36.65892442174935439, -249.5511627012433848 ) ) ;
#83496=ORIENTED_EDGE ( 'NONE', *, *, #126329, .T. ) ;
#83502=TOROIDAL_SURFACE ( 'NONE', #245846, 0.2000000000000000111, 0.1000000000000000056 ) ;
#83503=DIRECTION ( 'NONE',  ( 0.000000000000000000, -0.8814952561688437216, 0.4721928772777334582 ) ) ;
#83505=DIRECTION ( 'NONE',  ( 0.000000000000000000, 0.8814952561688476074, -0.4721928772777262417 ) ) ;
#83514=AXIS2_PLACEMENT_3D ( 'NONE', #253703, #176767, #214579 ) ;
#83529=AXIS2_PLACEMENT_3D ( 'NONE', #49085, #206887, #128647 ) ;
#83541=AXIS2_PLACEMENT_3D ( 'NONE', #253308, #109947, #113807 ) ;
#83546=EDGE_LOOP ( 'NONE', ( #229868, #17284, #221729, #50902, #33565 ) ) ;
#83560=ORIENTED_EDGE ( 'NONE', *, *, #203819, .T. ) ;
#83576=CARTESIAN_POINT ( 'NONE',  ( 22.39999999999999503, 10.71943444926881384, -226.8179467668883831 ) ) ;
#83578=DIRECTION ( 'NONE',  ( 0.000000000000000000, 0.8814952561688437216, -0.4721928772777334582 ) ) ;
#83591=ORIENTED_EDGE ( 'NONE', *, *, #162978, .T. ) ;
#83592=AXIS2_PLACEMENT_3D ( 'NONE', #51808, #250034, #209625 ) ;
#83680=CARTESIAN_POINT ( 'NONE',  ( -20.94999999999999929, 46.01637179467461891, -256.6614375746592600 ) ) ;
#83686=VERTEX_POINT ( 'NONE', #223258 ) ;
#83696=EDGE_LOOP ( 'NONE', ( #217326, #145104, #83721, #190521 ) ) ;
#83721=ORIENTED_EDGE ( 'NONE', *, *, #22693, .T. ) ;
#83751=DIRECTION ( 'NONE',  ( -1.000000000000000000, -0.000000000000000000, -0.000000000000000000 ) ) ;
#83758=EDGE_LOOP ( 'NONE', ( #237857, #120986, #113601, #79317 ) ) ;
#83764=ORIENTED_EDGE ( 'NONE', *, *, #106969, .F. ) ;
#83787=ORIENTED_EDGE ( 'NONE', *, *, #89388, .T. ) ;
#83795=EDGE_CURVE ( 'NONE', #222562, #238367, #87544, .T. ) ;
#83877=CARTESIAN_POINT ( 'NONE',  ( -21.05000000000000071, 3.338403738567107926, -231.7022719401450388 ) ) ;
#83888=LINE ( 'NONE', #146456, #158835 ) ;
#83909=DIRECTION ( 'NONE',  ( 0.000000000000000000, 0.8814952561688430555, -0.4721928772777346239 ) ) ;
#83922=DIRECTION ( 'NONE',  ( 1.000000000000000000, 0.000000000000000000, 0.000000000000000000 ) ) ;
#83924=CARTESIAN_POINT ( 'NONE',  ( -21.05000000000000071, 4.260086453440760756, -245.2296700999207246 ) ) ;
#83952=EDGE_CURVE ( 'NONE', #195393, #135120, #191651, .T. ) ;
#83970=ORIENTED_EDGE ( 'NONE', *, *, #38786, .T. ) ;
#83989=DIRECTION ( 'NONE',  ( -1.000000000000000000, -0.000000000000000000, -0.000000000000000000 ) ) ;
#83996=CIRCLE ( 'NONE', #4903, 0.1000000000000013933 ) ;
#84014=AXIS2_PLACEMENT_3D ( 'NONE', #155173, #172184, #13082 ) ;
#84016=DIRECTION ( 'NONE',  ( 2.694716079187271467E-16, -0.4721928772777345129, -0.8814952561688430555 ) ) ;
#84025=CARTESIAN_POINT ( 'NONE',  ( -20.64999999999999858, 26.18196512540240661, -241.1028522842020152 ) ) ;
#84059=CIRCLE ( 'NONE', #21587, 0.4999999999999935607 ) ;
#84097=FACE_OUTER_BOUND ( 'NONE', #130664, .T. ) ;
#84108=DIRECTION ( 'NONE',  ( 0.000000000000000000, 0.8814952561688476074, -0.4721928772777262417 ) ) ;
#84152=FACE_OUTER_BOUND ( 'NONE', #202810, .T. ) ;
#84181=SPHERICAL_SURFACE ( 'NONE', #210645, 0.1000000000000000056 ) ;
#84183=AXIS2_PLACEMENT_3D ( 'NONE', #207335, #246445, #67802 ) ;
#84191=DIRECTION ( 'NONE',  ( 0.000000000000000000, -0.4721928772777285732, -0.8814952561688463861 ) ) ;
#84199=AXIS2_PLACEMENT_3D ( 'NONE', #171110, #155380, #75812 ) ;
#84213=ORIENTED_EDGE ( 'NONE', *, *, #136665, .F. ) ;
#84237=ORIENTED_EDGE ( 'NONE', *, *, #61772, .T. ) ;
#84257=DIRECTION ( 'NONE',  ( 1.000000000000000000, 0.000000000000000000, 0.000000000000000000 ) ) ;
#84270=FACE_OUTER_BOUND ( 'NONE', #77168, .T. ) ;
#84289=VERTEX_POINT ( 'NONE', #174611 ) ;
#84301=DIRECTION ( 'NONE',  ( -1.000000000000000000, 0.000000000000000000, 0.000000000000000000 ) ) ;
#84308=FACE_OUTER_BOUND ( 'NONE', #242567, .T. ) ;
#84336=AXIS2_PLACEMENT_3D ( 'NONE', #209482, #229060, #30881 ) ;
#84337=VECTOR ( 'NONE', #99382, 1000.000000000000000 ) ;
#84346=CARTESIAN_POINT ( 'NONE',  ( 18.59999999999999076, 36.65892442174935439, -249.5511627012433848 ) ) ;
#84354=VERTEX_POINT ( 'NONE', #182257 ) ;
#84369=CARTESIAN_POINT ( 'NONE',  ( -23.25000000000000000, 28.37802281961254636, -258.4449340416662722 ) ) ;
#84376=CARTESIAN_POINT ( 'NONE',  ( -18.54118089899633048, 8.873505991743348531, -245.4030529781414884 ) ) ;
#84383=DIRECTION ( 'NONE',  ( 0.000000000000000000, 0.8855159391400492241, -0.4646089985449236570 ) ) ;
#84400=EDGE_CURVE ( 'NONE', #135784, #195479, #105224, .T. ) ;
#84404=DIRECTION ( 'NONE',  ( -1.000000000000000000, -0.000000000000000000, -0.000000000000000000 ) ) ;
#84441=EDGE_LOOP ( 'NONE', ( #12980, #110301, #103793, #14228 ) ) ;
#84456=ORIENTED_EDGE ( 'NONE', *, *, #27177, .T. ) ;
#84465=VERTEX_POINT ( 'NONE', #46567 ) ;
#84471=CARTESIAN_POINT ( 'NONE',  ( -23.15000000000000213, 36.65892442174935439, -249.5511627012433848 ) ) ;
#84492=ADVANCED_FACE ( 'NONE', ( #247345 ), #146948, .F. ) ;
#84540=CARTESIAN_POINT ( 'NONE',  ( -20.64999999999999858, 21.35054858842500281, -233.1262234518673893 ) ) ;
#84554=ADVANCED_FACE ( 'NONE', ( #35716 ), #250423, .F. ) ;
#84564=LINE ( 'NONE', #218983, #12415 ) ;
#84580=TOROIDAL_SURFACE ( 'NONE', #183778, 2.100000000000002309, 0.1000000000000000056 ) ;
#84587=DIRECTION ( 'NONE',  ( 1.000000000000000000, 0.000000000000000000, 0.000000000000000000 ) ) ;
#84601=FACE_OUTER_BOUND ( 'NONE', #123851, .T. ) ;
#84609=FACE_OUTER_BOUND ( 'NONE', #256242, .T. ) ;
#84643=DIRECTION ( 'NONE',  ( -0.000000000000000000, -0.9371753822965326330, 0.3488585713686107592 ) ) ;
#84683=FACE_OUTER_BOUND ( 'NONE', #171433, .T. ) ;
#84695=ORIENTED_EDGE ( 'NONE', *, *, #251919, .F. ) ;
#84719=CARTESIAN_POINT ( 'NONE',  ( 20.94999999999999929, 18.81166555858609257, -229.8642012822692777 ) ) ;
#84756=FACE_OUTER_BOUND ( 'NONE', #19400, .T. ) ;
#84794=DIRECTION ( 'NONE',  ( 0.000000000000000000, 0.8814952561688429444, -0.4721928772777349570 ) ) ;
#84807=EDGE_LOOP ( 'NONE', ( #224209, #166596, #14974, #121364 ) ) ;
#84850=DIRECTION ( 'NONE',  ( 0.000000000000000000, 0.8814952561688437216, -0.4721928772777334582 ) ) ;
#84875=DIRECTION ( 'NONE',  ( 0.000000000000000000, -0.5868805631290353597, -0.8096735173027127530 ) ) ;
#84880=DIRECTION ( 'NONE',  ( 0.000000000000000000, -0.8454177738465993297, -0.5341055959866553016 ) ) ;
#84882=DIRECTION ( 'NONE',  ( 2.952720810173290098E-16, -0.4721928772777359007, -0.8814952561688425003 ) ) ;
#84894=DIRECTION ( 'NONE',  ( 0.000000000000000000, -0.8814952561688425003, 0.4721928772777359007 ) ) ;
#84918=CARTESIAN_POINT ( 'NONE',  ( -22.59999999999999787, 12.58798907299599179, -223.3278890275437050 ) ) ;
#84956=DIRECTION ( 'NONE',  ( -0.000000000000000000, 0.8814952561688430555, -0.4721928772777346239 ) ) ;
#84963=CARTESIAN_POINT ( 'NONE',  ( 18.59999999999999076, 13.59055429284667227, -238.6121134008722038 ) ) ;
#85020=DIRECTION ( 'NONE',  ( -2.952720810173288619E-16, 0.4721928772777346239, 0.8814952561688430555 ) ) ;
#85140=CARTESIAN_POINT ( 'NONE',  ( -20.85000000000000142, 42.90983634497241894, -254.2202269430244996 ) ) ;
#85190=EDGE_CURVE ( 'NONE', #255363, #199581, #229296, .T. ) ;
#85192=ORIENTED_EDGE ( 'NONE', *, *, #135401, .T. ) ;
#85218=FACE_OUTER_BOUND ( 'NONE', #29391, .T. ) ;
#85261=CIRCLE ( 'NONE', #160346, 0.2000000000000058675 ) ;
#85278=AXIS2_PLACEMENT_3D ( 'NONE', #210696, #109013, #94592 ) ;
#85293=EDGE_CURVE ( 'NONE', #6683, #141753, #233867, .T. ) ;
#85383=CIRCLE ( 'NONE', #206048, 0.5999999999999978684 ) ;
#85385=CARTESIAN_POINT ( 'NONE',  ( -23.25000000000000000, 38.51006445970392633, -250.5427677435266389 ) ) ;
#85398=DIRECTION ( 'NONE',  ( 0.000000000000000000, -0.4721928772776973204, -0.8814952561688629284 ) ) ;
#85401=CIRCLE ( 'NONE', #6331, 0.1000000000000013933 ) ;
#85413=DIRECTION ( 'NONE',  ( 0.000000000000000000, 0.4721928772777346239, 0.8814952561688430555 ) ) ;
#85429=AXIS2_PLACEMENT_3D ( 'NONE', #110337, #96853, #170370 ) ;
#85450=CIRCLE ( 'NONE', #231273, 0.09999999999999441280 ) ;
#85461=FACE_OUTER_BOUND ( 'NONE', #185189, .T. ) ;
#85514=VERTEX_POINT ( 'NONE', #233007 ) ;
#85549=DIRECTION ( 'NONE',  ( 0.000000000000000000, -0.4721928772777331251, -0.8814952561688439436 ) ) ;
#85605=ADVANCED_FACE ( 'NONE', ( #120767 ), #26593, .T. ) ;
#85608=DIRECTION ( 'NONE',  ( 1.000000000000000000, -3.448943450116722089E-16, -6.438528483529608630E-16 ) ) ;
#85644=EDGE_LOOP ( 'NONE', ( #21002, #177567, #153801, #196471 ) ) ;
#85650=VERTEX_POINT ( 'NONE', #159885 ) ;
#85733=DIRECTION ( 'NONE',  ( 0.000000000000000000, 0.8814952561688476074, -0.4721928772777262417 ) ) ;
#85734=EDGE_CURVE ( 'NONE', #240580, #122934, #129961, .T. ) ;
#85771=CIRCLE ( 'NONE', #14914, 0.09999999999999507894 ) ;
#85777=EDGE_CURVE ( 'NONE', #109034, #46953, #92747, .T. ) ;
#85793=ORIENTED_EDGE ( 'NONE', *, *, #11765, .T. ) ;
#85805=ORIENTED_EDGE ( 'NONE', *, *, #25297, .F. ) ;
#85810=CIRCLE ( 'NONE', #231598, 0.5999999999999992006 ) ;
#85813=CARTESIAN_POINT ( 'NONE',  ( -20.85000000000000142, 43.35377423437995503, -245.1717807829448930 ) ) ;
#85819=CIRCLE ( 'NONE', #23541, 0.1000000000000013933 ) ;
#85844=ORIENTED_EDGE ( 'NONE', *, *, #107151, .F. ) ;
#85851=DIRECTION ( 'NONE',  ( 0.000000000000000000, 0.8814952561688437216, -0.4721928772777334582 ) ) ;
#85861=CARTESIAN_POINT ( 'NONE',  ( -20.54999999999999716, 19.96675702282871256, -237.7735354486364088 ) ) ;
#85890=DIRECTION ( 'NONE',  ( -0.000000000000000000, 0.8496786552930076786, 0.5273008465188218086 ) ) ;
#85905=CARTESIAN_POINT ( 'NONE',  ( 20.94999999999999574, 14.72981487416292623, -236.4853282537515895 ) ) ;
#85909=EDGE_CURVE ( 'NONE', #227159, #53948, #9360, .T. ) ;
#85914=ORIENTED_EDGE ( 'NONE', *, *, #81576, .F. ) ;
#85915=EDGE_LOOP ( 'NONE', ( #197825, #22624, #215241, #115993, #101556 ) ) ;
#85960=ORIENTED_EDGE ( 'NONE', *, *, #192513, .F. ) ;
#86016=EDGE_CURVE ( 'NONE', #176897, #243045, #171906, .T. ) ;
#86057=VERTEX_POINT ( 'NONE', #21359 ) ;
#86059=CARTESIAN_POINT ( 'NONE',  ( 23.24999999999999289, 9.088433780795693195, -230.0744959993385805 ) ) ;
#86081=DIRECTION ( 'NONE',  ( -1.000000000000000000, -0.000000000000000000, -0.000000000000000000 ) ) ;
#86167=CIRCLE ( 'NONE', #52865, 11.80000000000000604 ) ;
#86188=CARTESIAN_POINT ( 'NONE',  ( -18.59999999999999787, 43.08613539620618837, -254.3146655184800409 ) ) ;
#86193=DIRECTION ( 'NONE',  ( 1.000000000000000000, 0.000000000000000000, 0.000000000000000000 ) ) ;
#86201=EDGE_CURVE ( 'NONE', #123298, #39898, #6899, .T. ) ;
#86203=CARTESIAN_POINT ( 'NONE',  ( 18.49999999999999645, 18.18127959618848166, -237.5711165786817389 ) ) ;
#86220=EDGE_CURVE ( 'NONE', #21212, #92552, #47121, .T. ) ;
#86223=DIRECTION ( 'NONE',  ( -0.000000000000000000, 0.8814952561688430555, -0.4721928772777346239 ) ) ;
#86255=DIRECTION ( 'NONE',  ( 4.408576920032446123E-17, 0.8096735173027155286, -0.5868805631290315850 ) ) ;
#86319=FACE_OUTER_BOUND ( 'NONE', #160676, .T. ) ;
#86328=AXIS2_PLACEMENT_3D ( 'NONE', #222715, #24557, #109186 ) ;
#86356=CARTESIAN_POINT ( 'NONE',  ( 21.05000000000000071, 28.34113089492129589, -239.5930034413672161 ) ) ;
#86413=EDGE_CURVE ( 'NONE', #196849, #16167, #62405, .T. ) ;
#86415=EDGE_LOOP ( 'NONE', ( #189637, #46035, #109512, #217308 ) ) ;
#86418=EDGE_CURVE ( 'NONE', #41254, #132235, #246867, .T. ) ;
#86419=EDGE_CURVE ( 'NONE', #46846, #43496, #13827, .T. ) ;
#86454=EDGE_LOOP ( 'NONE', ( #168756, #67655, #162965, #211668 ) ) ;
#86460=CARTESIAN_POINT ( 'NONE',  ( -21.05000000000000071, 4.436385504674529301, -245.3241086753762659 ) ) ;
#86475=DIRECTION ( 'NONE',  ( 1.734723475976814920E-13, -0.4608403197577645716, -0.8874830700839093645 ) ) ;
#86476=CARTESIAN_POINT ( 'NONE',  ( -21.08376601933334271, 1.568551483692875781, -230.6818607317798637 ) ) ;
#86486=SPHERICAL_SURFACE ( 'NONE', #154150, 0.1000000000000000056 ) ;
#86487=EDGE_LOOP ( 'NONE', ( #55225, #111368, #216579, #138036 ) ) ;
#86507=CARTESIAN_POINT ( 'NONE',  ( -22.39999999999999858, -3.187427350888460076, -228.3200064793908837 ) ) ;
#86512=CARTESIAN_POINT ( 'NONE',  ( -18.50000000000000000, 36.65892442174935439, -249.5511627012433848 ) ) ;
#86524=ORIENTED_EDGE ( 'NONE', *, *, #135504, .T. ) ;
#86526=DIRECTION ( 'NONE',  ( 0.000000000000000000, 0.8814952561688476074, -0.4721928772777262417 ) ) ;
#86538=ORIENTED_EDGE ( 'NONE', *, *, #211549, .T. ) ;
#86542=DIRECTION ( 'NONE',  ( 1.000000000000000000, 0.000000000000000000, 0.000000000000000000 ) ) ;
#86548=CARTESIAN_POINT ( 'NONE',  ( 18.59999999999999432, 45.93315328338058379, -256.6017782078560003 ) ) ;
#86589=AXIS2_PLACEMENT_3D ( 'NONE', #244506, #46297, #63298 ) ;
#86593=AXIS2_PLACEMENT_3D ( 'NONE', #225978, #143903, #86475 ) ;
#86601=CARTESIAN_POINT ( 'NONE',  ( 21.05000000000000071, 7.128833340093095217, -233.7327013124392749 ) ) ;
#86625=CARTESIAN_POINT ( 'NONE',  ( 21.05000000000000426, 10.23297665902167886, -228.1194301247179510 ) ) ;
#86653=VERTEX_POINT ( 'NONE', #53097 ) ;
#86658=DIRECTION ( 'NONE',  ( 1.000000000000000000, 0.000000000000000000, 0.000000000000000000 ) ) ;
#86665=CARTESIAN_POINT ( 'NONE',  ( -22.50000000000000000, -3.140208063160686791, -228.2318569537739847 ) ) ;
#86694=PLANE ( 'NONE',  #86589 ) ;
#86697=AXIS2_PLACEMENT_3D ( 'NONE', #4514, #237988, #198871 ) ;
#86706=CIRCLE ( 'NONE', #232523, 0.1999999999999938494 ) ;
#86745=ADVANCED_FACE ( 'NONE', ( #13991 ), #156091, .T. ) ;
#86763=CARTESIAN_POINT ( 'NONE',  ( 21.05000000000002203, 1.363275264940671860, -230.6442496871288768 ) ) ;
#86779=ADVANCED_FACE ( 'NONE', ( #73990 ), #153543, .F. ) ;
#86801=EDGE_CURVE ( 'NONE', #28426, #194531, #93109, .T. ) ;
#86843=AXIS2_PLACEMENT_3D ( 'NONE', #38287, #117811, #158271 ) ;
#86861=AXIS2_PLACEMENT_3D ( 'NONE', #19705, #199638, #80928 ) ;
#86866=LINE ( 'NONE', #146844, #130739 ) ;
#86884=DIRECTION ( 'NONE',  ( 0.000000000000000000, -0.5954378521545836689, -0.8034013718071036925 ) ) ;
#86885=AXIS2_PLACEMENT_3D ( 'NONE', #10256, #187618, #228010 ) ;
#86889=ADVANCED_FACE ( 'NONE', ( #79055 ), #142977, .T. ) ;
#86907=CARTESIAN_POINT ( 'NONE',  ( -20.64999999999999858, 7.128833340093095217, -233.7327013124392749 ) ) ;
#86941=EDGE_CURVE ( 'NONE', #193742, #104543, #26690, .T. ) ;
#86950=AXIS2_PLACEMENT_3D ( 'NONE', #63771, #222835, #203285 ) ;
#86951=VECTOR ( 'NONE', #201997, 1000.000000000000000 ) ;
#86994=CIRCLE ( 'NONE', #182904, 0.09999999999999036049 ) ;
#87001=CARTESIAN_POINT ( 'NONE',  ( 18.59999999999999432, 14.81796439977981272, -236.5325475414793743 ) ) ;
#87034=ORIENTED_EDGE ( 'NONE', *, *, #45912, .T. ) ;
#87058=LINE ( 'NONE', #166656, #214001 ) ;
#87076=ORIENTED_EDGE ( 'NONE', *, *, #40060, .T. ) ;
#87095=ADVANCED_FACE ( 'NONE', ( #85461 ), #186515, .T. ) ;
#87219=CARTESIAN_POINT ( 'NONE',  ( 18.59999999999999432, 45.93315328338058379, -256.6017782078560003 ) ) ;
#87243=TOROIDAL_SURFACE ( 'NONE', #41489, 12.77499999999999858, 0.1000000000000000056 ) ;
#87262=CIRCLE ( 'NONE', #91390, 0.1000000000000013933 ) ;
#87265=EDGE_CURVE ( 'NONE', #123343, #94806, #89857, .T. ) ;
#87282=ORIENTED_EDGE ( 'NONE', *, *, #113254, .F. ) ;
#87321=CYLINDRICAL_SURFACE ( 'NONE', #168960, 0.1000000000000013933 ) ;
#87335=AXIS2_PLACEMENT_3D ( 'NONE', #223008, #9120, #106916 ) ;
#87363=ORIENTED_EDGE ( 'NONE', *, *, #24600, .T. ) ;
#87394=VERTEX_POINT ( 'NONE', #64361 ) ;
#87407=DIRECTION ( 'NONE',  ( 0.000000000000000000, -0.4721928772777242433, -0.8814952561688484955 ) ) ;
#87421=DIRECTION ( 'NONE',  ( -0.000000000000000000, 0.4721928772777345684, 0.8814952561688429444 ) ) ;
#87435=ORIENTED_EDGE ( 'NONE', *, *, #105893, .F. ) ;
#87437=FACE_OUTER_BOUND ( 'NONE', #13296, .T. ) ;
#87511=CARTESIAN_POINT ( 'NONE',  ( 23.15000000000000213, 28.50120599808395028, -258.2149742250584268 ) ) ;
#87519=CARTESIAN_POINT ( 'NONE',  ( 22.59999999999999432, 12.58798907299599001, -223.3278890275437050 ) ) ;
#87525=CARTESIAN_POINT ( 'NONE',  ( 19.99999999999998934, 31.49702336731128582, -233.4564499823349877 ) ) ;
#87526=EDGE_LOOP ( 'NONE', ( #181061, #216219, #223680, #58561, #228717, #37980 ) ) ;
#87544=CIRCLE ( 'NONE', #229233, 0.1999999999999997335 ) ;
#87570=LINE ( 'NONE', #230975, #101794 ) ;
#87630=ORIENTED_EDGE ( 'NONE', *, *, #104793, .T. ) ;
#87640=ORIENTED_EDGE ( 'NONE', *, *, #88560, .T. ) ;
#87645=EDGE_LOOP ( 'NONE', ( #218505, #107269, #170274, #46653 ) ) ;
#87681=ADVANCED_FACE ( 'NONE', ( #81025 ), #216704, .T. ) ;
#87683=ORIENTED_EDGE ( 'NONE', *, *, #139127, .F. ) ;
#87686=ORIENTED_EDGE ( 'NONE', *, *, #235472, .F. ) ;
#87700=CARTESIAN_POINT ( 'NONE',  ( -23.15000000000000213, 28.50120599808395028, -258.2149742250584268 ) ) ;
#87713=ORIENTED_EDGE ( 'NONE', *, *, #246795, .F. ) ;
#87768=CARTESIAN_POINT ( 'NONE',  ( 21.05000000000000071, 20.66107731230508548, -234.7421556583769302 ) ) ;
#87769=CARTESIAN_POINT ( 'NONE',  ( -21.07933241753356413, 1.594255136103273296, -230.6620461068241923 ) ) ;
#87848=DIRECTION ( 'NONE',  ( -1.000000000000000000, -8.674042436075324885E-17, -1.619280515896126624E-16 ) ) ;
#87856=DIRECTION ( 'NONE',  ( 0.000000000000000000, -0.4721928772777346239, -0.8814952561688430555 ) ) ;
#87873=DIRECTION ( 'NONE',  ( 0.000000000000000000, 0.8814952561688436106, -0.4721928772777334027 ) ) ;
#87896=DIRECTION ( 'NONE',  ( 0.000000000000000000, -0.4721928772777346239, -0.8814952561688430555 ) ) ;
#87943=DIRECTION ( 'NONE',  ( -1.000000000000000000, 0.000000000000000000, 0.000000000000000000 ) ) ;
#87979=AXIS2_PLACEMENT_3D ( 'NONE', #181258, #2584, #215230 ) ;
#87980=EDGE_CURVE ( 'NONE', #177802, #124483, #185731, .T. ) ;
#87993=CARTESIAN_POINT ( 'NONE',  ( -22.49544290803746094, 12.61946619309018303, -223.3444065952058395 ) ) ;
#88023=CARTESIAN_POINT ( 'NONE',  ( 18.59999999999997655, 43.08613539620618837, -254.3146655184800409 ) ) ;
#88041=ORIENTED_EDGE ( 'NONE', *, *, #212801, .T. ) ;
#88052=ORIENTED_EDGE ( 'NONE', *, *, #181840, .F. ) ;
#88060=DIRECTION ( 'NONE',  ( 0.000000000000000000, 0.8814952561688442767, -0.4721928772777322925 ) ) ;
#88065=CARTESIAN_POINT ( 'NONE',  ( -23.15000000000000213, 19.16534496950139399, -238.0132401564540032 ) ) ;
#88086=CARTESIAN_POINT ( 'NONE',  ( -23.15000000000000213, 23.47541653617480861, -229.1594947991076197 ) ) ;
#88091=ORIENTED_EDGE ( 'NONE', *, *, #110966, .T. ) ;
#88093=CIRCLE ( 'NONE', #142293, 0.09999999999999564793 ) ;
#88110=CARTESIAN_POINT ( 'NONE',  ( 18.59999999999999787, 16.44800918141279311, -240.8068063186265135 ) ) ;
#88115=CARTESIAN_POINT ( 'NONE',  ( -21.05000000000000071, 16.52766025697963315, -240.8672687545768270 ) ) ;
#88162=CIRCLE ( 'NONE', #104902, 0.09999999999999939493 ) ;
#88183=CARTESIAN_POINT ( 'NONE',  ( 20.94999999999999574, 18.52348994230296242, -223.9544021632493127 ) ) ;
#88202=EDGE_LOOP ( 'NONE', ( #244887, #187973, #158919, #111255 ) ) ;
#88209=CARTESIAN_POINT ( 'NONE',  ( -18.59999999999999787, 31.44980407958351165, -233.5445995079518866 ) ) ;
#88219=EDGE_LOOP ( 'NONE', ( #100139, #108522, #135707, #179451 ) ) ;
#88237=CARTESIAN_POINT ( 'NONE',  ( 18.52165635395190435, 8.844262510478683836, -245.4073689581170186 ) ) ;
#88240=AXIS2_PLACEMENT_3D ( 'NONE', #190459, #170926, #107024 ) ;
#88243=DIRECTION ( 'NONE',  ( 0.000000000000000000, -0.3280696808754172689, -0.9446535261620007118 ) ) ;
#88250=CARTESIAN_POINT ( 'NONE',  ( -20.54999999999999716, 25.94586868676353575, -241.5435999122864530 ) ) ;
#88263=EDGE_LOOP ( 'NONE', ( #50101, #91107, #209579, #64234 ) ) ;
#88273=AXIS2_PLACEMENT_3D ( 'NONE', #229375, #92405, #33775 ) ;
#88275=LINE ( 'NONE', #143125, #231197 ) ;
#88311=ORIENTED_EDGE ( 'NONE', *, *, #202973, .T. ) ;
#88325=VERTEX_POINT ( 'NONE', #24007 ) ;
#88344=EDGE_CURVE ( 'NONE', #85650, #40168, #194314, .T. ) ;
#88352=CARTESIAN_POINT ( 'NONE',  ( 21.05000000000000426, 18.88693907895052249, -227.8658253555367992 ) ) ;
#88387=DIRECTION ( 'NONE',  ( 0.000000000000000000, 0.8814952561688437216, -0.4721928772777334582 ) ) ;
#88393=CYLINDRICAL_SURFACE ( 'NONE', #6132, 0.09999999999999568956 ) ;
#88395=CARTESIAN_POINT ( 'NONE',  ( -20.85000000000000142, 36.22724532936083364, -235.9903003947922286 ) ) ;
#88409=DIRECTION ( 'NONE',  ( 0.000000000000000000, 0.4721928772777346239, 0.8814952561688430555 ) ) ;
#88428=ADVANCED_FACE ( 'NONE', ( #9547 ), #168997, .F. ) ;
#88444=DIRECTION ( 'NONE',  ( -1.000000000000000000, -0.000000000000000000, -0.000000000000000000 ) ) ;
#88471=FACE_OUTER_BOUND ( 'NONE', #178676, .T. ) ;
#88475=CARTESIAN_POINT ( 'NONE',  ( 20.95052659398289308, 18.75486878932230184, -228.0717596309566204 ) ) ;
#88492=AXIS2_PLACEMENT_3D ( 'NONE', #36090, #70946, #30522 ) ;
#88493=AXIS2_PLACEMENT_3D ( 'NONE', #247762, #204769, #224343 ) ;
#88503=AXIS2_PLACEMENT_3D ( 'NONE', #257718, #235637, #60848 ) ;
#88512=EDGE_CURVE ( 'NONE', #50036, #103521, #240271, .T. ) ;
#88518=ORIENTED_EDGE ( 'NONE', *, *, #34849, .F. ) ;
#88522=FACE_OUTER_BOUND ( 'NONE', #49598, .T. ) ;
#88560=EDGE_CURVE ( 'NONE', #102673, #138714, #89831, .T. ) ;
#88581=EDGE_CURVE ( 'NONE', #136977, #182052, #57061, .T. ) ;
#88582=DIRECTION ( 'NONE',  ( 0.000000000000000000, 0.8814952561688430555, -0.4721928772777346239 ) ) ;
#88584=ORIENTED_EDGE ( 'NONE', *, *, #103385, .F. ) ;
#88601=ORIENTED_EDGE ( 'NONE', *, *, #44171, .T. ) ;
#88668=DIRECTION ( 'NONE',  ( -0.000000000000000000, 0.4721928772777345684, 0.8814952561688429444 ) ) ;
#88681=EDGE_LOOP ( 'NONE', ( #15059, #194332, #157657 ) ) ;
#88686=CYLINDRICAL_SURFACE ( 'NONE', #57354, 0.1000000000000013933 ) ;
#88703=CARTESIAN_POINT ( 'NONE',  ( -21.05000000000000071, 1.599488064139765742, -230.7125547273896586 ) ) ;
#88739=DIRECTION ( 'NONE',  ( 1.000000000000000000, 0.000000000000000000, 0.000000000000000000 ) ) ;
#88767=ADVANCED_FACE ( 'NONE', ( #115918 ), #95056, .F. ) ;
#88788=CARTESIAN_POINT ( 'NONE',  ( 18.49999999999999289, 33.67810952736942198, -236.3734420906320395 ) ) ;
#88796=CARTESIAN_POINT ( 'NONE',  ( -18.50000000000000000, 16.60731133254646963, -240.9277311905271688 ) ) ;
#88802=DIRECTION ( 'NONE',  ( 0.7071067811865473507, 0.3338907855510733769, 0.6233112732207618523 ) ) ;
#88835=ORIENTED_EDGE ( 'NONE', *, *, #43480, .F. ) ;
#88847=DIRECTION ( 'NONE',  ( -0.000000000000000000, -0.4721928772777346239, -0.8814952561688430555 ) ) ;
#88881=EDGE_CURVE ( 'NONE', #199335, #89573, #159649, .T. ) ;
#88893=VERTEX_POINT ( 'NONE', #198000 ) ;
#88902=CARTESIAN_POINT ( 'NONE',  ( 20.12500000000000000, 18.88320179786139619, -228.9684431863134932 ) ) ;
#88930=LINE ( 'NONE', #10703, #189752 ) ;
#88937=DIRECTION ( 'NONE',  ( 1.000000000000000000, 0.000000000000000000, 0.000000000000000000 ) ) ;
#88950=CARTESIAN_POINT ( 'NONE',  ( -23.25000000000000000, 28.51339163295720169, -258.4040038037771865 ) ) ;
#88956=ORIENTED_EDGE ( 'NONE', *, *, #154099, .F. ) ;
#88957=CARTESIAN_POINT ( 'NONE',  ( -22.50000000000000000, 12.62988036037870998, -223.4632815780722410 ) ) ;
#88963=CARTESIAN_POINT ( 'NONE',  ( 18.49999999999998934, 34.44688795055758135, -235.1500552906961730 ) ) ;
#88971=CIRCLE ( 'NONE', #138837, 0.1000000000000009354 ) ;
#88986=CARTESIAN_POINT ( 'NONE',  ( 18.48197441912073558, 38.23830283804237951, -261.1947035615960431 ) ) ;
#88996=CARTESIAN_POINT ( 'NONE',  ( 23.15000000000000213, 23.68770167995059239, -252.8127582590406348 ) ) ;
#88998=EDGE_CURVE ( 'NONE', #71933, #19770, #256642, .T. ) ;
#89006=ORIENTED_EDGE ( 'NONE', *, *, #210732, .T. ) ;
#89043=ORIENTED_EDGE ( 'NONE', *, *, #197330, .F. ) ;
#89061=CARTESIAN_POINT ( 'NONE',  ( -21.08198257630413508, 1.577455038876691917, -230.6765707231475631 ) ) ;
#89062=VECTOR ( 'NONE', #82433, 1000.000000000000000 ) ;
#89086=EDGE_CURVE ( 'NONE', #245346, #67371, #203869, .T. ) ;
#89108=ORIENTED_EDGE ( 'NONE', *, *, #234861, .F. ) ;
#89134=DIRECTION ( 'NONE',  ( 3.469446951953634384E-14, -0.8814952561688430555, 0.4721928772777346239 ) ) ;
#89139=FACE_OUTER_BOUND ( 'NONE', #157774, .T. ) ;
#89141=ADVANCED_FACE ( 'NONE', ( #23421 ), #104188, .T. ) ;
#89149=CIRCLE ( 'NONE', #105694, 0.1000000000000075273 ) ;
#89150=DIRECTION ( 'NONE',  ( -3.265361837132813586E-16, 0.4721928772777344019, 0.8814952561688430555 ) ) ;
#89177=PLANE ( 'NONE',  #129889 ) ;
#89192=DIRECTION ( 'NONE',  ( -1.000000000000000000, 0.000000000000000000, 0.000000000000000000 ) ) ;
#89202=DIRECTION ( 'NONE',  ( 0.000000000000000000, 0.8814952561688476074, -0.4721928772777262417 ) ) ;
#89215=CIRCLE ( 'NONE', #5811, 0.2000000000000058675 ) ;
#89246=FACE_OUTER_BOUND ( 'NONE', #10012, .T. ) ;
#89248=CIRCLE ( 'NONE', #197581, 0.1000000000000075273 ) ;
#89253=VERTEX_POINT ( 'NONE', #147181 ) ;
#89259=DIRECTION ( 'NONE',  ( 1.000000000000000000, 0.000000000000000000, 0.000000000000000000 ) ) ;
#89266=CARTESIAN_POINT ( 'NONE',  ( -23.25000000000000000, 19.98118924431957311, -235.6825596947570602 ) ) ;
#89272=ORIENTED_EDGE ( 'NONE', *, *, #52909, .F. ) ;
#89283=AXIS2_PLACEMENT_3D ( 'NONE', #198997, #93466, #255050 ) ;
#89318=EDGE_CURVE ( 'NONE', #257030, #100823, #72535, .T. ) ;
#89329=DIRECTION ( 'NONE',  ( -0.000000000000000000, -0.9371753822965315228, 0.3488585713686134238 ) ) ;
#89344=DIRECTION ( 'NONE',  ( 1.000000000000000000, -0.000000000000000000, -0.000000000000000000 ) ) ;
#89388=EDGE_CURVE ( 'NONE', #159212, #13871, #14098, .T. ) ;
#89390=ORIENTED_EDGE ( 'NONE', *, *, #144390, .T. ) ;
#89427=AXIS2_PLACEMENT_3D ( 'NONE', #119352, #197583, #201440 ) ;
#89446=PLANE ( 'NONE',  #106688 ) ;
#89457=DIRECTION ( 'NONE',  ( 0.000000000000000000, 0.8814952561688437216, -0.4721928772777334582 ) ) ;
#89465=DIRECTION ( 'NONE',  ( 0.000000000000000000, 0.8814952561688476074, -0.4721928772777262417 ) ) ;
#89473=ORIENTED_EDGE ( 'NONE', *, *, #155932, .T. ) ;
#89477=TOROIDAL_SURFACE ( 'NONE', #118564, 0.9750000000000019762, 0.1000000000000000056 ) ;
#89483=DIRECTION ( 'NONE',  ( 0.000000000000000000, 0.8814952561688432775, -0.4721928772777344019 ) ) ;
#89517=ORIENTED_EDGE ( 'NONE', *, *, #145301, .F. ) ;
#89564=DIRECTION ( 'NONE',  ( 0.000000000000000000, 0.8496786552930076786, 0.5273008465188218086 ) ) ;
#89565=ORIENTED_EDGE ( 'NONE', *, *, #79417, .T. ) ;
#89573=VERTEX_POINT ( 'NONE', #29528 ) ;
#89577=DIRECTION ( 'NONE',  ( 1.836970198721029441E-16, -0.4721928772777346239, -0.8814952561688430555 ) ) ;
#89590=ORIENTED_EDGE ( 'NONE', *, *, #106181, .T. ) ;
#89629=VERTEX_POINT ( 'NONE', #49051 ) ;
#89636=ORIENTED_EDGE ( 'NONE', *, *, #234855, .T. ) ;
#89650=CARTESIAN_POINT ( 'NONE',  ( 21.14999999999998082, 1.580567032079710055, -244.0902705724231794 ) ) ;
#89674=DIRECTION ( 'NONE',  ( 0.000000000000000000, -0.8814952561688476074, 0.4721928772777262417 ) ) ;
#89679=DIRECTION ( 'NONE',  ( 1.000000000000000000, 0.000000000000000000, 0.000000000000000000 ) ) ;
#89698=DIRECTION ( 'NONE',  ( 0.000000000000000000, -0.8814952561688438326, 0.4721928772777330696 ) ) ;
#89712=VECTOR ( 'NONE', #205353, 1000.000000000000000 ) ;
#89738=VERTEX_POINT ( 'NONE', #111604 ) ;
#89750=LINE ( 'NONE', #70233, #67550 ) ;
#89769=CARTESIAN_POINT ( 'NONE',  ( 21.14999999999999858, 20.97908333644147660, -233.6079013178409411 ) ) ;
#89795=DIRECTION ( 'NONE',  ( 0.000000000000000000, 0.8814952561688476074, -0.4721928772777262417 ) ) ;
#89805=VECTOR ( 'NONE', #115089, 1000.000000000000000 ) ;
#89827=DIRECTION ( 'NONE',  ( 1.000000000000000000, 0.000000000000000000, 0.000000000000000000 ) ) ;
#89831=CIRCLE ( 'NONE', #140267, 0.1000000000000035444 ) ;
#89836=CARTESIAN_POINT ( 'NONE',  ( -18.50000000000000000, 2.272311100394797556, -217.9150152700588876 ) ) ;
#89838=CARTESIAN_POINT ( 'NONE',  ( 20.85000000000000142, 36.65892442174935439, -249.5511627012433848 ) ) ;
#89843=EDGE_CURVE ( 'NONE', #136089, #186480, #156132, .T. ) ;
#89855=FACE_OUTER_BOUND ( 'NONE', #149652, .T. ) ;
#89857=B_SPLINE_CURVE_WITH_KNOTS ( 'NONE', 3,
 ( #506, #98300, #240425, #196156, #241707, #97015, #220850, #177898, #57911, #237853, #22686, #60482, #180453, #77465, #120507, #21403, #61786, #17510, #42230 ),
 .UNSPECIFIED., .F., .F.,
 ( 4, 3, 3, 3, 3, 3, 4 ),
 ( 0.000000000000000000, 7.110282409888900811E-05, 0.0001508797727291396576, 0.0002027344179858381486, 0.0002343294522348978305, 0.0002454816334821145599, 0.0002619873080085490967 ),
 .UNSPECIFIED. ) ;
#89879=DIRECTION ( 'NONE',  ( 0.000000000000000000, 0.8814952561688437216, -0.4721928772777334582 ) ) ;
#89880=EDGE_LOOP ( 'NONE', ( #45403, #200934, #242712, #123592 ) ) ;
#89889=CARTESIAN_POINT ( 'NONE',  ( -18.50000000000000000, 7.128833340093095217, -233.7327013124392749 ) ) ;
#89890=AXIS2_PLACEMENT_3D ( 'NONE', #167508, #112648, #132205 ) ;
#89895=VERTEX_POINT ( 'NONE', #61582 ) ;
#89908=CARTESIAN_POINT ( 'NONE',  ( -18.59999999999999787, 18.62343931468261360, -223.9512205031617498 ) ) ;
#89912=AXIS2_PLACEMENT_3D ( 'NONE', #118130, #197653, #119425 ) ;
#89934=CARTESIAN_POINT ( 'NONE',  ( 21.05000000000000071, 19.09887790564731702, -232.6007267402957837 ) ) ;
#89936=VERTEX_POINT ( 'NONE', #211370 ) ;
#89937=ORIENTED_EDGE ( 'NONE', *, *, #35904, .T. ) ;
#89940=AXIS2_PLACEMENT_3D ( 'NONE', #163224, #107080, #184053 ) ;
#89962=EDGE_LOOP ( 'NONE', ( #28096, #225867, #31093, #215154 ) ) ;
#89970=DIRECTION ( 'NONE',  ( -0.000000000000000000, -0.8814952561688430555, 0.4721928772777346239 ) ) ;
#89979=AXIS2_PLACEMENT_3D ( 'NONE', #46674, #190060, #29733 ) ;
#90008=ORIENTED_EDGE ( 'NONE', *, *, #135401, .F. ) ;
#90010=FACE_OUTER_BOUND ( 'NONE', #119202, .T. ) ;
#90027=ORIENTED_EDGE ( 'NONE', *, *, #45469, .F. ) ;
#90043=AXIS2_PLACEMENT_3D ( 'NONE', #180574, #138830, #158468 ) ;
#90048=DIRECTION ( 'NONE',  ( -0.000000000000000000, -0.4721928772777346239, -0.8814952561688430555 ) ) ;
#90072=FACE_OUTER_BOUND ( 'NONE', #96977, .T. ) ;
#90079=ORIENTED_EDGE ( 'NONE', *, *, #316, .F. ) ;
#90101=CIRCLE ( 'NONE', #135884, 0.3999999999999994671 ) ;
#90167=CARTESIAN_POINT ( 'NONE',  ( 20.94999999999999929, 21.02001357433058004, -233.7432701311855965 ) ) ;
#90185=ORIENTED_EDGE ( 'NONE', *, *, #120897, .F. ) ;
#90197=DIRECTION ( 'NONE',  ( 0.000000000000000000, -0.8814952561688430555, 0.4721928772777346239 ) ) ;
#90212=ORIENTED_EDGE ( 'NONE', *, *, #253740, .F. ) ;
#90237=LINE ( 'NONE', #88957, #128275 ) ;
#90263=CARTESIAN_POINT ( 'NONE',  ( 18.49999999999999289, 33.69766839675185821, -236.3369293616048310 ) ) ;
#90268=CARTESIAN_POINT ( 'NONE',  ( 21.30740335185486245, 10.13763019447862668, -227.9063222794615342 ) ) ;
#90278=DIRECTION ( 'NONE',  ( -1.000000000000000000, -0.000000000000000000, -0.000000000000000000 ) ) ;
#90298=CIRCLE ( 'NONE', #44541, 0.1000000000000013933 ) ;
#90300=DIRECTION ( 'NONE',  ( -0.000000000000000000, -0.4721928772777346239, -0.8814952561688430555 ) ) ;
#90360=DIRECTION ( 'NONE',  ( 1.000000000000000000, 0.000000000000000000, 0.000000000000000000 ) ) ;
#90362=ORIENTED_EDGE ( 'NONE', *, *, #82000, .F. ) ;
#90377=CARTESIAN_POINT ( 'NONE',  ( -18.59999999999999787, -1.293555411365099994, -227.7000673772910204 ) ) ;
#90446=AXIS2_PLACEMENT_3D ( 'NONE', #21207, #156865, #221911 ) ;
#90451=DIRECTION ( 'NONE',  ( 0.000000000000000000, -0.8814952561688430555, 0.4721928772777346239 ) ) ;
#90484=CARTESIAN_POINT ( 'NONE',  ( 18.59999999999999076, 18.62343931468261715, -223.9512205031617214 ) ) ;
#90492=CARTESIAN_POINT ( 'NONE',  ( -18.59999999999999787, 36.65892442174935439, -249.5511627012433848 ) ) ;
#90514=CARTESIAN_POINT ( 'NONE',  ( -23.15000000000000213, 2.319530388122572617, -217.8268657444419887 ) ) ;
#90518=ORIENTED_EDGE ( 'NONE', *, *, #51761, .F. ) ;
#90597=ORIENTED_EDGE ( 'NONE', *, *, #67063, .T. ) ;
#90599=DIRECTION ( 'NONE',  ( -0.000000000000000000, -0.8814952561688430555, 0.4721928772777346239 ) ) ;
#90609=ORIENTED_EDGE ( 'NONE', *, *, #122468, .T. ) ;
#90612=CARTESIAN_POINT ( 'NONE',  ( -23.15000000000000213, 36.65892442174935439, -249.5511627012433848 ) ) ;
#90632=AXIS2_PLACEMENT_3D ( 'NONE', #103791, #106362, #9851 ) ;
#90646=CARTESIAN_POINT ( 'NONE',  ( 18.59999999999999787, 42.94477010600542854, -254.3363632230312703 ) ) ;
#90652=CARTESIAN_POINT ( 'NONE',  ( -18.59999999999999787, 7.128833340093095217, -233.7327013124392749 ) ) ;
#90661=EDGE_LOOP ( 'NONE', ( #145859, #220717, #149650 ) ) ;
#90678=CARTESIAN_POINT ( 'NONE',  ( 23.24999999999999289, 28.81810206650552075, -238.0339362645743222 ) ) ;
#90684=CARTESIAN_POINT ( 'NONE',  ( 23.24999999999999645, 34.81737220036617941, -252.9889942003018461 ) ) ;
#90787=CARTESIAN_POINT ( 'NONE',  ( -21.53752568622134334, 1.193029429793917684, -230.4407734565325825 ) ) ;
#90830=DIRECTION ( 'NONE',  ( -1.000000000000000000, 0.000000000000000000, 0.000000000000000000 ) ) ;
#90833=EDGE_CURVE ( 'NONE', #74336, #108268, #155926, .T. ) ;
#90848=LINE ( 'NONE', #12630, #55381 ) ;
#90865=CARTESIAN_POINT ( 'NONE',  ( -20.99780126800958513, 36.04544038259461303, -236.0569647481114259 ) ) ;
#90876=ADVANCED_FACE ( 'NONE', ( #135025 ), #251125, .F. ) ;
#90889=AXIS2_PLACEMENT_3D ( 'NONE', #157098, #254834, #76246 ) ;
#90939=EDGE_CURVE ( 'NONE', #203639, #218161, #139296, .T. ) ;
#90971=DIRECTION ( 'NONE',  ( 1.000000000000000000, 0.000000000000000000, 0.000000000000000000 ) ) ;
#90986=TOROIDAL_SURFACE ( 'NONE', #86861, 0.2000000000000000111, 0.1000000000000000056 ) ;
#91009=ADVANCED_FACE ( 'NONE', ( #178051 ), #210258, .F. ) ;
#91027=DIRECTION ( 'NONE',  ( -1.000000000000000000, 3.448943450116724061E-16, 6.438528483529607644E-16 ) ) ;
#91034=AXIS2_PLACEMENT_3D ( 'NONE', #17211, #97984, #176289 ) ;
#91056=ORIENTED_EDGE ( 'NONE', *, *, #188648, .T. ) ;
#91057=ORIENTED_EDGE ( 'NONE', *, *, #200445, .F. ) ;
#91071=CARTESIAN_POINT ( 'NONE',  ( 21.06086055315984140, 22.02847682286311937, -231.7596878716482820 ) ) ;
#91091=CIRCLE ( 'NONE', #228668, 3.899999999999993694 ) ;
#91094=ORIENTED_EDGE ( 'NONE', *, *, #94922, .F. ) ;
#91107=ORIENTED_EDGE ( 'NONE', *, *, #257731, .T. ) ;
#91132=CYLINDRICAL_SURFACE ( 'NONE', #88273, 0.09999999999999939493 ) ;
#91134=DIRECTION ( 'NONE',  ( 1.000000000000000000, 0.000000000000000000, 0.000000000000000000 ) ) ;
#91138=CARTESIAN_POINT ( 'NONE',  ( -21.04999999999999716, 1.434589632855153063, -230.7797184520195231 ) ) ;
#91139=DIRECTION ( 'NONE',  ( -1.000000000000000000, 0.000000000000000000, 0.000000000000000000 ) ) ;
#91159=EDGE_CURVE ( 'NONE', #17866, #1479, #209146, .T. ) ;
#91174=CIRCLE ( 'NONE', #128587, 0.1000000000000013933 ) ;
#91176=ADVANCED_FACE ( 'NONE', ( #149205 ), #64509, .T. ) ;
#91177=FACE_OUTER_BOUND ( 'NONE', #246747, .T. ) ;
#91194=FACE_OUTER_BOUND ( 'NONE', #178535, .T. ) ;
#91231=VERTEX_POINT ( 'NONE', #134733 ) ;
#91241=DIRECTION ( 'NONE',  ( 0.000000000000000000, 0.8814952561688476074, -0.4721928772777262417 ) ) ;
#91268=LINE ( 'NONE', #229494, #221770 ) ;
#91277=EDGE_LOOP ( 'NONE', ( #190638, #106173 ) ) ;
#91285=FACE_OUTER_BOUND ( 'NONE', #170594, .T. ) ;
#91292=ORIENTED_EDGE ( 'NONE', *, *, #161393, .T. ) ;
#91295=( BOUNDED_SURFACE ( )  B_SPLINE_SURFACE ( 3, 2, ( 
 ( #33520, #113014, #192557 ),
 ( #246112, #146981, #217223 ),
 ( #214668, #236795, #256299 ),
 ( #36055, #98530, #95995 ) ),
 .UNSPECIFIED., .F., .F., .F. ) 
 B_SPLINE_SURFACE_WITH_KNOTS ( ( 4, 4 ),
 ( 3, 3 ),
 ( -1.992221491942114397E-18, 0.0003124336117481551524 ),
 ( 0.000000000000000000, 1.000000000000000000 ),
 .UNSPECIFIED. ) 
 GEOMETRIC_REPRESENTATION_ITEM ( )  RATIONAL_B_SPLINE_SURFACE ( (
 ( 1.000000000000000000, 0.7040654476016252605, 1.000000000000000000),
 ( 1.000000000000000000, 0.7039193538783552473, 1.000000000000000000),
 ( 1.000000000000000000, 0.7089171279143997584, 1.000000000000000000),
 ( 1.000000000000000000, 0.7071067811865408004, 1.000000000000000000) ) ) 
 REPRESENTATION_ITEM ( '' )  SURFACE ( )  );
#91319=ORIENTED_EDGE ( 'NONE', *, *, #125382, .F. ) ;
#91322=DIRECTION ( 'NONE',  ( -1.000000000000000000, 0.000000000000000000, 0.000000000000000000 ) ) ;
#91323=CARTESIAN_POINT ( 'NONE',  ( -23.25000000000000000, 7.128833340093095217, -233.7327013124392749 ) ) ;
#91328=AXIS2_PLACEMENT_3D ( 'NONE', #256498, #916, #80449 ) ;
#91338=CIRCLE ( 'NONE', #49630, 0.4999999999999978351 ) ;
#91390=AXIS2_PLACEMENT_3D ( 'NONE', #1594, #255877, #240237 ) ;
#91406=LINE ( 'NONE', #87525, #242607 ) ;
#91409=CIRCLE ( 'NONE', #37244, 0.1999999999999997335 ) ;
#91458=CIRCLE ( 'NONE', #216345, 0.09999999999999986677 ) ;
#91471=CARTESIAN_POINT ( 'NONE',  ( 21.30000000000002558, 7.128833340093095217, -233.7327013124392749 ) ) ;
#91474=ADVANCED_FACE ( 'NONE', ( #32500 ), #50704, .T. ) ;
#91493=FACE_OUTER_BOUND ( 'NONE', #144416, .T. ) ;
#91507=CARTESIAN_POINT ( 'NONE',  ( 20.75572585718056473, 18.81329300187470821, -229.9153261448354613 ) ) ;
#91516=AXIS2_PLACEMENT_3D ( 'NONE', #135252, #229253, #131412 ) ;
#91572=CARTESIAN_POINT ( 'NONE',  ( 18.49999999999808864, 33.89065584167517642, -236.2246875831560260 ) ) ;
#91595=EDGE_LOOP ( 'NONE', ( #150880, #239354, #214987 ) ) ;
#91604=DIRECTION ( 'NONE',  ( 0.000000000000000000, 0.8814952561688442767, -0.4721928772777324035 ) ) ;
#91607=ORIENTED_EDGE ( 'NONE', *, *, #233730, .T. ) ;
#91639=EDGE_CURVE ( 'NONE', #260, #94806, #214511, .T. ) ;
#91662=DIRECTION ( 'NONE',  ( 0.000000000000000000, 0.8814952561688444987, -0.4721928772777320149 ) ) ;
#91747=VERTEX_POINT ( 'NONE', #141812 ) ;
#91756=DIRECTION ( 'NONE',  ( -1.000000000000000000, 0.000000000000000000, 0.000000000000000000 ) ) ;
#91765=CIRCLE ( 'NONE', #83541, 0.8750000000000007772 ) ;
#91771=CARTESIAN_POINT ( 'NONE',  ( -20.64999999999999858, 18.56623428888383387, -239.8594038951179073 ) ) ;
#91780=ADVANCED_FACE ( 'NONE', ( #221334 ), #139226, .F. ) ;
#91783=CIRCLE ( 'NONE', #71141, 0.1000000000000013933 ) ;
#91811=ORIENTED_EDGE ( 'NONE', *, *, #47315, .T. ) ;
#91834=EDGE_CURVE ( 'NONE', #195967, #19319, #27303, .T. ) ;
#91854=EDGE_LOOP ( 'NONE', ( #23297, #242582, #184399, #33558 ) ) ;
#91857=TOROIDAL_SURFACE ( 'NONE', #50149, 12.97499999999999609, 0.1000000000000000056 ) ;
#91862=CARTESIAN_POINT ( 'NONE',  ( -23.15000000000000213, 3.558777552609279304, -231.8203201594644725 ) ) ;
#91892=EDGE_LOOP ( 'NONE', ( #188164, #53210, #198344, #58415 ) ) ;
#91900=CARTESIAN_POINT ( 'NONE',  ( 18.52928932188133615, 33.76313540251413770, -236.3387713816553060 ) ) ;
#91935=AXIS2_PLACEMENT_3D ( 'NONE', #109272, #31076, #207118 ) ;
#91986=DIRECTION ( 'NONE',  ( 0.000000000000000000, -0.8814952561688430555, 0.4721928772777346239 ) ) ;
#92024=DIRECTION ( 'NONE',  ( 0.000000000000000000, -0.4721928772777346794, -0.8814952561688431665 ) ) ;
#92041=LINE ( 'NONE', #13797, #227109 ) ;
#92073=ORIENTED_EDGE ( 'NONE', *, *, #73375, .F. ) ;
#92122=AXIS2_PLACEMENT_3D ( 'NONE', #136684, #173315, #132866 ) ;
#92132=PLANE ( 'NONE',  #22107 ) ;
#92135=DIRECTION ( 'NONE',  ( -1.000000000000000000, -0.000000000000000000, -0.000000000000000000 ) ) ;
#92207=LINE ( 'NONE', #250009, #42904 ) ;
#92248=CARTESIAN_POINT ( 'NONE',  ( 22.47809213839789066, -3.122838153047792442, -228.1985781362319017 ) ) ;
#92270=DIRECTION ( 'NONE',  ( -1.000000000000000000, -0.000000000000000000, -0.000000000000000000 ) ) ;
#92272=FACE_OUTER_BOUND ( 'NONE', #12587, .T. ) ;
#92342=FACE_OUTER_BOUND ( 'NONE', #73483, .T. ) ;
#92344=DIRECTION ( 'NONE',  ( 0.000000000000000000, -0.4721928772777346239, -0.8814952561688430555 ) ) ;
#92347=CARTESIAN_POINT ( 'NONE',  ( 20.95378194480896639, 18.77190308950016018, -228.0183910527138380 ) ) ;
#92350=LINE ( 'NONE', #71536, #178779 ) ;
#92361=DIRECTION ( 'NONE',  ( 2.940209281316624467E-16, -0.4721928772777302941, -0.8814952561688453869 ) ) ;
#92362=ORIENTED_EDGE ( 'NONE', *, *, #195168, .F. ) ;
#92376=CARTESIAN_POINT ( 'NONE',  ( 22.50000000000000000, 7.128833340093095217, -233.7327013124392749 ) ) ;
#92378=DIRECTION ( 'NONE',  ( -1.000000000000000000, 7.166229603267617241E-16, 4.447280054184918885E-16 ) ) ;
#92405=DIRECTION ( 'NONE',  ( 0.000000000000000000, 0.8814952561688430555, -0.4721928772777346239 ) ) ;
#92416=CIRCLE ( 'NONE', #138195, 4.300000000000035350 ) ;
#92422=CARTESIAN_POINT ( 'NONE',  ( 21.05000000000000071, 13.54362637910787370, -238.4879411198429580 ) ) ;
#92437=EDGE_CURVE ( 'NONE', #234056, #209722, #202596, .T. ) ;
#92446=CARTESIAN_POINT ( 'NONE',  ( 22.39999999999999503, 12.58895012248959766, -223.3279127647276141 ) ) ;
#92464=DIRECTION ( 'NONE',  ( 1.000000000000000000, 0.000000000000000000, 0.000000000000000000 ) ) ;
#92486=DIRECTION ( 'NONE',  ( -0.000000000000000000, -0.4721928772777346239, -0.8814952561688430555 ) ) ;
#92492=VERTEX_POINT ( 'NONE', #202474 ) ;
#92509=VERTEX_POINT ( 'NONE', #180343 ) ;
#92541=ADVANCED_FACE ( 'NONE', ( #197315 ), #177794, .F. ) ;
#92552=VERTEX_POINT ( 'NONE', #199920 ) ;
#92554=ADVANCED_FACE ( 'NONE', ( #23863 ), #61674, .F. ) ;
#92557=CARTESIAN_POINT ( 'NONE',  ( 21.14999999999999858, 21.15538238767524604, -233.7023398932965108 ) ) ;
#92567=CARTESIAN_POINT ( 'NONE',  ( -21.09096482362058822, 1.538026365827115383, -230.6931075182510256 ) ) ;
#92573=CARTESIAN_POINT ( 'NONE',  ( 20.95512820512820440, 22.85550638026973047, -230.1049725544161220 ) ) ;
#92582=TOROIDAL_SURFACE ( 'NONE', #246529, 0.9750000000000019762, 0.1000000000000000056 ) ;
#92602=CARTESIAN_POINT ( 'NONE',  ( 23.24999999999999289, 2.272311100394802885, -217.9150152700588592 ) ) ;
#92622=AXIS2_PLACEMENT_3D ( 'NONE', #201807, #123565, #144376 ) ;
#92642=CYLINDRICAL_SURFACE ( 'NONE', #186718, 0.09999999999999986677 ) ;
#92673=ORIENTED_EDGE ( 'NONE', *, *, #215551, .T. ) ;
#92704=VERTEX_POINT ( 'NONE', #224588 ) ;
#92714=ORIENTED_EDGE ( 'NONE', *, *, #158180, .F. ) ;
#92718=CARTESIAN_POINT ( 'NONE',  ( 18.49999999999999289, 34.58225676390223668, -235.1091250528070589 ) ) ;
#92743=DIRECTION ( 'NONE',  ( 0.000000000000000000, -0.4721928772777346239, -0.8814952561688430555 ) ) ;
#92747=CIRCLE ( 'NONE', #180252, 4.099999999999996980 ) ;
#92748=VECTOR ( 'NONE', #244788, 1000.000000000000000 ) ;
#92762=CARTESIAN_POINT ( 'NONE',  ( 20.94999999999999929, 28.08470566095357057, -239.2860081655328770 ) ) ;
#92773=CARTESIAN_POINT ( 'NONE',  ( 20.74897398619101807, 18.90132073407816904, -228.0187643500604793 ) ) ;
#92806=ORIENTED_EDGE ( 'NONE', *, *, #40552, .F. ) ;
#92817=CARTESIAN_POINT ( 'NONE',  ( 20.95346350065193519, 18.82834646935051026, -229.9178759252477278 ) ) ;
#92819=DIRECTION ( 'NONE',  ( 0.000000000000000000, 0.8814952561688438326, -0.4721928772777331806 ) ) ;
#92843=CARTESIAN_POINT ( 'NONE',  ( 18.59999999999999076, 33.89981536720674171, -236.1713368690715527 ) ) ;
#92850=CARTESIAN_POINT ( 'NONE',  ( 18.59999996954842771, 38.22950387605726519, -261.1959452426659141 ) ) ;
#92880=CARTESIAN_POINT ( 'NONE',  ( -21.05000000000000071, 12.71802988599559114, -223.5105008658000543 ) ) ;
#92902=DIRECTION ( 'NONE',  ( 1.000000000000000000, -0.000000000000000000, 0.000000000000000000 ) ) ;
#92924=DIRECTION ( 'NONE',  ( 1.000000000000000000, 0.000000000000000000, 0.000000000000000000 ) ) ;
#92928=VECTOR ( 'NONE', #203188, 1000.000000000000000 ) ;
#92933=DIRECTION ( 'NONE',  ( 0.000000000000000000, 0.4721928772776164407, 0.8814952561689062271 ) ) ;
#92935=ADVANCED_FACE ( 'NONE', ( #27189 ), #198679, .T. ) ;
#92938=CIRCLE ( 'NONE', #176183, 0.9750000000000036415 ) ;
#92962=DIRECTION ( 'NONE',  ( 0.000000000000000000, 0.8814952561688429444, -0.4721928772777349570 ) ) ;
#92968=ADVANCED_FACE ( 'NONE', ( #165386 ), #46699, .T. ) ;
#92980=EDGE_CURVE ( 'NONE', #156438, #194512, #32112, .T. ) ;
#92981=AXIS2_PLACEMENT_3D ( 'NONE', #147529, #144940, #146229 ) ;
#93003=AXIS2_PLACEMENT_3D ( 'NONE', #37074, #175304, #194860 ) ;
#93019=ORIENTED_EDGE ( 'NONE', *, *, #24298, .T. ) ;
#93023=DIRECTION ( 'NONE',  ( 0.000000000000000000, -0.8814952561688430555, 0.4721928772777346239 ) ) ;
#93063=DIRECTION ( 'NONE',  ( -0.7071067811865388020, 0.6233112732207695128, -0.3338907855510773737 ) ) ;
#93109=CIRCLE ( 'NONE', #80621, 0.09999999999999978351 ) ;
#93118=VERTEX_POINT ( 'NONE', #170572 ) ;
#93127=ORIENTED_EDGE ( 'NONE', *, *, #147802, .T. ) ;
#93134=AXIS2_PLACEMENT_3D ( 'NONE', #25958, #84587, #8952 ) ;
#93145=CARTESIAN_POINT ( 'NONE',  ( -22.50014994444009275, 12.60373254347260641, -223.3361492492173852 ) ) ;
#93197=CARTESIAN_POINT ( 'NONE',  ( 21.04999999999988702, 1.599564567716171615, -230.7124193606981351 ) ) ;
#93204=ORIENTED_EDGE ( 'NONE', *, *, #58381, .T. ) ;
#93247=EDGE_CURVE ( 'NONE', #35062, #198003, #57186, .T. ) ;
#93265=PLANE ( 'NONE',  #70273 ) ;
#93273=FACE_OUTER_BOUND ( 'NONE', #49137, .T. ) ;
#93293=DIRECTION ( 'NONE',  ( 0.000000000000000000, 0.8814952561688442767, -0.4721928772777321814 ) ) ;
#93302=CARTESIAN_POINT ( 'NONE',  ( -23.25000000000000000, 46.46967969402478360, -243.0849751855955674 ) ) ;
#93324=CARTESIAN_POINT ( 'NONE',  ( -20.64999999999999858, 19.25956423861613231, -238.0467473098318010 ) ) ;
#93341=VECTOR ( 'NONE', #34865, 1000.000000000000000 ) ;
#93363=ORIENTED_EDGE ( 'NONE', *, *, #188462, .F. ) ;
#93364=CARTESIAN_POINT ( 'NONE',  ( -22.47071067811865319, 0.3704148268516942455, -229.9999874772930752 ) ) ;
#93375=DIRECTION ( 'NONE',  ( 0.000000000000000000, -0.4721928772777285732, -0.8814952561688463861 ) ) ;
#93392=CARTESIAN_POINT ( 'NONE',  ( 18.51997666896936678, 8.990719673716817795, -245.3850630519680465 ) ) ;
#93407=EDGE_CURVE ( 'NONE', #18374, #19709, #132226, .T. ) ;
#93441=LINE ( 'NONE', #156022, #114040 ) ;
#93442=ADVANCED_FACE ( 'NONE', ( #167656, #247157 ), #46384, .T. ) ;
#93457=CIRCLE ( 'NONE', #126794, 4.049999999999997158 ) ;
#93462=AXIS2_PLACEMENT_3D ( 'NONE', #34023, #52240, #93948 ) ;
#93466=DIRECTION ( 'NONE',  ( 0.000000000000000000, 0.4721928772777346239, 0.8814952561688430555 ) ) ;
#93472=EDGE_CURVE ( 'NONE', #197260, #18671, #69703, .T. ) ;
#93484=DIRECTION ( 'NONE',  ( 0.000000000000000000, 0.8814952561688440547, -0.4721928772777327921 ) ) ;
#93493=VERTEX_POINT ( 'NONE', #252286 ) ;
#93509=CARTESIAN_POINT ( 'NONE',  ( 18.59999999999999076, 34.53503747617446606, -235.1972745784239578 ) ) ;
#93525=EDGE_CURVE ( 'NONE', #26083, #245346, #7329, .T. ) ;
#93538=CARTESIAN_POINT ( 'NONE',  ( 22.43288208788031568, -3.137965819587316574, -228.2274994902323328 ) ) ;
#93541=EDGE_LOOP ( 'NONE', ( #218965, #166793, #143360, #142214 ) ) ;
#93557=VERTEX_POINT ( 'NONE', #50234 ) ;
#93559=DIRECTION ( 'NONE',  ( -1.000000000000000000, 0.000000000000000000, 0.000000000000000000 ) ) ;
#93580=EDGE_CURVE ( 'NONE', #11331, #76756, #219700, .T. ) ;
#93587=FACE_OUTER_BOUND ( 'NONE', #24893, .T. ) ;
#93613=ADVANCED_FACE ( 'NONE', ( #194921 ), #16289, .F. ) ;
#93620=ORIENTED_EDGE ( 'NONE', *, *, #104260, .F. ) ;
#93627=LINE ( 'NONE', #190172, #65854 ) ;
#93629=CARTESIAN_POINT ( 'NONE',  ( -20.64999999999999858, 19.96675702282871256, -237.7735354486364088 ) ) ;
#93705=LINE ( 'NONE', #148558, #137042 ) ;
#93708=EDGE_CURVE ( 'NONE', #170273, #43771, #11630, .T. ) ;
#93717=DIRECTION ( 'NONE',  ( 0.000000000000000000, 0.8814952561688476074, -0.4721928772777262417 ) ) ;
#93754=ORIENTED_EDGE ( 'NONE', *, *, #221006, .F. ) ;
#93766=VECTOR ( 'NONE', #12396, 1000.000000000000000 ) ;
#93791=ORIENTED_EDGE ( 'NONE', *, *, #220100, .F. ) ;
#93812=DIRECTION ( 'NONE',  ( 1.000000000000000000, 0.000000000000000000, 0.000000000000000000 ) ) ;
#93824=ORIENTED_EDGE ( 'NONE', *, *, #72631, .F. ) ;
#93850=DIRECTION ( 'NONE',  ( 0.000000000000000000, 0.8814952561688476074, -0.4721928772777262417 ) ) ;
#93882=DIRECTION ( 'NONE',  ( 1.000000000000000000, 1.394253735153569469E-16, 2.602809386958778209E-16 ) ) ;
#93907=ORIENTED_EDGE ( 'NONE', *, *, #131151, .T. ) ;
#93927=EDGE_LOOP ( 'NONE', ( #23012, #49955, #227460, #213618 ) ) ;
#93948=DIRECTION ( 'NONE',  ( 0.000000000000000000, 0.9994937237965558774, 0.03181660087586650476 ) ) ;
#93958=CIRCLE ( 'NONE', #135645, 0.1000000000000007550 ) ;
#94020=DIRECTION ( 'NONE',  ( 1.000000000000000000, 0.000000000000000000, 0.000000000000000000 ) ) ;
#94056=CARTESIAN_POINT ( 'NONE',  ( 20.22516295850462598, 18.77592805117411601, -228.7415353349608438 ) ) ;
#94085=EDGE_CURVE ( 'NONE', #11913, #50748, #3393, .T. ) ;
#94098=ORIENTED_EDGE ( 'NONE', *, *, #83795, .F. ) ;
#94107=DIRECTION ( 'NONE',  ( 0.000000000000000000, -0.4721928772776973204, -0.8814952561688629284 ) ) ;
#94121=ORIENTED_EDGE ( 'NONE', *, *, #107306, .F. ) ;
#94131=CARTESIAN_POINT ( 'NONE',  ( 18.52928932304239495, 33.73464088294735319, -236.3235076462605377 ) ) ;
#94140=VECTOR ( 'NONE', #124027, 1000.000000000000000 ) ;
#94167=CARTESIAN_POINT ( 'NONE',  ( -18.50000000000000000, 13.71992543034163958, -238.5823796952984992 ) ) ;
#94214=LINE ( 'NONE', #198458, #237509 ) ;
#94236=CARTESIAN_POINT ( 'NONE',  ( -23.15000000000000213, 27.73205844876672899, -240.0613753537626565 ) ) ;
#94277=CARTESIAN_POINT ( 'NONE',  ( 20.85000000000000142, 28.55432187084631934, -258.5393726171218418 ) ) ;
#94285=DIRECTION ( 'NONE',  ( -0.000000000000000000, 0.8814952561688430555, -0.4721928772777346239 ) ) ;
#94287=ORIENTED_EDGE ( 'NONE', *, *, #174064, .F. ) ;
#94294=CARTESIAN_POINT ( 'NONE',  ( -20.94999999999999929, 46.32970330538243786, -243.0551226933711746 ) ) ;
#94319=VERTEX_POINT ( 'NONE', #174779 ) ;
#94343=CIRCLE ( 'NONE', #253134, 0.09999999999999700795 ) ;
#94355=DIRECTION ( 'NONE',  ( 0.000000000000000000, 0.8814952561688428334, -0.4721928772777349570 ) ) ;
#94358=CARTESIAN_POINT ( 'NONE',  ( 20.85000000000000142, 43.21392023178792385, -245.1418509714632421 ) ) ;
#94443=CIRCLE ( 'NONE', #219350, 0.3999999999999994671 ) ;
#94460=CARTESIAN_POINT ( 'NONE',  ( -21.13614978966381841, 10.19766428898124211, -228.0037713484281880 ) ) ;
#94466=CARTESIAN_POINT ( 'NONE',  ( -21.05000000000000426, 10.02604994829658125, -228.1850015638761136 ) ) ;
#94470=EDGE_CURVE ( 'NONE', #231732, #215045, #68586, .T. ) ;
#94479=CARTESIAN_POINT ( 'NONE',  ( 21.04999999999436966, 1.394874610627388156, -230.6776777473732807 ) ) ;
#94490=DIRECTION ( 'NONE',  ( 0.000000000000000000, -0.5868805631290126001, -0.8096735173027292953 ) ) ;
#94503=DIRECTION ( 'NONE',  ( 0.000000000000000000, 0.8814952561688426114, -0.4721928772777353456 ) ) ;
#94540=CARTESIAN_POINT ( 'NONE',  ( -20.94999999999999929, 18.86061765788380740, -226.6874733728449485 ) ) ;
#94574=AXIS2_PLACEMENT_3D ( 'NONE', #90492, #170089, #249590 ) ;
#94592=DIRECTION ( 'NONE',  ( 0.000000000000000000, -0.4721928772777358452, -0.8814952561688423893 ) ) ;
#94601=ADVANCED_FACE ( 'NONE', ( #30761 ), #93265, .F. ) ;
#94606=ORIENTED_EDGE ( 'NONE', *, *, #237461, .T. ) ;
#94634=AXIS2_PLACEMENT_3D ( 'NONE', #33704, #235696, #256486 ) ;
#94645=ORIENTED_EDGE ( 'NONE', *, *, #154936, .F. ) ;
#94672=ORIENTED_EDGE ( 'NONE', *, *, #252209, .F. ) ;
#94685=( BOUNDED_SURFACE ( )  B_SPLINE_SURFACE ( 3, 2, ( 
 ( #154735, #19043, #218503 ),
 ( #234232, #236798, #76441 ),
 ( #115574, #214670, #255024 ),
 ( #156016, #55567, #98534 ),
 ( #217225, #235516, #116863 ),
 ( #196391, #17742, #197673 ) ),
 .UNSPECIFIED., .F., .F., .T. ) 
 B_SPLINE_SURFACE_WITH_KNOTS ( ( 4, 2, 4 ),
 ( 3, 3 ),
 ( 0.0001792624049599491926, 0.0003686986002124538345, 0.0005581347954649585035 ),
 ( 0.000000000000000000, 1.000000000000000000 ),
 .UNSPECIFIED. ) 
 GEOMETRIC_REPRESENTATION_ITEM ( )  RATIONAL_B_SPLINE_SURFACE ( (
 ( 1.000000000000000000, 0.9238795325112717505, 1.000000000000000000),
 ( 1.000000000000000000, 0.9229318695244472792, 1.000000000000000000),
 ( 1.000000000000000000, 0.8926288119222632877, 1.000000000000000000),
 ( 1.000000000000000000, 0.8123777807279800589, 1.000000000000000000),
 ( 1.000000000000000000, 0.7629087100925328047, 1.000000000000000000),
 ( 1.000000000000000000, 0.7071067811865475727, 1.000000000000000000) ) ) 
 REPRESENTATION_ITEM ( '' )  SURFACE ( )  );
#94698=DIRECTION ( 'NONE',  ( -1.000000000000000000, 0.000000000000000000, 0.000000000000000000 ) ) ;
#94711=DIRECTION ( 'NONE',  ( 1.000000000000000000, 0.000000000000000000, 0.000000000000000000 ) ) ;
#94714=ORIENTED_EDGE ( 'NONE', *, *, #190461, .T. ) ;
#94723=FACE_OUTER_BOUND ( 'NONE', #242349, .T. ) ;
#94731=CARTESIAN_POINT ( 'NONE',  ( -20.94999999999999929, 18.82290990851282331, -233.3604470821920529 ) ) ;
#94753=AXIS2_PLACEMENT_3D ( 'NONE', #14521, #253088, #57452 ) ;
#94758=ADVANCED_FACE ( 'NONE', ( #181800 ), #227339, .F. ) ;
#94768=ORIENTED_EDGE ( 'NONE', *, *, #47847, .T. ) ;
#94770=FACE_OUTER_BOUND ( 'NONE', #110403, .T. ) ;
#94785=CARTESIAN_POINT ( 'NONE',  ( -20.54999999999999716, 19.73066058418984170, -238.2142830767208466 ) ) ;
#94790=AXIS2_PLACEMENT_3D ( 'NONE', #190826, #53852, #228654 ) ;
#94806=VERTEX_POINT ( 'NONE', #26599 ) ;
#94817=DIRECTION ( 'NONE',  ( 0.000000000000000000, -0.4721928772777346239, -0.8814952561688430555 ) ) ;
#94833=FACE_OUTER_BOUND ( 'NONE', #147938, .T. ) ;
#94861=DIRECTION ( 'NONE',  ( -0.7071067811865474617, -0.3338907855510734324, -0.6233112732207618523 ) ) ;
#94895=AXIS2_PLACEMENT_3D ( 'NONE', #69584, #149123, #43586 ) ;
#94907=CARTESIAN_POINT ( 'NONE',  ( 20.95539060131842746, 18.89207542883556101, -227.9818558096623065 ) ) ;
#94922=EDGE_CURVE ( 'NONE', #60388, #30618, #169859, .T. ) ;
#94923=DIRECTION ( 'NONE',  ( 0.000000000000000000, 0.8814952561688430555, -0.4721928772777346239 ) ) ;
#94961=CYLINDRICAL_SURFACE ( 'NONE', #151736, 0.5000000000000008882 ) ;
#94993=CARTESIAN_POINT ( 'NONE',  ( 18.49999999999999289, 29.08883969319483498, -237.9520757887960940 ) ) ;
#94994=TOROIDAL_SURFACE ( 'NONE', #182510, 11.90000000000000391, 0.1000000000000000056 ) ;
#95043=ORIENTED_EDGE ( 'NONE', *, *, #119453, .F. ) ;
#95056=PLANE ( 'NONE',  #226233 ) ;
#95072=CARTESIAN_POINT ( 'NONE',  ( 21.05000000000000071, 40.27305497204160645, -251.4871534980821082 ) ) ;
#95087=DIRECTION ( 'NONE',  ( 1.000000000000000000, 0.000000000000000000, 0.000000000000000000 ) ) ;
#95094=CARTESIAN_POINT ( 'NONE',  ( -18.59999999999999787, 13.71992543034163958, -238.5823796952984992 ) ) ;
#95123=CIRCLE ( 'NONE', #190999, 0.5000000000000001110 ) ;
#95140=DIRECTION ( 'NONE',  ( 0.000000000000000000, 0.8814952561688476074, -0.4721928772777262417 ) ) ;
#95200=CARTESIAN_POINT ( 'NONE',  ( 20.95512820512820440, 22.85550638026973047, -230.1049725544161220 ) ) ;
#95229=ORIENTED_EDGE ( 'NONE', *, *, #236920, .T. ) ;
#95307=DIRECTION ( 'NONE',  ( 1.000000000000000000, 0.000000000000000000, 0.000000000000000000 ) ) ;
#95309=CARTESIAN_POINT ( 'NONE',  ( 21.14999999999999858, 22.98593783141596703, -230.0732594427593938 ) ) ;
#95310=CYLINDRICAL_SURFACE ( 'NONE', #185476, 0.09999999999999986677 ) ;
#95344=VERTEX_POINT ( 'NONE', #88788 ) ;
#95345=DIRECTION ( 'NONE',  ( 1.000000000000000000, 0.000000000000000000, 0.000000000000000000 ) ) ;
#95394=CARTESIAN_POINT ( 'NONE',  ( 21.05000000000000071, 36.65892442174935439, -249.5511627012433848 ) ) ;
#95415=ADVANCED_FACE ( 'NONE', ( #178659 ), #199430, .T. ) ;
#95422=CARTESIAN_POINT ( 'NONE',  ( 18.49999999999999289, 33.67810952736942198, -236.3734420906320679 ) ) ;
#95438=DIRECTION ( 'NONE',  ( 1.000000000000000000, -0.000000000000000000, -0.000000000000000000 ) ) ;
#95464=DIRECTION ( 'NONE',  ( 1.000000000000000000, 0.000000000000000000, 0.000000000000000000 ) ) ;
#95477=CIRCLE ( 'NONE', #228767, 11.74999999999999112 ) ;
#95528=CARTESIAN_POINT ( 'NONE',  ( -18.59999999999999787, 18.81339837015603322, -226.7756228984618190 ) ) ;
#95530=CARTESIAN_POINT ( 'NONE',  ( -20.64999999999999858, 36.65892442174935439, -249.5511627012433848 ) ) ;
#95550=AXIS2_PLACEMENT_3D ( 'NONE', #246442, #126490, #185184 ) ;
#95553=CARTESIAN_POINT ( 'NONE',  ( -20.90851465518106167, 46.44433919924416898, -243.0795225066946159 ) ) ;
#95557=DIRECTION ( 'NONE',  ( 0.000000000000000000, 0.6046243595031880469, 0.7965107556683460599 ) ) ;
#95579=DIRECTION ( 'NONE',  ( 0.000000000000000000, -0.8814952561688476074, 0.4721928772777262417 ) ) ;
#95580=ADVANCED_FACE ( 'NONE', ( #181208 ), #243731, .T. ) ;
#95592=EDGE_CURVE ( 'NONE', #207603, #15847, #178593, .T. ) ;
#95626=CARTESIAN_POINT ( 'NONE',  ( 18.59999999999999076, 28.81810206650552075, -238.0339362645743222 ) ) ;
#95631=DIRECTION ( 'NONE',  ( 1.000000000000000000, -0.000000000000000000, -0.000000000000000000 ) ) ;
#95667=ORIENTED_EDGE ( 'NONE', *, *, #254894, .T. ) ;
#95722=ORIENTED_EDGE ( 'NONE', *, *, #95798, .T. ) ;
#95737=ORIENTED_EDGE ( 'NONE', *, *, #70450, .F. ) ;
#95745=CARTESIAN_POINT ( 'NONE',  ( 18.49999999999999289, 9.070023979453765151, -245.4580351522096748 ) ) ;
#95747=LINE ( 'NONE', #159605, #162335 ) ;
#95770=DIRECTION ( 'NONE',  ( 0.000000000000000000, 0.8814952561688428334, -0.4721928772777350125 ) ) ;
#95771=ORIENTED_EDGE ( 'NONE', *, *, #147447, .T. ) ;
#95772=ORIENTED_EDGE ( 'NONE', *, *, #214510, .F. ) ;
#95776=DIRECTION ( 'NONE',  ( 0.000000000000000000, 0.4721928772777346239, 0.8814952561688430555 ) ) ;
#95787=ORIENTED_EDGE ( 'NONE', *, *, #204280, .T. ) ;
#95798=EDGE_CURVE ( 'NONE', #173295, #1463, #92350, .T. ) ;
#95827=ORIENTED_EDGE ( 'NONE', *, *, #242514, .F. ) ;
#95841=EDGE_CURVE ( 'NONE', #155156, #38568, #70263, .T. ) ;
#95877=AXIS2_PLACEMENT_3D ( 'NONE', #195150, #131292, #251226 ) ;
#95915=VERTEX_POINT ( 'NONE', #96191 ) ;
#95951=EDGE_CURVE ( 'NONE', #186480, #156438, #6074, .T. ) ;
#95987=CARTESIAN_POINT ( 'NONE',  ( -18.40000000000000213, 8.812905490826906885, -245.4119551738195071 ) ) ;
#95990=CARTESIAN_POINT ( 'NONE',  ( -21.04999999999999716, 36.17635217701701578, -235.9630383263116187 ) ) ;
#95995=CARTESIAN_POINT ( 'NONE',  ( -22.60000000000094289, -3.180729737798059009, -228.0957332317256885 ) ) ;
#96017=DIRECTION ( 'NONE',  ( 0.000000000000000000, -0.8740096314914906905, 0.4859085964048265316 ) ) ;
#96018=FACE_OUTER_BOUND ( 'NONE', #5659, .T. ) ;
#96028=DIRECTION ( 'NONE',  ( 0.000000000000000000, -0.8814952561685467369, 0.4721928772782874595 ) ) ;
#96046=ORIENTED_EDGE ( 'NONE', *, *, #173663, .F. ) ;
#96055=CARTESIAN_POINT ( 'NONE',  ( 21.14999999999999858, 1.363275264940682741, -230.6442496871288483 ) ) ;
#96087=DIRECTION ( 'NONE',  ( 1.000000000000000000, 0.000000000000000000, 0.000000000000000000 ) ) ;
#96113=DIRECTION ( 'NONE',  ( 0.000000000000000000, 0.8814952561688476074, -0.4721928772777262417 ) ) ;
#96117=CARTESIAN_POINT ( 'NONE',  ( -23.25000000000000000, 4.360421613930902218, -245.4659189663672691 ) ) ;
#96134=DIRECTION ( 'NONE',  ( 0.000000000000000000, 0.8814952561688476074, -0.4721928772777262417 ) ) ;
#96143=CARTESIAN_POINT ( 'NONE',  ( 21.05000000000000071, 18.71355990949045633, -229.9253020726244188 ) ) ;
#96156=CARTESIAN_POINT ( 'NONE',  ( -20.94999999999999929, 16.50669723772569952, -240.7258389668962479 ) ) ;
#96161=EDGE_LOOP ( 'NONE', ( #36241, #196926, #22254, #182017 ) ) ;
#96191=CARTESIAN_POINT ( 'NONE',  ( -23.25000000000000000, 11.39998237908105416, -245.7725481090871540 ) ) ;
#96207=ORIENTED_EDGE ( 'NONE', *, *, #158030, .T. ) ;
#96230=ORIENTED_EDGE ( 'NONE', *, *, #194300, .F. ) ;
#96253=DIRECTION ( 'NONE',  ( 2.952720810173289605E-16, -0.4721928772777354011, -0.8814952561688425003 ) ) ;
#96271=CIRCLE ( 'NONE', #133699, 0.09999999999999939493 ) ;
#96277=DIRECTION ( 'NONE',  ( 0.000000000000000000, 0.8814952561688476074, -0.4721928772777262417 ) ) ;
#96353=DIRECTION ( 'NONE',  ( 1.000000000000000000, 0.000000000000000000, 0.000000000000000000 ) ) ;
#96375=CARTESIAN_POINT ( 'NONE',  ( -23.25000000000000000, 43.27008861172207332, -245.2265230569236110 ) ) ;
#96378=ORIENTED_EDGE ( 'NONE', *, *, #191032, .T. ) ;
#96391=CIRCLE ( 'NONE', #108875, 0.1000000000000013933 ) ;
#96434=ORIENTED_EDGE ( 'NONE', *, *, #163668, .T. ) ;
#96494=DIRECTION ( 'NONE',  ( 1.000000000000000000, 0.000000000000000000, 0.000000000000000000 ) ) ;
#96555=AXIS2_PLACEMENT_3D ( 'NONE', #56997, #136546, #139092 ) ;
#96582=DIRECTION ( 'NONE',  ( 0.7071067811865708874, -0.3338907855511046296, -0.6233112732207185536 ) ) ;
#96621=CARTESIAN_POINT ( 'NONE',  ( -20.54999999999999716, 12.46703344576493144, -249.9218526068032133 ) ) ;
#96653=ORIENTED_EDGE ( 'NONE', *, *, #40329, .F. ) ;
#96654=AXIS2_PLACEMENT_3D ( 'NONE', #214219, #35609, #115112 ) ;
#96660=CYLINDRICAL_SURFACE ( 'NONE', #171160, 0.09999999999999031886 ) ;
#96714=CIRCLE ( 'NONE', #55195, 0.1000000000000013933 ) ;
#96717=DIRECTION ( 'NONE',  ( -2.915501640297154776E-16, 0.4721928772777346794, 0.8814952561688429444 ) ) ;
#96784=EDGE_CURVE ( 'NONE', #29239, #241214, #55889, .T. ) ;
#96793=DIRECTION ( 'NONE',  ( 0.000000000000000000, 0.8814952561688427224, -0.4721928772777352901 ) ) ;
#96799=DIRECTION ( 'NONE',  ( 0.000000000000000000, -0.4721928772777380656, -0.8814952561688412791 ) ) ;
#96811=CARTESIAN_POINT ( 'NONE',  ( 18.59999999999999432, 16.60731133254646963, -240.9277311905271688 ) ) ;
#96851=DIRECTION ( 'NONE',  ( -0.000000000000000000, -0.8814952561688430555, 0.4721928772777346239 ) ) ;
#96853=DIRECTION ( 'NONE',  ( 2.342056488767300981E-15, 0.8096735173027139743, -0.5868805631290339164 ) ) ;
#96861=ORIENTED_EDGE ( 'NONE', *, *, #123043, .T. ) ;
#96876=AXIS2_PLACEMENT_3D ( 'NONE', #36352, #175856, #18041 ) ;
#96884=VECTOR ( 'NONE', #121797, 1000.000000000000000 ) ;
#96899=LINE ( 'NONE', #94358, #52681 ) ;
#96915=AXIS2_PLACEMENT_3D ( 'NONE', #126435, #5175, #48178 ) ;
#96961=DIRECTION ( 'NONE',  ( 0.000000000000000000, 0.8814952561688434995, -0.4721928772777335137 ) ) ;
#96969=CARTESIAN_POINT ( 'NONE',  ( -18.59999999999999787, 30.14024212288317628, -235.5657495473015501 ) ) ;
#96977=EDGE_LOOP ( 'NONE', ( #203227, #19683, #158798, #45285 ) ) ;
#96985=AXIS2_PLACEMENT_3D ( 'NONE', #162714, #25756, #223937 ) ;
#96996=VECTOR ( 'NONE', #804, 1000.000000000000000 ) ;
#96997=CARTESIAN_POINT ( 'NONE',  ( -21.09610168723073542, 10.11132180231042810, -228.0938213842520383 ) ) ;
#97015=CARTESIAN_POINT ( 'NONE',  ( 21.11101077988997332, 10.14857762567122457, -228.0630360965454315 ) ) ;
#97016=VERTEX_POINT ( 'NONE', #243535 ) ;
#97026=EDGE_LOOP ( 'NONE', ( #137960, #97311, #32941 ) ) ;
#97040=ORIENTED_EDGE ( 'NONE', *, *, #202684, .F. ) ;
#97044=VERTEX_POINT ( 'NONE', #29661 ) ;
#97047=CARTESIAN_POINT ( 'NONE',  ( -23.25000000000000000, 36.65892442174935439, -249.5511627012433848 ) ) ;
#97079=DIRECTION ( 'NONE',  ( 1.000000000000000000, -0.000000000000000000, -0.000000000000000000 ) ) ;
#97114=EDGE_CURVE ( 'NONE', #218153, #28211, #29479, .T. ) ;
#97116=ORIENTED_EDGE ( 'NONE', *, *, #156373, .T. ) ;
#97125=DIRECTION ( 'NONE',  ( 0.000000000000000000, 0.8814952561688444987, -0.4721928772777320149 ) ) ;
#97144=CARTESIAN_POINT ( 'NONE',  ( -18.50000000000000711, 18.86061765788380740, -226.6874733728449485 ) ) ;
#97168=DIRECTION ( 'NONE',  ( -0.000000000000000000, -0.4721928772777351790, -0.8814952561688427224 ) ) ;
#97178=FACE_OUTER_BOUND ( 'NONE', #247088, .T. ) ;
#97226=VERTEX_POINT ( 'NONE', #164672 ) ;
#97235=CARTESIAN_POINT ( 'NONE',  ( 23.15000000000000213, 11.43341603104965110, -245.8667934851861787 ) ) ;
#97252=DIRECTION ( 'NONE',  ( -0.000000000000000000, -0.8814952561688430555, 0.4721928772777346239 ) ) ;
#97279=ORIENTED_EDGE ( 'NONE', *, *, #219735, .T. ) ;
#97311=ORIENTED_EDGE ( 'NONE', *, *, #12578, .T. ) ;
#97317=CARTESIAN_POINT ( 'NONE',  ( 18.49999999999999645, 36.65892442174935439, -249.5511627012433848 ) ) ;
#97328=DIRECTION ( 'NONE',  ( 1.000000000000000000, 0.000000000000000000, 0.000000000000000000 ) ) ;
#97371=AXIS2_PLACEMENT_3D ( 'NONE', #95626, #193471, #16130 ) ;
#97375=DIRECTION ( 'NONE',  ( 0.000000000000000000, -0.8814952561688476074, 0.4721928772777262417 ) ) ;
#97380=DIRECTION ( 'NONE',  ( 0.000000000000000000, 0.8814952561688438326, -0.4721928772777332362 ) ) ;
#97388=ADVANCED_FACE ( 'NONE', ( #225887 ), #171133, .F. ) ;
#97404=VERTEX_POINT ( 'NONE', #151553 ) ;
#97441=DIRECTION ( 'NONE',  ( 0.000000000000000000, 0.4721928772777331251, 0.8814952561688439436 ) ) ;
#97446=CARTESIAN_POINT ( 'NONE',  ( 21.04999999999999716, 18.76843759928042843, -228.0065070820658093 ) ) ;
#97463=LINE ( 'NONE', #233187, #254225 ) ;
#97478=VERTEX_POINT ( 'NONE', #197048 ) ;
#97487=CARTESIAN_POINT ( 'NONE',  ( 21.00023020733503643, 1.495312417593671173, -230.7149783752102508 ) ) ;
#97506=EDGE_LOOP ( 'NONE', ( #198689, #23660, #14096 ) ) ;
#97547=FACE_OUTER_BOUND ( 'NONE', #71976, .T. ) ;
#97560=EDGE_LOOP ( 'NONE', ( #55075, #239630, #32648, #203166 ) ) ;
#97562=CIRCLE ( 'NONE', #30989, 4.000000000000010658 ) ;
#97573=EDGE_CURVE ( 'NONE', #57307, #71383, #58746, .T. ) ;
#97591=AXIS2_PLACEMENT_3D ( 'NONE', #13824, #12561, #16412 ) ;
#97595=DIRECTION ( 'NONE',  ( 1.000000000000000000, 0.000000000000000000, 0.000000000000000000 ) ) ;
#97673=CIRCLE ( 'NONE', #243431, 0.09999999999999986677 ) ;
#97678=CARTESIAN_POINT ( 'NONE',  ( 21.00000000000000000, 30.37633856152204359, -235.1250019192171408 ) ) ;
#97679=ORIENTED_EDGE ( 'NONE', *, *, #33768, .F. ) ;
#97681=VERTEX_POINT ( 'NONE', #224327 ) ;
#97739=CIRCLE ( 'NONE', #168744, 0.1000000000000013933 ) ;
#97748=EDGE_LOOP ( 'NONE', ( #218369, #218680, #147091, #164044 ) ) ;
#97758=CARTESIAN_POINT ( 'NONE',  ( -18.50000000000000000, 31.44980407958351165, -233.5445995079518866 ) ) ;
#97853=VECTOR ( 'NONE', #101278, 1000.000000000000000 ) ;
#97856=EDGE_CURVE ( 'NONE', #19319, #186847, #225877, .T. ) ;
#97878=CARTESIAN_POINT ( 'NONE',  ( -20.64999999999999858, 23.68770167995059595, -252.8127582590406348 ) ) ;
#97879=VECTOR ( 'NONE', #45017, 1000.000000000000000 ) ;
#97883=AXIS2_PLACEMENT_3D ( 'NONE', #15653, #75620, #234669 ) ;
#97891=ORIENTED_EDGE ( 'NONE', *, *, #230098, .F. ) ;
#97898=CARTESIAN_POINT ( 'NONE',  ( -23.15000000000000213, 24.21659883365190069, -253.0960739854072870 ) ) ;
#97912=ORIENTED_EDGE ( 'NONE', *, *, #64395, .T. ) ;
#97919=EDGE_CURVE ( 'NONE', #209722, #97226, #5305, .T. ) ;
#97931=TOROIDAL_SURFACE ( 'NONE', #14796, 0.9750000000000019762, 0.1000000000000000056 ) ;
#97952=EDGE_CURVE ( 'NONE', #203639, #234056, #192915, .T. ) ;
#97955=FACE_OUTER_BOUND ( 'NONE', #42218, .T. ) ;
#97968=AXIS2_PLACEMENT_3D ( 'NONE', #159817, #239341, #38573 ) ;
#97970=CARTESIAN_POINT ( 'NONE',  ( 18.49999999999999289, 33.67810952736942198, -236.3734420906320395 ) ) ;
#97984=DIRECTION ( 'NONE',  ( 0.000000000000000000, -0.4721928772777346239, -0.8814952561688430555 ) ) ;
#97990=CIRCLE ( 'NONE', #14845, 12.97500000000000320 ) ;
#98007=LINE ( 'NONE', #18509, #240857 ) ;
#98008=FACE_OUTER_BOUND ( 'NONE', #102021, .T. ) ;
#98059=FACE_OUTER_BOUND ( 'NONE', #241831, .T. ) ;
#98081=DIRECTION ( 'NONE',  ( -1.000000000000000000, -1.394253735153569469E-16, -2.602809386958778209E-16 ) ) ;
#98088=EDGE_LOOP ( 'NONE', ( #175779, #196366, #172930, #130719 ) ) ;
#98089=CARTESIAN_POINT ( 'NONE',  ( -20.85000000000000142, 46.46967969402478360, -243.0849751855955674 ) ) ;
#98101=AXIS2_PLACEMENT_3D ( 'NONE', #231085, #31611, #94107 ) ;
#98106=FACE_OUTER_BOUND ( 'NONE', #50195, .T. ) ;
#98126=FACE_OUTER_BOUND ( 'NONE', #99869, .T. ) ;
#98137=DIRECTION ( 'NONE',  ( 0.000000000000000000, 0.8454177738465994407, 0.5341055959866553016 ) ) ;
#98147=CARTESIAN_POINT ( 'NONE',  ( 20.94999999999999929, 30.48950451747912993, -239.6099224343151946 ) ) ;
#98163=ORIENTED_EDGE ( 'NONE', *, *, #141038, .T. ) ;
#98184=ADVANCED_FACE ( 'NONE', ( #127488 ), #172167, .T. ) ;
#98189=VERTEX_POINT ( 'NONE', #190030 ) ;
#98214=CARTESIAN_POINT ( 'NONE',  ( -18.31331870001019624, 38.21057351245658396, -261.2006551925339863 ) ) ;
#98226=CARTESIAN_POINT ( 'NONE',  ( -21.05000000000000071, 28.37802281961254636, -258.4449340416662722 ) ) ;
#98264=VECTOR ( 'NONE', #58687, 1000.000000000000000 ) ;
#98268=AXIS2_PLACEMENT_3D ( 'NONE', #203492, #43140, #240055 ) ;
#98281=ADVANCED_FACE ( 'NONE', ( #54359 ), #135169, .F. ) ;
#98300=CARTESIAN_POINT ( 'NONE',  ( 21.14250536705908345, 10.20666781488608166, -227.9869634596271908 ) ) ;
#98302=DIRECTION ( 'NONE',  ( 1.387778780781341167E-13, 0.4721928772776973204, 0.8814952561688629284 ) ) ;
#98332=AXIS2_PLACEMENT_3D ( 'NONE', #172866, #73741, #133686 ) ;
#98335=DIRECTION ( 'NONE',  ( -0.000000000000000000, -0.8814952561688430555, 0.4721928772777346239 ) ) ;
#98363=ORIENTED_EDGE ( 'NONE', *, *, #229809, .T. ) ;
#98380=ADVANCED_FACE ( 'NONE', ( #94770 ), #84580, .T. ) ;
#98424=ORIENTED_EDGE ( 'NONE', *, *, #124554, .T. ) ;
#98428=VERTEX_POINT ( 'NONE', #238122 ) ;
#98433=ORIENTED_EDGE ( 'NONE', *, *, #100390, .F. ) ;
#98453=CARTESIAN_POINT ( 'NONE',  ( 23.24999999999999645, 28.36802138732021206, -238.7571110118315971 ) ) ;
#98528=ORIENTED_EDGE ( 'NONE', *, *, #219597, .T. ) ;
#98530=CARTESIAN_POINT ( 'NONE',  ( -22.50000000000093792, -3.180729737798012824, -228.0957332317256032 ) ) ;
#98534=CARTESIAN_POINT ( 'NONE',  ( 21.05000000000000071, 10.23309999692112804, -228.1193230868212254 ) ) ;
#98565=EDGE_CURVE ( 'NONE', #89253, #192243, #96271, .T. ) ;
#98580=DIRECTION ( 'NONE',  ( 1.000000000000000000, 0.000000000000000000, 0.000000000000000000 ) ) ;
#98621=VERTEX_POINT ( 'NONE', #144147 ) ;
#98675=VECTOR ( 'NONE', #9702, 1000.000000000000000 ) ;
#98682=DIRECTION ( 'NONE',  ( 0.000000000000000000, -0.4721928772777346239, -0.8814952561688430555 ) ) ;
#98749=VERTEX_POINT ( 'NONE', #170210 ) ;
#98756=FACE_OUTER_BOUND ( 'NONE', #136085, .T. ) ;
#98757=DIRECTION ( 'NONE',  ( 1.000000000000000000, 0.000000000000000000, 0.000000000000000000 ) ) ;
#98772=DIRECTION ( 'NONE',  ( 1.000000000000000000, 0.000000000000000000, 0.000000000000000000 ) ) ;
#98778=VECTOR ( 'NONE', #171569, 1000.000000000000000 ) ;
#98790=ORIENTED_EDGE ( 'NONE', *, *, #6850, .F. ) ;
#98807=DIRECTION ( 'NONE',  ( 0.000000000000000000, 0.4583618696494374256, 0.8887656589064814039 ) ) ;
#98830=CARTESIAN_POINT ( 'NONE',  ( 23.15000000000000213, -8.729782940176418649, -238.4538547387928986 ) ) ;
#98841=CARTESIAN_POINT ( 'NONE',  ( 23.14999999999999858, 28.40523720341322544, -239.6697522603257937 ) ) ;
#98843=CARTESIAN_POINT ( 'NONE',  ( 21.13507111622890022, 22.98723109724109293, -230.0690844087343407 ) ) ;
#98845=AXIS2_PLACEMENT_3D ( 'NONE', #75874, #194571, #233678 ) ;
#98870=AXIS2_PLACEMENT_3D ( 'NONE', #74981, #230169, #94503 ) ;
#98877=DIRECTION ( 'NONE',  ( 0.000000000000000000, -0.4721928772777212457, -0.8814952561688502719 ) ) ;
#98964=DIRECTION ( 'NONE',  ( -1.000000000000000000, -0.000000000000000000, -0.000000000000000000 ) ) ;
#98969=EDGE_LOOP ( 'NONE', ( #73508, #247708, #36377, #395, #29637 ) ) ;
#98982=CIRCLE ( 'NONE', #132320, 4.049999999999994493 ) ;
#99012=ORIENTED_EDGE ( 'NONE', *, *, #187446, .T. ) ;
#99029=AXIS2_PLACEMENT_3D ( 'NONE', #90612, #150612, #213140 ) ;
#99044=CARTESIAN_POINT ( 'NONE',  ( 22.45305468355011058, -3.275978944803229709, -228.2735455795371422 ) ) ;
#99085=DIRECTION ( 'NONE',  ( 0.000000000000000000, 0.8814952561688429444, -0.4721928772777345684 ) ) ;
#99095=VECTOR ( 'NONE', #145942, 1000.000000000000000 ) ;
#99106=DIRECTION ( 'NONE',  ( -1.000000000000000000, -2.081668171172181135E-13, -2.775557561562908012E-13 ) ) ;
#99150=ADVANCED_FACE ( 'NONE', ( #162829 ), #50274, .T. ) ;
#99160=CARTESIAN_POINT ( 'NONE',  ( -21.05000000000000071, 13.63177590472475487, -238.5351604075707144 ) ) ;
#99203=FACE_OUTER_BOUND ( 'NONE', #161985, .T. ) ;
#99235=B_SPLINE_CURVE_WITH_KNOTS ( 'NONE', 3,
 ( #50542, #212233, #208384, #33627, #11461, #251324, #107982, #51829, #188793, #10169 ),
 .UNSPECIFIED., .F., .F.,
 ( 4, 3, 3, 4 ),
 ( 0.000000000000000000, 0.0002000000000008579659, 0.001000000000082967942, 0.001967863649483335853 ),
 .UNSPECIFIED. ) ;
#99236=ORIENTED_EDGE ( 'NONE', *, *, #93708, .T. ) ;
#99237=ORIENTED_EDGE ( 'NONE', *, *, #58658, .F. ) ;
#99244=DIRECTION ( 'NONE',  ( 0.000000000000000000, -0.8814952561688425003, 0.4721928772777359007 ) ) ;
#99248=ORIENTED_EDGE ( 'NONE', *, *, #31213, .T. ) ;
#99276=CARTESIAN_POINT ( 'NONE',  ( 18.55857864376267941, 33.84113875905941171, -236.2808750561533486 ) ) ;
#99285=DIRECTION ( 'NONE',  ( 0.000000000000000000, 0.8814952561688429444, -0.4721928772777345684 ) ) ;
#99296=DIRECTION ( 'NONE',  ( -1.000000000000000000, -0.000000000000000000, -0.000000000000000000 ) ) ;
#99313=AXIS2_PLACEMENT_3D ( 'NONE', #116129, #210100, #110982 ) ;
#99328=CARTESIAN_POINT ( 'NONE',  ( 21.05000000000000071, 1.627786319807488669, -244.0021210468063089 ) ) ;
#99341=EDGE_CURVE ( 'NONE', #51015, #69221, #179318, .T. ) ;
#99365=VECTOR ( 'NONE', #102253, 1000.000000000000000 ) ;
#99375=CARTESIAN_POINT ( 'NONE',  ( -20.64999999999999858, 19.35378350773087419, -238.0802544632095987 ) ) ;
#99382=DIRECTION ( 'NONE',  ( 0.000000000000000000, 0.9371753822965315228, -0.3488585713686134238 ) ) ;
#99385=CARTESIAN_POINT ( 'NONE',  ( -20.86777300164945004, 46.46797214202639026, -243.0846070113367432 ) ) ;
#99386=VERTEX_POINT ( 'NONE', #66283 ) ;
#99396=DIRECTION ( 'NONE',  ( 0.000000000000000000, -0.4721928772777346239, -0.8814952561688430555 ) ) ;
#99405=AXIS2_PLACEMENT_3D ( 'NONE', #233465, #54787, #35285 ) ;
#99422=DIRECTION ( 'NONE',  ( 0.000000000000000000, 0.8814952561688429444, -0.4721928772777345684 ) ) ;
#99425=ADVANCED_FACE ( 'NONE', ( #17836 ), #236895, .F. ) ;
#99429=EDGE_CURVE ( 'NONE', #167398, #195393, #255122, .T. ) ;
#99473=AXIS2_PLACEMENT_3D ( 'NONE', #80317, #140307, #41260 ) ;
#99515=ORIENTED_EDGE ( 'NONE', *, *, #87265, .T. ) ;
#99544=CARTESIAN_POINT ( 'NONE',  ( -22.47071067811865319, 7.128833340093095217, -233.7327013124392749 ) ) ;
#99555=AXIS2_PLACEMENT_3D ( 'NONE', #148479, #49377, #128917 ) ;
#99571=ORIENTED_EDGE ( 'NONE', *, *, #250111, .T. ) ;
#99610=ORIENTED_EDGE ( 'NONE', *, *, #4667, .T. ) ;
#99618=EDGE_CURVE ( 'NONE', #78573, #31642, #163793, .T. ) ;
#99620=DIRECTION ( 'NONE',  ( -0.000000000000000000, 0.4721928772777345684, 0.8814952561688429444 ) ) ;
#99624=DIRECTION ( 'NONE',  ( -1.000000000000000000, 0.000000000000000000, 0.000000000000000000 ) ) ;
#99634=VECTOR ( 'NONE', #250186, 1000.000000000000114 ) ;
#99635=CARTESIAN_POINT ( 'NONE',  ( -21.59142135623730852, 21.72201384040852901, -232.6445455858938658 ) ) ;
#99680=LINE ( 'NONE', #236644, #71895 ) ;
#99704=DIRECTION ( 'NONE',  ( 0.000000000000000000, -0.7960711469212456981, 0.6052030477777622375 ) ) ;
#99711=EDGE_CURVE ( 'NONE', #114510, #70602, #204397, .T. ) ;
#99727=DIRECTION ( 'NONE',  ( 0.000000000000000000, -0.4721928772777597705, -0.8814952561688296218 ) ) ;
#99733=ORIENTED_EDGE ( 'NONE', *, *, #248185, .T. ) ;
#99758=ORIENTED_EDGE ( 'NONE', *, *, #28529, .F. ) ;
#99764=CARTESIAN_POINT ( 'NONE',  ( 21.05000000000000071, 4.481636728799211156, -245.1292951062512770 ) ) ;
#99782=EDGE_CURVE ( 'NONE', #72959, #229996, #243302, .T. ) ;
#99813=ORIENTED_EDGE ( 'NONE', *, *, #83952, .T. ) ;
#99869=EDGE_LOOP ( 'NONE', ( #193674, #165885, #228020, #208960 ) ) ;
#99896=CARTESIAN_POINT ( 'NONE',  ( 18.59999999999999076, 34.53503747617446606, -235.1972745784239578 ) ) ;
#99912=ORIENTED_EDGE ( 'NONE', *, *, #24863, .T. ) ;
#99915=AXIS2_PLACEMENT_3D ( 'NONE', #192053, #129494, #51201 ) ;
#99920=EDGE_LOOP ( 'NONE', ( #58619, #72721, #237746, #193270 ) ) ;
#99954=DIRECTION ( 'NONE',  ( 0.000000000000000000, 0.8814952561688430555, -0.4721928772777346239 ) ) ;
#99962=CARTESIAN_POINT ( 'NONE',  ( -23.15000000000000213, -8.777002227904194598, -238.5420042644097975 ) ) ;
#99966=ORIENTED_EDGE ( 'NONE', *, *, #212258, .F. ) ;
#99972=CARTESIAN_POINT ( 'NONE',  ( -20.94999999999999929, 43.30036367478129478, -245.0872390055602352 ) ) ;
#99993=LINE ( 'NONE', #158750, #234316 ) ;
#99999=EDGE_CURVE ( 'NONE', #222451, #117081, #63113, .T. ) ;
#100009=CARTESIAN_POINT ( 'NONE',  ( 21.04999999999999716, 18.83004532744374870, -227.9662487122261609 ) ) ;
#100011=DIRECTION ( 'NONE',  ( 1.000000000000000000, 1.541880601228652843E-16, 2.878400969107353907E-16 ) ) ;
#100034=CIRCLE ( 'NONE', #20993, 0.1000000000000076522 ) ;
#100049=CARTESIAN_POINT ( 'NONE',  ( 18.49999999999999645, 42.96960653111219131, -254.4772109693542745 ) ) ;
#100057=CARTESIAN_POINT ( 'NONE',  ( 21.93340585898891604, 0.6726324846061126905, -230.2742912564565927 ) ) ;
#100061=CARTESIAN_POINT ( 'NONE',  ( 18.39999999999999858, 37.95493834378066111, -261.2294694241335264 ) ) ;
#100063=DIRECTION ( 'NONE',  ( 1.000000000000000000, 0.000000000000000000, 0.000000000000000000 ) ) ;
#100091=DIRECTION ( 'NONE',  ( -0.7071067811865474617, -0.3338907855510734324, -0.6233112732207618523 ) ) ;
#100127=EDGE_LOOP ( 'NONE', ( #23001, #135983, #29384, #183378 ) ) ;
#100134=CARTESIAN_POINT ( 'NONE',  ( 21.06490991615909536, 22.95056430979463968, -230.0412660441067487 ) ) ;
#100139=ORIENTED_EDGE ( 'NONE', *, *, #166615, .T. ) ;
#100162=AXIS2_PLACEMENT_3D ( 'NONE', #68848, #44142, #148371 ) ;
#100178=EDGE_CURVE ( 'NONE', #224941, #227874, #83888, .T. ) ;
#100199=VERTEX_POINT ( 'NONE', #27852 ) ;
#100243=ORIENTED_EDGE ( 'NONE', *, *, #100178, .F. ) ;
#100252=CARTESIAN_POINT ( 'NONE',  ( -18.59999999999999787, 46.02130280899747561, -256.6489974955837852 ) ) ;
#100264=AXIS2_PLACEMENT_3D ( 'NONE', #127900, #131743, #232146 ) ;
#100281=AXIS2_PLACEMENT_3D ( 'NONE', #160749, #158195, #180283 ) ;
#100318=CARTESIAN_POINT ( 'NONE',  ( -23.25000000000000000, 34.80778438379478246, -248.5595576589601592 ) ) ;
#100351=DIRECTION ( 'NONE',  ( 1.000000000000000000, 0.000000000000000000, 0.000000000000000000 ) ) ;
#100370=AXIS2_PLACEMENT_3D ( 'NONE', #88250, #249924, #248634 ) ;
#100390=EDGE_CURVE ( 'NONE', #165408, #7150, #57343, .T. ) ;
#100464=EDGE_CURVE ( 'NONE', #89253, #24478, #114777, .T. ) ;
#100477=EDGE_CURVE ( 'NONE', #85514, #78573, #246474, .T. ) ;
#100523=CARTESIAN_POINT ( 'NONE',  ( 18.59999999999999076, 28.95347087985017609, -237.9930060266852081 ) ) ;
#100546=VERTEX_POINT ( 'NONE', #100318 ) ;
#100563=ORIENTED_EDGE ( 'NONE', *, *, #166800, .F. ) ;
#100623=CARTESIAN_POINT ( 'NONE',  ( 18.59999999999999076, 14.77103648604101593, -236.4083752604500717 ) ) ;
#100672=EDGE_CURVE ( 'NONE', #64541, #9313, #152014, .T. ) ;
#100698=DIRECTION ( 'NONE',  ( 0.000000000000000000, 0.8753622295931610120, -0.4834676483506316624 ) ) ;
#100719=CARTESIAN_POINT ( 'NONE',  ( -20.94999999999999929, 36.65892442174935439, -249.5511627012433848 ) ) ;
#100724=CYLINDRICAL_SURFACE ( 'NONE', #178105, 0.09999999999999939493 ) ;
#100759=CARTESIAN_POINT ( 'NONE',  ( -20.94999999999999929, 18.18127959618848521, -237.5711165786817389 ) ) ;
#100762=AXIS2_PLACEMENT_3D ( 'NONE', #221749, #62713, #99244 ) ;
#100768=FACE_OUTER_BOUND ( 'NONE', #57348, .T. ) ;
#100802=AXIS2_PLACEMENT_3D ( 'NONE', #24445, #42692, #183495 ) ;
#100818=DIRECTION ( 'NONE',  ( -1.000000000000000000, 0.000000000000000000, 0.000000000000000000 ) ) ;
#100823=VERTEX_POINT ( 'NONE', #215788 ) ;
#100826=CYLINDRICAL_SURFACE ( 'NONE', #7424, 0.09999999999999939493 ) ;
#100831=EDGE_CURVE ( 'NONE', #203294, #41556, #99680, .T. ) ;
#100854=DIRECTION ( 'NONE',  ( 1.000000000000000000, -0.000000000000000000, -0.000000000000000000 ) ) ;
#100862=ORIENTED_EDGE ( 'NONE', *, *, #39632, .T. ) ;
#100890=ORIENTED_EDGE ( 'NONE', *, *, #246282, .T. ) ;
#100892=LINE ( 'NONE', #142614, #46063 ) ;
#100896=CARTESIAN_POINT ( 'NONE',  ( -18.49499033040907037, 9.017344637215625625, -245.4513013645828039 ) ) ;
#100907=VECTOR ( 'NONE', #22198, 1000.000000000000227 ) ;
#100951=CONICAL_SURFACE ( 'NONE', #92622, 4.049999999999996270, 0.7853981633974604915 ) ;
#100959=CARTESIAN_POINT ( 'NONE',  ( 21.05000000000000071, 4.184122562697137226, -245.3714803909117279 ) ) ;
#100963=CARTESIAN_POINT ( 'NONE',  ( -23.25000000000000000, 4.313202326203128933, -245.5540684919841681 ) ) ;
#100966=FACE_OUTER_BOUND ( 'NONE', #91595, .T. ) ;
#100967=LINE ( 'NONE', #240536, #203911 ) ;
#100972=EDGE_CURVE ( 'NONE', #185172, #248947, #255158, .T. ) ;
#101034=EDGE_CURVE ( 'NONE', #136073, #97044, #167761, .T. ) ;
#101041=ADVANCED_FACE ( 'NONE', ( #246916 ), #130304, .F. ) ;
#101065=CARTESIAN_POINT ( 'NONE',  ( -20.64999999999999858, 25.94586868676353575, -241.5435999122864530 ) ) ;
#101071=CARTESIAN_POINT ( 'NONE',  ( 22.24259225415828567, 0.5715038522256311593, -230.1077355066391306 ) ) ;
#101072=ORIENTED_EDGE ( 'NONE', *, *, #208362, .T. ) ;
#101087=EDGE_CURVE ( 'NONE', #196849, #199913, #38636, .T. ) ;
#101109=CARTESIAN_POINT ( 'NONE',  ( 21.97500000000000497, 30.46448808713892831, -235.1722212069449256 ) ) ;
#101110=AXIS2_PLACEMENT_3D ( 'NONE', #352, #98137, #219392 ) ;
#101112=CARTESIAN_POINT ( 'NONE',  ( 22.59999999999999432, -3.180729737797947099, -228.0957332317254895 ) ) ;
#101124=ORIENTED_EDGE ( 'NONE', *, *, #6324, .F. ) ;
#101162=CARTESIAN_POINT ( 'NONE',  ( -18.59999999999999787, 16.52766025697963315, -240.8672687545768270 ) ) ;
#101166=ORIENTED_EDGE ( 'NONE', *, *, #204280, .F. ) ;
#101198=DIRECTION ( 'NONE',  ( 2.952720810173290591E-16, -0.4721928772777342354, -0.8814952561688433885 ) ) ;
#101218=DIRECTION ( 'NONE',  ( 1.000000000000000000, 0.000000000000000000, 0.000000000000000000 ) ) ;
#101223=CARTESIAN_POINT ( 'NONE',  ( -23.25000000000000000, 27.73205844876672899, -240.0613753537626565 ) ) ;
#101252=CARTESIAN_POINT ( 'NONE',  ( -20.00857864376270001, 30.18117236077229038, -235.7011183606462339 ) ) ;
#101267=CARTESIAN_POINT ( 'NONE',  ( -21.05000000000000071, 10.30543449102040654, -228.0143625250146329 ) ) ;
#101278=DIRECTION ( 'NONE',  ( -0.000000000000000000, 0.8814952561688430555, -0.4721928772777346239 ) ) ;
#101289=EDGE_CURVE ( 'NONE', #65641, #156710, #9688, .T. ) ;
#101298=ORIENTED_EDGE ( 'NONE', *, *, #205081, .F. ) ;
#101301=DIRECTION ( 'NONE',  ( 1.000000000000000000, 0.000000000000000000, 0.000000000000000000 ) ) ;
#101308=CIRCLE ( 'NONE', #43119, 0.5000000000000000000 ) ;
#101315=CARTESIAN_POINT ( 'NONE',  ( 21.53699400387813512, 1.145497594119514240, -230.5275921507054022 ) ) ;
#101330=PLANE ( 'NONE',  #215018 ) ;
#101331=DIRECTION ( 'NONE',  ( 0.000000000000000000, 0.8814952561688437216, -0.4721928772777334582 ) ) ;
#101364=DIRECTION ( 'NONE',  ( -7.304098846218132695E-16, -0.4721928772777346794, -0.8814952561688431665 ) ) ;
#101375=ADVANCED_FACE ( 'NONE', ( #48410 ), #176325, .F. ) ;
#101377=DIRECTION ( 'NONE',  ( 1.000000000000000000, 0.000000000000000000, 0.000000000000000000 ) ) ;
#101389=CARTESIAN_POINT ( 'NONE',  ( -18.59999999999999787, 13.59055429284667404, -238.6121134008722038 ) ) ;
#101404=CIRCLE ( 'NONE', #113922, 0.09999999999999939493 ) ;
#101418=FACE_OUTER_BOUND ( 'NONE', #210189, .T. ) ;
#101429=DIRECTION ( 'NONE',  ( 1.000000000000000000, 0.000000000000000000, 0.000000000000000000 ) ) ;
#101450=ORIENTED_EDGE ( 'NONE', *, *, #141561, .T. ) ;
#101453=VERTEX_POINT ( 'NONE', #168422 ) ;
#101459=CYLINDRICAL_SURFACE ( 'NONE', #48556, 0.1000000000000013933 ) ;
#101530=AXIS2_PLACEMENT_3D ( 'NONE', #102897, #65077, #3823 ) ;
#101541=DIRECTION ( 'NONE',  ( 0.000000000000000000, -0.8814952561688430555, 0.4721928772777346239 ) ) ;
#101556=ORIENTED_EDGE ( 'NONE', *, *, #182508, .F. ) ;
#101564=DIRECTION ( 'NONE',  ( -1.000000000000000000, -1.394253735153569469E-16, -2.602809386958778209E-16 ) ) ;
#101613=CIRCLE ( 'NONE', #126770, 0.1000000000000013933 ) ;
#101634=DIRECTION ( 'NONE',  ( 0.000000000000000000, -0.8814952561688437216, 0.4721928772777334582 ) ) ;
#101650=DIRECTION ( 'NONE',  ( 0.000000000000000000, 0.8814952561688437216, -0.4721928772777334582 ) ) ;
#101655=ORIENTED_EDGE ( 'NONE', *, *, #61602, .F. ) ;
#101687=CARTESIAN_POINT ( 'NONE',  ( 19.97071067811864609, 34.48027702911268477, -235.0877241633741050 ) ) ;
#101710=CARTESIAN_POINT ( 'NONE',  ( -20.64999999999999858, 11.15983666280819975, -246.1019239270423213 ) ) ;
#101720=VECTOR ( 'NONE', #41189, 1000.000000000000000 ) ;
#101730=ORIENTED_EDGE ( 'NONE', *, *, #212501, .F. ) ;
#101747=VERTEX_POINT ( 'NONE', #102927 ) ;
#101762=ORIENTED_EDGE ( 'NONE', *, *, #46609, .F. ) ;
#101781=CARTESIAN_POINT ( 'NONE',  ( -18.59999999999999787, 42.90983634497241894, -254.2202269430244996 ) ) ;
#101789=CARTESIAN_POINT ( 'NONE',  ( 20.85000000000000142, 36.65892442174935439, -249.5511627012433848 ) ) ;
#101794=VECTOR ( 'NONE', #88847, 1000.000000000000000 ) ;
#101821=EDGE_CURVE ( 'NONE', #159212, #109684, #147250, .T. ) ;
#101838=TOROIDAL_SURFACE ( 'NONE', #201812, 11.65000000000000036, 0.1000000000000000056 ) ;
#101864=DIRECTION ( 'NONE',  ( 0.000000000000000000, 0.8814952561688437216, -0.4721928772777331806 ) ) ;
#101888=DIRECTION ( 'NONE',  ( -0.000000000000000000, 0.8096735173027139743, -0.5868805631290339164 ) ) ;
#101898=DIRECTION ( 'NONE',  ( 1.000000000000000000, 0.000000000000000000, 0.000000000000000000 ) ) ;
#101919=DIRECTION ( 'NONE',  ( 0.000000000000000000, -0.8814952561688437216, 0.4721928772777334582 ) ) ;
#101926=ORIENTED_EDGE ( 'NONE', *, *, #189380, .T. ) ;
#101952=ADVANCED_FACE ( 'NONE', ( #173246 ), #111958, .T. ) ;
#101983=VECTOR ( 'NONE', #106828, 1000.000000000000114 ) ;
#102021=EDGE_LOOP ( 'NONE', ( #12204, #46429, #55641, #202207, #92806, #140422, #153501, #24558, #222908, #36097 ) ) ;
#102029=ORIENTED_EDGE ( 'NONE', *, *, #7036, .T. ) ;
#102034=CARTESIAN_POINT ( 'NONE',  ( 19.90621891164687440, 34.56325637860300759, -235.0989470665489876 ) ) ;
#102094=DIRECTION ( 'NONE',  ( 0.000000000000000000, 0.8814952561688476074, -0.4721928772777262417 ) ) ;
#102118=DIRECTION ( 'NONE',  ( 0.000000000000000000, -0.9698110461157734008, -0.2438576117980102709 ) ) ;
#102128=ORIENTED_EDGE ( 'NONE', *, *, #240121, .T. ) ;
#102144=DIRECTION ( 'NONE',  ( 0.000000000000000000, -0.9941044884914576052, 0.1084263158146461931 ) ) ;
#102167=CYLINDRICAL_SURFACE ( 'NONE', #211128, 0.09999999999999986677 ) ;
#102177=CARTESIAN_POINT ( 'NONE',  ( 20.94999999999999929, 28.67750504931771616, -258.3094128005139396 ) ) ;
#102181=DIRECTION ( 'NONE',  ( 0.000000000000000000, 0.8814952561688429444, -0.4721928772777345684 ) ) ;
#102209=FACE_OUTER_BOUND ( 'NONE', #138925, .T. ) ;
#102253=DIRECTION ( 'NONE',  ( 1.000000000000000000, 0.000000000000000000, 0.000000000000000000 ) ) ;
#102280=CIRCLE ( 'NONE', #69024, 0.1000000000000046824 ) ;
#102286=ORIENTED_EDGE ( 'NONE', *, *, #16924, .F. ) ;
#102287=DIRECTION ( 'NONE',  ( 1.000000000000000000, 0.000000000000000000, 0.000000000000000000 ) ) ;
#102306=ADVANCED_FACE ( 'NONE', ( #124779 ), #189877, .F. ) ;
#102316=VERTEX_POINT ( 'NONE', #71233 ) ;
#102317=LINE ( 'NONE', #125764, #134827 ) ;
#102334=EDGE_LOOP ( 'NONE', ( #33408, #99237, #130644, #153102 ) ) ;
#102335=EDGE_CURVE ( 'NONE', #161618, #73607, #193435, .T. ) ;
#102349=EDGE_CURVE ( 'NONE', #105736, #130702, #222598, .T. ) ;
#102351=LINE ( 'NONE', #159813, #157003 ) ;
#102367=CIRCLE ( 'NONE', #98268, 0.09999999999999939493 ) ;
#102380=VECTOR ( 'NONE', #213394, 1000.000000000000000 ) ;
#102393=VERTEX_POINT ( 'NONE', #16395 ) ;
#102415=AXIS2_PLACEMENT_3D ( 'NONE', #192631, #152243, #13998 ) ;
#102419=CARTESIAN_POINT ( 'NONE',  ( 22.59999954896768770, -3.233352942053706158, -228.1919768569983660 ) ) ;
#102434=DIRECTION ( 'NONE',  ( -0.1538461538461546041, 0.4665713331247552942, 0.8710008909598968563 ) ) ;
#102438=LINE ( 'NONE', #82872, #225902 ) ;
#102441=CARTESIAN_POINT ( 'NONE',  ( -22.39999999999999858, 10.80758397488570743, -226.8651660546161111 ) ) ;
#102464=EDGE_LOOP ( 'NONE', ( #12816, #75796, #47433 ) ) ;
#102477=EDGE_CURVE ( 'NONE', #165408, #181106, #147614, .T. ) ;
#102525=COLOUR_RGB ( '', 0.31764706, 0.68627451, 0.89019608) ;
#102537=DIRECTION ( 'NONE',  ( -1.000000000000000000, 0.000000000000000000, 0.000000000000000000 ) ) ;
#102567=CIRCLE ( 'NONE', #135907, 12.77499999999998259 ) ;
#102568=EDGE_CURVE ( 'NONE', #157387, #234543, #87570, .T. ) ;
#102572=EDGE_CURVE ( 'NONE', #204007, #41070, #139411, .T. ) ;
#102593=LINE ( 'NONE', #123479, #130758 ) ;
#102598=DIRECTION ( 'NONE',  ( -0.000000000000000000, -0.4721928772777346239, -0.8814952561688430555 ) ) ;
#102611=DIRECTION ( 'NONE',  ( 1.000000000000000000, 0.000000000000000000, 0.000000000000000000 ) ) ;
#102622=CARTESIAN_POINT ( 'NONE',  ( 21.05000000000000071, 36.65892442174935439, -249.5511627012433848 ) ) ;
#102673=VERTEX_POINT ( 'NONE', #233537 ) ;
#102683=EDGE_CURVE ( 'NONE', #137100, #105632, #247579, .T. ) ;
#102694=ORIENTED_EDGE ( 'NONE', *, *, #158848, .F. ) ;
#102699=CARTESIAN_POINT ( 'NONE',  ( 21.05000000000000071, 36.02367271998545561, -235.8812521208699025 ) ) ;
#102705=LINE ( 'NONE', #2333, #237577 ) ;
#102706=ORIENTED_EDGE ( 'NONE', *, *, #214845, .T. ) ;
#102714=EDGE_LOOP ( 'NONE', ( #213037, #83238, #71962, #241158, #109618, #147816, #8951, #109899, #10535, #135733 ) ) ;
#102727=CARTESIAN_POINT ( 'NONE',  ( 20.94999999999999929, 46.33035574435032800, -243.0552603638194853 ) ) ;
#102789=CARTESIAN_POINT ( 'NONE',  ( -21.14999999999999858, 10.21728496540352182, -227.9671432372868765 ) ) ;
#102798=ORIENTED_EDGE ( 'NONE', *, *, #125107, .T. ) ;
#102824=AXIS2_PLACEMENT_3D ( 'NONE', #76934, #117355, #196880 ) ;
#102831=EDGE_LOOP ( 'NONE', ( #223337, #157417, #144654 ) ) ;
#102849=ADVANCED_FACE ( 'NONE', ( #79558 ), #159146, .T. ) ;
#102855=DIRECTION ( 'NONE',  ( 0.000000000000000000, 0.8814952561688428334, -0.4721928772777348460 ) ) ;
#102872=DIRECTION ( 'NONE',  ( 0.000000000000000000, -0.4721928772777346239, -0.8814952561688430555 ) ) ;
#102877=FACE_OUTER_BOUND ( 'NONE', #238470, .T. ) ;
#102878=EDGE_LOOP ( 'NONE', ( #29252, #193190, #51845, #194447 ) ) ;
#102879=FACE_OUTER_BOUND ( 'NONE', #104236, .T. ) ;
#102897=CARTESIAN_POINT ( 'NONE',  ( 18.59999999999999787, 23.48572414787547302, -255.8242635727748677 ) ) ;
#102918=EDGE_CURVE ( 'NONE', #155020, #231084, #131222, .T. ) ;
#102920=PLANE ( 'NONE',  #123279 ) ;
#102927=CARTESIAN_POINT ( 'NONE',  ( -18.59999999999999787, 43.00579525902548994, -254.2551217332645876 ) ) ;
#102953=DIRECTION ( 'NONE',  ( 0.000000000000000000, 0.8496786552930077896, 0.5273008465188220306 ) ) ;
#102954=EDGE_LOOP ( 'NONE', ( #134783, #97679, #134667, #91319 ) ) ;
#102955=TOROIDAL_SURFACE ( 'NONE', #19600, 1.900000000000002576, 0.1000000000000000056 ) ;
#103016=VERTEX_POINT ( 'NONE', #49438 ) ;
#103042=ORIENTED_EDGE ( 'NONE', *, *, #241327, .T. ) ;
#103067=CIRCLE ( 'NONE', #11530, 0.1000000000000013933 ) ;
#103071=DIRECTION ( 'NONE',  ( 2.952720810173288619E-16, -0.4721928772777346239, -0.8814952561688430555 ) ) ;
#103082=EDGE_CURVE ( 'NONE', #172562, #114431, #149840, .T. ) ;
#103101=FACE_OUTER_BOUND ( 'NONE', #32113, .T. ) ;
#103103=DIRECTION ( 'NONE',  ( 0.000000000000000000, 0.8814952561688429444, -0.4721928772777348460 ) ) ;
#103112=DIRECTION ( 'NONE',  ( -1.836970198721029441E-16, 0.4721928772777346239, 0.8814952561688430555 ) ) ;
#103118=CIRCLE ( 'NONE', #61446, 0.4999999999999970024 ) ;
#103148=ORIENTED_EDGE ( 'NONE', *, *, #144397, .F. ) ;
#103166=AXIS2_PLACEMENT_3D ( 'NONE', #204091, #163703, #85398 ) ;
#103179=ORIENTED_EDGE ( 'NONE', *, *, #52697, .T. ) ;
#103181=DIRECTION ( 'NONE',  ( 0.000000000000000000, -0.3488585713686133682, -0.9371753822965315228 ) ) ;
#103240=PLANE ( 'NONE',  #135257 ) ;
#103248=CARTESIAN_POINT ( 'NONE',  ( 22.49999999999999645, 12.55148283907650608, -223.4215551264213104 ) ) ;
#103249=EDGE_CURVE ( 'NONE', #213843, #100823, #257849, .T. ) ;
#103267=CIRCLE ( 'NONE', #169970, 0.09999999999999939493 ) ;
#103274=AXIS2_PLACEMENT_3D ( 'NONE', #54910, #112349, #134442 ) ;
#103296=ORIENTED_EDGE ( 'NONE', *, *, #187421, .T. ) ;
#103310=AXIS2_PLACEMENT_3D ( 'NONE', #221048, #20314, #18999 ) ;
#103311=FACE_OUTER_BOUND ( 'NONE', #238310, .T. ) ;
#103326=FACE_OUTER_BOUND ( 'NONE', #5949, .T. ) ;
#103342=ORIENTED_EDGE ( 'NONE', *, *, #150859, .F. ) ;
#103362=DIRECTION ( 'NONE',  ( -0.000000000000000000, 0.4721928772777345684, 0.8814952561688429444 ) ) ;
#103364=DIRECTION ( 'NONE',  ( 0.9880948137434723000, 0.07264505804272584910, 0.1356146547952018777 ) ) ;
#103385=EDGE_CURVE ( 'NONE', #208884, #38262, #52287, .T. ) ;
#103420=ADVANCED_FACE ( 'NONE', ( #51661 ), #27023, .T. ) ;
#103426=( GEOMETRIC_REPRESENTATION_CONTEXT ( 3 ) GLOBAL_UNCERTAINTY_ASSIGNED_CONTEXT ( ( #218796 ) ) GLOBAL_UNIT_ASSIGNED_CONTEXT ( ( #159335, #60196, #34565 ) ) REPRESENTATION_CONTEXT ( 'NONE', 'WORKASPACE' ) );
#103460=TOROIDAL_SURFACE ( 'NONE', #86885, 11.65000000000000036, 0.1000000000000000056 ) ;
#103462=VERTEX_POINT ( 'NONE', #46536 ) ;
#103479=AXIS2_PLACEMENT_3D ( 'NONE', #64849, #88243, #163969 ) ;
#103511=AXIS2_PLACEMENT_3D ( 'NONE', #98830, #80558, #160158 ) ;
#103521=VERTEX_POINT ( 'NONE', #166535 ) ;
#103570=EDGE_CURVE ( 'NONE', #246750, #254486, #222986, .T. ) ;
#103582=AXIS2_PLACEMENT_3D ( 'NONE', #64386, #202607, #220872 ) ;
#103601=CYLINDRICAL_SURFACE ( 'NONE', #86697, 0.09999999999999939493 ) ;
#103630=AXIS2_PLACEMENT_3D ( 'NONE', #91323, #131725, #194296 ) ;
#103654=VECTOR ( 'NONE', #3825, 1000.000000000000000 ) ;
#103658=CARTESIAN_POINT ( 'NONE',  ( -20.54999999999999716, 36.65892442174935439, -249.5511627012433848 ) ) ;
#103667=CARTESIAN_POINT ( 'NONE',  ( 21.07928932188134397, 1.596973512272234830, -230.6572452218043736 ) ) ;
#103695=EDGE_CURVE ( 'NONE', #230514, #19319, #243161, .T. ) ;
#103710=DIRECTION ( 'NONE',  ( -1.000000000000000000, -0.000000000000000000, -0.000000000000000000 ) ) ;
#103745=FACE_OUTER_BOUND ( 'NONE', #162108, .T. ) ;
#103772=AXIS2_PLACEMENT_3D ( 'NONE', #154196, #233699, #236249 ) ;
#103791=CARTESIAN_POINT ( 'NONE',  ( 21.05000000000000071, 7.128833340093095217, -233.7327013124392749 ) ) ;
#103793=ORIENTED_EDGE ( 'NONE', *, *, #165306, .F. ) ;
#103806=ORIENTED_EDGE ( 'NONE', *, *, #70319, .T. ) ;
#103817=DIRECTION ( 'NONE',  ( 0.000000000000000000, -0.8814952561688430555, 0.4721928772777346239 ) ) ;
#103841=SPHERICAL_SURFACE ( 'NONE', #196449, 0.1000000000000000056 ) ;
#103873=EDGE_CURVE ( 'NONE', #154195, #223089, #18614, .T. ) ;
#103893=EDGE_LOOP ( 'NONE', ( #192968, #108505, #48886, #103148 ) ) ;
#103925=FACE_OUTER_BOUND ( 'NONE', #74799, .T. ) ;
#103926=EDGE_CURVE ( 'NONE', #240913, #79572, #231326, .T. ) ;
#103928=CARTESIAN_POINT ( 'NONE',  ( -20.85000000000000142, 36.18002604163306302, -236.0784499204090991 ) ) ;
#103955=CARTESIAN_POINT ( 'NONE',  ( 21.05000000000000071, 7.128833340093095217, -233.7327013124392749 ) ) ;
#103960=DIRECTION ( 'NONE',  ( 0.000000000000000000, 0.8814952561688444987, -0.4721928772777320149 ) ) ;
#103982=DIRECTION ( 'NONE',  ( -1.000000000000000000, -0.000000000000000000, -0.000000000000000000 ) ) ;
#104011=CARTESIAN_POINT ( 'NONE',  ( -23.25000000000000000, 36.02367271998545561, -235.8812521208699309 ) ) ;
#104047=EDGE_CURVE ( 'NONE', #153891, #53948, #109139, .T. ) ;
#104063=VERTEX_POINT ( 'NONE', #45328 ) ;
#104104=EDGE_CURVE ( 'NONE', #226316, #235224, #88275, .T. ) ;
#104117=ORIENTED_EDGE ( 'NONE', *, *, #150187, .T. ) ;
#104154=TOROIDAL_SURFACE ( 'NONE', #25091, 12.77499999999999858, 0.1000000000000000056 ) ;
#104157=DIRECTION ( 'NONE',  ( 1.000000000000000000, 0.000000000000000000, 0.000000000000000000 ) ) ;
#104188=CYLINDRICAL_SURFACE ( 'NONE', #101530, 0.09999999999999939493 ) ;
#104192=CARTESIAN_POINT ( 'NONE',  ( 21.14999999999999858, 22.07612373182271881, -231.7717111801312342 ) ) ;
#104205=AXIS2_PLACEMENT_3D ( 'NONE', #13415, #176350, #92924 ) ;
#104236=EDGE_LOOP ( 'NONE', ( #20900, #203864, #64137, #251262 ) ) ;
#104245=EDGE_CURVE ( 'NONE', #43771, #196423, #178137, .T. ) ;
#104258=CARTESIAN_POINT ( 'NONE',  ( -20.94999999999999929, 4.481636728799211156, -245.1292951062512770 ) ) ;
#104260=EDGE_CURVE ( 'NONE', #200406, #2987, #80260, .T. ) ;
#104281=ORIENTED_EDGE ( 'NONE', *, *, #55510, .F. ) ;
#104319=VERTEX_POINT ( 'NONE', #62032 ) ;
#104330=DIRECTION ( 'NONE',  ( -1.000000000000000000, 0.000000000000000000, 0.000000000000000000 ) ) ;
#104343=EDGE_CURVE ( 'NONE', #226091, #225564, #77221, .T. ) ;
#104349=VERTEX_POINT ( 'NONE', #215938 ) ;
#104353=ORIENTED_EDGE ( 'NONE', *, *, #103695, .T. ) ;
#104368=DIRECTION ( 'NONE',  ( -1.000000000000000000, -0.000000000000000000, -0.000000000000000000 ) ) ;
#104391=EDGE_LOOP ( 'NONE', ( #212800, #173727, #6334, #133844 ) ) ;
#104401=DIRECTION ( 'NONE',  ( 1.000000000000000000, 0.000000000000000000, 0.000000000000000000 ) ) ;
#104425=CARTESIAN_POINT ( 'NONE',  ( -21.14999999999999858, 12.71802988599559292, -223.5105008658000258 ) ) ;
#104454=LINE ( 'NONE', #147459, #169554 ) ;
#104508=DIRECTION ( 'NONE',  ( 0.000000000000000000, -0.4721928772777346239, -0.8814952561688430555 ) ) ;
#104520=CARTESIAN_POINT ( 'NONE',  ( 20.94999999999999574, 16.52766025697963315, -240.8672687545768270 ) ) ;
#104543=VERTEX_POINT ( 'NONE', #250914 ) ;
#104558=CARTESIAN_POINT ( 'NONE',  ( 18.59999999999999787, 18.27574494880468592, -237.6039235467692947 ) ) ;
#104574=AXIS2_PLACEMENT_3D ( 'NONE', #89769, #92344, #207177 ) ;
#104599=VERTEX_POINT ( 'NONE', #233934 ) ;
#104631=DIRECTION ( 'NONE',  ( 0.000000000000000000, -0.8814952561688430555, 0.4721928772777346239 ) ) ;
#104633=CARTESIAN_POINT ( 'NONE',  ( -23.15000000000000213, 7.128833340093095217, -233.7327013124392749 ) ) ;
#104670=DIRECTION ( 'NONE',  ( 1.000000000000000000, 0.000000000000000000, 0.000000000000000000 ) ) ;
#104680=CARTESIAN_POINT ( 'NONE',  ( 23.15000000000000213, 24.26958830762006514, -252.6664436919618879 ) ) ;
#104681=VERTEX_POINT ( 'NONE', #57843 ) ;
#104692=AXIS2_PLACEMENT_3D ( 'NONE', #219751, #254969, #234176 ) ;
#104707=DIRECTION ( 'NONE',  ( 1.000000000000000000, 0.000000000000000000, 0.000000000000000000 ) ) ;
#104714=CARTESIAN_POINT ( 'NONE',  ( -18.59999999999999787, 18.92285928089247804, -233.3572654221044900 ) ) ;
#104732=DIRECTION ( 'NONE',  ( 1.000000000000000000, 0.000000000000000000, 0.000000000000000000 ) ) ;
#104733=EDGE_LOOP ( 'NONE', ( #100563, #10906, #132459, #58967 ) ) ;
#104749=CARTESIAN_POINT ( 'NONE',  ( -21.11101077989000530, 1.473603314416399579, -230.6860092427866959 ) ) ;
#104762=FACE_OUTER_BOUND ( 'NONE', #169447, .T. ) ;
#104769=ORIENTED_EDGE ( 'NONE', *, *, #124554, .F. ) ;
#104793=EDGE_CURVE ( 'NONE', #205599, #78573, #60644, .T. ) ;
#104814=DIRECTION ( 'NONE',  ( 0.000000000000000000, -0.8368562265788574983, -0.5474227397872651890 ) ) ;
#104822=CARTESIAN_POINT ( 'NONE',  ( 21.14999999999999858, 23.34004772283015328, -229.2004250369967338 ) ) ;
#104828=CARTESIAN_POINT ( 'NONE',  ( 18.59999999999999787, 7.128833340093095217, -233.7327013124392749 ) ) ;
#104839=DIRECTION ( 'NONE',  ( 0.000000000000000000, 0.5986962832864934914, 0.8009761297185696849 ) ) ;
#104902=AXIS2_PLACEMENT_3D ( 'NONE', #169321, #14071, #229265 ) ;
#104923=CIRCLE ( 'NONE', #9296, 0.1000000000000010186 ) ;
#104949=LINE ( 'NONE', #158568, #97879 ) ;
#104950=EDGE_CURVE ( 'NONE', #198415, #203294, #10737, .T. ) ;
#104961=ORIENTED_EDGE ( 'NONE', *, *, #197493, .F. ) ;
#104974=DIRECTION ( 'NONE',  ( 0.000000000000000000, 0.8814952561688398358, -0.4721928772777406746 ) ) ;
#105001=DIRECTION ( 'NONE',  ( 0.000000000000000000, 0.8814952561688429444, -0.4721928772777349015 ) ) ;
#105010=DIRECTION ( 'NONE',  ( 1.000000000000000000, 0.000000000000000000, 0.000000000000000000 ) ) ;
#105050=DIRECTION ( 'NONE',  ( 0.000000000000000000, -0.8814952561688430555, 0.4721928772777346239 ) ) ;
#105076=DIRECTION ( 'NONE',  ( 0.000000000000000000, -0.8096735173027155286, 0.5868805631290314739 ) ) ;
#105095=CARTESIAN_POINT ( 'NONE',  ( -23.15000000000000213, 2.319530388122572617, -217.8268657444419887 ) ) ;
#105101=CARTESIAN_POINT ( 'NONE',  ( 21.14999999999999858, 10.21728496540352360, -227.9671432372868765 ) ) ;
#105123=FACE_OUTER_BOUND ( 'NONE', #102714, .T. ) ;
#105141=ORIENTED_EDGE ( 'NONE', *, *, #223667, .F. ) ;
#105156=LINE ( 'NONE', #47777, #235313 ) ;
#105163=DIRECTION ( 'NONE',  ( 0.000000000000000000, -0.8814952561688430555, 0.4721928772777346239 ) ) ;
#105169=CARTESIAN_POINT ( 'NONE',  ( 20.94999999999999929, 28.15345123516638282, -259.0759448016705733 ) ) ;
#105181=ORIENTED_EDGE ( 'NONE', *, *, #57794, .T. ) ;
#105195=DIRECTION ( 'NONE',  ( 0.000000000000000000, 0.8814952561688431665, -0.4721928772777346794 ) ) ;
#105199=DIRECTION ( 'NONE',  ( 0.000000000000000000, -0.4721928772777346239, -0.8814952561688430555 ) ) ;
#105209=VERTEX_POINT ( 'NONE', #225590 ) ;
#105224=LINE ( 'NONE', #84369, #154424 ) ;
#105225=ORIENTED_EDGE ( 'NONE', *, *, #77797, .F. ) ;
#105253=CARTESIAN_POINT ( 'NONE',  ( 20.99551997958343108, 36.17041074700797054, -235.9598556649045520 ) ) ;
#105263=AXIS2_PLACEMENT_3D ( 'NONE', #68431, #130969, #89259 ) ;
#105319=CARTESIAN_POINT ( 'NONE',  ( -23.15000000000000213, 11.43341603104965110, -245.8667934851861787 ) ) ;
#105340=CYLINDRICAL_SURFACE ( 'NONE', #89979, 0.09999999999999438505 ) ;
#105344=VERTEX_POINT ( 'NONE', #109509 ) ;
#105353=ADVANCED_FACE ( 'NONE', ( #230775 ), #194150, .F. ) ;
#105382=DIRECTION ( 'NONE',  ( 0.000000000000000000, -0.4646089985449268767, -0.8855159391400474478 ) ) ;
#105413=EDGE_CURVE ( 'NONE', #230514, #43496, #206782, .T. ) ;
#105430=VERTEX_POINT ( 'NONE', #135484 ) ;
#105436=ORIENTED_EDGE ( 'NONE', *, *, #71200, .F. ) ;
#105448=AXIS2_PLACEMENT_3D ( 'NONE', #182752, #110900, #190464 ) ;
#105449=LINE ( 'NONE', #67641, #194740 ) ;
#105487=DIRECTION ( 'NONE',  ( 0.000000000000000000, 0.7965107556683636014, -0.6046243595031649543 ) ) ;
#105489=EDGE_LOOP ( 'NONE', ( #105653, #37376, #254147, #218491 ) ) ;
#105491=CARTESIAN_POINT ( 'NONE',  ( -21.59142135623730852, 29.47917209469435207, -236.7998429059379362 ) ) ;
#105522=AXIS2_PLACEMENT_3D ( 'NONE', #172267, #187941, #206214 ) ;
#105523=ORIENTED_EDGE ( 'NONE', *, *, #242813, .F. ) ;
#105540=CARTESIAN_POINT ( 'NONE',  ( -21.05000000000000071, 28.60154115857408641, -258.4512230915049713 ) ) ;
#105542=ORIENTED_EDGE ( 'NONE', *, *, #122478, .T. ) ;
#105549=FACE_OUTER_BOUND ( 'NONE', #127530, .T. ) ;
#105582=CIRCLE ( 'NONE', #93134, 0.1000000000000013933 ) ;
#105587=ADVANCED_FACE ( 'NONE', ( #168907 ), #101459, .F. ) ;
#105631=CIRCLE ( 'NONE', #197411, 0.09999999999999939493 ) ;
#105632=VERTEX_POINT ( 'NONE', #171468 ) ;
#105653=ORIENTED_EDGE ( 'NONE', *, *, #138895, .T. ) ;
#105667=CYLINDRICAL_SURFACE ( 'NONE', #243787, 11.80000000000000782 ) ;
#105686=ORIENTED_EDGE ( 'NONE', *, *, #178003, .F. ) ;
#105694=AXIS2_PLACEMENT_3D ( 'NONE', #219063, #69012, #145947 ) ;
#105704=ORIENTED_EDGE ( 'NONE', *, *, #126857, .F. ) ;
#105718=ORIENTED_EDGE ( 'NONE', *, *, #3426, .F. ) ;
#105736=VERTEX_POINT ( 'NONE', #72346 ) ;
#105752=CARTESIAN_POINT ( 'NONE',  ( -18.59999999999999787, 42.92545512184477730, -254.1955779480491344 ) ) ;
#105757=CARTESIAN_POINT ( 'NONE',  ( -20.94999999999999929, 7.128833340093095217, -233.7327013124392749 ) ) ;
#105770=CARTESIAN_POINT ( 'NONE',  ( -21.05000000000000071, 14.81796439977981272, -236.5325475414793743 ) ) ;
#105773=CYLINDRICAL_SURFACE ( 'NONE', #6093, 3.999999999999994671 ) ;
#105779=CARTESIAN_POINT ( 'NONE',  ( 18.59999999999999076, 43.21392023178792385, -245.1418509714632421 ) ) ;
#105784=CARTESIAN_POINT ( 'NONE',  ( 21.04999999999997584, 18.90422431703804307, -227.9828523687716313 ) ) ;
#105788=ORIENTED_EDGE ( 'NONE', *, *, #244793, .T. ) ;
#105893=EDGE_CURVE ( 'NONE', #116921, #132362, #227795, .T. ) ;
#105899=ORIENTED_EDGE ( 'NONE', *, *, #102349, .F. ) ;
#105904=ORIENTED_EDGE ( 'NONE', *, *, #35255, .F. ) ;
#105918=CIRCLE ( 'NONE', #251694, 0.09999999999999939493 ) ;
#106042=CARTESIAN_POINT ( 'NONE',  ( -21.12757541349819590, 1.425016164502732163, -230.6714675275338777 ) ) ;
#106060=VECTOR ( 'NONE', #240654, 1000.000000000000000 ) ;
#106065=CARTESIAN_POINT ( 'NONE',  ( -23.15000000000000213, 26.25728039895700761, -243.9792867493661106 ) ) ;
#106066=ORIENTED_EDGE ( 'NONE', *, *, #155310, .T. ) ;
#106119=EDGE_CURVE ( 'NONE', #170728, #218203, #160916, .T. ) ;
#106169=ORIENTED_EDGE ( 'NONE', *, *, #243765, .F. ) ;
#106173=ORIENTED_EDGE ( 'NONE', *, *, #248754, .T. ) ;
#106178=DIRECTION ( 'NONE',  ( 0.000000000000000000, 0.8814952561688430555, -0.4721928772777346239 ) ) ;
#106181=EDGE_CURVE ( 'NONE', #162761, #59200, #132299, .T. ) ;
#106194=EDGE_CURVE ( 'NONE', #117242, #71417, #24006, .T. ) ;
#106230=FACE_OUTER_BOUND ( 'NONE', #83470, .T. ) ;
#106236=ORIENTED_EDGE ( 'NONE', *, *, #245882, .F. ) ;
#106241=EDGE_LOOP ( 'NONE', ( #2133, #222039 ) ) ;
#106263=FACE_OUTER_BOUND ( 'NONE', #110551, .T. ) ;
#106280=CYLINDRICAL_SURFACE ( 'NONE', #130793, 0.09999999999999939493 ) ;
#106285=AXIS2_PLACEMENT_3D ( 'NONE', #153825, #132938, #115934 ) ;
#106293=CIRCLE ( 'NONE', #160522, 0.09999999999999986677 ) ;
#106297=ORIENTED_EDGE ( 'NONE', *, *, #65380, .T. ) ;
#106360=DIRECTION ( 'NONE',  ( -1.000000000000000000, 0.000000000000000000, 0.000000000000000000 ) ) ;
#106362=DIRECTION ( 'NONE',  ( -1.000000000000000000, -0.000000000000000000, -0.000000000000000000 ) ) ;
#106376=DIRECTION ( 'NONE',  ( 0.000000000000000000, 0.8814952561688438326, -0.4721928772777334582 ) ) ;
#106386=CARTESIAN_POINT ( 'NONE',  ( 20.94999999999999929, 29.00069016757795026, -237.9048565010683376 ) ) ;
#106393=CARTESIAN_POINT ( 'NONE',  ( 22.39999999999999503, 12.54173083476182882, -223.4160622903444562 ) ) ;
#106436=DIRECTION ( 'NONE',  ( -1.000000000000000000, -0.000000000000000000, -0.000000000000000000 ) ) ;
#106442=AXIS2_PLACEMENT_3D ( 'NONE', #83473, #104330, #221707 ) ;
#106454=DIRECTION ( 'NONE',  ( 0.000000000000000000, 0.9994937237965569876, 0.03181660087583042945 ) ) ;
#106456=ORIENTED_EDGE ( 'NONE', *, *, #100178, .T. ) ;
#106461=ORIENTED_EDGE ( 'NONE', *, *, #53034, .T. ) ;
#106465=( BOUNDED_SURFACE ( )  B_SPLINE_SURFACE ( 3, 2, ( 
 ( #174949, #191918, #151504 ),
 ( #195766, #91507, #35419 ),
 ( #135749, #172372, #51051 ),
 ( #75795, #234874, #130624 ),
 ( #210179, #31565, #176196 ),
 ( #94056, #70685, #73257 ),
 ( #52351, #56205, #13260 ),
 ( #232322, #111062, #114918 ),
 ( #215296, #250565, #190624 ),
 ( #71949, #36699, #92773 ),
 ( #113631, #231037, #214024 ),
 ( #74555, #251850, #152795 ) ),
 .UNSPECIFIED., .F., .F., .F. ) 
 B_SPLINE_SURFACE_WITH_KNOTS ( ( 4, 2, 2, 2, 2, 4 ),
 ( 3, 3 ),
 ( 3.174653483277204646, 3.943930578431714018, 4.713207673586222946, 5.482484768740731873, 5.867123316317986337, 6.251761863895240801 ),
 ( 0.000000000000000000, 1.000000000000000000 ),
 .UNSPECIFIED. ) 
 GEOMETRIC_REPRESENTATION_ITEM ( )  RATIONAL_B_SPLINE_SURFACE ( (
 ( 1.000000000000000000, 0.8659465255642335713, 1.000000000000000000),
 ( 1.000000000000000000, 0.8648614068459831161, 1.000000000000000000),
 ( 1.000000000000000000, 0.8489031841361811548, 1.000000000000000000),
 ( 1.000000000000000000, 0.7927507630123762361, 1.000000000000000000),
 ( 1.000000000000000000, 0.7523013859009685111, 1.000000000000000000),
 ( 1.000000000000000000, 0.6616226951196223505, 1.000000000000000000),
 ( 1.000000000000000000, 0.6112214368956626620, 1.000000000000000000),
 ( 1.000000000000000000, 0.5507684314381751101, 1.000000000000000000),
 ( 1.000000000000000000, 0.5333267243066852625, 1.000000000000000000),
 ( 1.000000000000000000, 0.5084565446564963676, 1.000000000000000000),
 ( 1.000000000000000000, 0.5010722703387235910, 1.000000000000000000),
 ( 1.000000000000000000, 0.5001234037138085897, 1.000000000000000000) ) ) 
 REPRESENTATION_ITEM ( '' )  SURFACE ( )  );
#106487=CIRCLE ( 'NONE', #89940, 11.80000000000000604 ) ;
#106488=( BOUNDED_SURFACE ( )  B_SPLINE_SURFACE ( 3, 2, ( 
 ( #237036, #179644, #196614 ),
 ( #100057, #19269, #220037 ),
 ( #140482, #101315, #58363 ),
 ( #97487, #20574, #120964 ) ),
 .UNSPECIFIED., .F., .F., .F. ) 
 B_SPLINE_SURFACE_WITH_KNOTS ( ( 4, 4 ),
 ( 3, 3 ),
 ( 5.204170427930421283E-18, 0.001979672783031532438 ),
 ( 0.000000000000000000, 1.000000000000000000 ),
 .UNSPECIFIED. ) 
 GEOMETRIC_REPRESENTATION_ITEM ( )  RATIONAL_B_SPLINE_SURFACE ( (
 ( 1.000000000000000000, 0.7103081912008247789, 1.000000000000000000),
 ( 1.000000000000000000, 0.7104998333562062562, 1.000000000000000000),
 ( 1.000000000000000000, 0.7107238315751961411, 1.000000000000000000),
 ( 1.000000000000000000, 0.7110073749541059307, 1.000000000000000000) ) ) 
 REPRESENTATION_ITEM ( '' )  SURFACE ( )  );
#106501=DIRECTION ( 'NONE',  ( 0.000000000000000000, -0.8814952561688430555, 0.4721928772777346239 ) ) ;
#106518=DIRECTION ( 'NONE',  ( 0.000000000000000000, -0.8814952561688437216, 0.4721928772777334582 ) ) ;
#106521=DIRECTION ( 'NONE',  ( 0.000000000000000000, 0.8814952561688476074, -0.4721928772777262417 ) ) ;
#106525=CARTESIAN_POINT ( 'NONE',  ( -21.05000000000000071, 36.02367271998545561, -235.8812521208699309 ) ) ;
#106557=VECTOR ( 'NONE', #188707, 1000.000000000000114 ) ;
#106608=EDGE_LOOP ( 'NONE', ( #179426, #2650, #115857, #41264, #38415 ) ) ;
#106610=DIRECTION ( 'NONE',  ( 1.000000000000000000, 0.000000000000000000, 0.000000000000000000 ) ) ;
#106621=CARTESIAN_POINT ( 'NONE',  ( 23.24999999999999289, 35.97645343225767789, -235.9694016464868298 ) ) ;
#106625=CARTESIAN_POINT ( 'NONE',  ( -21.05000000000000071, 18.60982576078065165, -226.6665746245395496 ) ) ;
#106644=ORIENTED_EDGE ( 'NONE', *, *, #47951, .T. ) ;
#106672=ADVANCED_FACE ( 'NONE', ( #187536 ), #166700, .T. ) ;
#106688=AXIS2_PLACEMENT_3D ( 'NONE', #189845, #171597, #227675 ) ;
#106691=CARTESIAN_POINT ( 'NONE',  ( -21.65000000000000213, 29.50054346320101928, -236.9717244483098568 ) ) ;
#106707=B_SPLINE_CURVE_WITH_KNOTS ( 'NONE', 3,
 ( #141354, #235311, #137482, #160938, #22721, #56644, #219594, #100896, #240457, #38406 ),
 .UNSPECIFIED., .F., .F.,
 ( 4, 2, 2, 2, 4 ),
 ( 0.000000000000000000, 3.990160268013564522E-05, 7.980320536027129044E-05, 0.0001596064107205425809, 0.0003192128214410908538 ),
 .UNSPECIFIED. ) ;
#106720=CIRCLE ( 'NONE', #31766, 0.1000000000000010186 ) ;
#106739=CARTESIAN_POINT ( 'NONE',  ( 21.05000000000000071, 28.08470566095357057, -239.2860081655328770 ) ) ;
#106749=EDGE_CURVE ( 'NONE', #39196, #57412, #58252, .T. ) ;
#106793=AXIS2_PLACEMENT_3D ( 'NONE', #22170, #84643, #203359 ) ;
#106820=DIRECTION ( 'NONE',  ( 0.000000000000000000, -0.4721928772777402861, -0.8814952561688399468 ) ) ;
#106828=DIRECTION ( 'NONE',  ( 0.000000000000000000, -0.8496786552930076786, -0.5273008465188218086 ) ) ;
#106831=CARTESIAN_POINT ( 'NONE',  ( 21.00000000000000000, 30.37633856152204359, -235.1250019192171408 ) ) ;
#106835=EDGE_CURVE ( 'NONE', #89253, #168386, #133944, .T. ) ;
#106842=SPHERICAL_SURFACE ( 'NONE', #190988, 0.1000000000000000056 ) ;
#106845=DIRECTION ( 'NONE',  ( -6.938893903907222067E-15, 0.4721928772777344019, 0.8814952561688432775 ) ) ;
#106846=ORIENTED_EDGE ( 'NONE', *, *, #85293, .T. ) ;
#106873=ADVANCED_FACE ( 'NONE', ( #37442 ), #7797, .T. ) ;
#106875=VECTOR ( 'NONE', #27779, 1000.000000000000227 ) ;
#106904=ORIENTED_EDGE ( 'NONE', *, *, #162978, .F. ) ;
#106916=DIRECTION ( 'NONE',  ( 0.000000000000000000, -0.8814952561688476074, 0.4721928772777262417 ) ) ;
#106926=ORIENTED_EDGE ( 'NONE', *, *, #16633, .T. ) ;
#106969=EDGE_CURVE ( 'NONE', #217845, #155156, #159962, .T. ) ;
#106992=CARTESIAN_POINT ( 'NONE',  ( -21.05000000000000071, 1.434427651312520480, -230.7796976835703049 ) ) ;
#107020=( GEOMETRIC_REPRESENTATION_CONTEXT ( 3 ) GLOBAL_UNCERTAINTY_ASSIGNED_CONTEXT ( ( #144310 ) ) GLOBAL_UNIT_ASSIGNED_CONTEXT ( ( #6955, #77749, #30417 ) ) REPRESENTATION_CONTEXT ( 'NONE', 'WORKASPACE' ) );
#107023=CARTESIAN_POINT ( 'NONE',  ( -18.50000000000000000, 2.272311100394797556, -217.9150152700588876 ) ) ;
#107024=DIRECTION ( 'NONE',  ( 0.000000000000000000, -0.8814952561688476074, 0.4721928772777262417 ) ) ;
#107048=CARTESIAN_POINT ( 'NONE',  ( 21.05000000000000071, 18.94619844861577462, -232.5189405348540674 ) ) ;
#107055=DIRECTION ( 'NONE',  ( 0.000000000000000000, -0.8814952561688516042, 0.4721928772777186922 ) ) ;
#107061=ADVANCED_FACE ( 'NONE', ( #125927 ), #41126, .F. ) ;
#107080=DIRECTION ( 'NONE',  ( 1.000000000000000000, 0.000000000000000000, 0.000000000000000000 ) ) ;
#107142=MANIFOLD_SOLID_BREP ( 'Stock-MAS-200-1', #16078 ) ;
#107151=EDGE_CURVE ( 'NONE', #217355, #151273, #66710, .T. ) ;
#107158=DIRECTION ( 'NONE',  ( 0.000000000000000000, 0.8814952561688438326, -0.4721928772777331806 ) ) ;
#107159=LINE ( 'NONE', #6782, #89062 ) ;
#107183=DIRECTION ( 'NONE',  ( 1.000000000000000000, 0.000000000000000000, 0.000000000000000000 ) ) ;
#107195=CIRCLE ( 'NONE', #232134, 0.09999999999999986677 ) ;
#107203=PLANE ( 'NONE',  #11193 ) ;
#107225=VECTOR ( 'NONE', #65258, 1000.000000000000000 ) ;
#107234=ORIENTED_EDGE ( 'NONE', *, *, #163180, .T. ) ;
#107246=AXIS2_PLACEMENT_3D ( 'NONE', #30042, #89970, #109532 ) ;
#107255=CARTESIAN_POINT ( 'NONE',  ( -20.64999999999999858, 26.29846678923107106, -241.7324770631975639 ) ) ;
#107269=ORIENTED_EDGE ( 'NONE', *, *, #152411, .T. ) ;
#107306=EDGE_CURVE ( 'NONE', #85514, #202898, #47045, .T. ) ;
#107318=DIRECTION ( 'NONE',  ( -2.827886303505247780E-16, -0.03181660087583047802, 0.9994937237965568766 ) ) ;
#107337=AXIS2_PLACEMENT_3D ( 'NONE', #4845, #201789, #106521 ) ;
#107368=DIRECTION ( 'NONE',  ( -1.000000000000000000, 0.000000000000000000, 0.000000000000000000 ) ) ;
#107386=ORIENTED_EDGE ( 'NONE', *, *, #196605, .F. ) ;
#107403=EDGE_CURVE ( 'NONE', #181106, #89738, #102705, .T. ) ;
#107429=CIRCLE ( 'NONE', #219842, 0.09999999999999568956 ) ;
#107441=FACE_OUTER_BOUND ( 'NONE', #55488, .T. ) ;
#107458=TOROIDAL_SURFACE ( 'NONE', #65948, 11.65000000000000036, 0.1000000000000000056 ) ;
#107507=ORIENTED_EDGE ( 'NONE', *, *, #198123, .F. ) ;
#107530=CARTESIAN_POINT ( 'NONE',  ( -18.50000000000000000, 38.28679861725831302, -261.0868692510649680 ) ) ;
#107537=CARTESIAN_POINT ( 'NONE',  ( 23.15000000000000213, 24.17260720300848575, -252.6908294531417027 ) ) ;
#107577=DIRECTION ( 'NONE',  ( 0.000000000000000000, -0.8814952561688476074, 0.4721928772777262417 ) ) ;
#107583=DIRECTION ( 'NONE',  ( 0.000000000000000000, 0.8814952561688437216, -0.4721928772777331806 ) ) ;
#107592=ADVANCED_FACE ( 'NONE', ( #167963 ), #58665, .T. ) ;
#107620=LINE ( 'NONE', #8530, #27690 ) ;
#107655=CARTESIAN_POINT ( 'NONE',  ( -23.15000000000000213, 19.25956423861613231, -238.0467473098318010 ) ) ;
#107656=DIRECTION ( 'NONE',  ( -0.000000000000000000, -0.3350715337780662550, -0.9421926911474181043 ) ) ;
#107686=DIRECTION ( 'NONE',  ( 0.000000000000000000, 0.8814952561688437216, -0.4721928772777334582 ) ) ;
#107697=VECTOR ( 'NONE', #1818, 1000.000000000000000 ) ;
#107706=VERTEX_POINT ( 'NONE', #33606 ) ;
#107707=DIRECTION ( 'NONE',  ( 0.000000000000000000, 0.8814952561688471633, -0.4721928772777269634 ) ) ;
#107728=DIRECTION ( 'NONE',  ( -1.000000000000000000, -0.000000000000000000, -0.000000000000000000 ) ) ;
#107741=DIRECTION ( 'NONE',  ( 0.000000000000000000, 0.8814952561688434995, -0.4721928772777339023 ) ) ;
#107757=EDGE_CURVE ( 'NONE', #234056, #74755, #241840, .T. ) ;
#107765=ORIENTED_EDGE ( 'NONE', *, *, #167359, .F. ) ;
#107818=EDGE_CURVE ( 'NONE', #98189, #167145, #17015, .T. ) ;
#107841=ORIENTED_EDGE ( 'NONE', *, *, #20177, .F. ) ;
#107848=ORIENTED_EDGE ( 'NONE', *, *, #173647, .T. ) ;
#107856=CARTESIAN_POINT ( 'NONE',  ( -23.25000000000000000, 10.69888912757691024, -235.6450824654141059 ) ) ;
#107873=ORIENTED_EDGE ( 'NONE', *, *, #31537, .T. ) ;
#107903=ADVANCED_FACE ( 'NONE', ( #255112 ), #79069, .T. ) ;
#107904=VERTEX_POINT ( 'NONE', #116943 ) ;
#107905=FACE_OUTER_BOUND ( 'NONE', #159339, .T. ) ;
#107944=DIRECTION ( 'NONE',  ( 0.7071067811865708874, -0.3338907855511046296, -0.6233112732207185536 ) ) ;
#107982=CARTESIAN_POINT ( 'NONE',  ( -21.78635804494510708, 10.36375008473801174, -227.4840496025197751 ) ) ;
#107986=DIRECTION ( 'NONE',  ( 0.000000000000000000, -0.8814952561688425003, 0.4721928772777359007 ) ) ;
#108026=CARTESIAN_POINT ( 'NONE',  ( -18.59999999999999787, 18.81339837015603322, -226.7756228984618190 ) ) ;
#108038=CARTESIAN_POINT ( 'NONE',  ( 20.94999999999999929, 28.56975825374500388, -258.1421690862028413 ) ) ;
#108054=SPHERICAL_SURFACE ( 'NONE', #71230, 0.1000000000000000056 ) ;
#108073=CARTESIAN_POINT ( 'NONE',  ( -18.59999999999999787, 14.81796439977981272, -236.5325475414793743 ) ) ;
#108076=TOROIDAL_SURFACE ( 'NONE', #208038, 0.9750000000000019762, 0.1000000000000000056 ) ;
#108077=CARTESIAN_POINT ( 'NONE',  ( 20.94999999999999574, 18.75483929237739744, -228.0790484105328630 ) ) ;
#108078=ORIENTED_EDGE ( 'NONE', *, *, #198996, .T. ) ;
#108087=EDGE_CURVE ( 'NONE', #236989, #223188, #48438, .T. ) ;
#108102=CARTESIAN_POINT ( 'NONE',  ( -21.45000000000000284, 29.50054346320101928, -236.9717244483098568 ) ) ;
#108118=CYLINDRICAL_SURFACE ( 'NONE', #257281, 2.000000000000003553 ) ;
#108121=CARTESIAN_POINT ( 'NONE',  ( -20.64999999999999858, 7.128833340093095217, -233.7327013124392749 ) ) ;
#108127=ADVANCED_FACE ( 'NONE', ( #151937 ), #188460, .F. ) ;
#108165=CIRCLE ( 'NONE', #241438, 2.000000000000003553 ) ;
#108186=CARTESIAN_POINT ( 'NONE',  ( -23.25000000000000000, 26.47476584046484049, -241.8269156386531051 ) ) ;
#108210=AXIS2_PLACEMENT_3D ( 'NONE', #234574, #130330, #215008 ) ;
#108213=DIRECTION ( 'NONE',  ( 1.000000000000000000, 0.000000000000000000, 0.000000000000000000 ) ) ;
#108230=ORIENTED_EDGE ( 'NONE', *, *, #163057, .F. ) ;
#108243=ADVANCED_FACE ( 'NONE', ( #25255 ), #66927, .T. ) ;
#108265=VERTEX_POINT ( 'NONE', #163465 ) ;
#108268=VERTEX_POINT ( 'NONE', #142592 ) ;
#108277=CARTESIAN_POINT ( 'NONE',  ( -21.05000000000000071, 10.30543449102040476, -228.0143625250146329 ) ) ;
#108283=CARTESIAN_POINT ( 'NONE',  ( -23.15000000000000213, 31.36165455396662693, -233.4973802202241302 ) ) ;
#108286=VECTOR ( 'NONE', #105050, 1000.000000000000000 ) ;
#108308=CARTESIAN_POINT ( 'NONE',  ( -21.53551880898957904, 1.194799103070417035, -230.4417267841993464 ) ) ;
#108320=LINE ( 'NONE', #153913, #4130 ) ;
#108328=AXIS2_PLACEMENT_3D ( 'NONE', #105169, #140480, #183481 ) ;
#108358=EDGE_CURVE ( 'NONE', #97478, #183016, #90298, .T. ) ;
#108364=ADVANCED_FACE ( 'NONE', ( #6949 ), #102167, .T. ) ;
#108378=EDGE_CURVE ( 'NONE', #5127, #155241, #206441, .T. ) ;
#108396=AXIS2_PLACEMENT_3D ( 'NONE', #188245, #5725, #50015 ) ;
#108400=LINE ( 'NONE', #208787, #217656 ) ;
#108451=CIRCLE ( 'NONE', #154296, 11.80000000000000071 ) ;
#108473=ORIENTED_EDGE ( 'NONE', *, *, #206539, .F. ) ;
#108479=ADVANCED_FACE ( 'NONE', ( #227282 ), #136078, .T. ) ;
#108480=VERTEX_POINT ( 'NONE', #210307 ) ;
#108483=DIRECTION ( 'NONE',  ( -0.000000000000000000, 0.4721928772777345684, 0.8814952561688429444 ) ) ;
#108498=DIRECTION ( 'NONE',  ( 1.000000000000000000, 0.000000000000000000, 0.000000000000000000 ) ) ;
#108505=ORIENTED_EDGE ( 'NONE', *, *, #219723, .T. ) ;
#108522=ORIENTED_EDGE ( 'NONE', *, *, #151628, .T. ) ;
#108532=ORIENTED_EDGE ( 'NONE', *, *, #66330, .F. ) ;
#108558=VECTOR ( 'NONE', #253884, 1000.000000000000000 ) ;
#108613=VECTOR ( 'NONE', #133353, 1000.000000000000000 ) ;
#108646=LINE ( 'NONE', #61519, #136021 ) ;
#108703=AXIS2_PLACEMENT_3D ( 'NONE', #227643, #129826, #114113 ) ;
#108725=FACE_OUTER_BOUND ( 'NONE', #97560, .T. ) ;
#108732=DIRECTION ( 'NONE',  ( 0.000000000000000000, 0.8814952561688476074, -0.4721928772777262417 ) ) ;
#108769=DIRECTION ( 'NONE',  ( -1.000000000000000000, 0.000000000000000000, 0.000000000000000000 ) ) ;
#108838=ORIENTED_EDGE ( 'NONE', *, *, #181686, .F. ) ;
#108875=AXIS2_PLACEMENT_3D ( 'NONE', #177137, #157593, #254066 ) ;
#108913=ORIENTED_EDGE ( 'NONE', *, *, #100972, .T. ) ;
#108914=CARTESIAN_POINT ( 'NONE',  ( 23.15000000000000213, 28.58935552370083144, -258.2621935127861548 ) ) ;
#108968=EDGE_LOOP ( 'NONE', ( #27722, #17831, #169936, #147025 ) ) ;
#109004=AXIS2_PLACEMENT_3D ( 'NONE', #176045, #151344, #252979 ) ;
#109010=DIRECTION ( 'NONE',  ( 1.000000000000000000, 0.000000000000000000, 0.000000000000000000 ) ) ;
#109013=DIRECTION ( 'NONE',  ( -1.000000000000000000, -1.394253735153569469E-16, -2.602809386958778209E-16 ) ) ;
#109032=VECTOR ( 'NONE', #202434, 1000.000000000000114 ) ;
#109034=VERTEX_POINT ( 'NONE', #146791 ) ;
#109058=DIRECTION ( 'NONE',  ( 0.000000000000000000, -0.8814952561688429444, 0.4721928772777349015 ) ) ;
#109084=ORIENTED_EDGE ( 'NONE', *, *, #166976, .F. ) ;
#109120=ADVANCED_FACE ( 'NONE', ( #123404 ), #202933, .F. ) ;
#109125=PLANE ( 'NONE',  #163674 ) ;
#109139=LINE ( 'NONE', #49177, #214405 ) ;
#109143=ORIENTED_EDGE ( 'NONE', *, *, #54050, .F. ) ;
#109158=CARTESIAN_POINT ( 'NONE',  ( -20.94999999999999929, 18.62343931468261360, -223.9512205031617498 ) ) ;
#109165=ORIENTED_EDGE ( 'NONE', *, *, #200438, .F. ) ;
#109170=ORIENTED_EDGE ( 'NONE', *, *, #128919, .F. ) ;
#109178=VERTEX_POINT ( 'NONE', #50261 ) ;
#109186=DIRECTION ( 'NONE',  ( 0.000000000000000000, 0.8814952561688444987, -0.4721928772777320149 ) ) ;
#109205=CARTESIAN_POINT ( 'NONE',  ( -21.05439746398122836, 18.83867787284056305, -226.6757208306117946 ) ) ;
#109224=VERTEX_POINT ( 'NONE', #90678 ) ;
#109231=EDGE_CURVE ( 'NONE', #52358, #218161, #124019, .T. ) ;
#109266=LINE ( 'NONE', #7618, #229420 ) ;
#109272=CARTESIAN_POINT ( 'NONE',  ( 18.59999999999999076, 28.91254064196106910, -237.8576372133405528 ) ) ;
#109273=CARTESIAN_POINT ( 'NONE',  ( 20.94999999999999574, 4.459011116736869340, -245.2267018908137857 ) ) ;
#109292=EDGE_CURVE ( 'NONE', #250592, #173747, #77513, .T. ) ;
#109312=AXIS2_PLACEMENT_3D ( 'NONE', #104258, #246365, #145964 ) ;
#109404=ADVANCED_FACE ( 'NONE', ( #236604 ), #20147, .F. ) ;
#109426=DIRECTION ( 'NONE',  ( 1.000000000000000000, 0.000000000000000000, 0.000000000000000000 ) ) ;
#109430=CARTESIAN_POINT ( 'NONE',  ( -21.14999999999999858, 1.627786319807483340, -244.0021210468063089 ) ) ;
#109444=CARTESIAN_POINT ( 'NONE',  ( -23.24999999999999645, 37.94390843806124991, -261.1300795796834109 ) ) ;
#109450=DIRECTION ( 'NONE',  ( 0.000000000000000000, -0.3488585713686463974, -0.9371753822965191993 ) ) ;
#109477=VERTEX_POINT ( 'NONE', #106065 ) ;
#109478=CIRCLE ( 'NONE', #5415, 0.09999999999999605038 ) ;
#109508=DIRECTION ( 'NONE',  ( 9.044546369203336152E-15, 0.2438576117979363023, -0.9698110461157920525 ) ) ;
#109509=CARTESIAN_POINT ( 'NONE',  ( -23.15000000000000213, 19.98118924431957311, -235.6825596947570602 ) ) ;
#109510=CARTESIAN_POINT ( 'NONE',  ( 23.24999999999999645, 28.46934351190515855, -239.7465010792843714 ) ) ;
#109512=ORIENTED_EDGE ( 'NONE', *, *, #196255, .F. ) ;
#109513=AXIS2_PLACEMENT_3D ( 'NONE', #176379, #133386, #36883 ) ;
#109515=VECTOR ( 'NONE', #100351, 1000.000000000000000 ) ;
#109532=DIRECTION ( 'NONE',  ( -1.000000000000000000, 0.000000000000000000, 0.000000000000000000 ) ) ;
#109538=AXIS2_PLACEMENT_3D ( 'NONE', #85140, #90300, #184273 ) ;
#109551=DIRECTION ( 'NONE',  ( 0.000000000000000000, 0.9994937237965558774, 0.03181660087586650476 ) ) ;
#109561=CARTESIAN_POINT ( 'NONE',  ( -21.05000000000000071, 1.626685360119048074, -230.7493234433891018 ) ) ;
#109571=DIRECTION ( 'NONE',  ( -0.000000000000000000, 0.4721928772777346239, 0.8814952561688430555 ) ) ;
#109590=AXIS2_PLACEMENT_3D ( 'NONE', #197987, #158897, #157632 ) ;
#109606=CARTESIAN_POINT ( 'NONE',  ( 18.59999999999999076, 19.00443933019177223, -232.7770257915295531 ) ) ;
#109618=ORIENTED_EDGE ( 'NONE', *, *, #114140, .T. ) ;
#109628=CIRCLE ( 'NONE', #255329, 0.1000000000000013933 ) ;
#109645=ORIENTED_EDGE ( 'NONE', *, *, #85190, .T. ) ;
#109648=DIRECTION ( 'NONE',  ( 0.000000000000000000, -0.8814952561688476074, 0.4721928772777262417 ) ) ;
#109649=ADVANCED_FACE ( 'NONE', ( #168691 ), #149093, .F. ) ;
#109656=B_SPLINE_CURVE_WITH_KNOTS ( 'NONE', 3,
 ( #112466, #214125, #190735, #53759, #51158, #75894, #232424, #35521 ),
 .UNSPECIFIED., .F., .F.,
 ( 4, 2, 2, 4 ),
 ( 0.000000000000000000, 0.0002114466876442058806, 0.0003171700314663111926, 0.0004228933752884164775 ),
 .UNSPECIFIED. ) ;
#109659=CIRCLE ( 'NONE', #251308, 0.09999999999998304689 ) ;
#109684=VERTEX_POINT ( 'NONE', #1538 ) ;
#109692=CIRCLE ( 'NONE', #118070, 0.1000000000000075273 ) ;
#109694=ORIENTED_EDGE ( 'NONE', *, *, #186639, .T. ) ;
#109732=ORIENTED_EDGE ( 'NONE', *, *, #61772, .F. ) ;
#109735=CARTESIAN_POINT ( 'NONE',  ( -23.25000000000000000, 30.38404434817536526, -239.4399867032565794 ) ) ;
#109752=CARTESIAN_POINT ( 'NONE',  ( 21.05000000000000071, 12.71802988599559470, -223.5105008658000258 ) ) ;
#109757=EDGE_CURVE ( 'NONE', #142016, #87394, #35576, .T. ) ;
#109792=EDGE_LOOP ( 'NONE', ( #55483, #171119, #171996, #27709 ) ) ;
#109804=ORIENTED_EDGE ( 'NONE', *, *, #42594, .T. ) ;
#109890=VERTEX_POINT ( 'NONE', #245308 ) ;
#109893=ORIENTED_EDGE ( 'NONE', *, *, #190569, .T. ) ;
#109899=ORIENTED_EDGE ( 'NONE', *, *, #95841, .T. ) ;
#109902=ORIENTED_EDGE ( 'NONE', *, *, #78408, .T. ) ;
#109936=DIRECTION ( 'NONE',  ( 0.000000000000000000, 0.5868805631290315850, 0.8096735173027156396 ) ) ;
#109937=ORIENTED_EDGE ( 'NONE', *, *, #158346, .F. ) ;
#109947=DIRECTION ( 'NONE',  ( 0.000000000000000000, -0.8814952561688430555, 0.4721928772777346239 ) ) ;
#109993=DIRECTION ( 'NONE',  ( 1.000000000000000000, 0.000000000000000000, 0.000000000000000000 ) ) ;
#109998=ORIENTED_EDGE ( 'NONE', *, *, #204603, .T. ) ;
#110006=ORIENTED_EDGE ( 'NONE', *, *, #153557, .T. ) ;
#110031=ADVANCED_FACE ( 'NONE', ( #178634 ), #139457, .T. ) ;
#110050=CARTESIAN_POINT ( 'NONE',  ( 21.05000000000000071, 7.081614052365321932, -233.8208508380561454 ) ) ;
#110056=VERTEX_POINT ( 'NONE', #252995 ) ;
#110096=VECTOR ( 'NONE', #10346, 1000.000000000000000 ) ;
#110155=CARTESIAN_POINT ( 'NONE',  ( -21.05000000000000071, 28.60154115857408641, -258.4512230915049713 ) ) ;
#110161=FACE_OUTER_BOUND ( 'NONE', #132138, .T. ) ;
#110177=CARTESIAN_POINT ( 'NONE',  ( -23.15000000000000213, 23.38726701055792745, -229.1122755113798348 ) ) ;
#110179=FACE_OUTER_BOUND ( 'NONE', #242314, .T. ) ;
#110189=AXIS2_PLACEMENT_3D ( 'NONE', #155909, #195034, #136290 ) ;
#110198=FACE_OUTER_BOUND ( 'NONE', #113942, .T. ) ;
#110204=TOROIDAL_SURFACE ( 'NONE', #1306, 11.70000000000000462, 0.1000000000000000056 ) ;
#110209=ORIENTED_EDGE ( 'NONE', *, *, #241272, .F. ) ;
#110260=CARTESIAN_POINT ( 'NONE',  ( -22.50000000000000000, 12.67709964810648238, -223.3751320524553705 ) ) ;
#110279=AXIS2_PLACEMENT_3D ( 'NONE', #232623, #34427, #129642 ) ;
#110301=ORIENTED_EDGE ( 'NONE', *, *, #50388, .F. ) ;
#110305=FACE_OUTER_BOUND ( 'NONE', #224953, .T. ) ;
#110310=CARTESIAN_POINT ( 'NONE',  ( 21.05000000000000071, 21.98309897467606433, -231.7335930323676791 ) ) ;
#110337=CARTESIAN_POINT ( 'NONE',  ( 18.59999999999999432, 16.56538529403860238, -240.6448716151659823 ) ) ;
#110377=ORIENTED_EDGE ( 'NONE', *, *, #140023, .F. ) ;
#110391=CARTESIAN_POINT ( 'NONE',  ( 23.14999999999998437, 12.67709964810647882, -223.3751320524553705 ) ) ;
#110396=CARTESIAN_POINT ( 'NONE',  ( 18.56579813702275317, 46.46179379974390855, -243.0832762246653260 ) ) ;
#110402=DIRECTION ( 'NONE',  ( 0.000000000000000000, -0.8814952561688438326, 0.4721928772777330696 ) ) ;
#110403=EDGE_LOOP ( 'NONE', ( #130774, #190371, #106904, #22617 ) ) ;
#110422=ORIENTED_EDGE ( 'NONE', *, *, #12355, .T. ) ;
#110433=CARTESIAN_POINT ( 'NONE',  ( -20.94999999999999929, 36.18002604163306302, -236.0784499204090991 ) ) ;
#110444=CARTESIAN_POINT ( 'NONE',  ( -21.05000000000000071, 12.71802988599559292, -223.5105008658000258 ) ) ;
#110459=DIRECTION ( 'NONE',  ( 1.000000000000000000, 0.000000000000000000, 0.000000000000000000 ) ) ;
#110513=ORIENTED_EDGE ( 'NONE', *, *, #189173, .F. ) ;
#110531=FACE_OUTER_BOUND ( 'NONE', #177599, .T. ) ;
#110533=CARTESIAN_POINT ( 'NONE',  ( -21.53752568617687047, 10.24627015979678291, -227.7034273308914578 ) ) ;
#110544=CARTESIAN_POINT ( 'NONE',  ( -23.25000000000000000, 43.35377423437995503, -245.1717807829448930 ) ) ;
#110551=EDGE_LOOP ( 'NONE', ( #171066, #218241, #84213, #194242 ) ) ;
#110574=AXIS2_PLACEMENT_3D ( 'NONE', #205840, #148448, #71491 ) ;
#110638=PLANE ( 'NONE',  #53529 ) ;
#110659=DIRECTION ( 'NONE',  ( 0.000000000000000000, 0.8814952561688428334, -0.4721928772777349570 ) ) ;
#110689=VERTEX_POINT ( 'NONE', #108277 ) ;
#110716=CARTESIAN_POINT ( 'NONE',  ( -23.15000000000000213, 28.00279607545604676, -239.9795148779844283 ) ) ;
#110718=DIRECTION ( 'NONE',  ( -1.000000000000000000, 0.000000000000000000, 0.000000000000000000 ) ) ;
#110733=DIRECTION ( 'NONE',  ( 0.000000000000000000, -0.9371753822965314118, 0.3488585713686133682 ) ) ;
#110776=ORIENTED_EDGE ( 'NONE', *, *, #97919, .F. ) ;
#110778=DIRECTION ( 'NONE',  ( -1.000000000000000000, 0.000000000000000000, 0.000000000000000000 ) ) ;
#110780=ORIENTED_EDGE ( 'NONE', *, *, #173663, .T. ) ;
#110795=ORIENTED_EDGE ( 'NONE', *, *, #54190, .F. ) ;
#110854=ORIENTED_EDGE ( 'NONE', *, *, #236578, .F. ) ;
#110859=CARTESIAN_POINT ( 'NONE',  ( 23.24999999999999645, 7.128833340093095217, -233.7327013124392749 ) ) ;
#110900=DIRECTION ( 'NONE',  ( 1.000000000000000000, 1.541880601228652843E-16, 2.878400969107353907E-16 ) ) ;
#110949=( GEOMETRIC_REPRESENTATION_CONTEXT ( 3 ) GLOBAL_UNCERTAINTY_ASSIGNED_CONTEXT ( ( #233204 ) ) GLOBAL_UNIT_ASSIGNED_CONTEXT ( ( #178182, #191020, #59146 ) ) REPRESENTATION_CONTEXT ( 'NONE', 'WORKASPACE' ) );
#110955=LINE ( 'NONE', #190518, #64819 ) ;
#110956=ORIENTED_EDGE ( 'NONE', *, *, #91834, .F. ) ;
#110964=VECTOR ( 'NONE', #115217, 1000.000000000000000 ) ;
#110966=EDGE_CURVE ( 'NONE', #214701, #208046, #249265, .T. ) ;
#110982=DIRECTION ( 'NONE',  ( 1.000000000000000000, 0.000000000000000000, 0.000000000000000000 ) ) ;
#111022=DIRECTION ( 'NONE',  ( 0.000000000000000000, 0.8814952561688437216, -0.4721928772777334582 ) ) ;
#111036=LINE ( 'NONE', #90167, #1249 ) ;
#111046=CARTESIAN_POINT ( 'NONE',  ( -22.39999999999999858, 12.54173083476182526, -223.4160622903444846 ) ) ;
#111050=CARTESIAN_POINT ( 'NONE',  ( 20.04142135623731136, 34.40595771266846725, -235.0146864773515176 ) ) ;
#111062=CARTESIAN_POINT ( 'NONE',  ( 20.41140022480129446, 18.75715215813852765, -228.1517052862273829 ) ) ;
#111094=EDGE_LOOP ( 'NONE', ( #81131, #216073, #77449, #163594 ) ) ;
#111098=ORIENTED_EDGE ( 'NONE', *, *, #253371, .F. ) ;
#111100=ORIENTED_EDGE ( 'NONE', *, *, #202167, .T. ) ;
#111111=FACE_OUTER_BOUND ( 'NONE', #88219, .T. ) ;
#111126=ORIENTED_EDGE ( 'NONE', *, *, #11424, .T. ) ;
#111139=CARTESIAN_POINT ( 'NONE',  ( 18.31325810956315792, 38.21040716756283473, -261.2006724472523160 ) ) ;
#111150=ORIENTED_EDGE ( 'NONE', *, *, #40837, .F. ) ;
#111176=EDGE_LOOP ( 'NONE', ( #180334, #34652, #84456, #185546 ) ) ;
#111177=LINE ( 'NONE', #92880, #31932 ) ;
#111178=CARTESIAN_POINT ( 'NONE',  ( -18.50000000000000000, 46.32970330538243786, -243.0551226933711746 ) ) ;
#111254=DIRECTION ( 'NONE',  ( 1.000000000000000000, 0.000000000000000000, 0.000000000000000000 ) ) ;
#111255=ORIENTED_EDGE ( 'NONE', *, *, #197393, .F. ) ;
#111262=CARTESIAN_POINT ( 'NONE',  ( 23.14999999999998437, 5.216452187118270523, -237.3027570999230988 ) ) ;
#111264=ORIENTED_EDGE ( 'NONE', *, *, #63348, .F. ) ;
#111286=VERTEX_POINT ( 'NONE', #108283 ) ;
#111311=CYLINDRICAL_SURFACE ( 'NONE', #55230, 11.80000000000000604 ) ;
#111325=ORIENTED_EDGE ( 'NONE', *, *, #57581, .T. ) ;
#111347=DIRECTION ( 'NONE',  ( 0.000000000000000000, -0.4721928772777346239, -0.8814952561688430555 ) ) ;
#111356=CARTESIAN_POINT ( 'NONE',  ( -18.59999999999999787, 38.30077178631846380, -261.1858881914067751 ) ) ;
#111368=ORIENTED_EDGE ( 'NONE', *, *, #191441, .T. ) ;
#111401=DIRECTION ( 'NONE',  ( 0.000000000000000000, -0.8814952561688430555, 0.4721928772777346239 ) ) ;
#111428=TOROIDAL_SURFACE ( 'NONE', #257119, 0.2000000000000000111, 0.1000000000000000056 ) ;
#111436=CARTESIAN_POINT ( 'NONE',  ( -22.50000000000000000, 12.54152817314150248, -223.4164406214577241 ) ) ;
#111439=CIRCLE ( 'NONE', #257142, 6.258578643762719551 ) ;
#111461=CARTESIAN_POINT ( 'NONE',  ( 23.14999999999999503, 35.97645343225767789, -235.9694016464868298 ) ) ;
#111486=VECTOR ( 'NONE', #239314, 1000.000000000000114 ) ;
#111488=CARTESIAN_POINT ( 'NONE',  ( 21.05000000000000071, 1.560941917020248759, -230.7743948584411839 ) ) ;
#111507=ORIENTED_EDGE ( 'NONE', *, *, #170924, .F. ) ;
#111516=AXIS2_PLACEMENT_3D ( 'NONE', #234505, #212403, #170749 ) ;
#111565=CIRCLE ( 'NONE', #223966, 0.2000000000000101419 ) ;
#111604=CARTESIAN_POINT ( 'NONE',  ( 21.05000000000000071, 28.58935552370083144, -258.2621935127861548 ) ) ;
#111647=VECTOR ( 'NONE', #114395, 1000.000000000000000 ) ;
#111660=ORIENTED_EDGE ( 'NONE', *, *, #230109, .T. ) ;
#111672=ADVANCED_FACE ( 'NONE', ( #213146 ), #12313, .F. ) ;
#111680=CARTESIAN_POINT ( 'NONE',  ( 18.49351773456764292, 9.003734232116954672, -245.4495432009024114 ) ) ;
#111727=EDGE_LOOP ( 'NONE', ( #149388, #252158, #17518, #67590 ) ) ;
#111744=AXIS2_PLACEMENT_3D ( 'NONE', #214475, #133663, #191099 ) ;
#111771=ADVANCED_FACE ( 'NONE', ( #174069 ), #224660, .T. ) ;
#111798=ORIENTED_EDGE ( 'NONE', *, *, #24520, .F. ) ;
#111806=CARTESIAN_POINT ( 'NONE',  ( 20.94999999999999929, 42.92545512184477730, -254.1955779480491344 ) ) ;
#111826=CIRCLE ( 'NONE', #145116, 11.90000000000000746 ) ;
#111835=CARTESIAN_POINT ( 'NONE',  ( -21.07094088545303379, 10.02599695582151007, -228.1148069861733063 ) ) ;
#111871=AXIS2_PLACEMENT_3D ( 'NONE', #155176, #232127, #52174 ) ;
#111875=EDGE_LOOP ( 'NONE', ( #65519, #192418, #109170, #3298 ) ) ;
#111902=DIRECTION ( 'NONE',  ( -1.000000000000000000, -1.394253735153569469E-16, -2.602809386958778209E-16 ) ) ;
#111927=DIRECTION ( 'NONE',  ( -1.000000000000000000, 0.000000000000000000, 0.000000000000000000 ) ) ;
#111937=CARTESIAN_POINT ( 'NONE',  ( 21.09787244211736379, 22.06134468089375744, -231.7765419340705648 ) ) ;
#111958=CYLINDRICAL_SURFACE ( 'NONE', #76506, 0.09999999999999939493 ) ;
#111973=EDGE_LOOP ( 'NONE', ( #186699, #170784, #36082, #113646 ) ) ;
#112004=CARTESIAN_POINT ( 'NONE',  ( -21.05000000000000071, 1.658775325997247752, -230.6916041481598540 ) ) ;
#112021=CARTESIAN_POINT ( 'NONE',  ( 21.05000000000000071, 11.36448785225375424, -246.7787679937655980 ) ) ;
#112037=CIRCLE ( 'NONE', #145324, 4.150000000000009237 ) ;
#112053=VECTOR ( 'NONE', #246528, 1000.000000000000000 ) ;
#112073=CARTESIAN_POINT ( 'NONE',  ( -20.94999999999999929, 14.77103648604101060, -236.4083752604501001 ) ) ;
#112092=LINE ( 'NONE', #35144, #58432 ) ;
#112095=B_SPLINE_CURVE_WITH_KNOTS ( 'NONE', 3,
 ( #132315, #94466, #232725, #153204, #256058, #54061, #73662, #155769 ),
 .UNSPECIFIED., .F., .F.,
 ( 4, 2, 2, 4 ),
 ( 0.000000000000000000, 9.550056980123548204E-05, 0.0001910011396024709641, 0.0003820022792049855131 ),
 .UNSPECIFIED. ) ;
#112102=ORIENTED_EDGE ( 'NONE', *, *, #62005, .F. ) ;
#112137=ORIENTED_EDGE ( 'NONE', *, *, #108087, .F. ) ;
#112152=CIRCLE ( 'NONE', #37128, 0.1000000000000075273 ) ;
#112233=EDGE_CURVE ( 'NONE', #235869, #246507, #145729, .T. ) ;
#112255=CARTESIAN_POINT ( 'NONE',  ( 18.59999999999999432, 13.71992543034163958, -238.5823796952984992 ) ) ;
#112266=DIRECTION ( 'NONE',  ( 1.000000000000000000, 0.000000000000000000, 0.000000000000000000 ) ) ;
#112282=DIRECTION ( 'NONE',  ( -2.952720810173288619E-16, 0.4721928772777346239, 0.8814952561688430555 ) ) ;
#112284=ORIENTED_EDGE ( 'NONE', *, *, #234052, .F. ) ;
#112288=CARTESIAN_POINT ( 'NONE',  ( -21.05000000000000071, 18.67052684763574533, -226.7323173977782460 ) ) ;
#112303=ADVANCED_FACE ( 'NONE', ( #185288 ), #2775, .T. ) ;
#112339=EDGE_LOOP ( 'NONE', ( #153471, #11647, #28454, #186216, #48666 ) ) ;
#112342=ORIENTED_EDGE ( 'NONE', *, *, #167359, .T. ) ;
#112349=DIRECTION ( 'NONE',  ( 1.000000000000000000, 0.000000000000000000, 0.000000000000000000 ) ) ;
#112368=ORIENTED_EDGE ( 'NONE', *, *, #117106, .T. ) ;
#112374=ORIENTED_EDGE ( 'NONE', *, *, #250416, .F. ) ;
#112391=DIRECTION ( 'NONE',  ( 1.000000000000000000, -3.448943450116723075E-16, -6.438528483529606658E-16 ) ) ;
#112407=DIRECTION ( 'NONE',  ( -0.000000000000000000, 0.4721928772777345684, 0.8814952561688429444 ) ) ;
#112438=CARTESIAN_POINT ( 'NONE',  ( 18.50000000000000355, 38.28679861725832012, -261.0868692510649680 ) ) ;
#112466=CARTESIAN_POINT ( 'NONE',  ( 18.60000000000000142, 9.105964803472835101, -245.3658845043482586 ) ) ;
#112470=CARTESIAN_POINT ( 'NONE',  ( 20.94999999999999929, 31.15787740146373608, -259.8205824356103903 ) ) ;
#112490=ORIENTED_EDGE ( 'NONE', *, *, #8015, .T. ) ;
#112512=CARTESIAN_POINT ( 'NONE',  ( 18.49999999999998934, 19.05165861791954285, -232.6888762659126826 ) ) ;
#112513=DIRECTION ( 'NONE',  ( -1.000000000000000000, -3.448943450116728005E-16, -6.438528483529605672E-16 ) ) ;
#112544=DIRECTION ( 'NONE',  ( -1.000000000000000000, 0.000000000000000000, 0.000000000000000000 ) ) ;
#112569=CARTESIAN_POINT ( 'NONE',  ( 21.05000000000000071, 7.128833340093095217, -233.7327013124392749 ) ) ;
#112583=DIRECTION ( 'NONE',  ( -3.440080580676164606E-14, 0.8127272543710891695, -0.5826443254700338636 ) ) ;
#112594=DIRECTION ( 'NONE',  ( 1.000000000000000000, -0.000000000000000000, -0.000000000000000000 ) ) ;
#112608=VECTOR ( 'NONE', #41972, 1000.000000000000000 ) ;
#112615=AXIS2_PLACEMENT_3D ( 'NONE', #203710, #121628, #62910 ) ;
#112648=DIRECTION ( 'NONE',  ( 0.000000000000000000, 0.8814952561688430555, -0.4721928772777346239 ) ) ;
#112666=ORIENTED_EDGE ( 'NONE', *, *, #113254, .T. ) ;
#112691=CARTESIAN_POINT ( 'NONE',  ( -20.54999999999999716, 36.65892442174935439, -249.5511627012433848 ) ) ;
#112718=EDGE_CURVE ( 'NONE', #158507, #93493, #241786, .T. ) ;
#112739=EDGE_CURVE ( 'NONE', #5127, #253511, #125278, .T. ) ;
#112744=CIRCLE ( 'NONE', #216791, 0.09999999999999939493 ) ;
#112761=DIRECTION ( 'NONE',  ( 2.952720810173288126E-16, -0.4721928772777345684, -0.8814952561688429444 ) ) ;
#112778=AXIS2_PLACEMENT_3D ( 'NONE', #172318, #234810, #17067 ) ;
#112786=VECTOR ( 'NONE', #188709, 1000.000000000000000 ) ;
#112810=ORIENTED_EDGE ( 'NONE', *, *, #157994, .T. ) ;
#112828=DIRECTION ( 'NONE',  ( 0.000000000000000000, -0.5826443254699606999, -0.8127272543711416830 ) ) ;
#112852=CARTESIAN_POINT ( 'NONE',  ( -23.15000000000000213, 19.89303971870268839, -235.6353404070293038 ) ) ;
#112914=VERTEX_POINT ( 'NONE', #77848 ) ;
#112953=EDGE_LOOP ( 'NONE', ( #208130, #138630, #134857, #169807 ) ) ;
#112956=VECTOR ( 'NONE', #124470, 1000.000000000000000 ) ;
#112975=CARTESIAN_POINT ( 'NONE',  ( -20.54999999999999716, 11.15983666280819975, -246.1019239270423213 ) ) ;
#112994=EDGE_LOOP ( 'NONE', ( #53121, #238131, #229197 ) ) ;
#113009=CARTESIAN_POINT ( 'NONE',  ( -21.05000000000000071, 36.02918351690956200, -236.0543695120161090 ) ) ;
#113013=CARTESIAN_POINT ( 'NONE',  ( 18.59999999999999076, 33.67810952736942198, -236.3734420906320395 ) ) ;
#113014=CARTESIAN_POINT ( 'NONE',  ( -22.39999999999999858, -3.229117512539506407, -228.1842305956903090 ) ) ;
#113063=ORIENTED_EDGE ( 'NONE', *, *, #14638, .F. ) ;
#113072=SPHERICAL_SURFACE ( 'NONE', #77019, 0.1000000000000000056 ) ;
#113077=CIRCLE ( 'NONE', #444, 2.099999999999989875 ) ;
#113078=AXIS2_PLACEMENT_3D ( 'NONE', #219952, #165118, #7320 ) ;
#113084=DIRECTION ( 'NONE',  ( 0.000000000000000000, 0.8814952561688476074, -0.4721928772777262417 ) ) ;
#113113=CARTESIAN_POINT ( 'NONE',  ( -21.05000000000000071, 36.65892442174935439, -249.5511627012433848 ) ) ;
#113137=EDGE_LOOP ( 'NONE', ( #155365, #92673, #159365, #141841 ) ) ;
#113163=CIRCLE ( 'NONE', #697, 11.65000000000001457 ) ;
#113185=DIRECTION ( 'NONE',  ( 1.000000000000000000, 0.000000000000000000, 0.000000000000000000 ) ) ;
#113186=ORIENTED_EDGE ( 'NONE', *, *, #125400, .T. ) ;
#113200=CARTESIAN_POINT ( 'NONE',  ( 20.95545211741311320, 18.81481477104959055, -227.9829527115510643 ) ) ;
#113204=FACE_OUTER_BOUND ( 'NONE', #227446, .T. ) ;
#113208=FACE_OUTER_BOUND ( 'NONE', #64979, .T. ) ;
#113230=EDGE_CURVE ( 'NONE', #102673, #208784, #50408, .T. ) ;
#113254=EDGE_CURVE ( 'NONE', #101747, #250639, #196177, .T. ) ;
#113268=EDGE_CURVE ( 'NONE', #4633, #74203, #229516, .T. ) ;
#113294=CARTESIAN_POINT ( 'NONE',  ( -22.49072729836730034, -3.113923299533181588, -228.1818618411975308 ) ) ;
#113299=AXIS2_PLACEMENT_3D ( 'NONE', #157962, #60083, #220470 ) ;
#113343=ADVANCED_FACE ( 'NONE', ( #5366 ), #204555, .T. ) ;
#113345=CIRCLE ( 'NONE', #67552, 0.09999999999999939493 ) ;
#113346=DIRECTION ( 'NONE',  ( -0.000000000000000000, 0.4721928772777346239, 0.8814952561688430555 ) ) ;
#113351=DIRECTION ( 'NONE',  ( 0.7071067811865473507, 0.3338907855510732658, 0.6233112732207619633 ) ) ;
#113385=CARTESIAN_POINT ( 'NONE',  ( 18.59999999999999787, 18.92285928089247804, -233.3572654221044900 ) ) ;
#113434=ORIENTED_EDGE ( 'NONE', *, *, #103873, .F. ) ;
#113444=VECTOR ( 'NONE', #209804, 1000.000000000000000 ) ;
#113458=CARTESIAN_POINT ( 'NONE',  ( 21.05000000000000071, 18.80454058543246276, -232.7833891117047074 ) ) ;
#113485=CARTESIAN_POINT ( 'NONE',  ( 20.94999999999999929, 31.15787740146373253, -259.8205824356103903 ) ) ;
#113497=CIRCLE ( 'NONE', #192612, 0.09999999999999983902 ) ;
#113509=ORIENTED_EDGE ( 'NONE', *, *, #256562, .T. ) ;
#113513=AXIS2_PLACEMENT_3D ( 'NONE', #29008, #11993, #210185 ) ;
#113530=VECTOR ( 'NONE', #41370, 1000.000000000000000 ) ;
#113554=CARTESIAN_POINT ( 'NONE',  ( 22.57320508075687115, 12.67709964810647882, -223.3751320524553705 ) ) ;
#113560=ORIENTED_EDGE ( 'NONE', *, *, #253780, .T. ) ;
#113578=DIRECTION ( 'NONE',  ( 1.000000000000000000, 0.000000000000000000, 0.000000000000000000 ) ) ;
#113594=ORIENTED_EDGE ( 'NONE', *, *, #217790, .F. ) ;
#113596=DIRECTION ( 'NONE',  ( 0.000000000000000000, -0.4721928772777489458, -0.8814952561688353949 ) ) ;
#113601=ORIENTED_EDGE ( 'NONE', *, *, #46609, .T. ) ;
#113608=ORIENTED_EDGE ( 'NONE', *, *, #66443, .F. ) ;
#113624=CIRCLE ( 'NONE', #134274, 0.1000000000000013933 ) ;
#113631=CARTESIAN_POINT ( 'NONE',  ( 20.87631937322875331, 18.75490874231121552, -228.0812301260858987 ) ) ;
#113646=ORIENTED_EDGE ( 'NONE', *, *, #36088, .F. ) ;
#113649=CIRCLE ( 'NONE', #22662, 0.5000000000000008882 ) ;
#113657=ORIENTED_EDGE ( 'NONE', *, *, #36107, .F. ) ;
#113667=ORIENTED_EDGE ( 'NONE', *, *, #226879, .T. ) ;
#113680=ORIENTED_EDGE ( 'NONE', *, *, #142822, .T. ) ;
#113701=CARTESIAN_POINT ( 'NONE',  ( 18.56308993302910437, 33.83802916238668246, -236.2638560227619564 ) ) ;
#113703=DIRECTION ( 'NONE',  ( 0.000000000000000000, 0.8814952561688476074, -0.4721928772777262417 ) ) ;
#113709=CARTESIAN_POINT ( 'NONE',  ( 18.49999999999999289, 33.78138312054863945, -236.4287629273227651 ) ) ;
#113722=EDGE_LOOP ( 'NONE', ( #94645, #148951, #187065, #56525 ) ) ;
#113740=CARTESIAN_POINT ( 'NONE',  ( 18.49999999999999645, 7.128833340093095217, -233.7327013124392749 ) ) ;
#113742=DIRECTION ( 'NONE',  ( 1.000000000000000000, -0.000000000000000000, -0.000000000000000000 ) ) ;
#113773=FACE_OUTER_BOUND ( 'NONE', #29749, .T. ) ;
#113807=DIRECTION ( 'NONE',  ( 1.000000000000000000, 0.000000000000000000, 0.000000000000000000 ) ) ;
#113830=TOROIDAL_SURFACE ( 'NONE', #80671, 0.6000000000000015321, 0.1000000000000000056 ) ;
#113835=EDGE_LOOP ( 'NONE', ( #113434, #25333, #48869, #81830 ) ) ;
#113853=ORIENTED_EDGE ( 'NONE', *, *, #4664, .T. ) ;
#113859=EDGE_CURVE ( 'NONE', #67371, #98189, #89750, .T. ) ;
#113893=CIRCLE ( 'NONE', #134719, 0.09999999999999031886 ) ;
#113917=ORIENTED_EDGE ( 'NONE', *, *, #238606, .F. ) ;
#113919=DIRECTION ( 'NONE',  ( -0.000000000000000000, 0.8814952561688430555, -0.4721928772777346239 ) ) ;
#113922=AXIS2_PLACEMENT_3D ( 'NONE', #25117, #142461, #26393 ) ;
#113942=EDGE_LOOP ( 'NONE', ( #255227, #52650 ) ) ;
#113951=DIRECTION ( 'NONE',  ( -1.000000000000000000, -0.000000000000000000, -0.000000000000000000 ) ) ;
#113958=CIRCLE ( 'NONE', #197346, 0.5999999999999992006 ) ;
#113960=CARTESIAN_POINT ( 'NONE',  ( -18.58744394320964233, 38.15605368352883175, -261.2055860874503992 ) ) ;
#113991=CARTESIAN_POINT ( 'NONE',  ( -22.50000000000000711, 12.58798907299599534, -223.3278890275437334 ) ) ;
#113996=LINE ( 'NONE', #51433, #161454 ) ;
#114003=AXIS2_PLACEMENT_3D ( 'NONE', #121132, #215061, #118555 ) ;
#114022=ORIENTED_EDGE ( 'NONE', *, *, #232160, .T. ) ;
#114032=B_SPLINE_CURVE_WITH_KNOTS ( 'NONE', 3,
 ( #233452, #57333, #218987, #156496, #135590, #95200 ),
 .UNSPECIFIED., .F., .F.,
 ( 4, 2, 4 ),
 ( 0.000000000000000000, 0.0001497467027049253347, 0.0002994934054098506693 ),
 .UNSPECIFIED. ) ;
#114040=VECTOR ( 'NONE', #34799, 1000.000000000000114 ) ;
#114057=ORIENTED_EDGE ( 'NONE', *, *, #31655, .F. ) ;
#114103=CARTESIAN_POINT ( 'NONE',  ( -20.64999999999999858, 25.94586868676353575, -241.5435999122864530 ) ) ;
#114108=DIRECTION ( 'NONE',  ( -0.000000000000000000, 0.8814952561688428334, -0.4721928772777352346 ) ) ;
#114113=DIRECTION ( 'NONE',  ( 0.000000000000000000, -0.8814952561673441433, 0.4721928772805327745 ) ) ;
#114117=DIRECTION ( 'NONE',  ( -3.265361837132814079E-16, 0.4721928772777359007, 0.8814952561688425003 ) ) ;
#114138=CARTESIAN_POINT ( 'NONE',  ( -21.05000000000000071, 30.43677443282724937, -239.5249545687858870 ) ) ;
#114140=EDGE_CURVE ( 'NONE', #104543, #129019, #201692, .T. ) ;
#114151=ADVANCED_FACE ( 'NONE', ( #199132 ), #124736, .T. ) ;
#114162=EDGE_CURVE ( 'NONE', #11331, #160449, #99993, .T. ) ;
#114235=CARTESIAN_POINT ( 'NONE',  ( 23.15000000000000213, 11.39998237908105594, -245.7725481090871540 ) ) ;
#114285=CARTESIAN_POINT ( 'NONE',  ( -21.05000000000000071, 36.02367271998545561, -235.8812521208699025 ) ) ;
#114303=EDGE_LOOP ( 'NONE', ( #51143, #56208, #155342, #161415 ) ) ;
#114333=ORIENTED_EDGE ( 'NONE', *, *, #247014, .T. ) ;
#114344=CARTESIAN_POINT ( 'NONE',  ( -23.15000000000000213, 36.65892442174935439, -249.5511627012433848 ) ) ;
#114348=ORIENTED_EDGE ( 'NONE', *, *, #125400, .F. ) ;
#114394=CARTESIAN_POINT ( 'NONE',  ( 22.50000000000000000, -3.092988775432913506, -228.1437074281570858 ) ) ;
#114395=DIRECTION ( 'NONE',  ( 1.000000000000000000, 0.000000000000000000, 0.000000000000000000 ) ) ;
#114414=DIRECTION ( 'NONE',  ( 0.000000000000000000, -0.4721928772777346239, -0.8814952561688430555 ) ) ;
#114424=VERTEX_POINT ( 'NONE', #12508 ) ;
#114427=CARTESIAN_POINT ( 'NONE',  ( 21.14999999999999858, 21.10816309994747186, -233.7904894189133813 ) ) ;
#114431=VERTEX_POINT ( 'NONE', #114138 ) ;
#114445=CARTESIAN_POINT ( 'NONE',  ( 21.07094088545302668, 10.02599695582151007, -228.1148069861733063 ) ) ;
#114497=DIRECTION ( 'NONE',  ( 0.000000000000000000, -0.8814952561688398358, 0.4721928772777406746 ) ) ;
#114505=VECTOR ( 'NONE', #67764, 1000.000000000000000 ) ;
#114510=VERTEX_POINT ( 'NONE', #34107 ) ;
#114521=DIRECTION ( 'NONE',  ( -1.000000000000000000, -0.000000000000000000, -0.000000000000000000 ) ) ;
#114533=CARTESIAN_POINT ( 'NONE',  ( 21.14999999999999858, 21.06723286205836487, -233.6551206055687260 ) ) ;
#114548=ORIENTED_EDGE ( 'NONE', *, *, #80936, .F. ) ;
#114611=CARTESIAN_POINT ( 'NONE',  ( -23.25000000000000000, 10.69888912757691024, -235.6450824654141059 ) ) ;
#114627=ORIENTED_EDGE ( 'NONE', *, *, #59368, .T. ) ;
#114667=DIRECTION ( 'NONE',  ( -1.000000000000000000, -0.000000000000000000, -0.000000000000000000 ) ) ;
#114681=CARTESIAN_POINT ( 'NONE',  ( -23.15000000000000213, 31.49702336731128582, -233.4564499823349877 ) ) ;
#114717=B_SPLINE_CURVE_WITH_KNOTS ( 'NONE', 3,
 ( #224717, #87769, #146461, #245591, #65654, #167358, #89061, #86476, #246852, #68231, #166081, #147776, #227296, #104749, #48656, #106042, #128210, #209026, #10830 ),
 .UNSPECIFIED., .F., .F.,
 ( 4, 3, 3, 3, 3, 3, 4 ),
 ( 0.000000000000000000, 1.655171619026003227E-05, 2.773500582848852791E-05, 5.941817267378676065E-05, 0.0001114174635873525684, 0.0001914169455916370536, 0.0002627181070750628472 ),
 .UNSPECIFIED. ) ;
#114748=ADVANCED_FACE ( 'NONE', ( #180012 ), #204673, .T. ) ;
#114750=AXIS2_PLACEMENT_3D ( 'NONE', #213980, #233554, #152751 ) ;
#114768=ORIENTED_EDGE ( 'NONE', *, *, #194260, .F. ) ;
#114777=LINE ( 'NONE', #36558, #67406 ) ;
#114833=DIRECTION ( 'NONE',  ( 0.000000000000000000, 0.8814952561688437216, -0.4721928772777334582 ) ) ;
#114838=CARTESIAN_POINT ( 'NONE',  ( -21.05000000000000071, 18.60982576078065165, -226.6665746245395496 ) ) ;
#114840=DIRECTION ( 'NONE',  ( -0.000000000000000000, -0.8454177738465993297, -0.5341055959866553016 ) ) ;
#114865=ADVANCED_FACE ( 'NONE', ( #205975 ), #203418, .F. ) ;
#114890=AXIS2_PLACEMENT_3D ( 'NONE', #143390, #140832, #243779 ) ;
#114891=DIRECTION ( 'NONE',  ( 0.000000000000000000, 0.8814952561688476074, -0.4721928772777262417 ) ) ;
#114913=EDGE_CURVE ( 'NONE', #251809, #85514, #29932, .T. ) ;
#114918=CARTESIAN_POINT ( 'NONE',  ( 20.44999100639848066, 18.89797881968811666, -228.1939261438453173 ) ) ;
#114984=CARTESIAN_POINT ( 'NONE',  ( 18.49999999999999289, 33.72439408143423378, -236.3982354565453363 ) ) ;
#114988=CARTESIAN_POINT ( 'NONE',  ( 23.14999999999999147, 7.128833340093095217, -233.7327013124392749 ) ) ;
#114990=DIRECTION ( 'NONE',  ( -1.000000000000000000, -0.000000000000000000, -0.000000000000000000 ) ) ;
#114994=ORIENTED_EDGE ( 'NONE', *, *, #42607, .F. ) ;
#115002=DIRECTION ( 'NONE',  ( 1.000000000000000000, -0.000000000000000000, -0.000000000000000000 ) ) ;
#115076=CARTESIAN_POINT ( 'NONE',  ( -18.59999999999999787, 13.35316836840606669, -247.8440497049677731 ) ) ;
#115089=DIRECTION ( 'NONE',  ( -0.000000000000000000, 0.8814952561688430555, -0.4721928772777346239 ) ) ;
#115112=DIRECTION ( 'NONE',  ( 0.000000000000000000, -0.8814952561688398358, 0.4721928772777406746 ) ) ;
#115114=CARTESIAN_POINT ( 'NONE',  ( -20.94999999999999929, 26.34542992457388522, -244.0265060370938954 ) ) ;
#115126=CARTESIAN_POINT ( 'NONE',  ( -20.94999027547553894, 46.33166059915855328, -243.0555356998360423 ) ) ;
#115140=CARTESIAN_POINT ( 'NONE',  ( -20.54999999999999716, 19.25956423861613231, -238.0467473098318010 ) ) ;
#115173=CARTESIAN_POINT ( 'NONE',  ( 20.94999999999999929, 18.94908112497232011, -227.8991131484155517 ) ) ;
#115193=DIRECTION ( 'NONE',  ( 0.000000000000000000, -0.4721928772777344019, -0.8814952561688431665 ) ) ;
#115217=DIRECTION ( 'NONE',  ( 1.000000000000000000, 0.000000000000000000, 0.000000000000000000 ) ) ;
#115236=AXIS2_PLACEMENT_3D ( 'NONE', #42125, #83751, #40850 ) ;
#115246=DIRECTION ( 'NONE',  ( 1.000000000000000000, 0.000000000000000000, 0.000000000000000000 ) ) ;
#115252=CARTESIAN_POINT ( 'NONE',  ( -18.44232395689977722, 38.17981730268489571, -261.2023171126317607 ) ) ;
#115262=DIRECTION ( 'NONE',  ( -2.915501640297154776E-16, 0.4721928772777348460, 0.8814952561688429444 ) ) ;
#115266=ADVANCED_FACE ( 'NONE', ( #194786 ), #216879, .T. ) ;
#115306=AXIS2_PLACEMENT_3D ( 'NONE', #231200, #130786, #107368 ) ;
#115323=CARTESIAN_POINT ( 'NONE',  ( 21.14999999999999858, 12.71802988599559470, -223.5105008658000258 ) ) ;
#115327=CYLINDRICAL_SURFACE ( 'NONE', #222524, 11.79999999999999361 ) ;
#115333=CIRCLE ( 'NONE', #248611, 12.87500000000000000 ) ;
#115337=ORIENTED_EDGE ( 'NONE', *, *, #109292, .F. ) ;
#115338=ORIENTED_EDGE ( 'NONE', *, *, #180098, .F. ) ;
#115347=PLANE ( 'NONE',  #152791 ) ;
#115371=DIRECTION ( 'NONE',  ( -1.836970198721030427E-16, 0.4721928772777346239, 0.8814952561688430555 ) ) ;
#115391=DIRECTION ( 'NONE',  ( 0.000000000000000000, 0.8814952561688444987, -0.4721928772777320149 ) ) ;
#115400=TOROIDAL_SURFACE ( 'NONE', #27967, 4.099999999999999645, 0.1000000000000000056 ) ;
#115422=DIRECTION ( 'NONE',  ( 1.000000000000000000, 0.000000000000000000, 0.000000000000000000 ) ) ;
#115460=EDGE_CURVE ( 'NONE', #118204, #136977, #255492, .T. ) ;
#115518=DIRECTION ( 'NONE',  ( -0.000000000000000000, 0.4721928772777345684, 0.8814952561688429444 ) ) ;
#115555=AXIS2_PLACEMENT_3D ( 'NONE', #124548, #184492, #60688 ) ;
#115563=CARTESIAN_POINT ( 'NONE',  ( -18.46093223321767596, 8.897120040860684753, -245.4351526656046758 ) ) ;
#115565=EDGE_CURVE ( 'NONE', #188452, #97404, #130063, .T. ) ;
#115574=CARTESIAN_POINT ( 'NONE',  ( 21.09096482362047098, 10.09888019307431684, -228.1046399456574818 ) ) ;
#115592=DIRECTION ( 'NONE',  ( 1.000000000000000000, 0.000000000000000000, 0.000000000000000000 ) ) ;
#115649=CARTESIAN_POINT ( 'NONE',  ( 23.14999999999999858, 36.65892442174935439, -249.5511627012433848 ) ) ;
#115662=AXIS2_PLACEMENT_3D ( 'NONE', #157301, #158584, #20357 ) ;
#115696=ORIENTED_EDGE ( 'NONE', *, *, #9740, .F. ) ;
#115706=CYLINDRICAL_SURFACE ( 'NONE', #63396, 4.049999999999997158 ) ;
#115719=DIRECTION ( 'NONE',  ( 0.000000000000000000, 0.8814952561688476074, -0.4721928772777262417 ) ) ;
#115739=FACE_OUTER_BOUND ( 'NONE', #222350, .T. ) ;
#115782=CARTESIAN_POINT ( 'NONE',  ( -23.25000000000000000, 23.34004772283015328, -229.2004250369967338 ) ) ;
#115791=AXIS2_PLACEMENT_3D ( 'NONE', #11640, #110718, #16771 ) ;
#115795=CIRCLE ( 'NONE', #186547, 4.000000000000010658 ) ;
#115845=CIRCLE ( 'NONE', #165755, 1.999999999999997335 ) ;
#115857=ORIENTED_EDGE ( 'NONE', *, *, #36088, .T. ) ;
#115858=VECTOR ( 'NONE', #233312, 1000.000000000000000 ) ;
#115885=FACE_OUTER_BOUND ( 'NONE', #10327, .T. ) ;
#115902=EDGE_LOOP ( 'NONE', ( #99610, #32365, #13874, #199472 ) ) ;
#115918=FACE_OUTER_BOUND ( 'NONE', #162273, .T. ) ;
#115934=DIRECTION ( 'NONE',  ( 0.000000000000000000, 0.8814952561688438326, -0.4721928772777332362 ) ) ;
#115942=DIRECTION ( 'NONE',  ( -0.000000000000000000, -0.4721928772777346239, -0.8814952561688430555 ) ) ;
#115943=ORIENTED_EDGE ( 'NONE', *, *, #103385, .T. ) ;
#115944=EDGE_LOOP ( 'NONE', ( #170302, #150520, #83253, #189733 ) ) ;
#115949=FACE_OUTER_BOUND ( 'NONE', #53326, .T. ) ;
#115993=ORIENTED_EDGE ( 'NONE', *, *, #97573, .F. ) ;
#116003=VECTOR ( 'NONE', #200272, 1000.000000000000114 ) ;
#116014=CARTESIAN_POINT ( 'NONE',  ( -20.94999999999999929, 36.65892442174935439, -249.5511627012433848 ) ) ;
#116040=AXIS2_PLACEMENT_3D ( 'NONE', #118212, #158650, #219870 ) ;
#116049=ORIENTED_EDGE ( 'NONE', *, *, #190767, .F. ) ;
#116098=DIRECTION ( 'NONE',  ( 0.000000000000000000, 0.8814952561688476074, -0.4721928772777262417 ) ) ;
#116122=CARTESIAN_POINT ( 'NONE',  ( -21.05000000000000071, 16.44800918141279666, -240.8068063186265135 ) ) ;
#116129=CARTESIAN_POINT ( 'NONE',  ( -23.15000000000000213, 31.44980407958351165, -233.5445995079518866 ) ) ;
#116145=CIRCLE ( 'NONE', #132708, 0.09999999999999986677 ) ;
#116154=VECTOR ( 'NONE', #190439, 1000.000000000000000 ) ;
#116162=ADVANCED_FACE ( 'NONE', ( #162741 ), #217540, .T. ) ;
#116236=EDGE_LOOP ( 'NONE', ( #202168, #53066, #73835, #219439 ) ) ;
#116271=CIRCLE ( 'NONE', #178836, 0.09999999999999834022 ) ;
#116278=ORIENTED_EDGE ( 'NONE', *, *, #150810, .F. ) ;
#116289=LINE ( 'NONE', #100523, #52384 ) ;
#116320=CARTESIAN_POINT ( 'NONE',  ( -23.15000000000000213, 11.60058429089262333, -246.3380203656811887 ) ) ;
#116324=CIRCLE ( 'NONE', #82949, 0.1000000000000053763 ) ;
#116338=AXIS2_PLACEMENT_3D ( 'NONE', #145197, #42269, #163494 ) ;
#116349=CIRCLE ( 'NONE', #3907, 0.1000000000000053901 ) ;
#116376=ORIENTED_EDGE ( 'NONE', *, *, #9386, .T. ) ;
#116380=VERTEX_POINT ( 'NONE', #231700 ) ;
#116392=DIRECTION ( 'NONE',  ( -0.000000000000000000, 0.4721928772777345684, 0.8814952561688429444 ) ) ;
#116401=CARTESIAN_POINT ( 'NONE',  ( 22.47071067811865319, 7.128833340093095217, -233.7327013124392749 ) ) ;
#116414=EDGE_CURVE ( 'NONE', #248047, #50036, #193003, .T. ) ;
#116421=DIRECTION ( 'NONE',  ( 0.000000000000000000, -0.7965107556683636014, 0.6046243595031649543 ) ) ;
#116426=VERTEX_POINT ( 'NONE', #110444 ) ;
#116433=AXIS2_PLACEMENT_3D ( 'NONE', #66412, #225459, #46823 ) ;
#116436=CARTESIAN_POINT ( 'NONE',  ( 20.85000000000000142, 45.93315328338058379, -256.6017782078560003 ) ) ;
#116452=CYLINDRICAL_SURFACE ( 'NONE', #185718, 0.1000000000000013933 ) ;
#116481=EDGE_CURVE ( 'NONE', #135978, #88325, #93441, .T. ) ;
#116491=EDGE_CURVE ( 'NONE', #11331, #3782, #247131, .T. ) ;
#116524=ORIENTED_EDGE ( 'NONE', *, *, #166282, .T. ) ;
#116525=ORIENTED_EDGE ( 'NONE', *, *, #206539, .T. ) ;
#116526=DIRECTION ( 'NONE',  ( 1.000000000000000000, 0.000000000000000000, 0.000000000000000000 ) ) ;
#116545=CARTESIAN_POINT ( 'NONE',  ( -18.59999994787167310, 38.22877715459324577, -261.1960477947820891 ) ) ;
#116549=ORIENTED_EDGE ( 'NONE', *, *, #160975, .F. ) ;
#116665=CYLINDRICAL_SURFACE ( 'NONE', #90889, 0.09999999999999939493 ) ;
#116675=AXIS2_PLACEMENT_3D ( 'NONE', #212356, #149816, #187661 ) ;
#116681=CARTESIAN_POINT ( 'NONE',  ( -20.85000000000000142, 42.99798587058931076, -254.2674462307522560 ) ) ;
#116711=EDGE_CURVE ( 'NONE', #150487, #166239, #209744, .T. ) ;
#116741=EDGE_CURVE ( 'NONE', #240580, #159212, #167577, .T. ) ;
#116749=FACE_OUTER_BOUND ( 'NONE', #248298, .T. ) ;
#116756=CARTESIAN_POINT ( 'NONE',  ( -23.15000000000000213, 36.65892442174935439, -249.5511627012433848 ) ) ;
#116761=DIRECTION ( 'NONE',  ( 0.000000000000000000, 0.8814952561688476074, -0.4721928772777262417 ) ) ;
#116765=DIRECTION ( 'NONE',  ( -1.000000000000000000, -0.000000000000000000, -0.000000000000000000 ) ) ;
#116783=ORIENTED_EDGE ( 'NONE', *, *, #34638, .F. ) ;
#116793=DIRECTION ( 'NONE',  ( 0.000000000000000000, -0.4721928772778937189, -0.8814952561687577903 ) ) ;
#116848=ORIENTED_EDGE ( 'NONE', *, *, #175392, .F. ) ;
#116856=CARTESIAN_POINT ( 'NONE',  ( -20.94999999999999929, 13.63177590472475487, -238.5351604075707144 ) ) ;
#116858=VERTEX_POINT ( 'NONE', #91862 ) ;
#116863=CARTESIAN_POINT ( 'NONE',  ( 21.05000000000000071, 10.27563683788935300, -228.0699890633274833 ) ) ;
#116895=DIRECTION ( 'NONE',  ( 0.000000000000000000, -0.8814952561688476074, 0.4721928772777262417 ) ) ;
#116912=DIRECTION ( 'NONE',  ( -1.000000000000000000, 0.000000000000000000, 0.000000000000000000 ) ) ;
#116921=VERTEX_POINT ( 'NONE', #52725 ) ;
#116935=EDGE_CURVE ( 'NONE', #148681, #156004, #122449, .T. ) ;
#116943=CARTESIAN_POINT ( 'NONE',  ( -18.59999999999999787, 18.72524884453914851, -226.7284036107340341 ) ) ;
#116956=CARTESIAN_POINT ( 'NONE',  ( -20.64999999999999858, 29.23678660621682113, -237.4641088729839282 ) ) ;
#116957=CARTESIAN_POINT ( 'NONE',  ( -21.65000000000000213, 29.41239393758413811, -236.9245051605820720 ) ) ;
#116980=CARTESIAN_POINT ( 'NONE',  ( 20.94999999999999574, 16.44800918141279311, -240.8068063186265135 ) ) ;
#116994=AXIS2_PLACEMENT_3D ( 'NONE', #175089, #250716, #254541 ) ;
#117017=ORIENTED_EDGE ( 'NONE', *, *, #174907, .T. ) ;
#117049=CARTESIAN_POINT ( 'NONE',  ( 21.05000000000000071, 18.65488991999773916, -228.0822300706204544 ) ) ;
#117051=DIRECTION ( 'NONE',  ( -4.701977403289177357E-30, 0.8814952561688512711, -0.4721928772777193584 ) ) ;
#117068=CIRCLE ( 'NONE', #150409, 0.2000000000000027867 ) ;
#117080=CIRCLE ( 'NONE', #104574, 0.1000000000000013933 ) ;
#117081=VERTEX_POINT ( 'NONE', #26147 ) ;
#117093=DIRECTION ( 'NONE',  ( 1.000000000000000000, 0.000000000000000000, 0.000000000000000000 ) ) ;
#117106=EDGE_CURVE ( 'NONE', #256102, #19594, #124807, .T. ) ;
#117116=DIRECTION ( 'NONE',  ( 1.000000000000000000, 8.674042436075353235E-17, 1.619280515896125144E-16 ) ) ;
#117129=CARTESIAN_POINT ( 'NONE',  ( 19.97071067811864609, 34.39212750349580006, -235.0405048756463486 ) ) ;
#117153=EDGE_CURVE ( 'NONE', #46953, #109034, #72562, .T. ) ;
#117168=DIRECTION ( 'NONE',  ( -1.000000000000000000, 0.000000000000000000, 0.000000000000000000 ) ) ;
#117197=CARTESIAN_POINT ( 'NONE',  ( -18.50000000000000000, 2.319530388122570841, -217.8268657444419887 ) ) ;
#117211=DIRECTION ( 'NONE',  ( 1.000000000000000000, 0.000000000000000000, 0.000000000000000000 ) ) ;
#117242=VERTEX_POINT ( 'NONE', #9141 ) ;
#117269=ORIENTED_EDGE ( 'NONE', *, *, #67586, .F. ) ;
#117316=CARTESIAN_POINT ( 'NONE',  ( 23.24999999999999645, 20.42498087366621817, -235.1829032864613396 ) ) ;
#117355=DIRECTION ( 'NONE',  ( -1.000000000000000000, 0.000000000000000000, 0.000000000000000000 ) ) ;
#117364=DIRECTION ( 'NONE',  ( -1.000000000000000000, 0.000000000000000000, 0.000000000000000000 ) ) ;
#117386=CYLINDRICAL_SURFACE ( 'NONE', #126809, 0.09999999999999939493 ) ;
#117402=CARTESIAN_POINT ( 'NONE',  ( 18.59999999999999076, 46.01276039807270024, -256.6622985126337539 ) ) ;
#117421=DIRECTION ( 'NONE',  ( 0.000000000000000000, 0.8814952561688437216, -0.4721928772777334582 ) ) ;
#117443=CYLINDRICAL_SURFACE ( 'NONE', #80868, 0.09999999999999438505 ) ;
#117481=EDGE_CURVE ( 'NONE', #129778, #170331, #206008, .T. ) ;
#117487=VECTOR ( 'NONE', #33997, 1000.000000000000000 ) ;
#117497=EDGE_LOOP ( 'NONE', ( #23901, #105523, #105436, #137608 ) ) ;
#117541=DIRECTION ( 'NONE',  ( 0.000000000000000000, -0.8454177738465953329, -0.5341055959866617409 ) ) ;
#117548=CARTESIAN_POINT ( 'NONE',  ( 22.39999999999999503, 12.76524917372336887, -223.4223513401831269 ) ) ;
#117559=CARTESIAN_POINT ( 'NONE',  ( 18.59999999999998721, 43.27008861172207332, -245.2265230569236110 ) ) ;
#117580=CIRCLE ( 'NONE', #79941, 0.09999999999999438505 ) ;
#117652=VERTEX_POINT ( 'NONE', #235558 ) ;
#117700=DIRECTION ( 'NONE',  ( 0.000000000000000000, 0.8814952561688476074, -0.4721928772777262417 ) ) ;
#117717=DIRECTION ( 'NONE',  ( 1.000000000000000000, 0.000000000000000000, 0.000000000000000000 ) ) ;
#117755=TOROIDAL_SURFACE ( 'NONE', #176053, 0.2000000000000000111, 0.1000000000000000056 ) ;
#117784=ORIENTED_EDGE ( 'NONE', *, *, #214845, .F. ) ;
#117787=ORIENTED_EDGE ( 'NONE', *, *, #24545, .T. ) ;
#117811=DIRECTION ( 'NONE',  ( 0.000000000000000000, -0.8096735173027139743, 0.5868805631290339164 ) ) ;
#117816=CARTESIAN_POINT ( 'NONE',  ( -18.49999999999999289, 38.22547802645942028, -261.0781739499484502 ) ) ;
#117825=CIRCLE ( 'NONE', #17864, 0.1000000000000013933 ) ;
#117845=ADVANCED_FACE ( 'NONE', ( #182021 ), #199014, .F. ) ;
#117890=CARTESIAN_POINT ( 'NONE',  ( 18.39999999999999858, 8.841736820195473356, -245.4273993276876240 ) ) ;
#117919=CARTESIAN_POINT ( 'NONE',  ( 20.94999999999999929, 24.07562609839690637, -252.7152152143214892 ) ) ;
#117927=EDGE_CURVE ( 'NONE', #229988, #202898, #208000, .T. ) ;
#117936=FACE_OUTER_BOUND ( 'NONE', #232038, .T. ) ;
#117942=ADVANCED_FACE ( 'NONE', ( #158212 ), #1641, .F. ) ;
#117949=DIRECTION ( 'NONE',  ( 0.000000000000000000, -0.4721928772777343464, -0.8814952561688431665 ) ) ;
#117953=DIRECTION ( 'NONE',  ( -1.000000000000000000, 0.000000000000000000, 0.000000000000000000 ) ) ;
#118066=EDGE_CURVE ( 'NONE', #231868, #48459, #220468, .T. ) ;
#118070=AXIS2_PLACEMENT_3D ( 'NONE', #235277, #60486, #98302 ) ;
#118087=DIRECTION ( 'NONE',  ( 0.000000000000000000, 0.9424537609900487389, 0.3343365196859479638 ) ) ;
#118090=CARTESIAN_POINT ( 'NONE',  ( 23.14999999999999858, 36.65892442174935439, -249.5511627012433848 ) ) ;
#118093=ORIENTED_EDGE ( 'NONE', *, *, #23202, .F. ) ;
#118099=EDGE_CURVE ( 'NONE', #206320, #87394, #112152, .T. ) ;
#118116=LINE ( 'NONE', #73892, #120267 ) ;
#118130=CARTESIAN_POINT ( 'NONE',  ( 23.15000000000000213, 23.40438595358394736, -253.3416554127419431 ) ) ;
#118162=CARTESIAN_POINT ( 'NONE',  ( -18.50000000000000000, 1.091828907200461884, -220.1187534104809913 ) ) ;
#118178=ORIENTED_EDGE ( 'NONE', *, *, #219735, .F. ) ;
#118194=EDGE_CURVE ( 'NONE', #123343, #35945, #128888, .T. ) ;
#118204=VERTEX_POINT ( 'NONE', #113385 ) ;
#118212=CARTESIAN_POINT ( 'NONE',  ( -21.05000000000000071, 7.128833340093095217, -233.7327013124392749 ) ) ;
#118222=LINE ( 'NONE', #218580, #96996 ) ;
#118227=DIRECTION ( 'NONE',  ( 1.000000000000000000, 0.000000000000000000, 0.000000000000000000 ) ) ;
#118277=ORIENTED_EDGE ( 'NONE', *, *, #16924, .T. ) ;
#118292=CARTESIAN_POINT ( 'NONE',  ( 20.12499999999999645, 18.87266177492467278, -229.5208838261441713 ) ) ;
#118301=CIRCLE ( 'NONE', #172511, 11.90000000000000036 ) ;
#118340=CARTESIAN_POINT ( 'NONE',  ( 21.05000000000000071, 18.75112661735452591, -228.0439950614670011 ) ) ;
#118357=ADVANCED_FACE ( 'NONE', ( #257974 ), #158955, .T. ) ;
#118377=FACE_OUTER_BOUND ( 'NONE', #219879, .T. ) ;
#118384=ORIENTED_EDGE ( 'NONE', *, *, #130032, .T. ) ;
#118387=CARTESIAN_POINT ( 'NONE',  ( 21.05000000000000071, 36.65892442174935439, -249.5511627012433848 ) ) ;
#118406=AXIS2_PLACEMENT_3D ( 'NONE', #109444, #246411, #50742 ) ;
#118428=ORIENTED_EDGE ( 'NONE', *, *, #16237, .F. ) ;
#118459=DIRECTION ( 'NONE',  ( -0.000000000000000000, -0.8096735173027155286, 0.5868805631290315850 ) ) ;
#118493=CARTESIAN_POINT ( 'NONE',  ( -22.50000000000000000, 7.128833340093095217, -233.7327013124392749 ) ) ;
#118546=AXIS2_PLACEMENT_3D ( 'NONE', #145752, #204442, #207032 ) ;
#118548=AXIS2_PLACEMENT_3D ( 'NONE', #164535, #121583, #120304 ) ;
#118555=DIRECTION ( 'NONE',  ( 0.000000000000000000, 0.8814952561688438326, -0.4721928772777334582 ) ) ;
#118564=AXIS2_PLACEMENT_3D ( 'NONE', #199681, #60128, #203513 ) ;
#118690=CARTESIAN_POINT ( 'NONE',  ( -18.39999999999999858, 37.94390843806124280, -261.1300795796834109 ) ) ;
#118697=DIRECTION ( 'NONE',  ( 1.000000000000000000, 0.000000000000000000, 0.000000000000000000 ) ) ;
#118709=AXIS2_PLACEMENT_3D ( 'NONE', #256553, #254033, #195383 ) ;
#118710=VERTEX_POINT ( 'NONE', #244227 ) ;
#118730=VERTEX_POINT ( 'NONE', #82565 ) ;
#118745=ORIENTED_EDGE ( 'NONE', *, *, #88581, .F. ) ;
#118780=ORIENTED_EDGE ( 'NONE', *, *, #57794, .F. ) ;
#118847=ORIENTED_EDGE ( 'NONE', *, *, #3142, .F. ) ;
#118881=EDGE_CURVE ( 'NONE', #253481, #255363, #249856, .T. ) ;
#118884=CIRCLE ( 'NONE', #81409, 0.3999999999999994671 ) ;
#118918=EDGE_CURVE ( 'NONE', #136073, #26265, #241663, .T. ) ;
#118970=LINE ( 'NONE', #21173, #9489 ) ;
#119003=CARTESIAN_POINT ( 'NONE',  ( 22.48660254037844197, 12.58580559757026940, -223.4396719342083486 ) ) ;
#119023=PLANE ( 'NONE',  #5167 ) ;
#119052=FACE_OUTER_BOUND ( 'NONE', #197957, .T. ) ;
#119065=ORIENTED_EDGE ( 'NONE', *, *, #187704, .T. ) ;
#119090=ORIENTED_EDGE ( 'NONE', *, *, #201323, .F. ) ;
#119098=ORIENTED_EDGE ( 'NONE', *, *, #58668, .F. ) ;
#119103=DIRECTION ( 'NONE',  ( 1.000000000000000000, 0.000000000000000000, 0.000000000000000000 ) ) ;
#119116=CARTESIAN_POINT ( 'NONE',  ( -18.31572283045081306, 38.18901410207342906, -261.2028819903177919 ) ) ;
#119193=CARTESIAN_POINT ( 'NONE',  ( 19.99999999999998934, 31.36165455396662693, -233.4973802202241302 ) ) ;
#119202=EDGE_LOOP ( 'NONE', ( #54387, #159612, #168151, #105718 ) ) ;
#119257=DIRECTION ( 'NONE',  ( -1.000000000000000000, 0.000000000000000000, 0.000000000000000000 ) ) ;
#119305=CARTESIAN_POINT ( 'NONE',  ( -20.85000000000000142, 45.93315328338058379, -256.6017782078560003 ) ) ;
#119311=VECTOR ( 'NONE', #112513, 1000.000000000000000 ) ;
#119321=VECTOR ( 'NONE', #119460, 1000.000000000000000 ) ;
#119325=CARTESIAN_POINT ( 'NONE',  ( -21.05000000000000071, 1.627786319807483340, -244.0021210468063089 ) ) ;
#119326=VERTEX_POINT ( 'NONE', #233401 ) ;
#119327=DIRECTION ( 'NONE',  ( 1.000000000000000000, -7.166229603267617241E-16, -4.447280054184918885E-16 ) ) ;
#119346=CARTESIAN_POINT ( 'NONE',  ( -21.55000000000000426, 21.65523568329831505, -232.7692078405380300 ) ) ;
#119352=CARTESIAN_POINT ( 'NONE',  ( 18.59999999999997655, 36.65892442174935439, -249.5511627012433848 ) ) ;
#119369=DIRECTION ( 'NONE',  ( 0.000000000000000000, 0.4721928772777346239, 0.8814952561688430555 ) ) ;
#119398=DIRECTION ( 'NONE',  ( 0.000000000000000000, -0.5273008465188219196, 0.8496786552930077896 ) ) ;
#119399=ORIENTED_EDGE ( 'NONE', *, *, #144929, .F. ) ;
#119419=CARTESIAN_POINT ( 'NONE',  ( 22.47071067811865319, 0.3704148268517115650, -229.9999874772931037 ) ) ;
#119425=DIRECTION ( 'NONE',  ( 0.000000000000000000, 0.4721928772778128947, 0.8814952561688012000 ) ) ;
#119434=CARTESIAN_POINT ( 'NONE',  ( -18.45037301276669695, 8.829267269132847318, -245.4096027649236191 ) ) ;
#119453=EDGE_CURVE ( 'NONE', #88893, #72605, #129609, .T. ) ;
#119460=DIRECTION ( 'NONE',  ( -0.000000000000000000, -0.8814952561688430555, 0.4721928772777346239 ) ) ;
#119467=CARTESIAN_POINT ( 'NONE',  ( 22.49999999999998579, -3.180729737797959977, -228.0957332317255180 ) ) ;
#119482=ORIENTED_EDGE ( 'NONE', *, *, #59382, .T. ) ;
#119513=DIRECTION ( 'NONE',  ( -0.000000000000000000, 0.4721928772777346239, 0.8814952561688430555 ) ) ;
#119580=ADVANCED_FACE ( 'NONE', ( #46711 ), #162948, .T. ) ;
#119587=CARTESIAN_POINT ( 'NONE',  ( 20.46382478191414833, 18.86502014180634745, -229.9214093956406373 ) ) ;
#119597=FACE_OUTER_BOUND ( 'NONE', #175672, .T. ) ;
#119649=CARTESIAN_POINT ( 'NONE',  ( 21.05000000000000071, 13.60254931771583387, -238.7443143987590304 ) ) ;
#119659=DIRECTION ( 'NONE',  ( 0.000000000000000000, 0.8814952561688429444, -0.4721928772777349015 ) ) ;
#119700=CARTESIAN_POINT ( 'NONE',  ( 23.24999999999999289, 28.91254064196106910, -237.8576372133405528 ) ) ;
#119701=CIRCLE ( 'NONE', #90632, 11.70000000000001172 ) ;
#119706=EDGE_CURVE ( 'NONE', #137538, #26118, #242021, .T. ) ;
#119747=VECTOR ( 'NONE', #117949, 1000.000000000000000 ) ;
#119871=DIRECTION ( 'NONE',  ( 0.000000000000000000, -0.4721928772777346239, -0.8814952561688430555 ) ) ;
#119876=AXIS2_PLACEMENT_3D ( 'NONE', #254485, #238814, #237533 ) ;
#119900=CIRCLE ( 'NONE', #11551, 0.09999999999998797351 ) ;
#119902=AXIS2_PLACEMENT_3D ( 'NONE', #144165, #165034, #127199 ) ;
#119938=DIRECTION ( 'NONE',  ( 1.000000000000000000, 0.000000000000000000, 0.000000000000000000 ) ) ;
#119943=VERTEX_POINT ( 'NONE', #223751 ) ;
#119961=CARTESIAN_POINT ( 'NONE',  ( -20.54999999999999716, 23.45160524131172508, -253.2535058871250726 ) ) ;
#119962=FACE_OUTER_BOUND ( 'NONE', #252292, .T. ) ;
#119975=FACE_OUTER_BOUND ( 'NONE', #132992, .T. ) ;
#120035=AXIS2_PLACEMENT_3D ( 'NONE', #86507, #248190, #163514 ) ;
#120077=ORIENTED_EDGE ( 'NONE', *, *, #108358, .T. ) ;
#120119=EDGE_CURVE ( 'NONE', #17892, #9372, #1509, .T. ) ;
#120155=VERTEX_POINT ( 'NONE', #224411 ) ;
#120177=AXIS2_PLACEMENT_3D ( 'NONE', #118493, #41528, #178477 ) ;
#120217=AXIS2_PLACEMENT_3D ( 'NONE', #22738, #205186, #142641 ) ;
#120232=ORIENTED_EDGE ( 'NONE', *, *, #97952, .F. ) ;
#120237=CARTESIAN_POINT ( 'NONE',  ( -23.25000000000000000, 7.128833340093095217, -233.7327013124392749 ) ) ;
#120240=FACE_OUTER_BOUND ( 'NONE', #158518, .T. ) ;
#120252=STYLED_ITEM ( 'NONE', ( #33303 ), #107142 ) ;
#120257=CIRCLE ( 'NONE', #57653, 0.2000000000000058675 ) ;
#120267=VECTOR ( 'NONE', #153445, 999.9999999999998863 ) ;
#120297=EDGE_CURVE ( 'NONE', #101453, #159861, #25733, .T. ) ;
#120298=DIRECTION ( 'NONE',  ( 0.000000000000000000, -0.8096735173027155286, 0.5868805631290315850 ) ) ;
#120304=DIRECTION ( 'NONE',  ( 0.000000000000000000, 0.8814952561688446098, -0.4721928772777316263 ) ) ;
#120311=EDGE_CURVE ( 'NONE', #121060, #177802, #167051, .T. ) ;
#120317=CARTESIAN_POINT ( 'NONE',  ( 22.49231231312462853, 12.57605540120662191, -223.4344661467465016 ) ) ;
#120340=DIRECTION ( 'NONE',  ( 0.000000000000000000, 0.8814952561688476074, -0.4721928772777262417 ) ) ;
#120367=AXIS2_PLACEMENT_3D ( 'NONE', #21538, #643, #158496 ) ;
#120378=ORIENTED_EDGE ( 'NONE', *, *, #231421, .T. ) ;
#120394=VERTEX_POINT ( 'NONE', #113458 ) ;
#120419=FACE_OUTER_BOUND ( 'NONE', #125887, .T. ) ;
#120424=CARTESIAN_POINT ( 'NONE',  ( -20.64999999999999858, 25.94586868676353575, -241.5435999122864530 ) ) ;
#120451=CIRCLE ( 'NONE', #228761, 0.1000000000000084294 ) ;
#120458=CARTESIAN_POINT ( 'NONE',  ( 21.14999999999999858, 1.363275264940682741, -230.6442496871288483 ) ) ;
#120500=DIRECTION ( 'NONE',  ( 0.000000000000000000, -0.8814952561688476074, 0.4721928772777262417 ) ) ;
#120507=CARTESIAN_POINT ( 'NONE',  ( 21.08078803292165659, 10.04943488157321774, -228.1127893679160650 ) ) ;
#120515=ORIENTED_EDGE ( 'NONE', *, *, #79637, .T. ) ;
#120529=DIRECTION ( 'NONE',  ( 0.000000000000000000, 0.8814952561688476074, -0.4721928772777262417 ) ) ;
#120558=DIRECTION ( 'NONE',  ( 0.000000000000000000, 0.8814952561688418342, -0.4721928772777368444 ) ) ;
#120571=CARTESIAN_POINT ( 'NONE',  ( -23.25000000000000000, 28.42524210734032053, -258.3567845160494585 ) ) ;
#120634=AXIS2_PLACEMENT_3D ( 'NONE', #20532, #100011, #179605 ) ;
#120641=AXIS2_PLACEMENT_3D ( 'NONE', #94785, #137747, #59473 ) ;
#120659=ORIENTED_EDGE ( 'NONE', *, *, #255995, .T. ) ;
#120677=EDGE_CURVE ( 'NONE', #188830, #111286, #50595, .T. ) ;
#120702=CARTESIAN_POINT ( 'NONE',  ( 20.94999999999999929, 38.43293829866423295, -234.5626268121764895 ) ) ;
#120716=LINE ( 'NONE', #43721, #161090 ) ;
#120764=CARTESIAN_POINT ( 'NONE',  ( 21.14999999999999503, 4.136903274969363942, -245.4596299165286268 ) ) ;
#120765=DIRECTION ( 'NONE',  ( -1.000000000000000000, 0.000000000000000000, 0.000000000000000000 ) ) ;
#120767=FACE_OUTER_BOUND ( 'NONE', #84807, .T. ) ;
#120773=ORIENTED_EDGE ( 'NONE', *, *, #91834, .T. ) ;
#120804=CARTESIAN_POINT ( 'NONE',  ( 20.85000000000000142, 36.65892442174935439, -249.5511627012433848 ) ) ;
#120812=ORIENTED_EDGE ( 'NONE', *, *, #58053, .F. ) ;
#120813=DIRECTION ( 'NONE',  ( 1.000000000000000000, 0.000000000000000000, 0.000000000000000000 ) ) ;
#120825=CARTESIAN_POINT ( 'NONE',  ( 18.39999999999999858, 37.94390843806124991, -261.1300795796834109 ) ) ;
#120856=DIRECTION ( 'NONE',  ( -0.7071067811865473507, -0.3338907855510733769, -0.6233112732207618523 ) ) ;
#120885=LINE ( 'NONE', #99972, #225734 ) ;
#120887=AXIS2_PLACEMENT_3D ( 'NONE', #9593, #147848, #65726 ) ;
#120897=EDGE_CURVE ( 'NONE', #236113, #44305, #46755, .T. ) ;
#120914=ORIENTED_EDGE ( 'NONE', *, *, #194663, .T. ) ;
#120927=VECTOR ( 'NONE', #84301, 1000.000000000000000 ) ;
#120964=CARTESIAN_POINT ( 'NONE',  ( 21.07094088545369104, 1.604332817732096572, -230.6611890373810638 ) ) ;
#120975=LINE ( 'NONE', #19279, #208132 ) ;
#120986=ORIENTED_EDGE ( 'NONE', *, *, #71494, .T. ) ;
#120987=ORIENTED_EDGE ( 'NONE', *, *, #194627, .T. ) ;
#121000=DIRECTION ( 'NONE',  ( 0.000000000000000000, 0.8814952561688428334, -0.4721928772777349570 ) ) ;
#121006=AXIS2_PLACEMENT_3D ( 'NONE', #32449, #231916, #132813 ) ;
#121046=EDGE_CURVE ( 'NONE', #250592, #31642, #192706, .T. ) ;
#121055=DIRECTION ( 'NONE',  ( 0.000000000000000000, 0.8814952561688428334, -0.4721928772777350125 ) ) ;
#121060=VERTEX_POINT ( 'NONE', #167716 ) ;
#121074=CARTESIAN_POINT ( 'NONE',  ( 20.91682497891422798, 46.43483777265581836, -243.0774829958280918 ) ) ;
#121125=AXIS2_PLACEMENT_3D ( 'NONE', #250755, #72144, #151700 ) ;
#121132=CARTESIAN_POINT ( 'NONE',  ( 20.94999999999999929, 36.65892442174935439, -249.5511627012433848 ) ) ;
#121187=DIRECTION ( 'NONE',  ( 0.000000000000000000, -0.8127272543710951647, 0.5826443254700256480 ) ) ;
#121199=TOROIDAL_SURFACE ( 'NONE', #21242, 11.90000000000000213, 0.1000000000000000056 ) ;
#121220=ORIENTED_EDGE ( 'NONE', *, *, #161177, .T. ) ;
#121224=EDGE_CURVE ( 'NONE', #75284, #15820, #238484, .T. ) ;
#121267=DIRECTION ( 'NONE',  ( 0.000000000000000000, 0.4721928772776973204, 0.8814952561688629284 ) ) ;
#121282=DIRECTION ( 'NONE',  ( 1.000000000000000000, -0.000000000000000000, -0.000000000000000000 ) ) ;
#121305=CARTESIAN_POINT ( 'NONE',  ( 18.49505816908825651, 38.17690089667952691, -261.0709640404842844 ) ) ;
#121307=CARTESIAN_POINT ( 'NONE',  ( -18.50211644919735932, 46.36250628750309488, -243.0620573837409779 ) ) ;
#121333=ORIENTED_EDGE ( 'NONE', *, *, #97114, .F. ) ;
#121353=VERTEX_POINT ( 'NONE', #168722 ) ;
#121354=CIRCLE ( 'NONE', #150362, 12.87500000000000178 ) ;
#121364=ORIENTED_EDGE ( 'NONE', *, *, #232577, .F. ) ;
#121401=CYLINDRICAL_SURFACE ( 'NONE', #161753, 11.80000000000000604 ) ;
#121405=ORIENTED_EDGE ( 'NONE', *, *, #5801, .F. ) ;
#121499=FILL_AREA_STYLE ('',( #41953 ) ) ;
#121552=DIRECTION ( 'NONE',  ( 0.000000000000000000, -0.9994937237965558774, -0.03181660087586650476 ) ) ;
#121561=AXIS2_PLACEMENT_3D ( 'NONE', #170619, #233131, #212272 ) ;
#121583=DIRECTION ( 'NONE',  ( -1.000000000000000000, -0.000000000000000000, -0.000000000000000000 ) ) ;
#121598=ORIENTED_EDGE ( 'NONE', *, *, #174907, .F. ) ;
#121618=EDGE_CURVE ( 'NONE', #89573, #58384, #109659, .T. ) ;
#121628=DIRECTION ( 'NONE',  ( -1.000000000000000000, -0.000000000000000000, -0.000000000000000000 ) ) ;
#121652=VECTOR ( 'NONE', #69591, 1000.000000000000000 ) ;
#121681=AXIS2_PLACEMENT_3D ( 'NONE', #77127, #174998, #75848 ) ;
#121682=ORIENTED_EDGE ( 'NONE', *, *, #102335, .T. ) ;
#121702=ORIENTED_EDGE ( 'NONE', *, *, #221293, .T. ) ;
#121707=DIRECTION ( 'NONE',  ( 0.000000000000000000, -0.8814952561688449428, 0.4721928772777310157 ) ) ;
#121713=DIRECTION ( 'NONE',  ( 0.000000000000000000, 0.8814952561688476074, -0.4721928772777262417 ) ) ;
#121730=EDGE_CURVE ( 'NONE', #19594, #229988, #175469, .T. ) ;
#121743=ORIENTED_EDGE ( 'NONE', *, *, #244793, .F. ) ;
#121765=ORIENTED_EDGE ( 'NONE', *, *, #107818, .F. ) ;
#121770=DIRECTION ( 'NONE',  ( 0.000000000000000000, 0.8814952561688438326, -0.4721928772777331806 ) ) ;
#121788=EDGE_LOOP ( 'NONE', ( #247317, #89517, #143510, #112374 ) ) ;
#121797=DIRECTION ( 'NONE',  ( 1.000000000000000000, 0.000000000000000000, 0.000000000000000000 ) ) ;
#121801=CARTESIAN_POINT ( 'NONE',  ( 21.05000000000000071, 7.128833340093095217, -233.7327013124392749 ) ) ;
#121830=DIRECTION ( 'NONE',  ( -0.000000000000000000, 0.4721928772777345684, 0.8814952561688429444 ) ) ;
#121831=LINE ( 'NONE', #201348, #254916 ) ;
#121896=DIRECTION ( 'NONE',  ( 1.000000000000000000, 0.000000000000000000, 0.000000000000000000 ) ) ;
#121958=CARTESIAN_POINT ( 'NONE',  ( 18.59999999999999076, 43.00579525902548994, -254.2551217332645876 ) ) ;
#121974=AXIS2_PLACEMENT_3D ( 'NONE', #3700, #160246, #221444 ) ;
#121993=VERTEX_POINT ( 'NONE', #73510 ) ;
#122005=ORIENTED_EDGE ( 'NONE', *, *, #101289, .F. ) ;
#122026=AXIS2_PLACEMENT_3D ( 'NONE', #49864, #228524, #129408 ) ;
#122041=EDGE_LOOP ( 'NONE', ( #238105, #172228, #135519, #81135 ) ) ;
#122068=CARTESIAN_POINT ( 'NONE',  ( -23.15000000000000213, 36.65892442174935439, -249.5511627012433848 ) ) ;
#122111=LINE ( 'NONE', #142923, #8747 ) ;
#122149=CARTESIAN_POINT ( 'NONE',  ( -21.05000000000000071, 36.65892442174935439, -249.5511627012433848 ) ) ;
#122158=ORIENTED_EDGE ( 'NONE', *, *, #102918, .T. ) ;
#122174=CARTESIAN_POINT ( 'NONE',  ( -21.14999999999999858, 1.580567032079710055, -244.0902705724231794 ) ) ;
#122183=CARTESIAN_POINT ( 'NONE',  ( -21.07928932188134041, 10.02993822722537942, -228.1074463178628662 ) ) ;
#122196=FACE_OUTER_BOUND ( 'NONE', #124452, .T. ) ;
#122221=DIRECTION ( 'NONE',  ( 0.000000000000000000, 0.8814952561688449428, -0.4721928772777310157 ) ) ;
#122285=CARTESIAN_POINT ( 'NONE',  ( -22.43310005002225438, -3.137626837017164938, -228.2268448955577469 ) ) ;
#122298=CARTESIAN_POINT ( 'NONE',  ( 20.99749315643148151, 36.02367272165624712, -235.8812521217649305 ) ) ;
#122391=CARTESIAN_POINT ( 'NONE',  ( -21.51976009735018991, 10.39190259496836610, -227.6411649781647384 ) ) ;
#122442=LINE ( 'NONE', #24651, #79307 ) ;
#122449=CIRCLE ( 'NONE', #80901, 0.1999999999999997335 ) ;
#122464=CARTESIAN_POINT ( 'NONE',  ( 19.75857864376268935, 34.44688795055758135, -235.1500552906961730 ) ) ;
#122468=EDGE_CURVE ( 'NONE', #116858, #5127, #40, .T. ) ;
#122478=EDGE_CURVE ( 'NONE', #45529, #101453, #6460, .T. ) ;
#122490=EDGE_CURVE ( 'NONE', #76904, #250592, #47473, .T. ) ;
#122505=LINE ( 'NONE', #51576, #161017 ) ;
#122535=ORIENTED_EDGE ( 'NONE', *, *, #17216, .F. ) ;
#122555=FACE_OUTER_BOUND ( 'NONE', #2929, .T. ) ;
#122569=CARTESIAN_POINT ( 'NONE',  ( -18.58222699835055280, 46.46797214202639736, -243.0846070113367716 ) ) ;
#122587=DIRECTION ( 'NONE',  ( 1.000000000000000000, 0.000000000000000000, 0.000000000000000000 ) ) ;
#122639=DIRECTION ( 'NONE',  ( 1.000000000000000000, 0.000000000000000000, 0.000000000000000000 ) ) ;
#122686=ORIENTED_EDGE ( 'NONE', *, *, #51019, .T. ) ;
#122712=ORIENTED_EDGE ( 'NONE', *, *, #86220, .F. ) ;
#122729=ORIENTED_EDGE ( 'NONE', *, *, #209158, .F. ) ;
#122789=DIRECTION ( 'NONE',  ( 0.000000000000000000, -0.8814952561688425003, 0.4721928772777359007 ) ) ;
#122889=ADVANCED_FACE ( 'NONE', ( #257858 ), #110204, .F. ) ;
#122908=DIRECTION ( 'NONE',  ( 1.000000000000000000, 0.000000000000000000, 0.000000000000000000 ) ) ;
#122909=LINE ( 'NONE', #82452, #109032 ) ;
#122915=ORIENTED_EDGE ( 'NONE', *, *, #216461, .T. ) ;
#122928=CARTESIAN_POINT ( 'NONE',  ( 21.05000000000000071, 18.71171618620643429, -229.8673829423568691 ) ) ;
#122934=VERTEX_POINT ( 'NONE', #227440 ) ;
#122940=EDGE_LOOP ( 'NONE', ( #251800, #156499, #244288, #61101 ) ) ;
#122943=AXIS2_PLACEMENT_3D ( 'NONE', #206271, #44634, #62905 ) ;
#122962=DIRECTION ( 'NONE',  ( 1.000000000000000000, 0.000000000000000000, 0.000000000000000000 ) ) ;
#122966=EDGE_CURVE ( 'NONE', #109224, #97478, #126401, .T. ) ;
#122983=FACE_OUTER_BOUND ( 'NONE', #166563, .T. ) ;
#122989=CARTESIAN_POINT ( 'NONE',  ( -18.59999999999999787, 23.34004772283014972, -229.2004250369967338 ) ) ;
#123001=DIRECTION ( 'NONE',  ( 0.000000000000000000, 0.8814952561688439436, -0.4721928772777330696 ) ) ;
#123036=DIRECTION ( 'NONE',  ( -1.000000000000000000, 0.000000000000000000, 0.000000000000000000 ) ) ;
#123043=EDGE_CURVE ( 'NONE', #29239, #197260, #151792, .T. ) ;
#123093=VERTEX_POINT ( 'NONE', #12278 ) ;
#123120=LINE ( 'NONE', #162258, #34720 ) ;
#123131=FACE_OUTER_BOUND ( 'NONE', #77377, .T. ) ;
#123144=CARTESIAN_POINT ( 'NONE',  ( 23.14999999999999858, 35.97645343225767789, -235.9694016464868298 ) ) ;
#123170=LINE ( 'NONE', #188273, #144197 ) ;
#123203=VERTEX_POINT ( 'NONE', #219419 ) ;
#123218=DIRECTION ( 'NONE',  ( 1.000000000000000000, 0.000000000000000000, 0.000000000000000000 ) ) ;
#123221=EDGE_CURVE ( 'NONE', #5211, #19570, #101404, .T. ) ;
#123269=EDGE_CURVE ( 'NONE', #191683, #53873, #141193, .T. ) ;
#123271=( BOUNDED_SURFACE ( )  B_SPLINE_SURFACE ( 3, 2, ( 
 ( #225827, #45939, #4227 ),
 ( #125481, #245439, #66791 ),
 ( #246700, #124209, #102034 ),
 ( #181614, #203733, #2945 ),
 ( #5504, #68072, #151489 ),
 ( #28992, #148908, #111050 ) ),
 .UNSPECIFIED., .F., .F., .F. ) 
 B_SPLINE_SURFACE_WITH_KNOTS ( ( 4, 2, 4 ),
 ( 3, 3 ),
 ( 4.712388980384689674, 5.497787143782137953, 6.283185307179586232 ),
 ( 0.000000000000000000, 1.000000000000000000 ),
 .UNSPECIFIED. ) 
 GEOMETRIC_REPRESENTATION_ITEM ( )  RATIONAL_B_SPLINE_SURFACE ( (
 ( 1.000000000000000000, 0.7071067811865706654, 1.000000000000000000),
 ( 1.000000000000000000, 0.7727932973487074975, 1.000000000000000000),
 ( 1.000000000000000000, 0.8282379607655521170, 1.000000000000000000),
 ( 1.000000000000000000, 0.9038128468033841401, 1.000000000000000000),
 ( 1.000000000000000000, 0.9240297172248549407, 1.000000000000000000),
 ( 1.000000000000000000, 0.9238795325112804102, 1.000000000000000000) ) ) 
 REPRESENTATION_ITEM ( '' )  SURFACE ( )  );
#123279=AXIS2_PLACEMENT_3D ( 'NONE', #58655, #221578, #182501 ) ;
#123297=DIRECTION ( 'NONE',  ( 0.000000000000000000, 0.8814952561688476074, -0.4721928772777262417 ) ) ;
#123298=VERTEX_POINT ( 'NONE', #186754 ) ;
#123299=ADVANCED_FACE ( 'NONE', ( #103326 ), #123271, .T. ) ;
#123312=ADVANCED_FACE ( 'NONE', ( #91493 ), #133188, .T. ) ;
#123331=CARTESIAN_POINT ( 'NONE',  ( 21.05000000000000071, 23.49882452903949570, -253.1653563615082305 ) ) ;
#123343=VERTEX_POINT ( 'NONE', #188031 ) ;
#123344=LINE ( 'NONE', #211552, #151379 ) ;
#123350=DIRECTION ( 'NONE',  ( 0.000000000000000000, -0.7280513885558860254, 0.6855225566105367374 ) ) ;
#123355=EDGE_CURVE ( 'NONE', #117652, #134581, #178127, .T. ) ;
#123356=CARTESIAN_POINT ( 'NONE',  ( 22.57320508075688537, 12.62988036037870643, -223.4632815780722410 ) ) ;
#123363=ORIENTED_EDGE ( 'NONE', *, *, #146667, .F. ) ;
#123365=ORIENTED_EDGE ( 'NONE', *, *, #248484, .T. ) ;
#123382=LINE ( 'NONE', #240767, #53974 ) ;
#123401=ORIENTED_EDGE ( 'NONE', *, *, #108378, .F. ) ;
#123404=FACE_OUTER_BOUND ( 'NONE', #141219, .T. ) ;
#123446=CARTESIAN_POINT ( 'NONE',  ( 20.94999999999999574, 13.60254931771583387, -238.7443143987590304 ) ) ;
#123462=DIRECTION ( 'NONE',  ( 0.000000000000000000, 0.8814952561688444987, -0.4721928772777320149 ) ) ;
#123474=ORIENTED_EDGE ( 'NONE', *, *, #235472, .T. ) ;
#123479=CARTESIAN_POINT ( 'NONE',  ( 20.95512820512820440, 30.87711321140620413, -234.4019277376435184 ) ) ;
#123484=EDGE_LOOP ( 'NONE', ( #44098, #23971, #137553, #206421 ) ) ;
#123514=EDGE_LOOP ( 'NONE', ( #20403, #65210, #213511, #206127 ) ) ;
#123524=CARTESIAN_POINT ( 'NONE',  ( 21.00000000000000000, 30.46448808713892831, -235.1722212069449256 ) ) ;
#123526=EDGE_LOOP ( 'NONE', ( #82354, #42860, #204496 ) ) ;
#123527=EDGE_LOOP ( 'NONE', ( #79441, #37933, #217193, #89390 ) ) ;
#123565=DIRECTION ( 'NONE',  ( -1.000000000000000000, 0.000000000000000000, 0.000000000000000000 ) ) ;
#123574=AXIS2_PLACEMENT_3D ( 'NONE', #95094, #195507, #19416 ) ;
#123592=ORIENTED_EDGE ( 'NONE', *, *, #130836, .F. ) ;
#123632=CARTESIAN_POINT ( 'NONE',  ( -21.05000000000000071, 38.48566838331611706, -234.6475946777057970 ) ) ;
#123660=CARTESIAN_POINT ( 'NONE',  ( -21.03571358705827166, 18.69339893459851254, -226.5978988804882874 ) ) ;
#123677=DIRECTION ( 'NONE',  ( 0.000000000000000000, -0.8814952561688476074, 0.4721928772777262417 ) ) ;
#123706=EDGE_LOOP ( 'NONE', ( #110422, #246729, #221115, #164069, #61892, #65946, #74567, #200134, #211507, #28348, #95787 ) ) ;
#123731=AXIS2_PLACEMENT_3D ( 'NONE', #17248, #172505, #173791 ) ;
#123756=ORIENTED_EDGE ( 'NONE', *, *, #185527, .T. ) ;
#123762=CYLINDRICAL_SURFACE ( 'NONE', #151470, 0.1000000000000013933 ) ;
#123770=ORIENTED_EDGE ( 'NONE', *, *, #45063, .T. ) ;
#123779=CARTESIAN_POINT ( 'NONE',  ( 22.60000000000000497, -3.206176178680899991, -228.1422727337474896 ) ) ;
#123803=LINE ( 'NONE', #61255, #109515 ) ;
#123804=ORIENTED_EDGE ( 'NONE', *, *, #167276, .T. ) ;
#123821=ADVANCED_FACE ( 'NONE', ( #189004 ), #186444, .T. ) ;
#123825=CARTESIAN_POINT ( 'NONE',  ( 23.15000000000000213, 23.45160524131172153, -253.2535058871250726 ) ) ;
#123842=CARTESIAN_POINT ( 'NONE',  ( 18.50000000000000000, 38.28679861725831302, -261.0868692510649680 ) ) ;
#123851=EDGE_LOOP ( 'NONE', ( #29345, #235083, #107386, #25592, #125398 ) ) ;
#123856=CARTESIAN_POINT ( 'NONE',  ( -20.85000000000000142, 46.02130280899747561, -256.6489974955837852 ) ) ;
#123868=AXIS2_PLACEMENT_3D ( 'NONE', #40022, #76536, #56945 ) ;
#123890=EDGE_LOOP ( 'NONE', ( #130977, #141225, #108838, #129235 ) ) ;
#123927=VERTEX_POINT ( 'NONE', #98841 ) ;
#123946=ADVANCED_FACE ( 'NONE', ( #115885 ), #135428, .T. ) ;
#123959=ORIENTED_EDGE ( 'NONE', *, *, #227212, .T. ) ;
#123962=ORIENTED_EDGE ( 'NONE', *, *, #34338, .F. ) ;
#123979=AXIS2_PLACEMENT_3D ( 'NONE', #222069, #220815, #142553 ) ;
#123981=ORIENTED_EDGE ( 'NONE', *, *, #142319, .T. ) ;
#123983=ADVANCED_FACE ( 'NONE', ( #244795 ), #213129, .T. ) ;
#124001=ORIENTED_EDGE ( 'NONE', *, *, #146406, .T. ) ;
#124019=CIRCLE ( 'NONE', #182278, 0.09999999999999742428 ) ;
#124024=CARTESIAN_POINT ( 'NONE',  ( -22.14074124539699895, 0.6612868435708807446, -230.1558445308521073 ) ) ;
#124027=DIRECTION ( 'NONE',  ( -1.000000000000000000, -0.000000000000000000, -0.000000000000000000 ) ) ;
#124035=CARTESIAN_POINT ( 'NONE',  ( 20.85000000000000142, 36.65892442174935439, -249.5511627012433848 ) ) ;
#124077=DIRECTION ( 'NONE',  ( 0.000000000000000000, -0.5954378521545836689, -0.8034013718071036925 ) ) ;
#124102=CARTESIAN_POINT ( 'NONE',  ( -23.25000000000000000, 46.02130280899747561, -256.6489974955837852 ) ) ;
#124209=CARTESIAN_POINT ( 'NONE',  ( 19.87657994472041878, 34.50802439524682086, -235.0693608050739556 ) ) ;
#124241=ORIENTED_EDGE ( 'NONE', *, *, #213724, .T. ) ;
#124245=ORIENTED_EDGE ( 'NONE', *, *, #235407, .F. ) ;
#124293=CARTESIAN_POINT ( 'NONE',  ( -23.15000000000000213, 7.128833340093095217, -233.7327013124392749 ) ) ;
#124334=VECTOR ( 'NONE', #177483, 1000.000000000000000 ) ;
#124439=EDGE_CURVE ( 'NONE', #213275, #23820, #104949, .T. ) ;
#124452=EDGE_LOOP ( 'NONE', ( #168239, #130326, #188423, #128175 ) ) ;
#124470=DIRECTION ( 'NONE',  ( 0.000000000000000000, 0.8814952561688430555, -0.4721928772777346239 ) ) ;
#124483=VERTEX_POINT ( 'NONE', #85385 ) ;
#124493=DIRECTION ( 'NONE',  ( -1.000000000000000000, 0.000000000000000000, 0.000000000000000000 ) ) ;
#124501=AXIS2_PLACEMENT_3D ( 'NONE', #222697, #223989, #45363 ) ;
#124524=ORIENTED_EDGE ( 'NONE', *, *, #168457, .T. ) ;
#124548=CARTESIAN_POINT ( 'NONE',  ( 21.05000000000000071, 7.128833340093095217, -233.7327013124392749 ) ) ;
#124554=EDGE_CURVE ( 'NONE', #160790, #12413, #149277, .T. ) ;
#124571=EDGE_CURVE ( 'NONE', #32586, #105344, #188377, .T. ) ;
#124580=CARTESIAN_POINT ( 'NONE',  ( -20.64999999999999858, 19.73066058418984170, -238.2142830767208466 ) ) ;
#124599=DIRECTION ( 'NONE',  ( 0.000000000000000000, 0.8814952561688429444, -0.4721928772777349570 ) ) ;
#124616=DIRECTION ( 'NONE',  ( 0.000000000000000000, 0.8814952561688430555, -0.4721928772777346239 ) ) ;
#124651=AXIS2_PLACEMENT_3D ( 'NONE', #209560, #127455, #189998 ) ;
#124708=FACE_OUTER_BOUND ( 'NONE', #111727, .T. ) ;
#124710=CARTESIAN_POINT ( 'NONE',  ( 20.94999999999999929, 18.56623428888383387, -239.8594038951179073 ) ) ;
#124712=CARTESIAN_POINT ( 'NONE',  ( -23.15000000000000213, 23.68770167995059595, -252.8127582590406348 ) ) ;
#124736=SPHERICAL_SURFACE ( 'NONE', #1063, 0.1000000000000000056 ) ;
#124756=CARTESIAN_POINT ( 'NONE',  ( -20.64999999999999858, 23.45160524131172508, -253.2535058871250726 ) ) ;
#124764=CIRCLE ( 'NONE', #191436, 0.09999999999998906985 ) ;
#124779=FACE_OUTER_BOUND ( 'NONE', #141227, .T. ) ;
#124786=LINE ( 'NONE', #66083, #133551 ) ;
#124803=ORIENTED_EDGE ( 'NONE', *, *, #34677, .T. ) ;
#124807=( BOUNDED_CURVE ( )  B_SPLINE_CURVE ( 3, ( #126519, #211187, #169541, #48259 ),
 .UNSPECIFIED., .F., .T. ) 
 B_SPLINE_CURVE_WITH_KNOTS ( ( 4, 4 ),
 ( 1.570796326794908770, 3.141592653589791784 ),
 .UNSPECIFIED. ) 
 CURVE ( )  GEOMETRIC_REPRESENTATION_ITEM ( )  RATIONAL_B_SPLINE_CURVE ( ( 1.000000000000000000, 0.8047378541243681571, 0.8047378541243681571, 1.000000000000000000 ) ) 
 REPRESENTATION_ITEM ( '' )  );
#124840=ORIENTED_EDGE ( 'NONE', *, *, #27834, .F. ) ;
#124845=VERTEX_POINT ( 'NONE', #200896 ) ;
#124853=CARTESIAN_POINT ( 'NONE',  ( -20.54999999999999716, 26.18196512540240661, -241.1028522842020152 ) ) ;
#124888=AXIS2_PLACEMENT_3D ( 'NONE', #237890, #131409, #59211 ) ;
#124918=ORIENTED_EDGE ( 'NONE', *, *, #101034, .T. ) ;
#124926=FACE_OUTER_BOUND ( 'NONE', #10091, .T. ) ;
#124929=DIRECTION ( 'NONE',  ( -1.000000000000000000, -8.674042436075348305E-17, -1.619280515896124405E-16 ) ) ;
#124938=ORIENTED_EDGE ( 'NONE', *, *, #12161, .F. ) ;
#124956=ORIENTED_EDGE ( 'NONE', *, *, #104343, .T. ) ;
#124972=ORIENTED_EDGE ( 'NONE', *, *, #228667, .F. ) ;
#124973=EDGE_LOOP ( 'NONE', ( #72003, #175271, #165259, #132296 ) ) ;
#125005=CYLINDRICAL_SURFACE ( 'NONE', #240089, 0.09999999999999939493 ) ;
#125040=DIRECTION ( 'NONE',  ( 1.000000000000000000, -0.000000000000000000, -0.000000000000000000 ) ) ;
#125048=ADVANCED_FACE ( 'NONE', ( #243420 ), #204284, .T. ) ;
#125082=FACE_OUTER_BOUND ( 'NONE', #162477, .T. ) ;
#125100=CARTESIAN_POINT ( 'NONE',  ( 23.15000000000000213, 23.68770167995059239, -252.8127582590406348 ) ) ;
#125101=AXIS2_PLACEMENT_3D ( 'NONE', #6637, #238839, #28828 ) ;
#125107=EDGE_CURVE ( 'NONE', #104349, #126467, #248176, .T. ) ;
#125123=CARTESIAN_POINT ( 'NONE',  ( 21.05000000000000071, 38.43293829866423295, -234.5626268121764895 ) ) ;
#125138=CARTESIAN_POINT ( 'NONE',  ( 18.59999999999999787, 38.28679861725831302, -261.0868692510649680 ) ) ;
#125166=CARTESIAN_POINT ( 'NONE',  ( 18.59999999999999432, 13.71992543034163958, -238.5823796952984992 ) ) ;
#125237=AXIS2_PLACEMENT_3D ( 'NONE', #227288, #48650, #44810 ) ;
#125245=VERTEX_POINT ( 'NONE', #30823 ) ;
#125278=CIRCLE ( 'NONE', #233442, 4.049999999999997158 ) ;
#125289=EDGE_CURVE ( 'NONE', #103521, #131441, #177669, .T. ) ;
#125303=CARTESIAN_POINT ( 'NONE',  ( -22.47071067811865319, 0.3704148268516976872, -229.9999874772930752 ) ) ;
#125335=CARTESIAN_POINT ( 'NONE',  ( -20.94999999999999929, 16.44800918141279311, -240.8068063186265135 ) ) ;
#125336=AXIS2_PLACEMENT_3D ( 'NONE', #48140, #190233, #106820 ) ;
#125349=FACE_OUTER_BOUND ( 'NONE', #136728, .T. ) ;
#125357=ADVANCED_FACE ( 'NONE', ( #98059 ), #257120, .T. ) ;
#125373=CARTESIAN_POINT ( 'NONE',  ( -23.15000000000000213, 7.128833340093095217, -233.7327013124392749 ) ) ;
#125382=EDGE_CURVE ( 'NONE', #214701, #188486, #242730, .T. ) ;
#125393=FACE_OUTER_BOUND ( 'NONE', #36764, .T. ) ;
#125398=ORIENTED_EDGE ( 'NONE', *, *, #196277, .F. ) ;
#125400=EDGE_CURVE ( 'NONE', #201984, #253337, #19356, .T. ) ;
#125410=DIRECTION ( 'NONE',  ( 0.000000000000000000, -0.5341055959866553016, 0.8454177738465993297 ) ) ;
#125425=EDGE_LOOP ( 'NONE', ( #3722, #78082, #28047, #160688 ) ) ;
#125430=LINE ( 'NONE', #83680, #47306 ) ;
#125448=AXIS2_PLACEMENT_3D ( 'NONE', #143306, #199458, #119938 ) ;
#125457=CIRCLE ( 'NONE', #108703, 0.1999999999999896860 ) ;
#125470=DIRECTION ( 'NONE',  ( 0.000000000000000000, 0.8814952561688444987, -0.4721928772777320149 ) ) ;
#125472=CARTESIAN_POINT ( 'NONE',  ( 23.24999999999999289, 20.97908333644147660, -233.6079013178409411 ) ) ;
#125481=CARTESIAN_POINT ( 'NONE',  ( 19.81427058490562132, 34.45565372986682462, -235.1336912300558311 ) ) ;
#125510=AXIS2_PLACEMENT_3D ( 'NONE', #119305, #58012, #99704 ) ;
#125539=CARTESIAN_POINT ( 'NONE',  ( 21.13461538461538325, 22.21093039075207898, -231.7318303787629930 ) ) ;
#125584=AXIS2_PLACEMENT_3D ( 'NONE', #197156, #163190, #138448 ) ;
#125642=LINE ( 'NONE', #218630, #214741 ) ;
#125669=ORIENTED_EDGE ( 'NONE', *, *, #52829, .T. ) ;
#125723=CARTESIAN_POINT ( 'NONE',  ( -20.64999999999999858, 26.26625913865096251, -241.7830784256010759 ) ) ;
#125731=DIRECTION ( 'NONE',  ( 1.000000000000000000, 0.000000000000000000, 0.000000000000000000 ) ) ;
#125764=CARTESIAN_POINT ( 'NONE',  ( 18.49999999999999645, 18.14639373905162145, -237.6648341169113792 ) ) ;
#125775=EDGE_CURVE ( 'NONE', #161820, #152553, #122505, .T. ) ;
#125782=DIRECTION ( 'NONE',  ( 1.000000000000000000, 0.000000000000000000, 0.000000000000000000 ) ) ;
#125783=EDGE_LOOP ( 'NONE', ( #200666, #210960, #74554, #202825 ) ) ;
#125839=VERTEX_POINT ( 'NONE', #104192 ) ;
#125841=CARTESIAN_POINT ( 'NONE',  ( -21.14999999999999858, -3.187427350888460076, -228.3200064793908837 ) ) ;
#125872=EDGE_CURVE ( 'NONE', #138960, #199913, #256164, .T. ) ;
#125887=EDGE_LOOP ( 'NONE', ( #228522, #51154, #193137, #215190 ) ) ;
#125922=CARTESIAN_POINT ( 'NONE',  ( -20.94999999999999929, 4.260086453440760756, -245.2296700999207246 ) ) ;
#125927=FACE_OUTER_BOUND ( 'NONE', #50477, .T. ) ;
#125950=DIRECTION ( 'NONE',  ( -1.000000000000000000, -0.000000000000000000, -0.000000000000000000 ) ) ;
#125955=FACE_OUTER_BOUND ( 'NONE', #97748, .T. ) ;
#126020=LINE ( 'NONE', #205552, #52253 ) ;
#126071=DIRECTION ( 'NONE',  ( 0.000000000000000000, -0.8814952561689786137, 0.4721928772774816596 ) ) ;
#126101=CARTESIAN_POINT ( 'NONE',  ( 21.05000000000000071, 18.75506398265894958, -230.0044230565036116 ) ) ;
#126105=ADVANCED_FACE ( 'NONE', ( #26635 ), #227375, .T. ) ;
#126122=CIRCLE ( 'NONE', #167866, 12.87499999999998401 ) ;
#126137=FACE_OUTER_BOUND ( 'NONE', #67832, .T. ) ;
#126164=ORIENTED_EDGE ( 'NONE', *, *, #153141, .T. ) ;
#126201=EDGE_LOOP ( 'NONE', ( #133986, #69788, #245492, #220728 ) ) ;
#126203=ORIENTED_EDGE ( 'NONE', *, *, #215305, .F. ) ;
#126290=ORIENTED_EDGE ( 'NONE', *, *, #150810, .T. ) ;
#126298=ADVANCED_FACE ( 'NONE', ( #155590 ), #218065, .T. ) ;
#126315=ORIENTED_EDGE ( 'NONE', *, *, #162162, .T. ) ;
#126319=CIRCLE ( 'NONE', #13899, 0.1000000000000013933 ) ;
#126329=EDGE_CURVE ( 'NONE', #1255, #28426, #224049, .T. ) ;
#126335=ADVANCED_FACE ( 'NONE', ( #98106 ), #23775, .F. ) ;
#126337=CYLINDRICAL_SURFACE ( 'NONE', #178746, 0.09999999999999939493 ) ;
#126343=ORIENTED_EDGE ( 'NONE', *, *, #28764, .F. ) ;
#126347=CARTESIAN_POINT ( 'NONE',  ( -18.59999999999999787, 18.27574494880468592, -237.6039235467692947 ) ) ;
#126352=TOROIDAL_SURFACE ( 'NONE', #163951, 11.70000000000000639, 0.1000000000000000056 ) ;
#126374=CARTESIAN_POINT ( 'NONE',  ( -23.25000000000000000, 46.02130280899747561, -256.6489974955837852 ) ) ;
#126382=VERTEX_POINT ( 'NONE', #223209 ) ;
#126391=DIRECTION ( 'NONE',  ( 1.000000000000000000, 0.000000000000000000, 0.000000000000000000 ) ) ;
#126401=CIRCLE ( 'NONE', #47268, 0.2000000000000084766 ) ;
#126404=DIRECTION ( 'NONE',  ( 0.000000000000000000, 0.8814952561688476074, -0.4721928772777262417 ) ) ;
#126435=CARTESIAN_POINT ( 'NONE',  ( -20.54999999999999716, 29.14863708059993286, -237.4168895852561434 ) ) ;
#126444=VECTOR ( 'NONE', #168563, 1000.000000000000000 ) ;
#126457=ORIENTED_EDGE ( 'NONE', *, *, #191890, .T. ) ;
#126467=VERTEX_POINT ( 'NONE', #228367 ) ;
#126472=ORIENTED_EDGE ( 'NONE', *, *, #43480, .T. ) ;
#126490=DIRECTION ( 'NONE',  ( 0.000000000000000000, -0.5341055959866553016, 0.8454177738465993297 ) ) ;
#126519=CARTESIAN_POINT ( 'NONE',  ( -21.14999999999999858, 18.65704504850842582, -226.5784250989226507 ) ) ;
#126526=EDGE_LOOP ( 'NONE', ( #222188, #159033, #221997, #68884 ) ) ;
#126538=ORIENTED_EDGE ( 'NONE', *, *, #27177, .F. ) ;
#126583=CARTESIAN_POINT ( 'NONE',  ( -22.42357213249529124, 0.4119679992451404926, -230.0222526030509016 ) ) ;
#126651=CARTESIAN_POINT ( 'NONE',  ( 18.49999999999999289, 19.00443933019177223, -232.7770257915295531 ) ) ;
#126715=CARTESIAN_POINT ( 'NONE',  ( 21.05000000000000071, 28.60154115857409352, -258.4512230915049713 ) ) ;
#126728=ADVANCED_FACE ( 'NONE', ( #57403 ), #179951, .F. ) ;
#126761=EDGE_CURVE ( 'NONE', #5002, #29239, #98982, .T. ) ;
#126765=VERTEX_POINT ( 'NONE', #166831 ) ;
#126770=AXIS2_PLACEMENT_3D ( 'NONE', #93509, #209616, #188760 ) ;
#126786=ORIENTED_EDGE ( 'NONE', *, *, #171213, .T. ) ;
#126794=AXIS2_PLACEMENT_3D ( 'NONE', #51034, #107183, #129326 ) ;
#126795=AXIS2_PLACEMENT_3D ( 'NONE', #113013, #97252, #176855 ) ;
#126804=DIRECTION ( 'NONE',  ( 1.000000000000000000, 0.000000000000000000, 0.000000000000000000 ) ) ;
#126809=AXIS2_PLACEMENT_3D ( 'NONE', #32219, #79520, #159104 ) ;
#126816=EDGE_CURVE ( 'NONE', #39363, #86653, #170450, .T. ) ;
#126830=EDGE_LOOP ( 'NONE', ( #20262, #175569, #160652, #141288 ) ) ;
#126856=TOROIDAL_SURFACE ( 'NONE', #110279, 0.2000000000000000111, 0.1000000000000000056 ) ;
#126857=EDGE_CURVE ( 'NONE', #21030, #168386, #44292, .T. ) ;
#126894=DIRECTION ( 'NONE',  ( -0.000000000000000000, 0.8814952561688430555, -0.4721928772777346239 ) ) ;
#127022=ORIENTED_EDGE ( 'NONE', *, *, #153972, .T. ) ;
#127026=CARTESIAN_POINT ( 'NONE',  ( 20.04142135623730070, 31.36165455396662693, -233.4973802202241302 ) ) ;
#127028=CYLINDRICAL_SURFACE ( 'NONE', #63253, 0.5000000000000008882 ) ;
#127053=ADVANCED_FACE ( 'NONE', ( #37566 ), #36287, .T. ) ;
#127055=ADVANCED_FACE ( 'NONE', ( #197895 ), #106488, .F. ) ;
#127126=DIRECTION ( 'NONE',  ( 0.000000000000000000, 0.8814952561688438326, -0.4721928772777331806 ) ) ;
#127141=ADVANCED_FACE ( 'NONE', ( #63515 ), #66356, .T. ) ;
#127152=DIRECTION ( 'NONE',  ( -1.000000000000000000, 0.000000000000000000, 0.000000000000000000 ) ) ;
#127159=CIRCLE ( 'NONE', #214627, 0.09999999999999939493 ) ;
#127161=CIRCLE ( 'NONE', #106285, 7.791421356237338891 ) ;
#127192=AXIS2_PLACEMENT_3D ( 'NONE', #54239, #175512, #215870 ) ;
#127199=DIRECTION ( 'NONE',  ( 0.000000000000000000, 0.8814952561688437216, -0.4721928772777335692 ) ) ;
#127232=LINE ( 'NONE', #245902, #108286 ) ;
#127236=CARTESIAN_POINT ( 'NONE',  ( 23.15000000000000213, 1.627786319807483340, -244.0021210468063089 ) ) ;
#127238=CIRCLE ( 'NONE', #173067, 7.720710678118679837 ) ;
#127260=DIRECTION ( 'NONE',  ( 1.000000000000000000, 0.000000000000000000, 0.000000000000000000 ) ) ;
#127282=CIRCLE ( 'NONE', #164883, 0.1000000000000076522 ) ;
#127286=EDGE_LOOP ( 'NONE', ( #222447, #93754, #22553, #157672 ) ) ;
#127317=CARTESIAN_POINT ( 'NONE',  ( -20.85000000000000142, 46.46967969402478360, -243.0849751855955674 ) ) ;
#127332=DIRECTION ( 'NONE',  ( -0.000000000000000000, 0.4721928772777345684, 0.8814952561688429444 ) ) ;
#127344=DIRECTION ( 'NONE',  ( 0.000000000000000000, 0.8814952561688429444, -0.4721928772777348460 ) ) ;
#127345=DIRECTION ( 'NONE',  ( 1.734723475976817192E-14, -0.4721928772777346239, -0.8814952561688430555 ) ) ;
#127409=ORIENTED_EDGE ( 'NONE', *, *, #50388, .T. ) ;
#127415=DIRECTION ( 'NONE',  ( 1.000000000000000000, 0.000000000000000000, 0.000000000000000000 ) ) ;
#127423=DIRECTION ( 'NONE',  ( 0.000000000000000000, 0.8814952561688429444, -0.4721928772777345684 ) ) ;
#127434=EDGE_CURVE ( 'NONE', #62589, #212495, #191470, .T. ) ;
#127455=DIRECTION ( 'NONE',  ( 0.000000000000000000, -0.4721928772777346239, -0.8814952561688430555 ) ) ;
#127470=DIRECTION ( 'NONE',  ( 1.000000000000000000, 0.000000000000000000, 0.000000000000000000 ) ) ;
#127485=CARTESIAN_POINT ( 'NONE',  ( 21.05000000000000071, 23.49882452903949570, -253.1653563615082305 ) ) ;
#127488=FACE_OUTER_BOUND ( 'NONE', #226483, .T. ) ;
#127503=CARTESIAN_POINT ( 'NONE',  ( -21.12844524849339223, 18.76330736928263221, -226.6353469151677587 ) ) ;
#127526=CARTESIAN_POINT ( 'NONE',  ( -20.64999999999999858, 11.60058429089262333, -246.3380203656811887 ) ) ;
#127530=EDGE_LOOP ( 'NONE', ( #142815, #230005, #72493, #132246 ) ) ;
#127542=ORIENTED_EDGE ( 'NONE', *, *, #77294, .T. ) ;
#127554=VECTOR ( 'NONE', #56863, 1000.000000000000000 ) ;
#127568=CARTESIAN_POINT ( 'NONE',  ( 18.50000000000000000, 8.841736820195473356, -245.4273993276876240 ) ) ;
#127600=ORIENTED_EDGE ( 'NONE', *, *, #60887, .F. ) ;
#127628=ADVANCED_FACE ( 'NONE', ( #207568 ), #27674, .F. ) ;
#127630=DIRECTION ( 'NONE',  ( -0.000000000000000000, -0.8814952561688430555, 0.4721928772777344574 ) ) ;
#127633=DIRECTION ( 'NONE',  ( 0.000000000000000000, 0.4721928772776973204, 0.8814952561688629284 ) ) ;
#127647=DIRECTION ( 'NONE',  ( 1.000000000000000000, 0.000000000000000000, 0.000000000000000000 ) ) ;
#127656=AXIS2_PLACEMENT_3D ( 'NONE', #238681, #140872, #22220 ) ;
#127682=ORIENTED_EDGE ( 'NONE', *, *, #196716, .F. ) ;
#127690=CARTESIAN_POINT ( 'NONE',  ( -21.56666275994539816, 0.9959460939976478855, -230.4474815061071240 ) ) ;
#127703=AXIS2_PLACEMENT_3D ( 'NONE', #214917, #252750, #53287 ) ;
#127704=ORIENTED_EDGE ( 'NONE', *, *, #40552, .T. ) ;
#127793=ORIENTED_EDGE ( 'NONE', *, *, #46404, .T. ) ;
#127809=DIRECTION ( 'NONE',  ( 0.000000000000000000, 0.5868805631290353597, 0.8096735173027127530 ) ) ;
#127840=DIRECTION ( 'NONE',  ( 0.000000000000000000, 0.8814952561688444987, -0.4721928772777320149 ) ) ;
#127843=CARTESIAN_POINT ( 'NONE',  ( -21.05000000000000071, 9.685169582982728897, -235.1020606565447224 ) ) ;
#127853=AXIS2_PLACEMENT_3D ( 'NONE', #219718, #237996, #218421 ) ;
#127864=CARTESIAN_POINT ( 'NONE',  ( -21.05000000000000071, 1.561467271655390121, -230.7743560730225454 ) ) ;
#127889=VECTOR ( 'NONE', #38865, 1000.000000000000000 ) ;
#127891=ORIENTED_EDGE ( 'NONE', *, *, #243669, .T. ) ;
#127900=CARTESIAN_POINT ( 'NONE',  ( -18.59999999999999787, 45.93315328338058379, -256.6017782078560003 ) ) ;
#128070=CARTESIAN_POINT ( 'NONE',  ( 21.05000000000000071, 28.27358281186466371, -238.9334100630653381 ) ) ;
#128081=DIRECTION ( 'NONE',  ( -0.000000000000000000, -0.4721928772777346239, -0.8814952561688430555 ) ) ;
#128122=VERTEX_POINT ( 'NONE', #41468 ) ;
#128151=ORIENTED_EDGE ( 'NONE', *, *, #120311, .T. ) ;
#128153=DIRECTION ( 'NONE',  ( 1.000000000000000000, 1.394253735153569469E-16, 2.602809386958778209E-16 ) ) ;
#128155=ORIENTED_EDGE ( 'NONE', *, *, #132597, .F. ) ;
#128175=ORIENTED_EDGE ( 'NONE', *, *, #250735, .T. ) ;
#128196=ADVANCED_FACE ( 'NONE', ( #143088 ), #27045, .F. ) ;
#128210=CARTESIAN_POINT ( 'NONE',  ( -21.13498764882296044, 1.403758898530641952, -230.6640565874768640 ) ) ;
#128248=DIRECTION ( 'NONE',  ( 0.000000000000000000, 0.8814952561688428334, -0.4721928772777348460 ) ) ;
#128257=DIRECTION ( 'NONE',  ( 0.000000000000000000, -0.4721928772777343464, -0.8814952561688431665 ) ) ;
#128269=CARTESIAN_POINT ( 'NONE',  ( -21.07928932188134041, 1.596973512272247042, -230.6572452218044020 ) ) ;
#128275=VECTOR ( 'NONE', #186809, 1000.000000000000000 ) ;
#128287=SPHERICAL_SURFACE ( 'NONE', #129464, 0.1000000000000000056 ) ;
#128289=EDGE_CURVE ( 'NONE', #116380, #260, #111439, .T. ) ;
#128302=ORIENTED_EDGE ( 'NONE', *, *, #109757, .T. ) ;
#128332=AXIS2_PLACEMENT_3D ( 'NONE', #256088, #254815, #175368 ) ;
#128333=ADVANCED_FACE ( 'NONE', ( #158410 ), #15984, .T. ) ;
#128356=DIRECTION ( 'NONE',  ( 0.000000000000000000, 0.8814952561688438326, -0.4721928772777332362 ) ) ;
#128364=VECTOR ( 'NONE', #67968, 1000.000000000000000 ) ;
#128370=CARTESIAN_POINT ( 'NONE',  ( -18.59999999999999787, 46.01276039807270024, -256.6622985126337539 ) ) ;
#128388=AXIS2_PLACEMENT_3D ( 'NONE', #230445, #171789, #54365 ) ;
#128392=CARTESIAN_POINT ( 'NONE',  ( -18.49999999999998934, 38.23183114100727664, -261.0790748268677817 ) ) ;
#128406=ORIENTED_EDGE ( 'NONE', *, *, #125872, .T. ) ;
#128434=CARTESIAN_POINT ( 'NONE',  ( -22.48660254037843131, 12.63302488529805601, -223.3515224085914781 ) ) ;
#128442=DIRECTION ( 'NONE',  ( 1.000000000000000000, 0.000000000000000000, 0.000000000000000000 ) ) ;
#128456=CARTESIAN_POINT ( 'NONE',  ( -18.59999999999999787, 14.81796439977981272, -236.5325475414793743 ) ) ;
#128461=ORIENTED_EDGE ( 'NONE', *, *, #42882, .F. ) ;
#128470=CARTESIAN_POINT ( 'NONE',  ( 21.05000000000000071, 17.83900070254454562, -239.4698447713637677 ) ) ;
#128472=ADVANCED_FACE ( 'NONE', ( #85218 ), #20058, .T. ) ;
#128487=CIRCLE ( 'NONE', #82655, 7.900000000000010125 ) ;
#128494=CARTESIAN_POINT ( 'NONE',  ( -21.05000000000000071, 18.62343931468261360, -223.9512205031617498 ) ) ;
#128500=ORIENTED_EDGE ( 'NONE', *, *, #216948, .F. ) ;
#128538=EDGE_CURVE ( 'NONE', #250267, #126765, #236689, .T. ) ;
#128547=CIRCLE ( 'NONE', #120217, 0.1000000000000013933 ) ;
#128555=LINE ( 'NONE', #105095, #155856 ) ;
#128563=CARTESIAN_POINT ( 'NONE',  ( -23.15000000000000213, 23.34004772283015328, -229.2004250369967338 ) ) ;
#128587=AXIS2_PLACEMENT_3D ( 'NONE', #3659, #127470, #85733 ) ;
#128646=CARTESIAN_POINT ( 'NONE',  ( -21.05000000000000071, 14.88773611405353314, -236.3451124650200370 ) ) ;
#128647=DIRECTION ( 'NONE',  ( -1.000000000000000000, 0.000000000000000000, 0.000000000000000000 ) ) ;
#128651=LINE ( 'NONE', #231601, #67918 ) ;
#128686=CARTESIAN_POINT ( 'NONE',  ( -20.54999999999999716, 20.02211948220868365, -235.8179285081017156 ) ) ;
#128692=CARTESIAN_POINT ( 'NONE',  ( 18.42595409746882140, 8.812905803731212018, -245.4119551287989509 ) ) ;
#128705=ORIENTED_EDGE ( 'NONE', *, *, #169255, .T. ) ;
#128729=CIRCLE ( 'NONE', #91328, 0.09999999999999742428 ) ;
#128786=AXIS2_PLACEMENT_3D ( 'NONE', #22660, #162167, #6915 ) ;
#128795=ADVANCED_FACE ( 'NONE', ( #231360 ), #35740, .F. ) ;
#128796=CARTESIAN_POINT ( 'NONE',  ( -20.97625342178423224, 18.71344899774613424, -226.7788045575993863 ) ) ;
#128798=ORIENTED_EDGE ( 'NONE', *, *, #156278, .F. ) ;
#128804=CARTESIAN_POINT ( 'NONE',  ( -20.54999999999999716, 26.26625913865096251, -241.7830784256010759 ) ) ;
#128833=CARTESIAN_POINT ( 'NONE',  ( -22.40000000000000568, 10.80758397488571099, -226.8651660546161111 ) ) ;
#128846=ADVANCED_FACE ( 'NONE', ( #241616 ), #220146, .F. ) ;
#128850=ORIENTED_EDGE ( 'NONE', *, *, #101034, .F. ) ;
#128888=CIRCLE ( 'NONE', #145424, 0.09999999999999986677 ) ;
#128917=DIRECTION ( 'NONE',  ( 0.000000000000000000, 0.8127272543710951647, -0.5826443254700255370 ) ) ;
#128919=EDGE_CURVE ( 'NONE', #202163, #104681, #28661, .T. ) ;
#128954=CARTESIAN_POINT ( 'NONE',  ( -20.64999999999999858, 26.38661631484796644, -241.7796963509253203 ) ) ;
#129019=VERTEX_POINT ( 'NONE', #48547 ) ;
#129022=DIRECTION ( 'NONE',  ( -0.000000000000000000, -0.8814952561688430555, 0.4721928772777346239 ) ) ;
#129051=AXIS2_PLACEMENT_3D ( 'NONE', #168734, #224782, #104814 ) ;
#129052=ADVANCED_FACE ( 'NONE', ( #29034 ), #232634, .T. ) ;
#129062=CARTESIAN_POINT ( 'NONE',  ( 20.94999999999999929, 36.65892442174935439, -249.5511627012433848 ) ) ;
#129122=DIRECTION ( 'NONE',  ( 0.000000000000000000, 0.4721928772777351790, 0.8814952561688427224 ) ) ;
#129144=EDGE_CURVE ( 'NONE', #99386, #148681, #182925, .T. ) ;
#129164=DIRECTION ( 'NONE',  ( 0.000000000000000000, -0.8814952561688428334, 0.4721928772777349570 ) ) ;
#129177=ADVANCED_FACE ( 'NONE', ( #101418 ), #232822, .T. ) ;
#129182=VECTOR ( 'NONE', #29875, 1000.000000000000000 ) ;
#129186=ORIENTED_EDGE ( 'NONE', *, *, #148378, .F. ) ;
#129214=AXIS2_PLACEMENT_3D ( 'NONE', #92762, #95345, #251842 ) ;
#129224=CARTESIAN_POINT ( 'NONE',  ( -20.94999999999999929, 36.65892442174935439, -249.5511627012433848 ) ) ;
#129235=ORIENTED_EDGE ( 'NONE', *, *, #252195, .F. ) ;
#129256=CARTESIAN_POINT ( 'NONE',  ( -23.25000000000000000, 43.21392023178790964, -245.1418509714632421 ) ) ;
#129266=EDGE_LOOP ( 'NONE', ( #15291, #27952, #123474, #202220, #151591 ) ) ;
#129326=DIRECTION ( 'NONE',  ( 0.000000000000000000, 0.8814952561688438326, -0.4721928772777331806 ) ) ;
#129327=EDGE_LOOP ( 'NONE', ( #216497, #6549, #154741, #173793 ) ) ;
#129358=ORIENTED_EDGE ( 'NONE', *, *, #166615, .F. ) ;
#129365=EDGE_CURVE ( 'NONE', #23820, #105209, #170485, .T. ) ;
#129389=ORIENTED_EDGE ( 'NONE', *, *, #166195, .T. ) ;
#129393=DIRECTION ( 'NONE',  ( -0.000000000000000000, -0.4721928772777351790, -0.8814952561688427224 ) ) ;
#129408=DIRECTION ( 'NONE',  ( 2.952720810173290591E-16, -0.4721928772777312933, -0.8814952561688448318 ) ) ;
#129412=CARTESIAN_POINT ( 'NONE',  ( -23.25000000000000000, 3.470628026992396808, -231.7731008717366876 ) ) ;
#129464=AXIS2_PLACEMENT_3D ( 'NONE', #86548, #147853, #241799 ) ;
#129494=DIRECTION ( 'NONE',  ( 1.000000000000000000, 0.000000000000000000, 0.000000000000000000 ) ) ;
#129496=CARTESIAN_POINT ( 'NONE',  ( 23.14999999999999858, 37.60331017630482364, -247.7881721889056905 ) ) ;
#129501=VECTOR ( 'NONE', #49022, 1000.000000000000000 ) ;
#129514=CIRCLE ( 'NONE', #191905, 0.5000000000000054401 ) ;
#129516=CARTESIAN_POINT ( 'NONE',  ( -21.05000000000000071, 13.59055429284667404, -238.6121134008722038 ) ) ;
#129539=FACE_OUTER_BOUND ( 'NONE', #111094, .T. ) ;
#129558=DIRECTION ( 'NONE',  ( 0.000000000000000000, 0.8814952561688441657, -0.4721928772777325145 ) ) ;
#129575=ORIENTED_EDGE ( 'NONE', *, *, #195168, .T. ) ;
#129609=CIRCLE ( 'NONE', #4501, 0.1000000000000013933 ) ;
#129628=CARTESIAN_POINT ( 'NONE',  ( 21.11344571971278228, 22.93732951038863632, -230.1555751630206714 ) ) ;
#129640=CIRCLE ( 'NONE', #137995, 0.1000000000000013378 ) ;
#129642=DIRECTION ( 'NONE',  ( -3.265361837132814079E-16, 0.4721928772777359007, 0.8814952561688425003 ) ) ;
#129666=DIRECTION ( 'NONE',  ( 0.000000000000000000, 0.8814952561688430555, -0.4721928772777346239 ) ) ;
#129690=AXIS2_PLACEMENT_3D ( 'NONE', #66339, #104157, #63758 ) ;
#129696=ORIENTED_EDGE ( 'NONE', *, *, #151970, .F. ) ;
#129704=CIRCLE ( 'NONE', #29798, 0.09999999999999731326 ) ;
#129712=ORIENTED_EDGE ( 'NONE', *, *, #246333, .T. ) ;
#129723=CARTESIAN_POINT ( 'NONE',  ( 18.59999999999998366, 36.65892442174935439, -249.5511627012433848 ) ) ;
#129751=DIRECTION ( 'NONE',  ( -0.000000000000000000, 0.5474227397873200340, -0.8368562265788217491 ) ) ;
#129778=VERTEX_POINT ( 'NONE', #29373 ) ;
#129788=DIRECTION ( 'NONE',  ( 1.000000000000000000, 0.000000000000000000, 0.000000000000000000 ) ) ;
#129826=DIRECTION ( 'NONE',  ( 1.000000000000000000, -0.000000000000000000, -0.000000000000000000 ) ) ;
#129828=CARTESIAN_POINT ( 'NONE',  ( 18.59999999999999787, 45.93315328338058379, -256.6017782078560003 ) ) ;
#129858=CARTESIAN_POINT ( 'NONE',  ( 20.94999999999999929, 20.42498087366621817, -235.1829032864613396 ) ) ;
#129870=EDGE_CURVE ( 'NONE', #41664, #241914, #141033, .T. ) ;
#129885=ORIENTED_EDGE ( 'NONE', *, *, #97952, .T. ) ;
#129889=AXIS2_PLACEMENT_3D ( 'NONE', #209125, #249560, #130874 ) ;
#129917=DIRECTION ( 'NONE',  ( 0.000000000000000000, -0.4834676483507011624, -0.8753622295931228203 ) ) ;
#129939=FACE_OUTER_BOUND ( 'NONE', #246575, .T. ) ;
#129946=CARTESIAN_POINT ( 'NONE',  ( 18.55121869061587958, 46.45193731540634019, -243.0811559066744110 ) ) ;
#129961=CIRCLE ( 'NONE', #163322, 0.1000000000000076522 ) ;
#129971=DIRECTION ( 'NONE',  ( 0.000000000000000000, 0.8814952561688444987, -0.4721928772777320149 ) ) ;
#130032=EDGE_CURVE ( 'NONE', #162761, #170728, #238601, .T. ) ;
#130063=CIRCLE ( 'NONE', #184798, 0.09999999999999939493 ) ;
#130065=ORIENTED_EDGE ( 'NONE', *, *, #198123, .T. ) ;
#130086=ADVANCED_FACE ( 'NONE', ( #203806 ), #177849, .F. ) ;
#130093=CARTESIAN_POINT ( 'NONE',  ( 22.42196299218230493, -3.139091170936018749, -228.2296853193599304 ) ) ;
#130115=ADVANCED_FACE ( 'NONE', ( #65581 ), #20225, .T. ) ;
#130123=EDGE_LOOP ( 'NONE', ( #1054, #26346, #87282, #217203, #244225 ) ) ;
#130138=CARTESIAN_POINT ( 'NONE',  ( -23.15000000000000213, 19.73066058418984170, -238.2142830767208466 ) ) ;
#130158=DIRECTION ( 'NONE',  ( 0.000000000000000000, 0.8814952561688738086, -0.4721928772776773364 ) ) ;
#130159=DIRECTION ( 'NONE',  ( -1.000000000000000000, -0.000000000000000000, -0.000000000000000000 ) ) ;
#130170=DIRECTION ( 'NONE',  ( 0.000000000000000000, 0.8814952561688439436, -0.4721928772777330141 ) ) ;
#130189=CARTESIAN_POINT ( 'NONE',  ( 23.14999999999999503, 38.54769593086029289, -246.0251816765679962 ) ) ;
#130262=ADVANCED_FACE ( 'NONE', ( #30328 ), #146119, .T. ) ;
#130282=CARTESIAN_POINT ( 'NONE',  ( 22.50000000000000000, 12.54152817314149715, -223.4164406214577241 ) ) ;
#130300=ORIENTED_EDGE ( 'NONE', *, *, #171033, .T. ) ;
#130304=TOROIDAL_SURFACE ( 'NONE', #67775, 12.97499999999999787, 0.1000000000000000056 ) ;
#130326=ORIENTED_EDGE ( 'NONE', *, *, #116935, .T. ) ;
#130330=DIRECTION ( 'NONE',  ( 1.000000000000000000, 0.000000000000000000, 0.000000000000000000 ) ) ;
#130341=AXIS2_PLACEMENT_3D ( 'NONE', #59278, #80130, #234098 ) ;
#130384=CARTESIAN_POINT ( 'NONE',  ( 18.49999999999998934, 28.95347087985017609, -237.9930060266852081 ) ) ;
#130387=DIRECTION ( 'NONE',  ( 0.000000000000000000, 0.8814952561688476074, -0.4721928772777262417 ) ) ;
#130428=CARTESIAN_POINT ( 'NONE',  ( -23.15000000000000213, 28.51339163295720169, -258.4040038037771865 ) ) ;
#130457=AXIS2_PLACEMENT_3D ( 'NONE', #51332, #111347, #205286 ) ;
#130476=CARTESIAN_POINT ( 'NONE',  ( 20.94999999999999574, 18.18127959618848521, -237.5711165786817389 ) ) ;
#130555=EDGE_CURVE ( 'NONE', #234543, #102393, #78809, .T. ) ;
#130558=DIRECTION ( 'NONE',  ( -1.000000000000000000, 0.000000000000000000, 0.000000000000000000 ) ) ;
#130565=CARTESIAN_POINT ( 'NONE',  ( 20.94999999999999929, 43.53458741986633385, -253.2342671440096922 ) ) ;
#130603=VECTOR ( 'NONE', #125782, 1000.000000000000000 ) ;
#130612=AXIS2_PLACEMENT_3D ( 'NONE', #109606, #247842, #225675 ) ;
#130624=CARTESIAN_POINT ( 'NONE',  ( 20.21494484322136387, 18.87362850034901385, -229.4702142578394728 ) ) ;
#130644=ORIENTED_EDGE ( 'NONE', *, *, #7611, .F. ) ;
#130651=CYLINDRICAL_SURFACE ( 'NONE', #185631, 0.09999999999999939493 ) ;
#130664=EDGE_LOOP ( 'NONE', ( #35751, #198405, #31215, #194264, #68977 ) ) ;
#130691=LINE ( 'NONE', #12064, #24272 ) ;
#130700=ORIENTED_EDGE ( 'NONE', *, *, #202453, .T. ) ;
#130702=VERTEX_POINT ( 'NONE', #55968 ) ;
#130713=ADVANCED_FACE ( 'NONE', ( #215064 ), #36462, .F. ) ;
#130719=ORIENTED_EDGE ( 'NONE', *, *, #198996, .F. ) ;
#130730=CARTESIAN_POINT ( 'NONE',  ( -20.85000000000000142, 45.93315328338058379, -256.6017782078560003 ) ) ;
#130731=AXIS2_PLACEMENT_3D ( 'NONE', #109430, #88582, #188991 ) ;
#130739=VECTOR ( 'NONE', #202984, 1000.000000000000000 ) ;
#130758=VECTOR ( 'NONE', #81744, 1000.000000000000000 ) ;
#130774=ORIENTED_EDGE ( 'NONE', *, *, #157825, .F. ) ;
#130786=DIRECTION ( 'NONE',  ( 0.000000000000000000, 0.8814952561688430555, -0.4721928772777346239 ) ) ;
#130793=AXIS2_PLACEMENT_3D ( 'NONE', #142835, #183280, #120765 ) ;
#130822=EDGE_LOOP ( 'NONE', ( #141659, #124241, #182246, #252719 ) ) ;
#130830=CARTESIAN_POINT ( 'NONE',  ( -22.59999999999999787, 7.128833340093095217, -233.7327013124392749 ) ) ;
#130836=EDGE_CURVE ( 'NONE', #103016, #253481, #37741, .T. ) ;
#130874=DIRECTION ( 'NONE',  ( 0.000000000000000000, 0.8814952561688429444, -0.4721928772777345684 ) ) ;
#130900=CYLINDRICAL_SURFACE ( 'NONE', #243066, 2.000000000000003553 ) ;
#130904=ORIENTED_EDGE ( 'NONE', *, *, #82897, .T. ) ;
#130909=EDGE_CURVE ( 'NONE', #59204, #25443, #253784, .T. ) ;
#130953=ORIENTED_EDGE ( 'NONE', *, *, #46570, .T. ) ;
#130956=CARTESIAN_POINT ( 'NONE',  ( -18.45140287520620248, 38.03325571449392584, -261.0487029501068150 ) ) ;
#130969=DIRECTION ( 'NONE',  ( -0.000000000000000000, 0.8814952561688430555, -0.4721928772777346239 ) ) ;
#130977=ORIENTED_EDGE ( 'NONE', *, *, #246795, .T. ) ;
#131007=EDGE_CURVE ( 'NONE', #54485, #89738, #70860, .T. ) ;
#131044=CARTESIAN_POINT ( 'NONE',  ( 21.09107601085592165, 1.537665657181535694, -230.6930743813777838 ) ) ;
#131075=DIRECTION ( 'NONE',  ( -2.561896900575095617E-15, -0.9901894034181603077, -0.1397316906016231042 ) ) ;
#131081=AXIS2_PLACEMENT_3D ( 'NONE', #48095, #127647, #207195 ) ;
#131134=DIRECTION ( 'NONE',  ( 0.000000000000000000, 0.8814952561688429444, -0.4721928772777345684 ) ) ;
#131151=EDGE_CURVE ( 'NONE', #98428, #16612, #199854, .T. ) ;
#131155=CARTESIAN_POINT ( 'NONE',  ( 21.09706851349342216, 22.05831724336241351, -231.7743849847716149 ) ) ;
#131168=CARTESIAN_POINT ( 'NONE',  ( -20.54999999999999716, 29.14863708059993286, -237.4168895852561434 ) ) ;
#131206=DIRECTION ( 'NONE',  ( 0.000000000000000000, 0.8753622295931610120, -0.4834676483506316624 ) ) ;
#131222=CIRCLE ( 'NONE', #227085, 0.09999999999999469036 ) ;
#131257=CARTESIAN_POINT ( 'NONE',  ( 21.05000000000000071, 18.71171618620643429, -229.8673829423568691 ) ) ;
#131284=ORIENTED_EDGE ( 'NONE', *, *, #242103, .F. ) ;
#131292=DIRECTION ( 'NONE',  ( -0.000000000000000000, -0.4721928772777346239, -0.8814952561688430555 ) ) ;
#131303=CARTESIAN_POINT ( 'NONE',  ( -23.25000000000000000, 2.272311100394799332, -217.9150152700588592 ) ) ;
#131305=AXIS2_PLACEMENT_3D ( 'NONE', #164601, #85020, #163317 ) ;
#131306=FACE_OUTER_BOUND ( 'NONE', #98969, .T. ) ;
#131319=DIRECTION ( 'NONE',  ( 0.000000000000000000, 0.8814952561688444987, -0.4721928772777320149 ) ) ;
#131381=EDGE_CURVE ( 'NONE', #16167, #245180, #145835, .T. ) ;
#131409=DIRECTION ( 'NONE',  ( -1.000000000000000000, 0.000000000000000000, 0.000000000000000000 ) ) ;
#131412=DIRECTION ( 'NONE',  ( 0.000000000000000000, -0.4721928772777356231, -0.8814952561688425003 ) ) ;
#131413=VECTOR ( 'NONE', #51402, 1000.000000000000000 ) ;
#131441=VERTEX_POINT ( 'NONE', #17230 ) ;
#131477=DIRECTION ( 'NONE',  ( -1.000000000000000000, 0.000000000000000000, 0.000000000000000000 ) ) ;
#131478=CARTESIAN_POINT ( 'NONE',  ( 20.95512820512820440, 22.03025613173516462, -231.6455594930189648 ) ) ;
#131538=AXIS2_PLACEMENT_3D ( 'NONE', #2414, #162814, #203198 ) ;
#131585=CYLINDRICAL_SURFACE ( 'NONE', #138517, 0.09999999999999986677 ) ;
#131595=CARTESIAN_POINT ( 'NONE',  ( -21.05000000000000071, 7.128833340093095217, -233.7327013124392749 ) ) ;
#131596=VECTOR ( 'NONE', #223580, 1000.000000000000000 ) ;
#131611=ORIENTED_EDGE ( 'NONE', *, *, #245738, .T. ) ;
#131618=CARTESIAN_POINT ( 'NONE',  ( -20.94999999999999929, 28.71379363806100571, -258.2416688332294825 ) ) ;
#131651=AXIS2_PLACEMENT_3D ( 'NONE', #156007, #200246, #197664 ) ;
#131658=EDGE_LOOP ( 'NONE', ( #219561, #15949, #181062, #5193 ) ) ;
#131690=ORIENTED_EDGE ( 'NONE', *, *, #98565, .T. ) ;
#131714=ORIENTED_EDGE ( 'NONE', *, *, #58195, .F. ) ;
#131725=DIRECTION ( 'NONE',  ( 1.000000000000000000, 0.000000000000000000, 0.000000000000000000 ) ) ;
#131731=AXIS2_PLACEMENT_3D ( 'NONE', #240449, #241729, #61815 ) ;
#131743=DIRECTION ( 'NONE',  ( -3.890533409366483389E-14, 0.8127272543710891695, -0.5826443254700338636 ) ) ;
#131763=ORIENTED_EDGE ( 'NONE', *, *, #85909, .F. ) ;
#131779=CARTESIAN_POINT ( 'NONE',  ( -20.64999999999999858, 21.39147882631411335, -233.2615922652120730 ) ) ;
#131833=VECTOR ( 'NONE', #145567, 1000.000000000000000 ) ;
#131855=DIRECTION ( 'NONE',  ( 0.000000000000000000, 0.8814952561688437216, -0.4721928772777334582 ) ) ;
#131875=DIRECTION ( 'NONE',  ( 1.000000000000000000, 1.394253735153569469E-16, 2.602809386958778209E-16 ) ) ;
#131917=ORIENTED_EDGE ( 'NONE', *, *, #86220, .T. ) ;
#131934=DIRECTION ( 'NONE',  ( -1.000000000000000000, 0.000000000000000000, 0.000000000000000000 ) ) ;
#131947=ORIENTED_EDGE ( 'NONE', *, *, #204216, .T. ) ;
#131949=CARTESIAN_POINT ( 'NONE',  ( 23.15000000000000213, 20.40049075128452216, -254.1715885023028250 ) ) ;
#131954=LINE ( 'NONE', #232368, #239803 ) ;
#131983=CARTESIAN_POINT ( 'NONE',  ( 18.49362639424868604, 38.16301648980600447, -261.0688944849867426 ) ) ;
#132001=CARTESIAN_POINT ( 'NONE',  ( 21.10257677756356998, 1.500471753121898510, -230.6894370601294497 ) ) ;
#132010=AXIS2_PLACEMENT_3D ( 'NONE', #5279, #161845, #64002 ) ;
#132022=DIRECTION ( 'NONE',  ( 1.000000000000000000, 1.541880601228652843E-16, 2.878400969107353907E-16 ) ) ;
#132023=CARTESIAN_POINT ( 'NONE',  ( -23.25000000000000000, 43.08613539620618837, -254.3146655184800409 ) ) ;
#132061=CARTESIAN_POINT ( 'NONE',  ( -22.50000000000000000, 10.71943444926882449, -226.8179467668883547 ) ) ;
#132076=EDGE_CURVE ( 'NONE', #227951, #181985, #109266, .T. ) ;
#132100=CARTESIAN_POINT ( 'NONE',  ( -23.15000000000000213, 36.65892442174935439, -249.5511627012433848 ) ) ;
#132104=LINE ( 'NONE', #209070, #229428 ) ;
#132122=ORIENTED_EDGE ( 'NONE', *, *, #12069, .F. ) ;
#132138=EDGE_LOOP ( 'NONE', ( #38777, #155883, #24501, #227844 ) ) ;
#132169=AXIS2_PLACEMENT_3D ( 'NONE', #33629, #193948, #15319 ) ;
#132178=CIRCLE ( 'NONE', #11375, 0.1000000000000019901 ) ;
#132192=DIRECTION ( 'NONE',  ( 0.000000000000000000, 0.8814952561688476074, -0.4721928772777262417 ) ) ;
#132205=DIRECTION ( 'NONE',  ( -1.000000000000000000, 0.000000000000000000, 0.000000000000000000 ) ) ;
#132226=CIRCLE ( 'NONE', #36394, 0.09999999999999986677 ) ;
#132235=VERTEX_POINT ( 'NONE', #149258 ) ;
#132246=ORIENTED_EDGE ( 'NONE', *, *, #29802, .F. ) ;
#132289=AXIS2_PLACEMENT_3D ( 'NONE', #244426, #87896, #89202 ) ;
#132296=ORIENTED_EDGE ( 'NONE', *, *, #140396, .F. ) ;
#132299=CIRCLE ( 'NONE', #28299, 0.09999999999999510669 ) ;
#132315=CARTESIAN_POINT ( 'NONE',  ( -21.05000000000000071, 9.997527148596390134, -228.1702915402975691 ) ) ;
#132320=AXIS2_PLACEMENT_3D ( 'NONE', #203357, #9003, #204620 ) ;
#132327=CARTESIAN_POINT ( 'NONE',  ( 21.05000000000000071, 1.622572661691780382, -230.6714771550865350 ) ) ;
#132330=ORIENTED_EDGE ( 'NONE', *, *, #139548, .F. ) ;
#132362=VERTEX_POINT ( 'NONE', #207950 ) ;
#132390=CARTESIAN_POINT ( 'NONE',  ( 20.94999999999999929, 36.65892442174935439, -249.5511627012433848 ) ) ;
#132407=CARTESIAN_POINT ( 'NONE',  ( 20.85000000000000142, 45.93315328338058379, -256.6017782078560003 ) ) ;
#132445=CARTESIAN_POINT ( 'NONE',  ( 21.14999999999999858, 22.07612373182271881, -231.7717111801312342 ) ) ;
#132456=EDGE_CURVE ( 'NONE', #179549, #97681, #246169, .T. ) ;
#132459=ORIENTED_EDGE ( 'NONE', *, *, #237801, .F. ) ;
#132460=( BOUNDED_SURFACE ( )  B_SPLINE_SURFACE ( 3, 2, ( 
 ( #93364, #68681, #210751 ),
 ( #230307, #30862, #9985 ),
 ( #90787, #172954, #229044 ),
 ( #252426, #170396, #72545 ) ),
 .UNSPECIFIED., .F., .F., .F. ) 
 B_SPLINE_SURFACE_WITH_KNOTS ( ( 4, 4 ),
 ( 3, 3 ),
 ( -3.469446951953614189E-18, 0.001979672783031568434 ),
 ( 0.000000000000000000, 1.000000000000000000 ),
 .UNSPECIFIED. ) 
 GEOMETRIC_REPRESENTATION_ITEM ( )  RATIONAL_B_SPLINE_SURFACE ( (
 ( 1.000000000000000000, 0.7103081912008257781, 1.000000000000000000),
 ( 1.000000000000000000, 0.7104998333563169455, 1.000000000000000000),
 ( 1.000000000000000000, 0.7107238315751489566, 1.000000000000000000),
 ( 1.000000000000000000, 0.7110073749541068189, 1.000000000000000000) ) ) 
 REPRESENTATION_ITEM ( '' )  SURFACE ( )  );
#132506=DIRECTION ( 'NONE',  ( 1.000000000000000000, 0.000000000000000000, 0.000000000000000000 ) ) ;
#132523=AXIS2_PLACEMENT_3D ( 'NONE', #257501, #140163, #181887 ) ;
#132533=DIRECTION ( 'NONE',  ( 0.000000000000000000, 0.5273008465187821736, -0.8496786552930323255 ) ) ;
#132536=LINE ( 'NONE', #112975, #256710 ) ;
#132551=DIRECTION ( 'NONE',  ( 1.000000000000000000, 0.000000000000000000, 0.000000000000000000 ) ) ;
#132556=DIRECTION ( 'NONE',  ( 0.000000000000000000, 0.8814952561688427224, -0.4721928772777352346 ) ) ;
#132562=DIRECTION ( 'NONE',  ( 0.000000000000000000, 0.8814952561688444987, -0.4721928772777320149 ) ) ;
#132575=CARTESIAN_POINT ( 'NONE',  ( -20.96428641293861617, 36.19089144327093521, -235.9708266132235792 ) ) ;
#132597=EDGE_CURVE ( 'NONE', #59200, #63323, #88093, .T. ) ;
#132600=CIRCLE ( 'NONE', #232587, 0.09999999999999939493 ) ;
#132604=CYLINDRICAL_SURFACE ( 'NONE', #240188, 4.049999999999997158 ) ;
#132617=FACE_OUTER_BOUND ( 'NONE', #237468, .T. ) ;
#132622=ORIENTED_EDGE ( 'NONE', *, *, #156072, .F. ) ;
#132635=DIRECTION ( 'NONE',  ( 0.000000000000000000, -0.8814952561688430555, 0.4721928772777346239 ) ) ;
#132637=FACE_OUTER_BOUND ( 'NONE', #174176, .T. ) ;
#132677=DIRECTION ( 'NONE',  ( 1.000000000000000000, 0.000000000000000000, 0.000000000000000000 ) ) ;
#132708=AXIS2_PLACEMENT_3D ( 'NONE', #112255, #169690, #190517 ) ;
#132741=DIRECTION ( 'NONE',  ( 0.000000000000000000, -0.3488585713686159218, -0.9371753822965306346 ) ) ;
#132745=AXIS2_PLACEMENT_3D ( 'NONE', #105491, #142077, #183785 ) ;
#132752=CARTESIAN_POINT ( 'NONE',  ( 23.15000000000000213, 23.68770167995059239, -252.8127582590406348 ) ) ;
#132777=FACE_OUTER_BOUND ( 'NONE', #59261, .T. ) ;
#132786=CARTESIAN_POINT ( 'NONE',  ( 21.04999999999999716, 22.00620749460749082, -231.7459716400360605 ) ) ;
#132802=CARTESIAN_POINT ( 'NONE',  ( 20.94999999999999929, 18.18127959618848877, -237.5711165786817389 ) ) ;
#132813=DIRECTION ( 'NONE',  ( 0.000000000000000000, -0.5826443254699606999, -0.8127272543711416830 ) ) ;
#132847=DIRECTION ( 'NONE',  ( -0.000000000000000000, 0.4721928772777345684, 0.8814952561688429444 ) ) ;
#132866=DIRECTION ( 'NONE',  ( 0.000000000000000000, 0.8814952561688437216, -0.4721928772777334582 ) ) ;
#132877=ORIENTED_EDGE ( 'NONE', *, *, #134450, .F. ) ;
#132878=ORIENTED_EDGE ( 'NONE', *, *, #190558, .T. ) ;
#132896=SPHERICAL_SURFACE ( 'NONE', #52195, 0.1000000000000000056 ) ;
#132897=AXIS2_PLACEMENT_3D ( 'NONE', #223483, #5707, #86526 ) ;
#132901=AXIS2_PLACEMENT_3D ( 'NONE', #19904, #156864, #117700 ) ;
#132919=DIRECTION ( 'NONE',  ( -7.304098846218136639E-16, -0.4721928772777346239, -0.8814952561688430555 ) ) ;
#132924=AXIS2_PLACEMENT_3D ( 'NONE', #256691, #36442, #233359 ) ;
#132938=DIRECTION ( 'NONE',  ( -1.000000000000000000, -0.000000000000000000, -0.000000000000000000 ) ) ;
#132943=VERTEX_POINT ( 'NONE', #39200 ) ;
#132992=EDGE_LOOP ( 'NONE', ( #18560, #206895, #26643, #91057 ) ) ;
#133013=ORIENTED_EDGE ( 'NONE', *, *, #9093, .T. ) ;
#133040=AXIS2_PLACEMENT_3D ( 'NONE', #29795, #225368, #8911 ) ;
#133059=EDGE_CURVE ( 'NONE', #229988, #107904, #25964, .T. ) ;
#133080=ADVANCED_FACE ( 'NONE', ( #204646 ), #92582, .F. ) ;
#133128=ORIENTED_EDGE ( 'NONE', *, *, #223610, .F. ) ;
#133135=EDGE_CURVE ( 'NONE', #104349, #148687, #44320, .T. ) ;
#133184=CARTESIAN_POINT ( 'NONE',  ( 23.14999999999999503, 23.34004772283015683, -229.2004250369967338 ) ) ;
#133188=SPHERICAL_SURFACE ( 'NONE', #172424, 0.1000000000000000056 ) ;
#133190=CYLINDRICAL_SURFACE ( 'NONE', #129214, 0.5000000000000008882 ) ;
#133193=CIRCLE ( 'NONE', #154086, 0.1999999999999987899 ) ;
#133206=EDGE_CURVE ( 'NONE', #73607, #151273, #67720, .T. ) ;
#133245=ADVANCED_FACE ( 'NONE', ( #53295 ), #91132, .T. ) ;
#133246=DIRECTION ( 'NONE',  ( 1.000000000000000000, 0.000000000000000000, 0.000000000000000000 ) ) ;
#133260=ADVANCED_FACE ( 'NONE', ( #151117 ), #152423, .F. ) ;
#133269=AXIS2_PLACEMENT_3D ( 'NONE', #150124, #6737, #189238 ) ;
#133286=ORIENTED_EDGE ( 'NONE', *, *, #28764, .T. ) ;
#133321=VECTOR ( 'NONE', #12971, 1000.000000000000000 ) ;
#133350=CARTESIAN_POINT ( 'NONE',  ( -18.59999999999999787, 43.02787096365918984, -254.3959382439171577 ) ) ;
#133353=DIRECTION ( 'NONE',  ( 1.000000000000000000, 0.000000000000000000, 0.000000000000000000 ) ) ;
#133366=DIRECTION ( 'NONE',  ( 0.000000000000000000, -0.5273008465187821736, 0.8496786552930323255 ) ) ;
#133385=LINE ( 'NONE', #212915, #69066 ) ;
#133386=DIRECTION ( 'NONE',  ( 1.000000000000000000, 0.000000000000000000, 0.000000000000000000 ) ) ;
#133401=DIRECTION ( 'NONE',  ( 1.000000000000000000, 0.000000000000000000, 0.000000000000000000 ) ) ;
#133453=AXIS2_PLACEMENT_3D ( 'NONE', #173260, #252725, #54536 ) ;
#133454=EDGE_CURVE ( 'NONE', #9313, #162761, #974, .T. ) ;
#133510=CARTESIAN_POINT ( 'NONE',  ( -23.15000000000000213, 25.94586868676353575, -241.5435999122864530 ) ) ;
#133532=LINE ( 'NONE', #214355, #223593 ) ;
#133542=ORIENTED_EDGE ( 'NONE', *, *, #55506, .T. ) ;
#133551=VECTOR ( 'NONE', #85608, 1000.000000000000000 ) ;
#133567=DIRECTION ( 'NONE',  ( -0.000000000000000000, -0.4721928772777346239, -0.8814952561688430555 ) ) ;
#133570=DIRECTION ( 'NONE',  ( 0.000000000000000000, 0.9994937237965558774, 0.03181660087586650476 ) ) ;
#133572=ADVANCED_FACE ( 'NONE', ( #68697 ), #7420, .T. ) ;
#133597=SPHERICAL_SURFACE ( 'NONE', #45970, 0.1000000000000000056 ) ;
#133614=AXIS2_PLACEMENT_3D ( 'NONE', #245397, #247942, #146275 ) ;
#133643=SURFACE_STYLE_FILL_AREA ( #121499 ) ;
#133663=DIRECTION ( 'NONE',  ( -1.000000000000000000, 0.000000000000000000, -0.000000000000000000 ) ) ;
#133686=DIRECTION ( 'NONE',  ( 0.000000000000000000, 0.4721928772777551075, 0.8814952561688320642 ) ) ;
#133694=CARTESIAN_POINT ( 'NONE',  ( 20.94999999999997442, 43.02787096365918984, -254.3959382439171577 ) ) ;
#133699=AXIS2_PLACEMENT_3D ( 'NONE', #123331, #64626, #183301 ) ;
#133706=DIRECTION ( 'NONE',  ( 0.000000000000000000, 0.5273008465188072647, -0.8496786552930167824 ) ) ;
#133747=ORIENTED_EDGE ( 'NONE', *, *, #219455, .F. ) ;
#133756=CARTESIAN_POINT ( 'NONE',  ( -23.25000000000000000, 45.99141771592758943, -256.5205054824189119 ) ) ;
#133779=EDGE_CURVE ( 'NONE', #24049, #237661, #55314, .T. ) ;
#133799=ORIENTED_EDGE ( 'NONE', *, *, #71201, .T. ) ;
#133844=ORIENTED_EDGE ( 'NONE', *, *, #199747, .F. ) ;
#133883=ORIENTED_EDGE ( 'NONE', *, *, #137221, .F. ) ;
#133917=DIRECTION ( 'NONE',  ( 0.000000000000000000, 0.8127272543710951647, -0.5826443254700255370 ) ) ;
#133923=CARTESIAN_POINT ( 'NONE',  ( -20.94999999999999929, 42.15997144203495139, -239.2817429668763793 ) ) ;
#133926=LINE ( 'NONE', #10140, #93341 ) ;
#133943=CARTESIAN_POINT ( 'NONE',  ( 22.49066049874202022, -3.113992299531016528, -228.1819822047424680 ) ) ;
#133944=LINE ( 'NONE', #213485, #111647 ) ;
#133986=ORIENTED_EDGE ( 'NONE', *, *, #250416, .T. ) ;
#133999=CARTESIAN_POINT ( 'NONE',  ( 21.53752568617667862, 10.24627015979879197, -227.7034273308927084 ) ) ;
#134030=LINE ( 'NONE', #3172, #99365 ) ;
#134044=CARTESIAN_POINT ( 'NONE',  ( 23.24999999999999645, 36.65892442174935439, -249.5511627012433848 ) ) ;
#134060=DIRECTION ( 'NONE',  ( -0.000000000000000000, -0.8814952561688430555, 0.4721928772777346239 ) ) ;
#134106=CARTESIAN_POINT ( 'NONE',  ( 23.24999999999999289, 12.71802988599559647, -223.5105008658000258 ) ) ;
#134108=EDGE_LOOP ( 'NONE', ( #200853, #46538, #242408, #26776, #83147 ) ) ;
#134115=CIRCLE ( 'NONE', #121681, 0.09999999999999939493 ) ;
#134150=EDGE_CURVE ( 'NONE', #253241, #43496, #37953, .T. ) ;
#134161=AXIS2_PLACEMENT_3D ( 'NONE', #88110, #236630, #114117 ) ;
#134248=DIRECTION ( 'NONE',  ( 1.000000000000000000, 0.000000000000000000, 0.000000000000000000 ) ) ;
#134274=AXIS2_PLACEMENT_3D ( 'NONE', #182818, #104508, #4149 ) ;
#134294=CIRCLE ( 'NONE', #88493, 7.900000000000007461 ) ;
#134392=ORIENTED_EDGE ( 'NONE', *, *, #136801, .F. ) ;
#134424=EDGE_LOOP ( 'NONE', ( #144221, #122535, #51405, #36006 ) ) ;
#134432=AXIS2_PLACEMENT_3D ( 'NONE', #146966, #210811, #132562 ) ;
#134435=ADVANCED_FACE ( 'NONE', ( #91177 ), #131585, .F. ) ;
#134442=DIRECTION ( 'NONE',  ( 0.000000000000000000, 0.8814952561688442767, -0.4721928772777324035 ) ) ;
#134444=ORIENTED_EDGE ( 'NONE', *, *, #23202, .T. ) ;
#134450=EDGE_CURVE ( 'NONE', #48019, #70426, #55127, .T. ) ;
#134456=FACE_OUTER_BOUND ( 'NONE', #85915, .T. ) ;
#134459=ORIENTED_EDGE ( 'NONE', *, *, #245555, .T. ) ;
#134482=VERTEX_POINT ( 'NONE', #16795 ) ;
#134508=ORIENTED_EDGE ( 'NONE', *, *, #42912, .F. ) ;
#134534=CARTESIAN_POINT ( 'NONE',  ( 23.14999999999999503, 23.42819724844704155, -229.2476443247244902 ) ) ;
#134571=LINE ( 'NONE', #15965, #249242 ) ;
#134581=VERTEX_POINT ( 'NONE', #257894 ) ;
#134610=SHAPE_REPRESENTATION_RELATIONSHIP ( 'NONE' , 'NONE' ,  #61981, #29580 ) ;
#134639=LINE ( 'NONE', #235061, #47749 ) ;
#134648=CARTESIAN_POINT ( 'NONE',  ( -20.94999999999999929, 18.14639373905162145, -237.6648341169113792 ) ) ;
#134650=ORIENTED_EDGE ( 'NONE', *, *, #193610, .T. ) ;
#134667=ORIENTED_EDGE ( 'NONE', *, *, #218316, .F. ) ;
#134695=ADVANCED_FACE ( 'NONE', ( #144387 ), #67442, .F. ) ;
#134699=DIRECTION ( 'NONE',  ( -1.000000000000000000, 0.000000000000000000, -0.000000000000000000 ) ) ;
#134719=AXIS2_PLACEMENT_3D ( 'NONE', #249867, #67380, #71254 ) ;
#134721=VECTOR ( 'NONE', #182305, 1000.000000000000000 ) ;
#134733=CARTESIAN_POINT ( 'NONE',  ( 18.49999999999999289, 33.98796489282361932, -236.2185561567993091 ) ) ;
#134734=EDGE_CURVE ( 'NONE', #62992, #167556, #222652, .T. ) ;
#134773=CARTESIAN_POINT ( 'NONE',  ( 20.94999999999999929, 34.98408343502854478, -248.6539962344157004 ) ) ;
#134779=VERTEX_POINT ( 'NONE', #51704 ) ;
#134783=ORIENTED_EDGE ( 'NONE', *, *, #82000, .T. ) ;
#134786=ADVANCED_FACE ( 'NONE', ( #189968 ), #187410, .F. ) ;
#134807=CARTESIAN_POINT ( 'NONE',  ( -21.55000000000000071, 21.48591740176965814, -233.0852932139783036 ) ) ;
#134827=VECTOR ( 'NONE', #44958, 1000.000000000000000 ) ;
#134857=ORIENTED_EDGE ( 'NONE', *, *, #251910, .F. ) ;
#134868=DIRECTION ( 'NONE',  ( 0.000000000000000000, 0.8814952561688432775, -0.4721928772777344019 ) ) ;
#134873=CARTESIAN_POINT ( 'NONE',  ( -23.25000000000000000, 19.97490019448090948, -235.9060780337186145 ) ) ;
#134908=ADVANCED_FACE ( 'NONE', ( #29638 ), #109125, .T. ) ;
#134967=AXIS2_PLACEMENT_3D ( 'NONE', #118690, #121282, #221591 ) ;
#134981=CARTESIAN_POINT ( 'NONE',  ( -23.15000000000000213, 25.94586868676353575, -241.5435999122864530 ) ) ;
#135014=AXIS2_PLACEMENT_3D ( 'NONE', #213977, #95307, #256897 ) ;
#135021=LINE ( 'NONE', #133756, #7422 ) ;
#135025=FACE_OUTER_BOUND ( 'NONE', #123484, .T. ) ;
#135068=ORIENTED_EDGE ( 'NONE', *, *, #213353, .F. ) ;
#135074=ORIENTED_EDGE ( 'NONE', *, *, #162010, .F. ) ;
#135088=DIRECTION ( 'NONE',  ( 0.000000000000000000, -0.4721928772777332917, -0.8814952561688437216 ) ) ;
#135093=ADVANCED_FACE ( 'NONE', ( #166276 ), #168856, .T. ) ;
#135098=DIRECTION ( 'NONE',  ( 0.000000000000000000, -0.8814952561688425003, 0.4721928772777359007 ) ) ;
#135114=CARTESIAN_POINT ( 'NONE',  ( -20.95000000000002416, 36.22724532936084074, -235.9903003947922002 ) ) ;
#135120=VERTEX_POINT ( 'NONE', #167555 ) ;
#135139=DIRECTION ( 'NONE',  ( 0.000000000000000000, 0.8814952561688437216, -0.4721928772777331806 ) ) ;
#135152=CYLINDRICAL_SURFACE ( 'NONE', #89283, 0.1000000000000013933 ) ;
#135158=EDGE_LOOP ( 'NONE', ( #131947, #101926, #243855, #29955 ) ) ;
#135160=DIRECTION ( 'NONE',  ( 0.000000000000000000, 0.000000000000000000, 1.000000000000000000 ) ) ;
#135169=CYLINDRICAL_SURFACE ( 'NONE', #180312, 0.09999999999999939493 ) ;
#135173=CARTESIAN_POINT ( 'NONE',  ( 18.59999999999999432, 14.85285025691667293, -236.4388300032497057 ) ) ;
#135175=CYLINDRICAL_SURFACE ( 'NONE', #184952, 0.09999999999999939493 ) ;
#135177=CARTESIAN_POINT ( 'NONE',  ( -23.15000000000000213, 36.65892442174935439, -249.5511627012433848 ) ) ;
#135182=EDGE_LOOP ( 'NONE', ( #242077, #144864, #27422 ) ) ;
#135188=CARTESIAN_POINT ( 'NONE',  ( -18.59999999999999787, 43.35377423437995503, -245.1717807829448930 ) ) ;
#135246=DIRECTION ( 'NONE',  ( -1.000000000000000000, -8.674042436075324885E-17, -1.619280515896126624E-16 ) ) ;
#135252=CARTESIAN_POINT ( 'NONE',  ( 23.14999999999998437, 7.128833340093095217, -233.7327013124392749 ) ) ;
#135255=AXIS2_PLACEMENT_3D ( 'NONE', #226543, #230423, #49213 ) ;
#135257=AXIS2_PLACEMENT_3D ( 'NONE', #182826, #44582, #4155 ) ;
#135300=DIRECTION ( 'NONE',  ( -0.000000000000000000, 0.8814952561688430555, -0.4721928772777346239 ) ) ;
#135324=DIRECTION ( 'NONE',  ( 0.000000000000000000, 0.8454177738465993297, 0.5341055959866553016 ) ) ;
#135384=ORIENTED_EDGE ( 'NONE', *, *, #219562, .F. ) ;
#135401=EDGE_CURVE ( 'NONE', #142601, #93118, #247039, .T. ) ;
#135422=AXIS2_PLACEMENT_3D ( 'NONE', #233227, #136649, #77959 ) ;
#135427=DIRECTION ( 'NONE',  ( 1.000000000000000000, 0.000000000000000000, 0.000000000000000000 ) ) ;
#135428=SPHERICAL_SURFACE ( 'NONE', #247575, 0.1000000000000000056 ) ;
#135459=ORIENTED_EDGE ( 'NONE', *, *, #187704, .F. ) ;
#135484=CARTESIAN_POINT ( 'NONE',  ( -22.39999999999999858, 12.62988036037870998, -223.4632815780722410 ) ) ;
#135498=CIRCLE ( 'NONE', #106442, 11.65000000000000391 ) ;
#135504=EDGE_CURVE ( 'NONE', #227159, #186480, #9425, .T. ) ;
#135519=ORIENTED_EDGE ( 'NONE', *, *, #80214, .T. ) ;
#135537=AXIS2_PLACEMENT_3D ( 'NONE', #151441, #113578, #131855 ) ;
#135550=AXIS2_PLACEMENT_3D ( 'NONE', #141232, #122962, #180363 ) ;
#135563=ADVANCED_FACE ( 'NONE', ( #177202 ), #196724, .F. ) ;
#135590=CARTESIAN_POINT ( 'NONE',  ( 20.95512820512820795, 22.89972396243220487, -230.1286587026982033 ) ) ;
#135594=EDGE_CURVE ( 'NONE', #33556, #236903, #113958, .T. ) ;
#135603=ORIENTED_EDGE ( 'NONE', *, *, #66136, .T. ) ;
#135611=AXIS2_PLACEMENT_3D ( 'NONE', #255987, #223000, #254710 ) ;
#135645=AXIS2_PLACEMENT_3D ( 'NONE', #225945, #145142, #102144 ) ;
#135649=DIRECTION ( 'NONE',  ( 0.000000000000000000, -0.8814952561688476074, 0.4721928772777262417 ) ) ;
#135652=DIRECTION ( 'NONE',  ( 1.000000000000000000, 0.000000000000000000, 0.000000000000000000 ) ) ;
#135660=FACE_OUTER_BOUND ( 'NONE', #247869, .T. ) ;
#135667=TOROIDAL_SURFACE ( 'NONE', #1816, 2.100000000000002309, 0.1000000000000000056 ) ;
#135678=DIRECTION ( 'NONE',  ( -1.000000000000000000, -0.000000000000000000, -0.000000000000000000 ) ) ;
#135682=EDGE_CURVE ( 'NONE', #235224, #257030, #234772, .T. ) ;
#135687=ORIENTED_EDGE ( 'NONE', *, *, #189191, .T. ) ;
#135699=DIRECTION ( 'NONE',  ( 0.7071067811865474617, 0.3338907855510734324, 0.6233112732207618523 ) ) ;
#135700=ORIENTED_EDGE ( 'NONE', *, *, #143648, .T. ) ;
#135701=FACE_OUTER_BOUND ( 'NONE', #70260, .T. ) ;
#135707=ORIENTED_EDGE ( 'NONE', *, *, #139614, .T. ) ;
#135733=ORIENTED_EDGE ( 'NONE', *, *, #37696, .T. ) ;
#135749=CARTESIAN_POINT ( 'NONE',  ( 20.58091095332355280, 18.80829090936573778, -229.7581893066683278 ) ) ;
#135760=CARTESIAN_POINT ( 'NONE',  ( 23.25000000000000000, 23.40438595358394736, -253.3416554127419431 ) ) ;
#135769=ORIENTED_EDGE ( 'NONE', *, *, #4276, .T. ) ;
#135784=VERTEX_POINT ( 'NONE', #143154 ) ;
#135815=CARTESIAN_POINT ( 'NONE',  ( 18.49999999999999289, 33.89981536720674171, -236.1713368690715527 ) ) ;
#135829=VERTEX_POINT ( 'NONE', #119325 ) ;
#135856=LINE ( 'NONE', #35532, #39207 ) ;
#135884=AXIS2_PLACEMENT_3D ( 'NONE', #254323, #234783, #114833 ) ;
#135889=DIRECTION ( 'NONE',  ( 1.000000000000000000, 0.000000000000000000, 0.000000000000000000 ) ) ;
#135898=FACE_OUTER_BOUND ( 'NONE', #149271, .T. ) ;
#135902=EDGE_CURVE ( 'NONE', #44729, #167145, #151781, .T. ) ;
#135907=AXIS2_PLACEMENT_3D ( 'NONE', #15385, #139129, #213557 ) ;
#135978=VERTEX_POINT ( 'NONE', #127026 ) ;
#135982=DIRECTION ( 'NONE',  ( 0.000000000000000000, -0.8814952561688429444, 0.4721928772777349570 ) ) ;
#135983=ORIENTED_EDGE ( 'NONE', *, *, #1437, .F. ) ;
#136014=DIRECTION ( 'NONE',  ( 0.000000000000000000, -0.8814952561688444987, 0.4721928772777320149 ) ) ;
#136021=VECTOR ( 'NONE', #244, 1000.000000000000000 ) ;
#136066=AXIS2_PLACEMENT_3D ( 'NONE', #69478, #231124, #52442 ) ;
#136071=CARTESIAN_POINT ( 'NONE',  ( -18.49372193242269802, 38.16337307575515325, -261.0689495423612243 ) ) ;
#136073=VERTEX_POINT ( 'NONE', #44927 ) ;
#136078=CONICAL_SURFACE ( 'NONE', #65374, 6.249999999999996447, 0.7853981633974431720 ) ;
#136079=CIRCLE ( 'NONE', #219308, 0.1000000000000019901 ) ;
#136082=ORIENTED_EDGE ( 'NONE', *, *, #60620, .F. ) ;
#136085=EDGE_LOOP ( 'NONE', ( #246701, #200120, #235832, #65228 ) ) ;
#136089=VERTEX_POINT ( 'NONE', #179939 ) ;
#136095=EDGE_CURVE ( 'NONE', #224941, #94319, #230886, .T. ) ;
#136111=AXIS2_PLACEMENT_3D ( 'NONE', #78072, #59775, #16846 ) ;
#136132=EDGE_CURVE ( 'NONE', #92509, #16880, #47495, .T. ) ;
#136144=LINE ( 'NONE', #119193, #58250 ) ;
#136154=FACE_OUTER_BOUND ( 'NONE', #43381, .T. ) ;
#136164=AXIS2_PLACEMENT_3D ( 'NONE', #222489, #141686, #25611 ) ;
#136173=EDGE_CURVE ( 'NONE', #191683, #168277, #10097, .T. ) ;
#136185=ADVANCED_FACE ( 'NONE', ( #37873 ), #117386, .T. ) ;
#136187=PLANE ( 'NONE',  #45588 ) ;
#136192=ORIENTED_EDGE ( 'NONE', *, *, #200438, .T. ) ;
#136242=CARTESIAN_POINT ( 'NONE',  ( -1.739115166359751170E-14, 31.44980407958350455, -233.5445995079518866 ) ) ;
#136251=DIRECTION ( 'NONE',  ( 0.000000000000000000, 0.8814952561688426114, -0.4721928772777353456 ) ) ;
#136276=EDGE_CURVE ( 'NONE', #195393, #50748, #226754, .T. ) ;
#136279=CARTESIAN_POINT ( 'NONE',  ( 21.05000000000000071, 20.42498087366621817, -235.1829032864613396 ) ) ;
#136290=DIRECTION ( 'NONE',  ( -1.000000000000000000, 0.000000000000000000, 0.000000000000000000 ) ) ;
#136363=CARTESIAN_POINT ( 'NONE',  ( -20.85000000000000142, 43.08613539620618837, -254.3146655184800409 ) ) ;
#136378=ORIENTED_EDGE ( 'NONE', *, *, #177467, .F. ) ;
#136472=ADVANCED_FACE ( 'NONE', ( #211049 ), #231909, .F. ) ;
#136476=ADVANCED_FACE ( 'NONE', ( #196601 ), #101838, .T. ) ;
#136477=DIRECTION ( 'NONE',  ( 0.000000000000000000, 0.8814952561688444987, -0.4721928772777320149 ) ) ;
#136499=CARTESIAN_POINT ( 'NONE',  ( 18.59999999999999432, 18.14639373905162145, -237.6648341169113792 ) ) ;
#136546=DIRECTION ( 'NONE',  ( 1.000000000000000000, -0.000000000000000000, -0.000000000000000000 ) ) ;
#136578=ORIENTED_EDGE ( 'NONE', *, *, #114162, .F. ) ;
#136616=CIRCLE ( 'NONE', #170010, 0.1999999999999997335 ) ;
#136627=DIRECTION ( 'NONE',  ( 0.000000000000000000, -0.8814952561688437216, 0.4721928772777334582 ) ) ;
#136639=ORIENTED_EDGE ( 'NONE', *, *, #148283, .F. ) ;
#136649=DIRECTION ( 'NONE',  ( -4.336808689941751101E-15, -0.03181660087581671820, 0.9994937237965574317 ) ) ;
#136665=EDGE_CURVE ( 'NONE', #218718, #142016, #105156, .T. ) ;
#136672=EDGE_CURVE ( 'NONE', #12413, #73105, #226952, .T. ) ;
#136684=CARTESIAN_POINT ( 'NONE',  ( -23.25000000000000000, -3.187427350888460076, -228.3200064793908837 ) ) ;
#136702=DIRECTION ( 'NONE',  ( 0.000000000000000000, -0.03181660087583042251, 0.9994937237965568766 ) ) ;
#136711=CARTESIAN_POINT ( 'NONE',  ( 21.14999999999999858, 22.98593783141595992, -230.0732594427593938 ) ) ;
#136728=EDGE_LOOP ( 'NONE', ( #109893, #28387, #166611 ) ) ;
#136745=EDGE_LOOP ( 'NONE', ( #43240, #224562, #185266, #15818 ) ) ;
#136781=ORIENTED_EDGE ( 'NONE', *, *, #140223, .T. ) ;
#136801=EDGE_CURVE ( 'NONE', #121993, #229490, #39720, .T. ) ;
#136863=EDGE_LOOP ( 'NONE', ( #234531, #238039, #200323, #170954 ) ) ;
#136913=CARTESIAN_POINT ( 'NONE',  ( 21.30000000000002558, 7.128833340093095217, -233.7327013124392749 ) ) ;
#136922=VERTEX_POINT ( 'NONE', #40802 ) ;
#136938=CARTESIAN_POINT ( 'NONE',  ( -22.39999999999999858, -3.275978944802467652, -228.2735455795363748 ) ) ;
#136956=CARTESIAN_POINT ( 'NONE',  ( -18.52328366898031931, 38.02497047517800155, -261.2215128630973027 ) ) ;
#136970=CIRCLE ( 'NONE', #128786, 0.1000000000000108025 ) ;
#136976=TOROIDAL_SURFACE ( 'NONE', #24009, 7.800000000000000711, 0.1000000000000000056 ) ;
#136977=VERTEX_POINT ( 'NONE', #104558 ) ;
#136999=CARTESIAN_POINT ( 'NONE',  ( 21.06089410995844702, 22.94958222544119764, -230.0402814468934594 ) ) ;
#137005=CIRCLE ( 'NONE', #16226, 0.1000000000000013933 ) ;
#137006=ORIENTED_EDGE ( 'NONE', *, *, #223574, .F. ) ;
#137015=EDGE_LOOP ( 'NONE', ( #235171, #142852, #95737, #256951 ) ) ;
#137042=VECTOR ( 'NONE', #190256, 1000.000000000000000 ) ;
#137046=VECTOR ( 'NONE', #107318, 1000.000000000000227 ) ;
#137063=DIRECTION ( 'NONE',  ( 0.000000000000000000, 0.8814952561688430555, -0.4721928772777346239 ) ) ;
#137073=ORIENTED_EDGE ( 'NONE', *, *, #79309, .T. ) ;
#137100=VERTEX_POINT ( 'NONE', #227094 ) ;
#137117=CYLINDRICAL_SURFACE ( 'NONE', #226220, 2.000000000000003553 ) ;
#137151=VERTEX_POINT ( 'NONE', #213967 ) ;
#137152=DIRECTION ( 'NONE',  ( -1.000000000000000000, 0.000000000000000000, 0.000000000000000000 ) ) ;
#137156=DIRECTION ( 'NONE',  ( 0.000000000000000000, 0.5341055959866798375, -0.8454177738465836756 ) ) ;
#137174=ORIENTED_EDGE ( 'NONE', *, *, #143648, .F. ) ;
#137188=CARTESIAN_POINT ( 'NONE',  ( -23.25000000000000000, -8.729782940176420425, -238.4538547387928986 ) ) ;
#137211=ADVANCED_FACE ( 'NONE', ( #152738 ), #253074, .T. ) ;
#137212=ADVANCED_FACE ( 'NONE', ( #250513 ), #211399, .F. ) ;
#137221=EDGE_CURVE ( 'NONE', #91231, #193742, #74496, .T. ) ;
#137226=CARTESIAN_POINT ( 'NONE',  ( 20.04142135623731136, 34.50923130584770604, -235.0700073140421864 ) ) ;
#137233=EDGE_LOOP ( 'NONE', ( #102128, #187798, #202478, #162432 ) ) ;
#137246=CIRCLE ( 'NONE', #162209, 0.1000000000000012546 ) ;
#137260=CARTESIAN_POINT ( 'NONE',  ( 22.49436431346199683, 12.57088205413893434, -223.4317334472834489 ) ) ;
#137293=CIRCLE ( 'NONE', #91516, 4.050000000000005151 ) ;
#137315=FACE_OUTER_BOUND ( 'NONE', #25364, .T. ) ;
#137356=CIRCLE ( 'NONE', #16597, 0.09999999999999568956 ) ;
#137393=ADVANCED_FACE ( 'NONE', ( #142121 ), #178727, .F. ) ;
#137434=FACE_OUTER_BOUND ( 'NONE', #44996, .T. ) ;
#137435=ORIENTED_EDGE ( 'NONE', *, *, #29543, .F. ) ;
#137480=DIRECTION ( 'NONE',  ( 0.000000000000000000, 0.2262561206234166566, 0.9740678456249555195 ) ) ;
#137482=CARTESIAN_POINT ( 'NONE',  ( -18.42554971533677133, 8.849916218358112374, -245.4285586339724716 ) ) ;
#137514=CIRCLE ( 'NONE', #245694, 12.77500000000000924 ) ;
#137518=DIRECTION ( 'NONE',  ( 0.000000000000000000, -0.8814952561688431665, 0.4721928772777346794 ) ) ;
#137531=ADVANCED_FACE ( 'NONE', ( #53299 ), #174585, .T. ) ;
#137538=VERTEX_POINT ( 'NONE', #31211 ) ;
#137553=ORIENTED_EDGE ( 'NONE', *, *, #139127, .T. ) ;
#137591=DIRECTION ( 'NONE',  ( -1.000000000000000000, 0.000000000000000000, 0.000000000000000000 ) ) ;
#137608=ORIENTED_EDGE ( 'NONE', *, *, #215335, .F. ) ;
#137618=DIRECTION ( 'NONE',  ( 1.000000000000000000, 1.394253735153569469E-16, 2.602809386958778209E-16 ) ) ;
#137621=EDGE_LOOP ( 'NONE', ( #213902, #33097, #236171, #109165 ) ) ;
#137635=FACE_OUTER_BOUND ( 'NONE', #58827, .T. ) ;
#137649=( BOUNDED_SURFACE ( )  B_SPLINE_SURFACE ( 3, 2, ( 
 ( #131257, #65195, #84719 ),
 ( #185147, #50414, #163040 ),
 ( #164313, #71314, #243829 ),
 ( #249929, #5194, #146010 ) ),
 .UNSPECIFIED., .F., .F., .F. ) 
 B_SPLINE_SURFACE_WITH_KNOTS ( ( 4, 4 ),
 ( 3, 3 ),
 ( 0.0002700421466196672679, 0.0004789321604330734573 ),
 ( 0.000000000000000000, 1.000000000000000000 ),
 .UNSPECIFIED. ) 
 GEOMETRIC_REPRESENTATION_ITEM ( )  RATIONAL_B_SPLINE_SURFACE ( (
 ( 1.000000000000000000, 0.7071067811865475727, 1.000000000000000000),
 ( 1.000000000000000000, 0.7163411249512025014, 1.000000000000000000),
 ( 1.000000000000000000, 0.7221957104841917330, 1.000000000000000000),
 ( 1.000000000000000000, 0.7250110520819895710, 1.000000000000000000) ) ) 
 REPRESENTATION_ITEM ( '' )  SURFACE ( )  );
#137651=ORIENTED_EDGE ( 'NONE', *, *, #51761, .T. ) ;
#137655=CARTESIAN_POINT ( 'NONE',  ( 21.05000000000000071, 28.37802281961254991, -258.4449340416662722 ) ) ;
#137667=VERTEX_POINT ( 'NONE', #137944 ) ;
#137685=DIRECTION ( 'NONE',  ( 0.000000000000000000, 0.4721928772777346239, 0.8814952561688430555 ) ) ;
#137747=DIRECTION ( 'NONE',  ( -1.000000000000000000, -0.000000000000000000, -0.000000000000000000 ) ) ;
#137763=VECTOR ( 'NONE', #183355, 1000.000000000000000 ) ;
#137790=DIRECTION ( 'NONE',  ( 1.000000000000000000, 1.394253735153569469E-16, 2.602809386958778209E-16 ) ) ;
#137803=CARTESIAN_POINT ( 'NONE',  ( -18.59999999999999787, 36.65892442174935439, -249.5511627012433848 ) ) ;
#137849=TOROIDAL_SURFACE ( 'NONE', #67125, 0.2000000000000000111, 0.1000000000000000056 ) ;
#137865=FACE_OUTER_BOUND ( 'NONE', #121788, .T. ) ;
#137868=CARTESIAN_POINT ( 'NONE',  ( 20.95429693346636313, 18.77218889732035834, -228.0090229569942721 ) ) ;
#137872=CARTESIAN_POINT ( 'NONE',  ( -21.05000000000000071, 28.50120599808395028, -258.2149742250584268 ) ) ;
#137889=CARTESIAN_POINT ( 'NONE',  ( -18.50000000000000000, 42.92545512184477730, -254.1955779480491344 ) ) ;
#137891=EDGE_LOOP ( 'NONE', ( #185166, #141037, #204715, #133747 ) ) ;
#137897=AXIS2_PLACEMENT_3D ( 'NONE', #54588, #231974, #216221 ) ;
#137932=LINE ( 'NONE', #217464, #127889 ) ;
#137944=CARTESIAN_POINT ( 'NONE',  ( -20.85000000000000142, 43.00579525902548994, -254.2551217332645876 ) ) ;
#137952=CARTESIAN_POINT ( 'NONE',  ( 20.94999999999999574, 18.92285928089247804, -233.3572654221044900 ) ) ;
#137960=ORIENTED_EDGE ( 'NONE', *, *, #242373, .F. ) ;
#137995=AXIS2_PLACEMENT_3D ( 'NONE', #158728, #94861, #218652 ) ;
#138009=ORIENTED_EDGE ( 'NONE', *, *, #228526, .T. ) ;
#138036=ORIENTED_EDGE ( 'NONE', *, *, #217492, .T. ) ;
#138074=PLANE ( 'NONE',  #140424 ) ;
#138085=EDGE_CURVE ( 'NONE', #21212, #123927, #126122, .T. ) ;
#138087=AXIS2_PLACEMENT_3D ( 'NONE', #38423, #117953, #84894 ) ;
#138110=ORIENTED_EDGE ( 'NONE', *, *, #124571, .F. ) ;
#138144=DIRECTION ( 'NONE',  ( 1.000000000000000000, 1.394253735153569469E-16, 2.602809386958778209E-16 ) ) ;
#138149=ORIENTED_EDGE ( 'NONE', *, *, #106749, .F. ) ;
#138193=ORIENTED_EDGE ( 'NONE', *, *, #214076, .T. ) ;
#138195=AXIS2_PLACEMENT_3D ( 'NONE', #22783, #240520, #136251 ) ;
#138214=EDGE_CURVE ( 'NONE', #54594, #41070, #65814, .T. ) ;
#138270=ORIENTED_EDGE ( 'NONE', *, *, #231237, .F. ) ;
#138272=CONICAL_SURFACE ( 'NONE', #29988, 4.299999999999964295, 0.7853981633974466137 ) ;
#138276=VERTEX_POINT ( 'NONE', #128370 ) ;
#138297=ADVANCED_FACE ( 'NONE', ( #151801 ), #18182, .F. ) ;
#138302=ORIENTED_EDGE ( 'NONE', *, *, #245738, .F. ) ;
#138348=CARTESIAN_POINT ( 'NONE',  ( 20.95083306685154056, 18.81202456654950339, -229.8754792376871023 ) ) ;
#138364=FACE_OUTER_BOUND ( 'NONE', #131658, .T. ) ;
#138417=AXIS2_PLACEMENT_3D ( 'NONE', #4100, #103181, #185309 ) ;
#138448=DIRECTION ( 'NONE',  ( 0.000000000000000000, -0.8814952561688444987, 0.4721928772777320149 ) ) ;
#138462=AXIS2_PLACEMENT_3D ( 'NONE', #115649, #224986, #187194 ) ;
#138495=DIRECTION ( 'NONE',  ( 1.000000000000000000, 0.000000000000000000, 0.000000000000000000 ) ) ;
#138503=CARTESIAN_POINT ( 'NONE',  ( -20.94999999999999929, 46.33035574435032089, -243.0552603638194853 ) ) ;
#138508=AXIS2_PLACEMENT_3D ( 'NONE', #251319, #229215, #89674 ) ;
#138517=AXIS2_PLACEMENT_3D ( 'NONE', #92446, #187732, #89879 ) ;
#138534=AXIS2_PLACEMENT_3D ( 'NONE', #89838, #91134, #254046 ) ;
#138543=VECTOR ( 'NONE', #141795, 1000.000000000000000 ) ;
#138557=ORIENTED_EDGE ( 'NONE', *, *, #113268, .F. ) ;
#138572=DIRECTION ( 'NONE',  ( 1.000000000000000000, 0.000000000000000000, 0.000000000000000000 ) ) ;
#138578=FACE_BOUND ( 'NONE', #106241, .T. ) ;
#138614=AXIS2_PLACEMENT_3D ( 'NONE', #226818, #70353, #109426 ) ;
#138617=ADVANCED_FACE ( 'NONE', ( #194154 ), #143258, .T. ) ;
#138630=ORIENTED_EDGE ( 'NONE', *, *, #15503, .T. ) ;
#138696=VECTOR ( 'NONE', #13439, 1000.000000000000000 ) ;
#138697=CARTESIAN_POINT ( 'NONE',  ( 20.94999999999999929, 23.49882452903949570, -253.1653563615082305 ) ) ;
#138699=DIRECTION ( 'NONE',  ( 0.000000000000000000, 0.8814952561688476074, -0.4721928772777262417 ) ) ;
#138707=EDGE_CURVE ( 'NONE', #45529, #134779, #105631, .T. ) ;
#138714=VERTEX_POINT ( 'NONE', #230706 ) ;
#138809=LINE ( 'NONE', #39789, #57678 ) ;
#138827=EDGE_CURVE ( 'NONE', #103521, #157381, #55735, .T. ) ;
#138830=DIRECTION ( 'NONE',  ( -1.000000000000000000, -0.000000000000000000, -0.000000000000000000 ) ) ;
#138837=AXIS2_PLACEMENT_3D ( 'NONE', #19095, #786, #79046 ) ;
#138872=EDGE_LOOP ( 'NONE', ( #141805, #224968, #123756, #226868 ) ) ;
#138895=EDGE_CURVE ( 'NONE', #198415, #129019, #159842, .T. ) ;
#138904=ORIENTED_EDGE ( 'NONE', *, *, #12161, .T. ) ;
#138925=EDGE_LOOP ( 'NONE', ( #80136, #1535, #67190, #181841 ) ) ;
#138956=PLANE ( 'NONE',  #153294 ) ;
#138960=VERTEX_POINT ( 'NONE', #46583 ) ;
#138970=EDGE_CURVE ( 'NONE', #86057, #130702, #67445, .T. ) ;
#138984=EDGE_CURVE ( 'NONE', #72339, #253511, #167867, .T. ) ;
#139017=CARTESIAN_POINT ( 'NONE',  ( -21.05000000000000071, 36.02918351690955490, -236.0543695120161374 ) ) ;
#139064=DIRECTION ( 'NONE',  ( 1.000000000000000000, 0.000000000000000000, 0.000000000000000000 ) ) ;
#139073=ORIENTED_EDGE ( 'NONE', *, *, #86418, .F. ) ;
#139092=DIRECTION ( 'NONE',  ( 0.000000000000000000, -0.8814952561688476074, 0.4721928772777262417 ) ) ;
#139105=LINE ( 'NONE', #140418, #204276 ) ;
#139127=EDGE_CURVE ( 'NONE', #120155, #201984, #113649, .T. ) ;
#139129=DIRECTION ( 'NONE',  ( 1.000000000000000000, 1.394253735153569469E-16, 2.602809386958778209E-16 ) ) ;
#139132=DIRECTION ( 'NONE',  ( -0.000000000000000000, 0.8814952561688430555, -0.4721928772777346239 ) ) ;
#139151=DIRECTION ( 'NONE',  ( -0.000000000000000000, 0.4721928772777346239, 0.8814952561688430555 ) ) ;
#139170=CIRCLE ( 'NONE', #26234, 0.1000000000000013933 ) ;
#139199=CARTESIAN_POINT ( 'NONE',  ( -23.25000000000000000, 33.22109292269086467, -247.7096104798602312 ) ) ;
#139206=EDGE_CURVE ( 'NONE', #87394, #170331, #56836, .T. ) ;
#139218=CIRCLE ( 'NONE', #185041, 0.09999999999999438505 ) ;
#139226=CYLINDRICAL_SURFACE ( 'NONE', #231468, 0.09999999999999939493 ) ;
#139232=DIRECTION ( 'NONE',  ( -1.000000000000000000, -0.000000000000000000, -0.000000000000000000 ) ) ;
#139235=CARTESIAN_POINT ( 'NONE',  ( 21.05000000000000071, 28.08470566095357057, -239.2860081655328770 ) ) ;
#139296=CIRCLE ( 'NONE', #89427, 7.900000000000013678 ) ;
#139300=CARTESIAN_POINT ( 'NONE',  ( -21.05000000000000071, 18.18127959618848166, -237.5711165786817389 ) ) ;
#139312=DIRECTION ( 'NONE',  ( 0.000000000000000000, 0.8814952561688444987, -0.4721928772777320149 ) ) ;
#139314=AXIS2_PLACEMENT_3D ( 'NONE', #88023, #167613, #247112 ) ;
#139319=FACE_OUTER_BOUND ( 'NONE', #67777, .T. ) ;
#139349=ORIENTED_EDGE ( 'NONE', *, *, #232288, .F. ) ;
#139389=TOROIDAL_SURFACE ( 'NONE', #214407, 0.2000000000000000111, 0.1000000000000000056 ) ;
#139411=CIRCLE ( 'NONE', #10264, 0.09999999999999939493 ) ;
#139417=ORIENTED_EDGE ( 'NONE', *, *, #252410, .T. ) ;
#139431=AXIS2_PLACEMENT_3D ( 'NONE', #214052, #35454, #46946 ) ;
#139436=ORIENTED_EDGE ( 'NONE', *, *, #168069, .T. ) ;
#139437=CARTESIAN_POINT ( 'NONE',  ( 23.14999999999999858, 7.128833340093095217, -233.7327013124392749 ) ) ;
#139443=AXIS2_PLACEMENT_3D ( 'NONE', #195343, #11565, #114497 ) ;
#139457=CYLINDRICAL_SURFACE ( 'NONE', #99405, 0.09999999999999986677 ) ;
#139487=CARTESIAN_POINT ( 'NONE',  ( -23.15000000000000213, 23.68770167995059595, -252.8127582590406348 ) ) ;
#139518=DIRECTION ( 'NONE',  ( 1.000000000000000000, 0.000000000000000000, 0.000000000000000000 ) ) ;
#139534=EDGE_LOOP ( 'NONE', ( #189047, #41179, #176660, #61992 ) ) ;
#139537=VECTOR ( 'NONE', #241969, 1000.000000000000000 ) ;
#139548=EDGE_CURVE ( 'NONE', #100199, #249188, #159631, .T. ) ;
#139602=DIRECTION ( 'NONE',  ( 0.000000000000000000, -0.4721928772777346794, -0.8814952561688431665 ) ) ;
#139608=DIRECTION ( 'NONE',  ( 0.000000000000000000, -0.9994937237965558774, -0.03181660087586650476 ) ) ;
#139614=EDGE_CURVE ( 'NONE', #224437, #101747, #17960, .T. ) ;
#139684=CARTESIAN_POINT ( 'NONE',  ( 18.52928932188133970, 33.71149860592453251, -236.3111109633099716 ) ) ;
#139732=ORIENTED_EDGE ( 'NONE', *, *, #118918, .T. ) ;
#139742=CARTESIAN_POINT ( 'NONE',  ( -20.94999999999999929, 43.18640298906419162, -245.2812653309023574 ) ) ;
#139761=CARTESIAN_POINT ( 'NONE',  ( -20.64999999999999858, 23.45160524131172508, -253.2535058871250726 ) ) ;
#139764=DIRECTION ( 'NONE',  ( 3.265361837132812600E-16, -0.4721928772777346239, -0.8814952561688430555 ) ) ;
#139771=CARTESIAN_POINT ( 'NONE',  ( -22.57320508075687115, 12.67709964810647882, -223.3751320524553705 ) ) ;
#139782=EDGE_CURVE ( 'NONE', #149025, #124845, #21259, .T. ) ;
#139807=EDGE_CURVE ( 'NONE', #39875, #72959, #18160, .T. ) ;
#139817=EDGE_CURVE ( 'NONE', #240363, #67785, #218053, .T. ) ;
#139854=CIRCLE ( 'NONE', #214875, 0.1000000000000013933 ) ;
#139866=ORIENTED_EDGE ( 'NONE', *, *, #87265, .F. ) ;
#139897=ORIENTED_EDGE ( 'NONE', *, *, #145341, .T. ) ;
#139898=EDGE_CURVE ( 'NONE', #101747, #137667, #107159, .T. ) ;
#139908=ORIENTED_EDGE ( 'NONE', *, *, #79868, .F. ) ;
#139930=DIRECTION ( 'NONE',  ( 1.000000000000000000, 0.000000000000000000, 0.000000000000000000 ) ) ;
#139933=EDGE_CURVE ( 'NONE', #9735, #24478, #22469, .T. ) ;
#139942=DIRECTION ( 'NONE',  ( -1.000000000000000000, 0.000000000000000000, 0.000000000000000000 ) ) ;
#139998=VERTEX_POINT ( 'NONE', #228416 ) ;
#140003=CARTESIAN_POINT ( 'NONE',  ( 20.94999999999999929, 20.42498087366621817, -235.1829032864613396 ) ) ;
#140023=EDGE_CURVE ( 'NONE', #104319, #102316, #163906, .T. ) ;
#140045=AXIS2_PLACEMENT_3D ( 'NONE', #148045, #105010, #28116 ) ;
#140061=AXIS2_PLACEMENT_3D ( 'NONE', #151880, #133567, #11054 ) ;
#140076=DIRECTION ( 'NONE',  ( 0.000000000000000000, 0.8814952561688476074, -0.4721928772777262417 ) ) ;
#140139=ADVANCED_FACE ( 'NONE', ( #216532 ), #117443, .F. ) ;
#140163=DIRECTION ( 'NONE',  ( 4.239556034732055511E-17, 0.8127272543710951647, -0.5826443254700257590 ) ) ;
#140172=DIRECTION ( 'NONE',  ( 1.000000000000000000, -0.000000000000000000, -0.000000000000000000 ) ) ;
#140186=ORIENTED_EDGE ( 'NONE', *, *, #39021, .F. ) ;
#140211=ORIENTED_EDGE ( 'NONE', *, *, #46754, .F. ) ;
#140213=CIRCLE ( 'NONE', #215264, 0.1000000000000013933 ) ;
#140223=EDGE_CURVE ( 'NONE', #81229, #218397, #5842, .T. ) ;
#140244=CARTESIAN_POINT ( 'NONE',  ( -18.51991288638472000, 8.990547036368365497, -245.3850893028505595 ) ) ;
#140250=EDGE_LOOP ( 'NONE', ( #139417, #16870, #139866, #233070 ) ) ;
#140267=AXIS2_PLACEMENT_3D ( 'NONE', #31724, #250726, #133366 ) ;
#140284=ADVANCED_FACE ( 'NONE', ( #200833 ), #164281, .F. ) ;
#140303=CARTESIAN_POINT ( 'NONE',  ( -23.15000000000000213, 24.12844930803501597, -253.0488546976795021 ) ) ;
#140307=DIRECTION ( 'NONE',  ( -1.000000000000000000, 0.000000000000000000, 0.000000000000000000 ) ) ;
#140381=CYLINDRICAL_SURFACE ( 'NONE', #194840, 0.1000000000000075273 ) ;
#140392=VECTOR ( 'NONE', #152187, 1000.000000000000000 ) ;
#140396=EDGE_CURVE ( 'NONE', #185172, #217355, #229390, .T. ) ;
#140401=AXIS2_PLACEMENT_3D ( 'NONE', #133510, #116526, #17416 ) ;
#140405=ORIENTED_EDGE ( 'NONE', *, *, #85734, .T. ) ;
#140418=CARTESIAN_POINT ( 'NONE',  ( 20.94999999999999574, 18.89897916088800756, -232.6070900604709379 ) ) ;
#140420=DIRECTION ( 'NONE',  ( 1.000000000000000000, 0.000000000000000000, 0.000000000000000000 ) ) ;
#140422=ORIENTED_EDGE ( 'NONE', *, *, #250407, .T. ) ;
#140424=AXIS2_PLACEMENT_3D ( 'NONE', #157704, #152557, #217601 ) ;
#140437=CARTESIAN_POINT ( 'NONE',  ( -21.09107601085565520, 10.09916211269090880, -228.1044125031166061 ) ) ;
#140447=CARTESIAN_POINT ( 'NONE',  ( -20.54999999999999716, 29.07070048091676995, -242.7637123387158624 ) ) ;
#140465=ORIENTED_EDGE ( 'NONE', *, *, #194627, .F. ) ;
#140477=CARTESIAN_POINT ( 'NONE',  ( -20.94999999999999929, 14.09264586382695938, -237.4630250429333671 ) ) ;
#140480=DIRECTION ( 'NONE',  ( 0.000000000000000000, -0.8814952561688430555, 0.4721928772777346239 ) ) ;
#140482=CARTESIAN_POINT ( 'NONE',  ( 21.46681500598086956, 1.083969783934416675, -230.4946333871058926 ) ) ;
#140505=AXIS2_PLACEMENT_3D ( 'NONE', #23298, #81917, #161518 ) ;
#140517=CARTESIAN_POINT ( 'NONE',  ( 19.75857864376268935, 34.44688795055758135, -235.1500552906961730 ) ) ;
#140595=AXIS2_PLACEMENT_3D ( 'NONE', #227548, #48907, #187165 ) ;
#140599=VERTEX_POINT ( 'NONE', #204036 ) ;
#140654=VERTEX_POINT ( 'NONE', #167513 ) ;
#140678=ADVANCED_FACE ( 'NONE', ( #172673 ), #126856, .T. ) ;
#140685=ORIENTED_EDGE ( 'NONE', *, *, #17983, .F. ) ;
#140689=LINE ( 'NONE', #220247, #196017 ) ;
#140705=DIRECTION ( 'NONE',  ( 0.000000000000000000, 0.8814952561688449428, -0.4721928772777310157 ) ) ;
#140706=LINE ( 'NONE', #198117, #149904 ) ;
#140724=DIRECTION ( 'NONE',  ( 0.000000000000000000, -0.4721928772777402861, -0.8814952561688399468 ) ) ;
#140779=ORIENTED_EDGE ( 'NONE', *, *, #115565, .T. ) ;
#140802=CARTESIAN_POINT ( 'NONE',  ( -20.54999999999999716, 27.82649702422227733, -239.8850763025288870 ) ) ;
#140815=CARTESIAN_POINT ( 'NONE',  ( -1.820710678118658388, 24.16915171043284261, -254.1248771717017974 ) ) ;
#140816=B_SPLINE_CURVE_WITH_KNOTS ( 'NONE', 3,
 ( #13782, #71206, #172904, #213252, #170337, #210695 ),
 .UNSPECIFIED., .F., .F.,
 ( 4, 2, 4 ),
 ( 0.000000000000000000, 0.0001568709654583473091, 0.0003137419309166946182 ),
 .UNSPECIFIED. ) ;
#140832=DIRECTION ( 'NONE',  ( 1.000000000000000000, 1.394253735153569469E-16, 2.602809386958778209E-16 ) ) ;
#140834=CARTESIAN_POINT ( 'NONE',  ( -18.50596464788227635, 46.37740828070796084, -243.0652246697500800 ) ) ;
#140845=DIRECTION ( 'NONE',  ( 1.000000000000000000, 0.000000000000000000, 0.000000000000000000 ) ) ;
#140857=EDGE_CURVE ( 'NONE', #234336, #239412, #56497, .T. ) ;
#140872=DIRECTION ( 'NONE',  ( 1.836970198721029441E-16, -0.4721928772777346239, -0.8814952561688430555 ) ) ;
#140884=VERTEX_POINT ( 'NONE', #216872 ) ;
#140913=VERTEX_POINT ( 'NONE', #215585 ) ;
#140926=CYLINDRICAL_SURFACE ( 'NONE', #113299, 12.87500000000000178 ) ;
#140952=ORIENTED_EDGE ( 'NONE', *, *, #158030, .F. ) ;
#140999=ORIENTED_EDGE ( 'NONE', *, *, #8237, .F. ) ;
#141033=CIRCLE ( 'NONE', #53530, 12.87500000000000178 ) ;
#141037=ORIENTED_EDGE ( 'NONE', *, *, #230586, .F. ) ;
#141038=EDGE_CURVE ( 'NONE', #250639, #216812, #181229, .T. ) ;
#141040=AXIS2_PLACEMENT_3D ( 'NONE', #150349, #231184, #49943 ) ;
#141071=CARTESIAN_POINT ( 'NONE',  ( 20.94999999999999574, 18.27667581256378071, -237.6066273148655057 ) ) ;
#141075=ORIENTED_EDGE ( 'NONE', *, *, #140, .T. ) ;
#141115=DIRECTION ( 'NONE',  ( 0.000000000000000000, -0.8814952561688476074, 0.4721928772777262417 ) ) ;
#141177=DIRECTION ( 'NONE',  ( 0.000000000000000000, -0.8814952561688429444, 0.4721928772777349570 ) ) ;
#141193=LINE ( 'NONE', #143746, #217965 ) ;
#141219=EDGE_LOOP ( 'NONE', ( #78074, #99571, #240640, #228152 ) ) ;
#141223=DIRECTION ( 'NONE',  ( 0.000000000000000000, 0.8814952561688476074, -0.4721928772777262417 ) ) ;
#141225=ORIENTED_EDGE ( 'NONE', *, *, #233730, .F. ) ;
#141227=EDGE_LOOP ( 'NONE', ( #170164, #72151, #55931, #34151 ) ) ;
#141232=CARTESIAN_POINT ( 'NONE',  ( 22.39999999999999503, -3.187427350888460076, -228.3200064793908837 ) ) ;
#141283=AXIS2_PLACEMENT_3D ( 'NONE', #80022, #216984, #237850 ) ;
#141288=ORIENTED_EDGE ( 'NONE', *, *, #256562, .F. ) ;
#141314=ADVANCED_FACE ( 'NONE', ( #82170 ), #48205, .F. ) ;
#141354=CARTESIAN_POINT ( 'NONE',  ( -18.39999999999999858, 8.841736820195469804, -245.4273993276876240 ) ) ;
#141369=CARTESIAN_POINT ( 'NONE',  ( -20.64999999999999858, 20.06933876993645782, -235.7297789824848451 ) ) ;
#141375=DIRECTION ( 'NONE',  ( 0.000000000000000000, 0.8814952561688437216, -0.4721928772777332362 ) ) ;
#141412=ADVANCED_FACE ( 'NONE', ( #163050 ), #87321, .F. ) ;
#141457=CIRCLE ( 'NONE', #153997, 7.800000000000003375 ) ;
#141460=DIRECTION ( 'NONE',  ( 0.000000000000000000, 0.8814952561688390587, -0.4721928772777420624 ) ) ;
#141462=CARTESIAN_POINT ( 'NONE',  ( -18.50000000000000000, -7.714568254029292582, -236.5586399380299270 ) ) ;
#141500=EDGE_CURVE ( 'NONE', #218982, #50959, #256326, .T. ) ;
#141501=ORIENTED_EDGE ( 'NONE', *, *, #60887, .T. ) ;
#141519=FACE_OUTER_BOUND ( 'NONE', #86487, .T. ) ;
#141541=ADVANCED_FACE ( 'NONE', ( #91194 ), #132896, .T. ) ;
#141549=ORIENTED_EDGE ( 'NONE', *, *, #232815, .T. ) ;
#141561=EDGE_CURVE ( 'NONE', #84465, #50748, #197946, .T. ) ;
#141574=DIRECTION ( 'NONE',  ( 1.000000000000000000, 1.394253735153569469E-16, 2.602809386958778209E-16 ) ) ;
#141649=DIRECTION ( 'NONE',  ( 1.000000000000000000, 0.000000000000000000, 0.000000000000000000 ) ) ;
#141659=ORIENTED_EDGE ( 'NONE', *, *, #194260, .T. ) ;
#141663=EDGE_LOOP ( 'NONE', ( #127793, #123770, #103806, #113680, #179228, #136781, #20469, #89473, #93907, #223674, #241082 ) ) ;
#141682=EDGE_LOOP ( 'NONE', ( #9512, #161453, #196808, #202417 ) ) ;
#141686=DIRECTION ( 'NONE',  ( 1.875376730785738212E-16, -0.4721928772777346239, -0.8814952561688430555 ) ) ;
#141691=CIRCLE ( 'NONE', #120887, 0.09999999999999939493 ) ;
#141739=AXIS2_PLACEMENT_3D ( 'NONE', #214456, #57941, #193629 ) ;
#141753=VERTEX_POINT ( 'NONE', #164007 ) ;
#141762=DIRECTION ( 'NONE',  ( 0.000000000000000000, 0.4721928772777346239, 0.8814952561688430555 ) ) ;
#141763=CARTESIAN_POINT ( 'NONE',  ( 21.05000000000000071, 28.50120599808395028, -258.2149742250584268 ) ) ;
#141795=DIRECTION ( 'NONE',  ( 0.000000000000000000, 0.8814952561688430555, -0.4721928772777346239 ) ) ;
#141805=ORIENTED_EDGE ( 'NONE', *, *, #222249, .T. ) ;
#141806=ADVANCED_FACE ( 'NONE', ( #126137 ), #203120, .T. ) ;
#141809=TOROIDAL_SURFACE ( 'NONE', #29434, 0.2000000000000000111, 0.1000000000000000056 ) ;
#141812=CARTESIAN_POINT ( 'NONE',  ( 23.14999999999998437, 9.041214493067920799, -230.1626455249554795 ) ) ;
#141820=VERTEX_POINT ( 'NONE', #63610 ) ;
#141833=CARTESIAN_POINT ( 'NONE',  ( -18.59999999999999787, 23.34004772283014972, -229.2004250369967338 ) ) ;
#141834=ORIENTED_EDGE ( 'NONE', *, *, #180699, .T. ) ;
#141841=ORIENTED_EDGE ( 'NONE', *, *, #69333, .T. ) ;
#141881=AXIS2_PLACEMENT_3D ( 'NONE', #158667, #236883, #176945 ) ;
#141938=FACE_OUTER_BOUND ( 'NONE', #33276, .T. ) ;
#141990=CARTESIAN_POINT ( 'NONE',  ( -21.05000000000000071, 35.97645343225767789, -235.9694016464868298 ) ) ;
#142008=AXIS2_PLACEMENT_3D ( 'NONE', #32050, #91986, #213207 ) ;
#142016=VERTEX_POINT ( 'NONE', #152167 ) ;
#142035=ORIENTED_EDGE ( 'NONE', *, *, #223667, .T. ) ;
#142043=ADVANCED_FACE ( 'NONE', ( #150852 ), #91295, .T. ) ;
#142049=DIRECTION ( 'NONE',  ( 0.7071067811865473507, 0.3338907855510733769, 0.6233112732207618523 ) ) ;
#142059=FACE_BOUND ( 'NONE', #242564, .T. ) ;
#142077=DIRECTION ( 'NONE',  ( -0.7071067811865474617, -0.3338907855510734324, -0.6233112732207618523 ) ) ;
#142079=CARTESIAN_POINT ( 'NONE',  ( -20.54999999999999716, 23.68770167995059595, -252.8127582590406348 ) ) ;
#142117=DIRECTION ( 'NONE',  ( 0.000000000000000000, -0.8814952561688430555, 0.4721928772777346239 ) ) ;
#142118=ORIENTED_EDGE ( 'NONE', *, *, #71201, .F. ) ;
#142121=FACE_OUTER_BOUND ( 'NONE', #54673, .T. ) ;
#142128=CARTESIAN_POINT ( 'NONE',  ( -22.57320508075687115, 12.62988036037873307, -223.4632815780722694 ) ) ;
#142162=EDGE_LOOP ( 'NONE', ( #78317, #35713 ) ) ;
#142173=CARTESIAN_POINT ( 'NONE',  ( -22.39999999999999858, 10.71943444926882449, -226.8179467668883547 ) ) ;
#142200=EDGE_LOOP ( 'NONE', ( #128406, #133799, #184136, #213477 ) ) ;
#142214=ORIENTED_EDGE ( 'NONE', *, *, #220100, .T. ) ;
#142293=AXIS2_PLACEMENT_3D ( 'NONE', #218096, #39519, #100698 ) ;
#142317=CARTESIAN_POINT ( 'NONE',  ( -20.54999999999999716, 7.128833340093095217, -233.7327013124392749 ) ) ;
#142319=EDGE_CURVE ( 'NONE', #38262, #75744, #40135, .T. ) ;
#142332=CIRCLE ( 'NONE', #175683, 4.099999999999996980 ) ;
#142373=VERTEX_POINT ( 'NONE', #60097 ) ;
#142374=ORIENTED_EDGE ( 'NONE', *, *, #125289, .T. ) ;
#142393=DIRECTION ( 'NONE',  ( 0.000000000000000000, -0.9994937237965558774, -0.03181660087586650476 ) ) ;
#142451=DIRECTION ( 'NONE',  ( -0.000000000000000000, 0.4721928772777346239, 0.8814952561688430555 ) ) ;
#142461=DIRECTION ( 'NONE',  ( 0.000000000000000000, 0.8814952561688430555, -0.4721928772777346239 ) ) ;
#142486=DIRECTION ( 'NONE',  ( 1.000000000000000000, 0.000000000000000000, 0.000000000000000000 ) ) ;
#142503=CARTESIAN_POINT ( 'NONE',  ( -18.59999999999999787, 45.99141771592758943, -256.5205054824189119 ) ) ;
#142505=VECTOR ( 'NONE', #176212, 1000.000000000000000 ) ;
#142534=FACE_OUTER_BOUND ( 'NONE', #126201, .T. ) ;
#142547=DIRECTION ( 'NONE',  ( 0.000000000000000000, -0.8814952561688437216, 0.4721928772777334582 ) ) ;
#142553=DIRECTION ( 'NONE',  ( 0.000000000000000000, -0.8814952561688476074, 0.4721928772777262417 ) ) ;
#142592=CARTESIAN_POINT ( 'NONE',  ( -18.59999999999999787, 14.85285025691667293, -236.4388300032497057 ) ) ;
#142595=ORIENTED_EDGE ( 'NONE', *, *, #206773, .F. ) ;
#142601=VERTEX_POINT ( 'NONE', #89934 ) ;
#142614=CARTESIAN_POINT ( 'NONE',  ( -20.54999999999999716, 34.89593390941166007, -248.6067769466879156 ) ) ;
#142627=CARTESIAN_POINT ( 'NONE',  ( 21.14999999999999503, -8.777002227904191045, -238.5420042644097975 ) ) ;
#142630=DIRECTION ( 'NONE',  ( -1.000000000000000000, -0.000000000000000000, -0.000000000000000000 ) ) ;
#142633=ORIENTED_EDGE ( 'NONE', *, *, #30021, .F. ) ;
#142641=DIRECTION ( 'NONE',  ( 0.000000000000000000, 0.8814952561688476074, -0.4721928772777262417 ) ) ;
#142713=EDGE_CURVE ( 'NONE', #240913, #17892, #140213, .T. ) ;
#142730=ADVANCED_FACE ( 'NONE', ( #139319 ), #1083, .T. ) ;
#142731=ORIENTED_EDGE ( 'NONE', *, *, #252195, .T. ) ;
#142739=DIRECTION ( 'NONE',  ( 1.000000000000000000, 0.000000000000000000, 0.000000000000000000 ) ) ;
#142761=ORIENTED_EDGE ( 'NONE', *, *, #52697, .F. ) ;
#142793=DIRECTION ( 'NONE',  ( 1.000000000000000000, 0.000000000000000000, 0.000000000000000000 ) ) ;
#142808=DIRECTION ( 'NONE',  ( 0.000000000000000000, 0.8814952561688437216, -0.4721928772777334582 ) ) ;
#142815=ORIENTED_EDGE ( 'NONE', *, *, #157063, .F. ) ;
#142822=EDGE_CURVE ( 'NONE', #158502, #233103, #94443, .T. ) ;
#142835=CARTESIAN_POINT ( 'NONE',  ( -23.15000000000000213, -8.729782940176420425, -238.4538547387928986 ) ) ;
#142844=CARTESIAN_POINT ( 'NONE',  ( -23.25000000000000000, 23.68770167995059595, -252.8127582590406348 ) ) ;
#142852=ORIENTED_EDGE ( 'NONE', *, *, #230109, .F. ) ;
#142877=DIRECTION ( 'NONE',  ( 0.000000000000000000, -0.6855225566104692358, -0.7280513885559494192 ) ) ;
#142878=DIRECTION ( 'NONE',  ( -1.000000000000000000, -0.000000000000000000, -0.000000000000000000 ) ) ;
#142911=CARTESIAN_POINT ( 'NONE',  ( -20.54999999999999716, 11.43341603104965110, -245.8667934851861787 ) ) ;
#142923=CARTESIAN_POINT ( 'NONE',  ( -20.05000000000000426, 30.14024212288317628, -235.5657495473015501 ) ) ;
#142953=EDGE_CURVE ( 'NONE', #135978, #155156, #23931, .T. ) ;
#142971=CARTESIAN_POINT ( 'NONE',  ( 20.94999999999999574, 18.18127959618848521, -237.5711165786817389 ) ) ;
#142974=ORIENTED_EDGE ( 'NONE', *, *, #34753, .F. ) ;
#142977=TOROIDAL_SURFACE ( 'NONE', #147290, 3.899999999999999467, 0.1000000000000000056 ) ;
#142981=AXIS2_PLACEMENT_3D ( 'NONE', #212966, #55137, #95579 ) ;
#142991=CARTESIAN_POINT ( 'NONE',  ( -21.05000000000000071, 9.997527148598553737, -228.1702915402926237 ) ) ;
#143008=CARTESIAN_POINT ( 'NONE',  ( -20.64999999999999858, 21.43869811404188752, -233.1734427395952025 ) ) ;
#143014=ORIENTED_EDGE ( 'NONE', *, *, #246573, .T. ) ;
#143047=AXIS2_PLACEMENT_3D ( 'NONE', #161477, #20680, #98877 ) ;
#143088=FACE_OUTER_BOUND ( 'NONE', #248167, .T. ) ;
#143113=ORIENTED_EDGE ( 'NONE', *, *, #15947, .T. ) ;
#143125=CARTESIAN_POINT ( 'NONE',  ( 23.15000000000000213, 28.15345123516638637, -259.0759448016705733 ) ) ;
#143154=CARTESIAN_POINT ( 'NONE',  ( -23.25000000000000000, 28.50120599808395028, -258.2149742250584268 ) ) ;
#143213=ORIENTED_EDGE ( 'NONE', *, *, #210720, .F. ) ;
#143258=TOROIDAL_SURFACE ( 'NONE', #218073, 11.65000000000000036, 0.1000000000000000056 ) ;
#143265=LINE ( 'NONE', #46723, #189597 ) ;
#143306=CARTESIAN_POINT ( 'NONE',  ( -21.45000000000000284, 29.41239393758413811, -236.9245051605820720 ) ) ;
#143331=DIRECTION ( 'NONE',  ( -1.000000000000000000, 0.000000000000000000, 0.000000000000000000 ) ) ;
#143349=ORIENTED_EDGE ( 'NONE', *, *, #145789, .T. ) ;
#143360=ORIENTED_EDGE ( 'NONE', *, *, #38217, .T. ) ;
#143390=CARTESIAN_POINT ( 'NONE',  ( 23.14999999999999503, 28.91254064196106910, -237.8576372133405528 ) ) ;
#143395=CARTESIAN_POINT ( 'NONE',  ( -18.53317502108577131, 46.43483777265582546, -243.0774829958280918 ) ) ;
#143427=CARTESIAN_POINT ( 'NONE',  ( 22.39999999999999858, 10.71943444926881561, -226.8179467668883547 ) ) ;
#143483=EDGE_CURVE ( 'NONE', #117242, #108268, #223982, .T. ) ;
#143487=ORIENTED_EDGE ( 'NONE', *, *, #144390, .F. ) ;
#143496=ORIENTED_EDGE ( 'NONE', *, *, #120119, .F. ) ;
#143498=ORIENTED_EDGE ( 'NONE', *, *, #194839, .T. ) ;
#143501=ORIENTED_EDGE ( 'NONE', *, *, #197330, .T. ) ;
#143510=ORIENTED_EDGE ( 'NONE', *, *, #51400, .F. ) ;
#143543=ORIENTED_EDGE ( 'NONE', *, *, #165420, .F. ) ;
#143554=ORIENTED_EDGE ( 'NONE', *, *, #51129, .F. ) ;
#143561=EDGE_CURVE ( 'NONE', #123203, #248473, #253032, .T. ) ;
#143592=CARTESIAN_POINT ( 'NONE',  ( 18.49999999999999645, 16.44800918141279311, -240.8068063186265135 ) ) ;
#143607=ORIENTED_EDGE ( 'NONE', *, *, #154248, .T. ) ;
#143609=FACE_OUTER_BOUND ( 'NONE', #173712, .T. ) ;
#143637=DIRECTION ( 'NONE',  ( 0.000000000000000000, 0.4721928772777346239, 0.8814952561688430555 ) ) ;
#143648=EDGE_CURVE ( 'NONE', #218497, #118710, #211730, .T. ) ;
#143697=ORIENTED_EDGE ( 'NONE', *, *, #157635, .F. ) ;
#143698=EDGE_CURVE ( 'NONE', #234543, #5211, #235841, .T. ) ;
#143718=CARTESIAN_POINT ( 'NONE',  ( -21.14999999999999858, 9.997527148596390134, -228.1702915402975691 ) ) ;
#143721=VERTEX_POINT ( 'NONE', #36397 ) ;
#143744=AXIS2_PLACEMENT_3D ( 'NONE', #252371, #214542, #97125 ) ;
#143746=CARTESIAN_POINT ( 'NONE',  ( -21.05000000000000071, 4.272272088314018390, -245.4186996786394843 ) ) ;
#143748=CIRCLE ( 'NONE', #127192, 0.09999999999999568956 ) ;
#143784=DIRECTION ( 'NONE',  ( 1.000000000000000000, 0.000000000000000000, 0.000000000000000000 ) ) ;
#143812=ADVANCED_FACE ( 'NONE', ( #200575 ), #228292, .T. ) ;
#143889=DIRECTION ( 'NONE',  ( 1.000000000000000000, 0.000000000000000000, 0.000000000000000000 ) ) ;
#143903=DIRECTION ( 'NONE',  ( -0.000000000000000000, 0.8874830700839094755, -0.4608403197577646826 ) ) ;
#143957=CYLINDRICAL_SURFACE ( 'NONE', #206608, 0.1000000000000013933 ) ;
#143965=AXIS2_PLACEMENT_3D ( 'NONE', #89889, #190306, #191609 ) ;
#144024=ORIENTED_EDGE ( 'NONE', *, *, #190569, .F. ) ;
#144028=CARTESIAN_POINT ( 'NONE',  ( 18.59999999999999787, 20.40049075128452216, -254.1715885023028250 ) ) ;
#144042=VERTEX_POINT ( 'NONE', #248693 ) ;
#144085=CARTESIAN_POINT ( 'NONE',  ( 21.17356465864818915, 1.513868036494046887, -230.6127096343352889 ) ) ;
#144097=CARTESIAN_POINT ( 'NONE',  ( 20.94999999999999929, 36.18002604163306302, -236.0784499204090991 ) ) ;
#144118=AXIS2_PLACEMENT_3D ( 'NONE', #7464, #84383, #2317 ) ;
#144131=EDGE_CURVE ( 'NONE', #248947, #48019, #195166, .T. ) ;
#144147=CARTESIAN_POINT ( 'NONE',  ( -18.50000000000000000, 42.90983634497242605, -254.2202269430244996 ) ) ;
#144151=EDGE_CURVE ( 'NONE', #116380, #218203, #144676, .T. ) ;
#144165=CARTESIAN_POINT ( 'NONE',  ( -22.39999999999999858, 7.128833340093095217, -233.7327013124392749 ) ) ;
#144188=DIRECTION ( 'NONE',  ( -0.000000000000000000, 0.8814952561688430555, -0.4721928772777346239 ) ) ;
#144197=VECTOR ( 'NONE', #241822, 1000.000000000000000 ) ;
#144221=ORIENTED_EDGE ( 'NONE', *, *, #196291, .T. ) ;
#144237=MECHANICAL_DESIGN_GEOMETRIC_PRESENTATION_REPRESENTATION('',(#256625),#107020);
#144310=UNCERTAINTY_MEASURE_WITH_UNIT (LENGTH_MEASURE( 1.000000000000000082E-05 ), #6955, 'distance_accuracy_value', 'NONE');
#144343=CARTESIAN_POINT ( 'NONE',  ( 22.39999999999999503, 0.2972451047845541261, -230.0732065135368316 ) ) ;
#144345=DIRECTION ( 'NONE',  ( 1.000000000000000000, 1.541880601228652843E-16, 2.878400969107353907E-16 ) ) ;
#144362=VECTOR ( 'NONE', #253095, 1000.000000000000000 ) ;
#144376=DIRECTION ( 'NONE',  ( 0.000000000000000000, -0.8814952561688438326, 0.4721928772777332917 ) ) ;
#144387=FACE_OUTER_BOUND ( 'NONE', #26651, .T. ) ;
#144390=EDGE_CURVE ( 'NONE', #48459, #12130, #113996, .T. ) ;
#144397=EDGE_CURVE ( 'NONE', #218982, #160449, #207252, .T. ) ;
#144405=DIRECTION ( 'NONE',  ( -0.000000000000000000, 0.4721928772777345684, 0.8814952561688429444 ) ) ;
#144416=EDGE_LOOP ( 'NONE', ( #245096, #106644, #211848 ) ) ;
#144422=CARTESIAN_POINT ( 'NONE',  ( 20.92356734117541706, 46.42459709376391430, -243.0752906381742662 ) ) ;
#144440=DIRECTION ( 'NONE',  ( 0.000000000000000000, -0.5273008465188072647, 0.8496786552930167824 ) ) ;
#144471=CARTESIAN_POINT ( 'NONE',  ( -20.94999999999999929, 18.86061765788380740, -226.6874733728449485 ) ) ;
#144532=AXIS2_PLACEMENT_3D ( 'NONE', #104828, #70915, #89150 ) ;
#144602=DIRECTION ( 'NONE',  ( 0.000000000000000000, 0.4721928772777351790, 0.8814952561688427224 ) ) ;
#144613=DIRECTION ( 'NONE',  ( 1.000000000000000000, 0.000000000000000000, 0.000000000000000000 ) ) ;
#144654=ORIENTED_EDGE ( 'NONE', *, *, #199548, .F. ) ;
#144676=CIRCLE ( 'NONE', #3013, 0.1000000000000046824 ) ;
#144681=FACE_OUTER_BOUND ( 'NONE', #33084, .T. ) ;
#144683=AXIS2_PLACEMENT_3D ( 'NONE', #100759, #203762, #141223 ) ;
#144717=VERTEX_POINT ( 'NONE', #5586 ) ;
#144719=ORIENTED_EDGE ( 'NONE', *, *, #200445, .T. ) ;
#144779=ORIENTED_EDGE ( 'NONE', *, *, #106194, .T. ) ;
#144784=EDGE_CURVE ( 'NONE', #221637, #6683, #11820, .T. ) ;
#144791=CARTESIAN_POINT ( 'NONE',  ( -23.25000000000000000, 45.99141771592758943, -256.5205054824189119 ) ) ;
#144813=EDGE_CURVE ( 'NONE', #139998, #45529, #130691, .T. ) ;
#144864=ORIENTED_EDGE ( 'NONE', *, *, #168287, .F. ) ;
#144880=CARTESIAN_POINT ( 'NONE',  ( 20.85000000000000142, 36.48445852813179613, -249.2750065094666923 ) ) ;
#144903=DIRECTION ( 'NONE',  ( 1.000000000000000000, 1.394253735153569469E-16, 2.602809386958778209E-16 ) ) ;
#144919=LINE ( 'NONE', #187928, #128364 ) ;
#144929=EDGE_CURVE ( 'NONE', #250188, #94806, #37511, .T. ) ;
#144940=DIRECTION ( 'NONE',  ( 1.000000000000000000, 0.000000000000000000, 0.000000000000000000 ) ) ;
#144954=CARTESIAN_POINT ( 'NONE',  ( -20.94999999999999929, 30.43677443282724937, -239.5249545687858870 ) ) ;
#144995=ADVANCED_FACE ( 'NONE', ( #219215 ), #107458, .T. ) ;
#145049=EDGE_CURVE ( 'NONE', #178909, #166239, #78403, .T. ) ;
#145104=ORIENTED_EDGE ( 'NONE', *, *, #163052, .T. ) ;
#145105=CARTESIAN_POINT ( 'NONE',  ( 18.59999999999999076, 19.05165861791954285, -232.6888762659126826 ) ) ;
#145110=DIRECTION ( 'NONE',  ( 0.000000000000000000, 0.8814952561688428334, -0.4721928772777350125 ) ) ;
#145115=ORIENTED_EDGE ( 'NONE', *, *, #249926, .F. ) ;
#145116=AXIS2_PLACEMENT_3D ( 'NONE', #156073, #116912, #75247 ) ;
#145130=EDGE_LOOP ( 'NONE', ( #46171, #132330, #137006, #215539 ) ) ;
#145142=DIRECTION ( 'NONE',  ( 0.000000000000000000, 0.1084263158146956119, 0.9941044884914522761 ) ) ;
#145157=AXIS2_PLACEMENT_3D ( 'NONE', #142128, #202112, #243799 ) ;
#145184=CYLINDRICAL_SURFACE ( 'NONE', #62548, 0.1000000000000013933 ) ;
#145185=DIRECTION ( 'NONE',  ( 1.000000000000000000, 0.000000000000000000, 0.000000000000000000 ) ) ;
#145197=CARTESIAN_POINT ( 'NONE',  ( -20.64999999999999858, 26.13474583767463244, -241.1910018098189141 ) ) ;
#145212=FACE_OUTER_BOUND ( 'NONE', #112994, .T. ) ;
#145214=FACE_OUTER_BOUND ( 'NONE', #8260, .T. ) ;
#145217=AXIS2_PLACEMENT_3D ( 'NONE', #241180, #179924, #63814 ) ;
#145219=CARTESIAN_POINT ( 'NONE',  ( -20.54999999999999716, 7.128833340093095217, -233.7327013124392749 ) ) ;
#145221=DIRECTION ( 'NONE',  ( 0.000000000000000000, -0.8814952561688425003, 0.4721928772777354011 ) ) ;
#145231=CARTESIAN_POINT ( 'NONE',  ( 21.05000000000000071, 1.627786319807486892, -244.0021210468063089 ) ) ;
#145248=DIRECTION ( 'NONE',  ( -0.000000000000000000, 0.4721928772777345684, 0.8814952561688429444 ) ) ;
#145267=DIRECTION ( 'NONE',  ( 0.000000000000000000, -0.8814952561688430555, 0.4721928772777346239 ) ) ;
#145291=FACE_OUTER_BOUND ( 'NONE', #135158, .T. ) ;
#145296=VECTOR ( 'NONE', #149821, 1000.000000000000000 ) ;
#145301=EDGE_CURVE ( 'NONE', #216206, #19709, #169575, .T. ) ;
#145303=DIRECTION ( 'NONE',  ( -1.000000000000000000, -0.000000000000000000, -0.000000000000000000 ) ) ;
#145324=AXIS2_PLACEMENT_3D ( 'NONE', #58484, #221406, #218849 ) ;
#145326=ADVANCED_FACE ( 'NONE', ( #59480 ), #240917, .F. ) ;
#145341=EDGE_CURVE ( 'NONE', #132362, #234056, #128487, .T. ) ;
#145370=DIRECTION ( 'NONE',  ( 0.000000000000000000, 0.9446535261619708468, -0.3280696808755038663 ) ) ;
#145408=( BOUNDED_SURFACE ( )  B_SPLINE_SURFACE ( 3, 2, ( 
 ( #87519, #30157, #227043 ),
 ( #28902, #31456, #6715 ),
 ( #187934, #204904, #165818 ),
 ( #206205, #9286, #50954 ) ),
 .UNSPECIFIED., .F., .F., .T. ) 
 B_SPLINE_SURFACE_WITH_KNOTS ( ( 4, 4 ),
 ( 3, 3 ),
 ( 0.0006461284895273867708, 0.0007503702773985852087 ),
 ( 0.000000000000000000, 1.000000000000000000 ),
 .UNSPECIFIED. ) 
 GEOMETRIC_REPRESENTATION_ITEM ( )  RATIONAL_B_SPLINE_SURFACE ( (
 ( 1.000000000000000000, 0.7071067811865532349, 1.000000000000000000),
 ( 1.000000000000000000, 0.7076476444648546194, 1.000000000000000000),
 ( 1.000000000000000000, 0.7075727925190693490, 1.000000000000000000),
 ( 1.000000000000000000, 0.7071067811865725528, 1.000000000000000000) ) ) 
 REPRESENTATION_ITEM ( '' )  SURFACE ( )  );
#145424=AXIS2_PLACEMENT_3D ( 'NONE', #189297, #208852, #186738 ) ;
#145468=ORIENTED_EDGE ( 'NONE', *, *, #172759, .F. ) ;
#145521=DIRECTION ( 'NONE',  ( 0.000000000000000000, 0.8814952561688432775, -0.4721928772777344019 ) ) ;
#145558=CARTESIAN_POINT ( 'NONE',  ( -20.00857864376270001, 30.18117236077229038, -235.7011183606462339 ) ) ;
#145561=DIRECTION ( 'NONE',  ( 1.000000000000000000, 0.000000000000000000, 0.000000000000000000 ) ) ;
#145567=DIRECTION ( 'NONE',  ( -0.000000000000000000, -0.9371753822965315228, 0.3488585713686134238 ) ) ;
#145609=DIRECTION ( 'NONE',  ( 0.000000000000000000, 0.8814952561688437216, -0.4721928772777334582 ) ) ;
#145647=DIRECTION ( 'NONE',  ( 0.000000000000000000, -0.9994937237965558774, -0.03181660087586650476 ) ) ;
#145658=CIRCLE ( 'NONE', #66584, 12.97500000000000320 ) ;
#145709=ORIENTED_EDGE ( 'NONE', *, *, #61692, .F. ) ;
#145729=CIRCLE ( 'NONE', #33362, 0.1999999999999997335 ) ;
#145739=VERTEX_POINT ( 'NONE', #18789 ) ;
#145747=DIRECTION ( 'NONE',  ( 0.000000000000000000, 0.8814952561688438326, -0.4721928772777334582 ) ) ;
#145752=CARTESIAN_POINT ( 'NONE',  ( 22.39999999999999503, 12.71802988599559647, -223.5105008658000258 ) ) ;
#145789=EDGE_CURVE ( 'NONE', #249188, #39196, #77460, .T. ) ;
#145823=DIRECTION ( 'NONE',  ( -4.408576920032447355E-17, -0.8096735173027155286, 0.5868805631290315850 ) ) ;
#145835=CIRCLE ( 'NONE', #200012, 0.09999999999999031886 ) ;
#145859=ORIENTED_EDGE ( 'NONE', *, *, #4667, .F. ) ;
#145868=ORIENTED_EDGE ( 'NONE', *, *, #14638, .T. ) ;
#145877=EDGE_CURVE ( 'NONE', #245302, #89895, #245393, .T. ) ;
#145898=AXIS2_PLACEMENT_3D ( 'NONE', #175485, #254935, #58060 ) ;
#145922=DIRECTION ( 'NONE',  ( -0.000000000000000000, 0.6046243595031743912, 0.7965107556683563850 ) ) ;
#145942=DIRECTION ( 'NONE',  ( 1.000000000000000000, 0.000000000000000000, 0.000000000000000000 ) ) ;
#145947=DIRECTION ( 'NONE',  ( 0.000000000000000000, 0.4721928772776973204, 0.8814952561688629284 ) ) ;
#145964=DIRECTION ( 'NONE',  ( 0.000000000000000000, 0.2262561206234166566, 0.9740678456249555195 ) ) ;
#145977=EDGE_CURVE ( 'NONE', #123203, #93557, #124764, .T. ) ;
#146010=CARTESIAN_POINT ( 'NONE',  ( 20.95512820512820440, 18.86447962780959386, -229.9497396848627488 ) ) ;
#146046=VERTEX_POINT ( 'NONE', #178901 ) ;
#146070=FACE_OUTER_BOUND ( 'NONE', #79228, .T. ) ;
#146081=VECTOR ( 'NONE', #155312, 1000.000000000000000 ) ;
#146119=( BOUNDED_SURFACE ( )  B_SPLINE_SURFACE ( 3, 2, ( 
 ( #10754, #90263, #95422 ),
 ( #94131, #175011, #114984 ),
 ( #34199, #54984, #215362 ),
 ( #113701, #32927, #231105 ),
 ( #13326, #91572, #75859 ),
 ( #92843, #135815, #193248 ) ),
 .UNSPECIFIED., .F., .F., .F. ) 
 B_SPLINE_SURFACE_WITH_KNOTS ( ( 4, 2, 4 ),
 ( 3, 3 ),
 ( 3.141592653589793116, 3.926990816987244948, 4.712388980384696779 ),
 ( 0.000000000000000000, 1.000000000000000000 ),
 .UNSPECIFIED. ) 
 GEOMETRIC_REPRESENTATION_ITEM ( )  RATIONAL_B_SPLINE_SURFACE ( (
 ( 1.000000000000000000, 0.9238795325112884038, 1.000000000000000000),
 ( 1.000000000000000000, 0.9240297172241500601, 1.000000000000000000),
 ( 1.000000000000000000, 0.9038128468041866093, 1.000000000000000000),
 ( 1.000000000000000000, 0.8282379607647167852, 1.000000000000000000),
 ( 1.000000000000000000, 0.7727932973493061297, 1.000000000000000000),
 ( 1.000000000000000000, 0.7071067811865475727, 1.000000000000000000) ) ) 
 REPRESENTATION_ITEM ( '' )  SURFACE ( )  );
#146166=CIRCLE ( 'NONE', #125336, 0.5999999999999978684 ) ;
#146170=CARTESIAN_POINT ( 'NONE',  ( -20.85000000000000142, 43.08613539620618837, -254.3146655184800409 ) ) ;
#146178=EDGE_CURVE ( 'NONE', #92492, #116426, #70629, .T. ) ;
#146185=EDGE_LOOP ( 'NONE', ( #32261, #175666, #185426, #139908 ) ) ;
#146187=CYLINDRICAL_SURFACE ( 'NONE', #9821, 11.75000000000000533 ) ;
#146201=DIRECTION ( 'NONE',  ( -1.000000000000000000, 0.000000000000000000, -0.000000000000000000 ) ) ;
#146210=LINE ( 'NONE', #105779, #215819 ) ;
#146223=LINE ( 'NONE', #225745, #9377 ) ;
#146229=DIRECTION ( 'NONE',  ( 0.000000000000000000, 0.8814952561688429444, -0.4721928772777349015 ) ) ;
#146243=DIRECTION ( 'NONE',  ( -1.000000000000000000, 0.000000000000000000, -0.000000000000000000 ) ) ;
#146268=AXIS2_PLACEMENT_3D ( 'NONE', #134106, #190261, #35066 ) ;
#146275=DIRECTION ( 'NONE',  ( 0.000000000000000000, 0.4721928772776973204, 0.8814952561688629284 ) ) ;
#146284=VECTOR ( 'NONE', #9050, 1000.000000000000000 ) ;
#146319=ORIENTED_EDGE ( 'NONE', *, *, #102568, .F. ) ;
#146321=AXIS2_PLACEMENT_3D ( 'NONE', #531, #218283, #60498 ) ;
#146361=ORIENTED_EDGE ( 'NONE', *, *, #47014, .F. ) ;
#146379=CYLINDRICAL_SURFACE ( 'NONE', #226050, 0.1000000000000075273 ) ;
#146406=EDGE_CURVE ( 'NONE', #249890, #148418, #108320, .T. ) ;
#146407=AXIS2_PLACEMENT_3D ( 'NONE', #207926, #150507, #51356 ) ;
#146431=DIRECTION ( 'NONE',  ( 1.000000000000000000, 0.000000000000000000, 0.000000000000000000 ) ) ;
#146456=CARTESIAN_POINT ( 'NONE',  ( -23.24999999999999645, 38.03205796367814173, -261.1772988674111957 ) ) ;
#146461=CARTESIAN_POINT ( 'NONE',  ( -21.07971444708686093, 1.590621248691514555, -230.6664026343516127 ) ) ;
#146503=CARTESIAN_POINT ( 'NONE',  ( -18.59999999999999787, 23.42819724844703444, -229.2476443247244902 ) ) ;
#146560=EDGE_CURVE ( 'NONE', #19570, #97016, #140706, .T. ) ;
#146561=ORIENTED_EDGE ( 'NONE', *, *, #55286, .T. ) ;
#146568=CARTESIAN_POINT ( 'NONE',  ( 20.94999999999999929, 23.68770167995059239, -252.8127582590406348 ) ) ;
#146598=AXIS2_PLACEMENT_3D ( 'NONE', #139437, #182455, #22097 ) ;
#146610=CIRCLE ( 'NONE', #179975, 0.1000000000000013933 ) ;
#146619=ORIENTED_EDGE ( 'NONE', *, *, #106835, .F. ) ;
#146626=CARTESIAN_POINT ( 'NONE',  ( -20.94999999999999929, 45.93315328338058379, -256.6017782078560003 ) ) ;
#146667=EDGE_CURVE ( 'NONE', #38262, #118710, #122442, .T. ) ;
#146688=CARTESIAN_POINT ( 'NONE',  ( 18.59999999999999787, 42.96960653111219131, -254.4772109693542745 ) ) ;
#146714=CARTESIAN_POINT ( 'NONE',  ( -23.15000000000000213, 26.34635675162282098, -241.8429480539297174 ) ) ;
#146724=EDGE_CURVE ( 'NONE', #104599, #81676, #5023, .T. ) ;
#146791=CARTESIAN_POINT ( 'NONE',  ( 20.94999999999999929, 40.27305497204160645, -251.4871534980821082 ) ) ;
#146807=TOROIDAL_SURFACE ( 'NONE', #134161, 0.2000000000000000111, 0.1000000000000000056 ) ;
#146819=DIRECTION ( 'NONE',  ( 0.000000000000000000, 0.8814952561688442767, -0.4721928772777324035 ) ) ;
#146829=ORIENTED_EDGE ( 'NONE', *, *, #68430, .T. ) ;
#146844=CARTESIAN_POINT ( 'NONE',  ( 20.95512820512820440, 30.05186296287165248, -235.9425146762463328 ) ) ;
#146848=CARTESIAN_POINT ( 'NONE',  ( -21.05000000000000071, 7.128833340093095217, -233.7327013124392749 ) ) ;
#146873=AXIS2_PLACEMENT_3D ( 'NONE', #128563, #107707, #208120 ) ;
#146881=FACE_OUTER_BOUND ( 'NONE', #30072, .T. ) ;
#146915=DIRECTION ( 'NONE',  ( 1.000000000000000000, -0.000000000000000000, -0.000000000000000000 ) ) ;
#146948=CYLINDRICAL_SURFACE ( 'NONE', #100370, 0.5000000000000008882 ) ;
#146966=CARTESIAN_POINT ( 'NONE',  ( 20.94999999999999929, 11.60058429089262333, -246.3380203656811887 ) ) ;
#146970=CARTESIAN_POINT ( 'NONE',  ( -20.94999999999999929, 33.13294339707397995, -247.6623911921324463 ) ) ;
#146981=CARTESIAN_POINT ( 'NONE',  ( -22.45354308602221138, -3.229117406951398372, -228.1842304028190540 ) ) ;
#147004=DIRECTION ( 'NONE',  ( 1.000000000000000000, 0.000000000000000000, 0.000000000000000000 ) ) ;
#147025=ORIENTED_EDGE ( 'NONE', *, *, #39002, .F. ) ;
#147040=DIRECTION ( 'NONE',  ( 0.7071067811865473507, 0.3338907855510733769, 0.6233112732207618523 ) ) ;
#147046=CARTESIAN_POINT ( 'NONE',  ( -21.14999999893457527, 18.71048982429471508, -226.6070540022291482 ) ) ;
#147047=FACE_OUTER_BOUND ( 'NONE', #169164, .T. ) ;
#147082=CARTESIAN_POINT ( 'NONE',  ( 23.14999999999999858, 36.65892442174935439, -249.5511627012433848 ) ) ;
#147084=CARTESIAN_POINT ( 'NONE',  ( -21.05000000000000071, 18.82290990851281975, -233.3604470821920529 ) ) ;
#147091=ORIENTED_EDGE ( 'NONE', *, *, #88344, .F. ) ;
#147098=AXIS2_PLACEMENT_3D ( 'NONE', #65747, #145267, #166170 ) ;
#147100=CARTESIAN_POINT ( 'NONE',  ( 21.14999999999999503, -3.187427350888460076, -228.3200064793908837 ) ) ;
#147106=ORIENTED_EDGE ( 'NONE', *, *, #62654, .F. ) ;
#147117=CIRCLE ( 'NONE', #80437, 12.97500000000000320 ) ;
#147181=CARTESIAN_POINT ( 'NONE',  ( 21.05000000000000071, 23.45160524131172153, -253.2535058871250726 ) ) ;
#147185=EDGE_CURVE ( 'NONE', #35657, #70952, #176531, .T. ) ;
#147188=FACE_OUTER_BOUND ( 'NONE', #112339, .T. ) ;
#147201=CARTESIAN_POINT ( 'NONE',  ( -20.54999999999999716, 34.98408343502854478, -248.6539962344157004 ) ) ;
#147210=AXIS2_PLACEMENT_3D ( 'NONE', #16153, #172680, #38264 ) ;
#147230=ORIENTED_EDGE ( 'NONE', *, *, #34653, .F. ) ;
#147246=ORIENTED_EDGE ( 'NONE', *, *, #22388, .F. ) ;
#147250=CIRCLE ( 'NONE', #59930, 0.1000000000000076522 ) ;
#147277=ORIENTED_EDGE ( 'NONE', *, *, #236106, .T. ) ;
#147290=AXIS2_PLACEMENT_3D ( 'NONE', #122068, #240735, #202877 ) ;
#147297=ORIENTED_EDGE ( 'NONE', *, *, #61382, .T. ) ;
#147324=AXIS2_PLACEMENT_3D ( 'NONE', #91471, #152758, #213986 ) ;
#147345=AXIS2_PLACEMENT_3D ( 'NONE', #51568, #115422, #93293 ) ;
#147405=ORIENTED_EDGE ( 'NONE', *, *, #175002, .T. ) ;
#147407=DIRECTION ( 'NONE',  ( 1.000000000000000000, 0.000000000000000000, 0.000000000000000000 ) ) ;
#147417=CARTESIAN_POINT ( 'NONE',  ( -20.54999999999999716, 11.36448785225375602, -246.7787679937655980 ) ) ;
#147419=CARTESIAN_POINT ( 'NONE',  ( -21.07928932188134397, 1.596973512272237716, -230.6572452218043736 ) ) ;
#147437=LINE ( 'NONE', #225656, #112053 ) ;
#147447=EDGE_CURVE ( 'NONE', #20946, #44944, #148266, .T. ) ;
#147459=CARTESIAN_POINT ( 'NONE',  ( -21.05000000000000071, 4.459011116736869340, -245.2267018908137857 ) ) ;
#147491=AXIS2_PLACEMENT_3D ( 'NONE', #238257, #59595, #154911 ) ;
#147497=CARTESIAN_POINT ( 'NONE',  ( -20.85000000000000142, 45.93315328338058379, -256.6017782078560003 ) ) ;
#147518=AXIS2_PLACEMENT_3D ( 'NONE', #221008, #131875, #113596 ) ;
#147529=CARTESIAN_POINT ( 'NONE',  ( 21.05000000000000071, 7.128833340093095217, -233.7327013124392749 ) ) ;
#147557=ORIENTED_EDGE ( 'NONE', *, *, #240003, .T. ) ;
#147566=ORIENTED_EDGE ( 'NONE', *, *, #135504, .F. ) ;
#147578=CARTESIAN_POINT ( 'NONE',  ( 21.05000000000000071, 11.41170713998153019, -246.6906184681487275 ) ) ;
#147596=DIRECTION ( 'NONE',  ( -1.000000000000000000, 0.000000000000000000, 0.000000000000000000 ) ) ;
#147604=DIRECTION ( 'NONE',  ( 7.304098846218132695E-16, 0.4721928772777346794, 0.8814952561688431665 ) ) ;
#147614=CIRCLE ( 'NONE', #35238, 0.09999999999999939493 ) ;
#147651=VERTEX_POINT ( 'NONE', #153739 ) ;
#147672=FACE_OUTER_BOUND ( 'NONE', #160094, .T. ) ;
#147679=AXIS2_PLACEMENT_3D ( 'NONE', #141833, #257885, #101377 ) ;
#147682=ORIENTED_EDGE ( 'NONE', *, *, #16825, .F. ) ;
#147693=DIRECTION ( 'NONE',  ( 0.000000000000000000, 0.4721928772776973204, 0.8814952561688629284 ) ) ;
#147699=DIRECTION ( 'NONE',  ( -0.000000000000000000, 0.4721928772777345684, 0.8814952561688429444 ) ) ;
#147702=CARTESIAN_POINT ( 'NONE',  ( 18.52326479938694703, 38.02489541698627562, -261.2215218409455133 ) ) ;
#147769=FACE_OUTER_BOUND ( 'NONE', #210662, .T. ) ;
#147772=ORIENTED_EDGE ( 'NONE', *, *, #250735, .F. ) ;
#147776=CARTESIAN_POINT ( 'NONE',  ( -21.09813707148783735, 1.515235338312543867, -230.6900842670254690 ) ) ;
#147802=EDGE_CURVE ( 'NONE', #108265, #143721, #256452, .T. ) ;
#147809=DIRECTION ( 'NONE',  ( 0.000000000000000000, 0.8814952561688437216, -0.4721928772777334582 ) ) ;
#147815=CIRCLE ( 'NONE', #39862, 0.1999999999999987899 ) ;
#147816=ORIENTED_EDGE ( 'NONE', *, *, #187643, .F. ) ;
#147818=AXIS2_PLACEMENT_3D ( 'NONE', #73506, #90451, #168775 ) ;
#147836=EDGE_LOOP ( 'NONE', ( #257138, #6837, #107841 ) ) ;
#147837=B_SPLINE_CURVE_WITH_KNOTS ( 'NONE', 3,
 ( #110310, #213253, #73786, #191159, #188563, #30805, #49049, #9928, #171606, #34655, #131155, #189851, #248537, #209407, #251089, #132445 ),
 .UNSPECIFIED., .F., .F.,
 ( 4, 3, 3, 3, 3, 4 ),
 ( 0.000000000000000000, 2.372700795694549170E-05, 5.739057815867263442E-05, 9.073899019180726251E-05, 0.0001243544287365786784, 0.0001585386695601235239 ),
 .UNSPECIFIED. ) ;
#147848=DIRECTION ( 'NONE',  ( 0.000000000000000000, 0.8814952561688430555, -0.4721928772777346239 ) ) ;
#147853=DIRECTION ( 'NONE',  ( -0.000000000000000000, 0.4721928772777345684, 0.8814952561688429444 ) ) ;
#147864=DIRECTION ( 'NONE',  ( 0.000000000000000000, -0.8814952561688430555, 0.4721928772777346239 ) ) ;
#147938=EDGE_LOOP ( 'NONE', ( #197675, #134444, #209589, #177726 ) ) ;
#147958=EDGE_CURVE ( 'NONE', #74683, #205943, #252399, .T. ) ;
#147981=DIRECTION ( 'NONE',  ( 1.000000000000000000, 0.000000000000000000, 0.000000000000000000 ) ) ;
#148006=DIRECTION ( 'NONE',  ( -1.000000000000000000, 0.000000000000000000, 0.000000000000000000 ) ) ;
#148008=VECTOR ( 'NONE', #118459, 1000.000000000000000 ) ;
#148031=CIRCLE ( 'NONE', #135550, 0.09999999999999986677 ) ;
#148033=DIRECTION ( 'NONE',  ( 0.000000000000000000, 0.8814952561688429444, -0.4721928772777348460 ) ) ;
#148039=CARTESIAN_POINT ( 'NONE',  ( 20.94999999999999574, 16.44800918141279666, -240.8068063186265135 ) ) ;
#148045=CARTESIAN_POINT ( 'NONE',  ( -23.25000000000000000, 43.35377423437995503, -245.1717807829448930 ) ) ;
#148132=DIRECTION ( 'NONE',  ( -0.000000000000000000, 0.4721928772777345684, 0.8814952561688429444 ) ) ;
#148142=DIRECTION ( 'NONE',  ( 0.000000000000000000, 0.8814952561688398358, -0.4721928772777406746 ) ) ;
#148150=CARTESIAN_POINT ( 'NONE',  ( 21.05000000000000071, 19.00443933019177223, -232.7770257915295531 ) ) ;
#148238=CARTESIAN_POINT ( 'NONE',  ( 18.46947024752518018, 8.797344559918837348, -245.4141666393988714 ) ) ;
#148266=B_SPLINE_CURVE_WITH_KNOTS ( 'NONE', 3,
 ( #112004, #27363, #228097, #91138, #10337, #28657 ),
 .UNSPECIFIED., .F., .F.,
 ( 4, 2, 4 ),
 ( 0.000000000000000000, 0.0001891491689349594741, 0.0003782983378699189482 ),
 .UNSPECIFIED. ) ;
#148283=EDGE_CURVE ( 'NONE', #237528, #199335, #254680, .T. ) ;
#148368=EDGE_LOOP ( 'NONE', ( #123401, #224478, #65262, #1457 ) ) ;
#148370=ORIENTED_EDGE ( 'NONE', *, *, #53986, .F. ) ;
#148371=DIRECTION ( 'NONE',  ( 2.952720810173290591E-16, -0.4721928772777342354, -0.8814952561688433885 ) ) ;
#148378=EDGE_CURVE ( 'NONE', #164610, #116921, #96899, .T. ) ;
#148391=CARTESIAN_POINT ( 'NONE',  ( 22.47110162079221141, -3.126931989555618241, -228.2062997596194975 ) ) ;
#148418=VERTEX_POINT ( 'NONE', #59060 ) ;
#148438=EDGE_CURVE ( 'NONE', #175441, #150487, #56748, .T. ) ;
#148448=DIRECTION ( 'NONE',  ( 1.000000000000000000, -0.000000000000000000, -0.000000000000000000 ) ) ;
#148479=CARTESIAN_POINT ( 'NONE',  ( -23.25000000000000000, 42.94477010600543565, -254.3363632230312703 ) ) ;
#148483=CARTESIAN_POINT ( 'NONE',  ( -21.64999999999999858, 29.24307565605548120, -237.2405905340223455 ) ) ;
#148488=AXIS2_PLACEMENT_3D ( 'NONE', #155935, #140172, #41122 ) ;
#148491=CARTESIAN_POINT ( 'NONE',  ( 23.25000000000000000, 31.49702336731128582, -233.4564499823349877 ) ) ;
#148558=CARTESIAN_POINT ( 'NONE',  ( 21.04999999999998650, 21.06723286205836487, -233.6551206055687260 ) ) ;
#148597=ADVANCED_FACE ( 'NONE', ( #247996 ), #107203, .T. ) ;
#148613=ADVANCED_FACE ( 'NONE', ( #134456 ), #106465, .T. ) ;
#148640=CARTESIAN_POINT ( 'NONE',  ( -18.59999999999999787, 43.62273694548321856, -253.2814864317374770 ) ) ;
#148647=AXIS2_PLACEMENT_3D ( 'NONE', #132023, #212855, #30375 ) ;
#148670=ORIENTED_EDGE ( 'NONE', *, *, #106119, .F. ) ;
#148681=VERTEX_POINT ( 'NONE', #242228 ) ;
#148687=VERTEX_POINT ( 'NONE', #45324 ) ;
#148717=CARTESIAN_POINT ( 'NONE',  ( -21.04999999999859739, 1.395114419150890628, -230.6779314796784206 ) ) ;
#148730=TOROIDAL_SURFACE ( 'NONE', #165474, 0.6000000000000004219, 0.1000000000000000056 ) ;
#148812=AXIS2_PLACEMENT_3D ( 'NONE', #201188, #142486, #184183 ) ;
#148883=CIRCLE ( 'NONE', #11515, 0.1000000000000013933 ) ;
#148892=ADVANCED_FACE ( 'NONE', ( #157287 ), #217212, .F. ) ;
#148896=ORIENTED_EDGE ( 'NONE', *, *, #198988, .F. ) ;
#148908=CARTESIAN_POINT ( 'NONE',  ( 20.00000000000001421, 34.40595771266847436, -235.0146864773514892 ) ) ;
#148951=ORIENTED_EDGE ( 'NONE', *, *, #166976, .T. ) ;
#148966=CIRCLE ( 'NONE', #215573, 0.1000000000000013933 ) ;
#148973=EDGE_LOOP ( 'NONE', ( #227178, #254654 ) ) ;
#149025=VERTEX_POINT ( 'NONE', #144097 ) ;
#149055=EDGE_LOOP ( 'NONE', ( #237467, #252895, #233684, #229652 ) ) ;
#149063=AXIS2_PLACEMENT_3D ( 'NONE', #116436, #112583, #16070 ) ;
#149093=PLANE ( 'NONE',  #161631 ) ;
#149102=CARTESIAN_POINT ( 'NONE',  ( 21.05000000000000071, 23.34004772283015683, -229.2004250369967338 ) ) ;
#149106=VECTOR ( 'NONE', #105163, 1000.000000000000000 ) ;
#149123=DIRECTION ( 'NONE',  ( -1.000000000000000000, -1.541880601228652843E-16, -2.878400969107353907E-16 ) ) ;
#149183=FACE_OUTER_BOUND ( 'NONE', #160281, .T. ) ;
#149205=FACE_OUTER_BOUND ( 'NONE', #9361, .T. ) ;
#149228=VERTEX_POINT ( 'NONE', #188380 ) ;
#149258=CARTESIAN_POINT ( 'NONE',  ( 23.14999999999999858, 28.32080209959243788, -238.8452605374484676 ) ) ;
#149268=MECHANICAL_DESIGN_GEOMETRIC_PRESENTATION_REPRESENTATION('',(#120252),#103426);
#149271=EDGE_LOOP ( 'NONE', ( #26095, #251565, #36668, #212905 ) ) ;
#149277=LINE ( 'NONE', #68441, #89712 ) ;
#149301=VERTEX_POINT ( 'NONE', #54005 ) ;
#149323=ORIENTED_EDGE ( 'NONE', *, *, #19898, .F. ) ;
#149361=VERTEX_POINT ( 'NONE', #98226 ) ;
#149388=ORIENTED_EDGE ( 'NONE', *, *, #250120, .T. ) ;
#149412=CARTESIAN_POINT ( 'NONE',  ( -22.39999999999999858, 12.71802988599559292, -223.5105008658000258 ) ) ;
#149444=DIRECTION ( 'NONE',  ( 1.000000000000000000, 0.000000000000000000, 0.000000000000000000 ) ) ;
#149524=ADVANCED_FACE ( 'NONE', ( #122983 ), #153235, .T. ) ;
#149550=AXIS2_PLACEMENT_3D ( 'NONE', #247551, #168056, #188856 ) ;
#149586=EDGE_CURVE ( 'NONE', #152553, #105430, #90237, .T. ) ;
#149589=FACE_OUTER_BOUND ( 'NONE', #112953, .T. ) ;
#149611=DIRECTION ( 'NONE',  ( 0.000000000000000000, 0.8814952561687762200, -0.4721928772778593575 ) ) ;
#149650=ORIENTED_EDGE ( 'NONE', *, *, #86419, .F. ) ;
#149652=EDGE_LOOP ( 'NONE', ( #61359, #15237, #2189, #215922 ) ) ;
#149655=ADVANCED_FACE ( 'NONE', ( #147672 ), #68133, .F. ) ;
#149687=EDGE_CURVE ( 'NONE', #251809, #119943, #136616, .T. ) ;
#149690=CARTESIAN_POINT ( 'NONE',  ( 20.94999999999999574, 4.272272088314021943, -245.4186996786394843 ) ) ;
#149729=ADVANCED_FACE ( 'NONE', ( #234916 ), #257200, .F. ) ;
#149740=DIRECTION ( 'NONE',  ( 0.000000000000000000, 0.8814952561688722543, -0.4721928772776801675 ) ) ;
#149756=DIRECTION ( 'NONE',  ( 1.000000000000000000, 3.403959061552269104E-14, 2.112458025737858499E-14 ) ) ;
#149790=ORIENTED_EDGE ( 'NONE', *, *, #27008, .F. ) ;
#149816=DIRECTION ( 'NONE',  ( -0.000000000000000000, 0.8127272543710891695, -0.5826443254700338636 ) ) ;
#149821=DIRECTION ( 'NONE',  ( -0.000000000000000000, 0.8814952561688430555, -0.4721928772777346239 ) ) ;
#149826=AXIS2_PLACEMENT_3D ( 'NONE', #71561, #173254, #151078 ) ;
#149839=ADVANCED_FACE ( 'NONE', ( #77111 ), #52398, .T. ) ;
#149840=LINE ( 'NONE', #69021, #101983 ) ;
#149904=VECTOR ( 'NONE', #20785, 1000.000000000000000 ) ;
#149905=ORIENTED_EDGE ( 'NONE', *, *, #70821, .T. ) ;
#149945=EDGE_LOOP ( 'NONE', ( #127682, #248244, #54815 ) ) ;
#149947=ORIENTED_EDGE ( 'NONE', *, *, #103082, .T. ) ;
#149993=PLANE ( 'NONE',  #165543 ) ;
#150019=CARTESIAN_POINT ( 'NONE',  ( 18.59999999999999076, 34.44688795055758135, -235.1500552906961730 ) ) ;
#150038=CIRCLE ( 'NONE', #104205, 0.09999999999999939493 ) ;
#150052=AXIS2_PLACEMENT_3D ( 'NONE', #82581, #104707, #121770 ) ;
#150060=DIRECTION ( 'NONE',  ( -1.000000000000000000, -1.394253735153569469E-16, -2.602809386958778209E-16 ) ) ;
#150091=CARTESIAN_POINT ( 'NONE',  ( 20.94999999999999574, 18.26942912180536638, -237.6183358664095238 ) ) ;
#150124=CARTESIAN_POINT ( 'NONE',  ( -23.25000000000000000, 45.93315328338058379, -256.6017782078560003 ) ) ;
#150178=DIRECTION ( 'NONE',  ( -1.000000000000000000, 1.638248138805453496E-14, 3.058301029676582006E-14 ) ) ;
#150185=ORIENTED_EDGE ( 'NONE', *, *, #145977, .F. ) ;
#150187=EDGE_CURVE ( 'NONE', #111286, #118730, #50798, .T. ) ;
#150255=ORIENTED_EDGE ( 'NONE', *, *, #34728, .F. ) ;
#150283=CARTESIAN_POINT ( 'NONE',  ( 18.33996824403459414, 38.15118265298796274, -261.2066690643014226 ) ) ;
#150295=DIRECTION ( 'NONE',  ( 0.000000000000000000, -0.8814952561679687548, 0.4721928772793668183 ) ) ;
#150302=ORIENTED_EDGE ( 'NONE', *, *, #43529, .T. ) ;
#150310=ORIENTED_EDGE ( 'NONE', *, *, #59368, .F. ) ;
#150335=DIRECTION ( 'NONE',  ( 0.7071067811865485719, -0.6233112732207607420, 0.3338907855510729328 ) ) ;
#150349=CARTESIAN_POINT ( 'NONE',  ( -18.59999999999999787, 1.006414599850383507, -224.3937905772586703 ) ) ;
#150362=AXIS2_PLACEMENT_3D ( 'NONE', #132100, #111254, #92962 ) ;
#150366=EDGE_LOOP ( 'NONE', ( #138904, #223513, #133128, #32134 ) ) ;
#150367=ADVANCED_FACE ( 'NONE', ( #124926 ), #4934, .T. ) ;
#150379=EDGE_CURVE ( 'NONE', #239691, #121060, #223720, .T. ) ;
#150390=ADVANCED_FACE ( 'NONE', ( #225273 ), #6236, .F. ) ;
#150409=AXIS2_PLACEMENT_3D ( 'NONE', #67078, #108769, #47490 ) ;
#150419=DIRECTION ( 'NONE',  ( 1.000000000000000000, 0.000000000000000000, 0.000000000000000000 ) ) ;
#150425=FACE_OUTER_BOUND ( 'NONE', #160600, .T. ) ;
#150436=CARTESIAN_POINT ( 'NONE',  ( -20.64999999999999858, 29.14863708059993286, -237.4168895852561434 ) ) ;
#150484=CARTESIAN_POINT ( 'NONE',  ( -23.15000000000000213, 18.38993523765006444, -239.7649653196623376 ) ) ;
#150487=VERTEX_POINT ( 'NONE', #17480 ) ;
#150507=DIRECTION ( 'NONE',  ( -1.000000000000000000, -1.394253735153569469E-16, -2.602809386958778209E-16 ) ) ;
#150515=ORIENTED_EDGE ( 'NONE', *, *, #201408, .F. ) ;
#150520=ORIENTED_EDGE ( 'NONE', *, *, #218124, .T. ) ;
#150522=ORIENTED_EDGE ( 'NONE', *, *, #101087, .F. ) ;
#150580=DIRECTION ( 'NONE',  ( -2.952720810173288619E-16, 0.4721928772777346239, 0.8814952561688430555 ) ) ;
#150602=ADVANCED_FACE ( 'NONE', ( #81279 ), #100826, .T. ) ;
#150604=DIRECTION ( 'NONE',  ( 0.000000000000000000, 0.8814952561688050858, -0.4721928772778054006 ) ) ;
#150609=LINE ( 'NONE', #128470, #93766 ) ;
#150612=DIRECTION ( 'NONE',  ( -1.000000000000000000, -0.000000000000000000, -0.000000000000000000 ) ) ;
#150619=FACE_OUTER_BOUND ( 'NONE', #23784, .T. ) ;
#150667=EDGE_CURVE ( 'NONE', #223188, #153027, #236395, .T. ) ;
#150669=DIRECTION ( 'NONE',  ( 0.000000000000000000, -0.8368562265788574983, -0.5474227397872651890 ) ) ;
#150671=ORIENTED_EDGE ( 'NONE', *, *, #48043, .T. ) ;
#150732=CARTESIAN_POINT ( 'NONE',  ( 21.14999999999999858, 20.93186404871370598, -233.6960508434578401 ) ) ;
#150749=CARTESIAN_POINT ( 'NONE',  ( 20.84999999999999787, 36.10799525571641766, -235.9264213948819133 ) ) ;
#150750=ORIENTED_EDGE ( 'NONE', *, *, #192733, .T. ) ;
#150805=DIRECTION ( 'NONE',  ( 1.000000000000000000, -0.000000000000000000, -0.000000000000000000 ) ) ;
#150806=CARTESIAN_POINT ( 'NONE',  ( 18.59999999999999787, 9.105964803472796021, -245.3658845043482586 ) ) ;
#150810=EDGE_CURVE ( 'NONE', #168386, #98749, #174080, .T. ) ;
#150845=CARTESIAN_POINT ( 'NONE',  ( -20.99749315643147440, 36.02367272165624712, -235.8812521217649305 ) ) ;
#150852=FACE_OUTER_BOUND ( 'NONE', #100127, .T. ) ;
#150859=EDGE_CURVE ( 'NONE', #109890, #26118, #228025, .T. ) ;
#150860=AXIS2_PLACEMENT_3D ( 'NONE', #22475, #223204, #2867 ) ;
#150880=ORIENTED_EDGE ( 'NONE', *, *, #52105, .T. ) ;
#150885=CYLINDRICAL_SURFACE ( 'NONE', #184369, 2.000000000000003553 ) ;
#150900=DIRECTION ( 'NONE',  ( 1.000000000000000000, 0.000000000000000000, 0.000000000000000000 ) ) ;
#150909=ORIENTED_EDGE ( 'NONE', *, *, #187321, .F. ) ;
#150929=ORIENTED_EDGE ( 'NONE', *, *, #22322, .F. ) ;
#150951=DIRECTION ( 'NONE',  ( 0.000000000000000000, 0.8814952561688444987, -0.4721928772777320149 ) ) ;
#150956=CARTESIAN_POINT ( 'NONE',  ( -21.93340585970945611, 10.58724339642471612, -227.2765004563009370 ) ) ;
#150979=DIRECTION ( 'NONE',  ( -1.000000000000000000, 0.000000000000000000, 0.000000000000000000 ) ) ;
#150999=ADVANCED_FACE ( 'NONE', ( #202328 ), #220617, .T. ) ;
#151011=DIRECTION ( 'NONE',  ( -0.000000000000000000, 0.03181660087583042251, -0.9994937237965568766 ) ) ;
#151055=CYLINDRICAL_SURFACE ( 'NONE', #21365, 0.1000000000000075273 ) ;
#151075=DIRECTION ( 'NONE',  ( 1.000000000000000000, 0.000000000000000000, 0.000000000000000000 ) ) ;
#151078=DIRECTION ( 'NONE',  ( 0.000000000000000000, 0.8814952561688438326, -0.4721928772777331251 ) ) ;
#151089=AXIS2_PLACEMENT_3D ( 'NONE', #235872, #95087, #195502 ) ;
#151109=CIRCLE ( 'NONE', #5324, 0.1000000000000013933 ) ;
#151111=CARTESIAN_POINT ( 'NONE',  ( -21.05000000000000071, 7.128833340093095217, -233.7327013124392749 ) ) ;
#151112=CIRCLE ( 'NONE', #105263, 0.8750000000000007772 ) ;
#151113=ORIENTED_EDGE ( 'NONE', *, *, #147958, .F. ) ;
#151117=FACE_OUTER_BOUND ( 'NONE', #218664, .T. ) ;
#151123=VECTOR ( 'NONE', #4112, 1000.000000000000000 ) ;
#151134=DIRECTION ( 'NONE',  ( 0.000000000000000000, 0.1084263158147437400, 0.9941044884914469471 ) ) ;
#151145=ORIENTED_EDGE ( 'NONE', *, *, #19018, .F. ) ;
#151197=DIRECTION ( 'NONE',  ( 1.000000000000000000, -3.448943450116723568E-16, -6.438528483529607644E-16 ) ) ;
#151202=CIRCLE ( 'NONE', #205149, 6.329289321881372388 ) ;
#151212=AXIS2_PLACEMENT_3D ( 'NONE', #81919, #161520, #20726 ) ;
#151226=EDGE_LOOP ( 'NONE', ( #208326, #106926, #16722, #63664, #63975, #159952, #248619, #211136, #109084, #66293, #238218, #91056, #123365, #111126, #170122, #88041, #150671, #191654, #212109, #149905, #152379, #67199, #50738, #236646, #68929, #48032, #244176 ) ) ;
#151248=DIRECTION ( 'NONE',  ( 0.000000000000000000, 0.8814952561688430555, -0.4721928772777346239 ) ) ;
#151273=VERTEX_POINT ( 'NONE', #97758 ) ;
#151280=DIRECTION ( 'NONE',  ( -4.336808689942052446E-15, 0.03181660087581661411, -0.9994937237965575427 ) ) ;
#151290=AXIS2_PLACEMENT_3D ( 'NONE', #205064, #47272, #70743 ) ;
#151344=DIRECTION ( 'NONE',  ( 1.000000000000000000, 0.000000000000000000, 0.000000000000000000 ) ) ;
#151379=VECTOR ( 'NONE', #241996, 1000.000000000000000 ) ;
#151415=EDGE_LOOP ( 'NONE', ( #34827, #120077, #256520, #165657 ) ) ;
#151421=AXIS2_PLACEMENT_3D ( 'NONE', #200023, #38377, #21406 ) ;
#151427=ORIENTED_EDGE ( 'NONE', *, *, #177467, .T. ) ;
#151429=AXIS2_PLACEMENT_3D ( 'NONE', #132802, #257801, #2229 ) ;
#151441=CARTESIAN_POINT ( 'NONE',  ( -21.05000000000000071, 13.71992543034163958, -238.5823796952984992 ) ) ;
#151470=AXIS2_PLACEMENT_3D ( 'NONE', #202009, #61212, #23403 ) ;
#151489=CARTESIAN_POINT ( 'NONE',  ( 20.04142135391667168, 34.45224226563739478, -235.0394798453100691 ) ) ;
#151504=CARTESIAN_POINT ( 'NONE',  ( 20.97107704358301916, 18.86446520529444726, -229.9504956209307238 ) ) ;
#151522=ADVANCED_FACE ( 'NONE', ( #92342 ), #103460, .T. ) ;
#151534=CARTESIAN_POINT ( 'NONE',  ( 21.14999999999999858, 2.272311100394802885, -217.9150152700588592 ) ) ;
#151553=CARTESIAN_POINT ( 'NONE',  ( 20.94999999999999929, 28.27358281186466371, -238.9334100630653381 ) ) ;
#151570=CARTESIAN_POINT ( 'NONE',  ( -20.85000000000000142, 36.48445852813179613, -249.2750065094666923 ) ) ;
#151580=DIRECTION ( 'NONE',  ( 0.000000000000000000, -0.8814952561688476074, 0.4721928772777262417 ) ) ;
#151582=CARTESIAN_POINT ( 'NONE',  ( 18.43630871534904969, 37.95950696621422793, -261.2289642737110853 ) ) ;
#151585=AXIS2_PLACEMENT_3D ( 'NONE', #30221, #52316, #152759 ) ;
#151591=ORIENTED_EDGE ( 'NONE', *, *, #96784, .F. ) ;
#151615=CARTESIAN_POINT ( 'NONE',  ( -20.85000000000000142, 43.24695311518262031, -245.0026972281755491 ) ) ;
#151621=ADVANCED_FACE ( 'NONE', ( #81412 ), #63152, .T. ) ;
#151628=EDGE_CURVE ( 'NONE', #137151, #224437, #134030, .T. ) ;
#151639=VECTOR ( 'NONE', #139518, 1000.000000000000000 ) ;
#151648=EDGE_CURVE ( 'NONE', #112914, #158507, #138809, .T. ) ;
#151660=AXIS2_PLACEMENT_3D ( 'NONE', #123446, #238248, #63456 ) ;
#151682=CARTESIAN_POINT ( 'NONE',  ( -21.05000000000000071, 14.64166534854604507, -236.4381089660238331 ) ) ;
#151700=DIRECTION ( 'NONE',  ( 2.952720810173290098E-16, -0.4721928772777322370, -0.8814952561688442767 ) ) ;
#151716=ORIENTED_EDGE ( 'NONE', *, *, #160659, .T. ) ;
#151736=AXIS2_PLACEMENT_3D ( 'NONE', #194093, #75438, #154972 ) ;
#151742=CARTESIAN_POINT ( 'NONE',  ( -18.59999999999999787, 18.18127959618848166, -237.5711165786817389 ) ) ;
#151781=CIRCLE ( 'NONE', #243324, 0.09999999999999939493 ) ;
#151782=DIRECTION ( 'NONE',  ( 2.827886303505248273E-16, 0.03181660087583042251, -0.9994937237965568766 ) ) ;
#151792=LINE ( 'NONE', #248296, #26459 ) ;
#151801=FACE_OUTER_BOUND ( 'NONE', #197058, .T. ) ;
#151830=ORIENTED_EDGE ( 'NONE', *, *, #108358, .F. ) ;
#151865=EDGE_CURVE ( 'NONE', #135784, #194512, #120451, .T. ) ;
#151880=CARTESIAN_POINT ( 'NONE',  ( -21.05000000000000071, 33.04479387145709524, -247.6151719044046899 ) ) ;
#151891=EDGE_CURVE ( 'NONE', #157381, #79099, #35638, .T. ) ;
#151910=DIRECTION ( 'NONE',  ( 0.000000000000000000, -0.8368562265788574983, -0.5474227397872651890 ) ) ;
#151926=DIRECTION ( 'NONE',  ( 0.000000000000000000, 0.8814952561688444987, -0.4721928772777320149 ) ) ;
#151937=FACE_OUTER_BOUND ( 'NONE', #188398, .T. ) ;
#151943=AXIS2_PLACEMENT_3D ( 'NONE', #36366, #76740, #55870 ) ;
#151970=EDGE_CURVE ( 'NONE', #153027, #236989, #245329, .T. ) ;
#151985=DIRECTION ( 'NONE',  ( -0.000000000000000000, 0.8127272543710918340, -0.5826443254700303109 ) ) ;
#152006=CARTESIAN_POINT ( 'NONE',  ( 18.59999999999999432, 42.92545512184477730, -254.1955779480491344 ) ) ;
#152014=LINE ( 'NONE', #213223, #30202 ) ;
#152031=DIRECTION ( 'NONE',  ( 0.000000000000000000, 0.4721928772777346239, 0.8814952561688430555 ) ) ;
#152050=EDGE_CURVE ( 'NONE', #195479, #186480, #87262, .T. ) ;
#152060=CIRCLE ( 'NONE', #172931, 0.09999999999999742428 ) ;
#152101=CARTESIAN_POINT ( 'NONE',  ( 23.24999999999999645, 36.65892442174935439, -249.5511627012433848 ) ) ;
#152112=DIRECTION ( 'NONE',  ( 1.000000000000000000, 0.000000000000000000, 0.000000000000000000 ) ) ;
#152118=CARTESIAN_POINT ( 'NONE',  ( 18.51565452909304099, 9.054758213346417506, -245.3745873853864055 ) ) ;
#152154=AXIS2_PLACEMENT_3D ( 'NONE', #95530, #250750, #211646 ) ;
#152167=CARTESIAN_POINT ( 'NONE',  ( 21.14999999999999858, 23.38726701055792745, -229.1122755113798348 ) ) ;
#152187=DIRECTION ( 'NONE',  ( 0.000000000000000000, 0.8814952561688430555, -0.4721928772777346239 ) ) ;
#152243=DIRECTION ( 'NONE',  ( 4.336808689942127388E-15, 0.8496786552930133407, 0.5273008465188128158 ) ) ;
#152272=CYLINDRICAL_SURFACE ( 'NONE', #18632, 0.1000000000000013933 ) ;
#152274=DIRECTION ( 'NONE',  ( 0.000000000000000000, 0.8814952561688429444, -0.4721928772777347350 ) ) ;
#152326=CARTESIAN_POINT ( 'NONE',  ( 21.05000000000000071, 40.18490544642472173, -251.4399342103543233 ) ) ;
#152356=CARTESIAN_POINT ( 'NONE',  ( -20.54999999999999716, 23.49882452903949925, -253.1653563615082305 ) ) ;
#152367=DIRECTION ( 'NONE',  ( 1.000000000000000000, 0.000000000000000000, 0.000000000000000000 ) ) ;
#152379=ORIENTED_EDGE ( 'NONE', *, *, #251499, .F. ) ;
#152411=EDGE_CURVE ( 'NONE', #116858, #57931, #8182, .T. ) ;
#152423=PLANE ( 'NONE',  #234047 ) ;
#152454=PLANE ( 'NONE',  #189192 ) ;
#152477=AXIS2_PLACEMENT_3D ( 'NONE', #122149, #102537, #41351 ) ;
#152481=ORIENTED_EDGE ( 'NONE', *, *, #215097, .T. ) ;
#152496=CARTESIAN_POINT ( 'NONE',  ( -20.54999999999999716, 23.94791789707936758, -237.8074276425068661 ) ) ;
#152517=CIRCLE ( 'NONE', #177463, 0.1999999999999987899 ) ;
#152539=CARTESIAN_POINT ( 'NONE',  ( -20.64999999999999858, 7.128833340093095217, -233.7327013124392749 ) ) ;
#152553=VERTEX_POINT ( 'NONE', #186368 ) ;
#152557=DIRECTION ( 'NONE',  ( 0.000000000000000000, 0.8814952561688430555, -0.4721928772777346239 ) ) ;
#152560=APPLICATION_CONTEXT ( 'automotive_design' ) ;
#152576=ORIENTED_EDGE ( 'NONE', *, *, #196291, .F. ) ;
#152592=CARTESIAN_POINT ( 'NONE',  ( -21.05000000000000071, 1.622572661696384477, -230.6714771550894056 ) ) ;
#152596=EDGE_LOOP ( 'NONE', ( #188468, #203883, #5649, #214369 ) ) ;
#152601=CARTESIAN_POINT ( 'NONE',  ( -18.59999999999999787, 18.26942912180536638, -237.6183358664095238 ) ) ;
#152642=ORIENTED_EDGE ( 'NONE', *, *, #231288, .T. ) ;
#152654=ORIENTED_EDGE ( 'NONE', *, *, #152657, .T. ) ;
#152657=EDGE_CURVE ( 'NONE', #104063, #63323, #25124, .T. ) ;
#152660=DIRECTION ( 'NONE',  ( 0.000000000000000000, 0.8814952561688437216, -0.4721928772777334582 ) ) ;
#152666=CARTESIAN_POINT ( 'NONE',  ( -20.94999999999999929, 40.18490544642472173, -251.4399342103543233 ) ) ;
#152698=EDGE_CURVE ( 'NONE', #97226, #118710, #212382, .T. ) ;
#152728=CARTESIAN_POINT ( 'NONE',  ( 20.94999999999999929, 28.50120599808395028, -258.2149742250584268 ) ) ;
#152738=FACE_OUTER_BOUND ( 'NONE', #89962, .T. ) ;
#152751=DIRECTION ( 'NONE',  ( 1.000000000000000000, 0.000000000000000000, 0.000000000000000000 ) ) ;
#152758=DIRECTION ( 'NONE',  ( -1.000000000000000000, -0.000000000000000000, -0.000000000000000000 ) ) ;
#152759=DIRECTION ( 'NONE',  ( 0.000000000000000000, -0.8814952561688398358, 0.4721928772777406746 ) ) ;
#152791=AXIS2_PLACEMENT_3D ( 'NONE', #194911, #16282, #254805 ) ;
#152795=CARTESIAN_POINT ( 'NONE',  ( 20.97250901189795158, 18.90193937995545781, -227.9863388870093104 ) ) ;
#152815=TOROIDAL_SURFACE ( 'NONE', #127853, 0.2000000000000000111, 0.1000000000000000056 ) ;
#152822=DIRECTION ( 'NONE',  ( 1.000000000000000000, 0.000000000000000000, 0.000000000000000000 ) ) ;
#152830=ADVANCED_FACE ( 'NONE', ( #184744 ), #242155, .F. ) ;
#152872=CARTESIAN_POINT ( 'NONE',  ( 21.95218792049437795, 10.44204081626609160, -227.3378460360148381 ) ) ;
#152873=CARTESIAN_POINT ( 'NONE',  ( 18.47135592147670025, 38.07830107212508608, -261.0558283097952312 ) ) ;
#152891=CARTESIAN_POINT ( 'NONE',  ( -21.44999999999999929, 21.48591740176965814, -233.0852932139783036 ) ) ;
#152943=CYLINDRICAL_SURFACE ( 'NONE', #141040, 0.1000000000000088596 ) ;
#152955=CIRCLE ( 'NONE', #173822, 11.64999999999999680 ) ;
#152991=ORIENTED_EDGE ( 'NONE', *, *, #119453, .T. ) ;
#152999=ORIENTED_EDGE ( 'NONE', *, *, #217799, .F. ) ;
#153027=VERTEX_POINT ( 'NONE', #171653 ) ;
#153058=VECTOR ( 'NONE', #115942, 1000.000000000000000 ) ;
#153065=CARTESIAN_POINT ( 'NONE',  ( -22.39999999999999858, 1.619487989037824871, -230.7814958294534335 ) ) ;
#153068=ORIENTED_EDGE ( 'NONE', *, *, #236442, .T. ) ;
#153084=CARTESIAN_POINT ( 'NONE',  ( 21.14999999999999858, 23.34004772283015683, -229.2004250369967338 ) ) ;
#153094=LINE ( 'NONE', #128686, #170775 ) ;
#153102=ORIENTED_EDGE ( 'NONE', *, *, #56707, .F. ) ;
#153117=AXIS2_PLACEMENT_3D ( 'NONE', #178578, #256744, #237239 ) ;
#153132=CARTESIAN_POINT ( 'NONE',  ( -23.15000000000000213, 36.65892442174935439, -249.5511627012433848 ) ) ;
#153134=CARTESIAN_POINT ( 'NONE',  ( -2.995603634470829482E-16, 12.37888392014804495, -249.8746333190754569 ) ) ;
#153138=EDGE_LOOP ( 'NONE', ( #42126, #156247, #41628, #154051 ) ) ;
#153141=EDGE_CURVE ( 'NONE', #255363, #89629, #241757, .T. ) ;
#153143=ORIENTED_EDGE ( 'NONE', *, *, #158346, .T. ) ;
#153146=DIRECTION ( 'NONE',  ( 0.000000000000000000, 0.4721928772777351790, 0.8814952561688427224 ) ) ;
#153148=EDGE_LOOP ( 'NONE', ( #225784, #119482, #174164 ) ) ;
#153170=DIRECTION ( 'NONE',  ( -1.000000000000000000, -0.000000000000000000, -0.000000000000000000 ) ) ;
#153184=EDGE_LOOP ( 'NONE', ( #114333, #64273, #121220 ) ) ;
#153204=CARTESIAN_POINT ( 'NONE',  ( -21.05000000000000782, 10.12198123692519403, -228.1806781248011191 ) ) ;
#153217=CARTESIAN_POINT ( 'NONE',  ( 21.04999999999999716, 1.443015084894189615, -230.7069270091447208 ) ) ;
#153223=ORIENTED_EDGE ( 'NONE', *, *, #227537, .F. ) ;
#153229=ADVANCED_FACE ( 'NONE', ( #158499, #215850 ), #16413, .T. ) ;
#153235=TOROIDAL_SURFACE ( 'NONE', #57505, 0.2000000000000000111, 0.1000000000000000056 ) ;
#153236=ORIENTED_EDGE ( 'NONE', *, *, #97919, .T. ) ;
#153284=CARTESIAN_POINT ( 'NONE',  ( -20.64999999999999858, 20.02211948220868365, -235.8179285081017156 ) ) ;
#153290=FACE_OUTER_BOUND ( 'NONE', #231052, .T. ) ;
#153294=AXIS2_PLACEMENT_3D ( 'NONE', #219804, #137685, #78988 ) ;
#153314=CARTESIAN_POINT ( 'NONE',  ( 21.05000000000000071, 30.48950451747912993, -239.6099224343151946 ) ) ;
#153334=ORIENTED_EDGE ( 'NONE', *, *, #44171, .F. ) ;
#153351=AXIS2_PLACEMENT_3D ( 'NONE', #252321, #55382, #54125 ) ;
#153391=FACE_OUTER_BOUND ( 'NONE', #232904, .T. ) ;
#153423=CARTESIAN_POINT ( 'NONE',  ( 23.14999999999999858, 30.38404434817536526, -239.4399867032566078 ) ) ;
#153445=DIRECTION ( 'NONE',  ( -0.000000000000000000, 0.8127272543710951647, -0.5826443254700256480 ) ) ;
#153451=CARTESIAN_POINT ( 'NONE',  ( -21.05000000000000071, 4.184122562697131897, -245.3714803909117279 ) ) ;
#153467=CARTESIAN_POINT ( 'NONE',  ( -21.05315837413033009, 36.17631400068042780, -235.9630178772233648 ) ) ;
#153471=ORIENTED_EDGE ( 'NONE', *, *, #214068, .T. ) ;
#153477=ORIENTED_EDGE ( 'NONE', *, *, #56707, .T. ) ;
#153501=ORIENTED_EDGE ( 'NONE', *, *, #40981, .F. ) ;
#153513=CARTESIAN_POINT ( 'NONE',  ( 0.000000000000000000, 0.000000000000000000, 0.000000000000000000 ) ) ;
#153533=LINE ( 'NONE', #73980, #231053 ) ;
#153543=PLANE ( 'NONE',  #184689 ) ;
#153548=LINE ( 'NONE', #133923, #61128 ) ;
#153557=EDGE_CURVE ( 'NONE', #161523, #173295, #39209, .T. ) ;
#153588=ORIENTED_EDGE ( 'NONE', *, *, #92437, .F. ) ;
#153590=DIRECTION ( 'NONE',  ( 0.000000000000000000, 0.8814952561694257005, -0.4721928772766468829 ) ) ;
#153592=ORIENTED_EDGE ( 'NONE', *, *, #181940, .F. ) ;
#153615=DIRECTION ( 'NONE',  ( 0.000000000000000000, 0.9994937237965558774, 0.03181660087586650476 ) ) ;
#153624=CARTESIAN_POINT ( 'NONE',  ( 22.40000000000000213, 10.80758397488569855, -226.8651660546161395 ) ) ;
#153631=ORIENTED_EDGE ( 'NONE', *, *, #215891, .F. ) ;
#153639=CARTESIAN_POINT ( 'NONE',  ( -20.94999999999999929, 18.18127959618848521, -237.5711165786817389 ) ) ;
#153646=ORIENTED_EDGE ( 'NONE', *, *, #237163, .T. ) ;
#153666=DIRECTION ( 'NONE',  ( 0.000000000000000000, -0.7960711469212456981, 0.6052030477777622375 ) ) ;
#153739=CARTESIAN_POINT ( 'NONE',  ( 21.05000000000000071, 11.43341603104965110, -245.8667934851861787 ) ) ;
#153746=CARTESIAN_POINT ( 'NONE',  ( 21.14999999999999858, 9.997527148596393687, -228.1702915402975407 ) ) ;
#153747=FACE_OUTER_BOUND ( 'NONE', #80643, .T. ) ;
#153765=CARTESIAN_POINT ( 'NONE',  ( -22.49510344025093644, -3.108862830562444834, -228.1724956784199208 ) ) ;
#153789=ORIENTED_EDGE ( 'NONE', *, *, #222391, .T. ) ;
#153794=EDGE_LOOP ( 'NONE', ( #101166, #62116, #114348, #1187 ) ) ;
#153801=ORIENTED_EDGE ( 'NONE', *, *, #27334, .F. ) ;
#153807=CARTESIAN_POINT ( 'NONE',  ( -18.59999999999999787, 43.35377423437995503, -245.1717807829448930 ) ) ;
#153816=FACE_OUTER_BOUND ( 'NONE', #228511, .T. ) ;
#153823=DIRECTION ( 'NONE',  ( 2.952720810173288619E-16, -0.4721928772777346239, -0.8814952561688430555 ) ) ;
#153825=CARTESIAN_POINT ( 'NONE',  ( -22.50000000000000000, 7.128833340093095217, -233.7327013124392749 ) ) ;
#153848=CARTESIAN_POINT ( 'NONE',  ( 21.05000000000000071, 36.65892442174935439, -249.5511627012433848 ) ) ;
#153856=ORIENTED_EDGE ( 'NONE', *, *, #62005, .T. ) ;
#153861=ORIENTED_EDGE ( 'NONE', *, *, #171635, .F. ) ;
#153865=DIRECTION ( 'NONE',  ( 0.000000000000000000, -0.4721928772777346239, -0.8814952561688430555 ) ) ;
#153876=AXIS2_PLACEMENT_3D ( 'NONE', #207584, #228430, #125470 ) ;
#153884=EDGE_CURVE ( 'NONE', #16612, #184466, #129704, .T. ) ;
#153891=VERTEX_POINT ( 'NONE', #248952 ) ;
#153907=ADVANCED_FACE ( 'NONE', ( #153747 ), #54580, .T. ) ;
#153913=CARTESIAN_POINT ( 'NONE',  ( -23.15000000000000213, 19.93396995659179893, -235.7707092203739307 ) ) ;
#153949=VERTEX_POINT ( 'NONE', #94993 ) ;
#153953=AXIS2_PLACEMENT_3D ( 'NONE', #108102, #204612, #83365 ) ;
#153972=EDGE_CURVE ( 'NONE', #237661, #21030, #79616, .T. ) ;
#153975=AXIS2_PLACEMENT_3D ( 'NONE', #3, #19591, #238628 ) ;
#153997=AXIS2_PLACEMENT_3D ( 'NONE', #97317, #176924, #253848 ) ;
#154001=DIRECTION ( 'NONE',  ( -1.000000000000000000, 0.000000000000000000, 0.000000000000000000 ) ) ;
#154051=ORIENTED_EDGE ( 'NONE', *, *, #91639, .F. ) ;
#154086=AXIS2_PLACEMENT_3D ( 'NONE', #12208, #170022, #33080 ) ;
#154099=EDGE_CURVE ( 'NONE', #84465, #19709, #46480, .T. ) ;
#154126=ORIENTED_EDGE ( 'NONE', *, *, #231421, .F. ) ;
#154150=AXIS2_PLACEMENT_3D ( 'NONE', #227308, #66954, #90360 ) ;
#154154=DIRECTION ( 'NONE',  ( 0.000000000000000000, -0.8814952561688430555, 0.4721928772777346239 ) ) ;
#154160=CARTESIAN_POINT ( 'NONE',  ( 18.59999999999999432, -3.616484641954614165, -226.0163245033746477 ) ) ;
#154163=CARTESIAN_POINT ( 'NONE',  ( 22.37643362114956247, 10.64233729798123029, -226.9638180893018955 ) ) ;
#154172=AXIS2_PLACEMENT_3D ( 'NONE', #162180, #241693, #63043 ) ;
#154177=AXIS2_PLACEMENT_3D ( 'NONE', #166043, #100854, #120500 ) ;
#154195=VERTEX_POINT ( 'NONE', #110391 ) ;
#154196=CARTESIAN_POINT ( 'NONE',  ( 20.85000000000000142, 36.46860332481993794, -249.8166405164294588 ) ) ;
#154248=EDGE_CURVE ( 'NONE', #19770, #139998, #34076, .T. ) ;
#154254=ORIENTED_EDGE ( 'NONE', *, *, #178070, .T. ) ;
#154261=ADVANCED_FACE ( 'NONE', ( #129939 ), #61578, .T. ) ;
#154275=FACE_OUTER_BOUND ( 'NONE', #149945, .T. ) ;
#154287=CARTESIAN_POINT ( 'NONE',  ( 23.24999999999999289, -0.1830918614494220220, -222.4987906021368360 ) ) ;
#154296=AXIS2_PLACEMENT_3D ( 'NONE', #27573, #70543, #107055 ) ;
#154301=CARTESIAN_POINT ( 'NONE',  ( -20.94403535211772294, 46.37740828070795374, -243.0652246697500800 ) ) ;
#154410=EDGE_CURVE ( 'NONE', #249890, #246507, #230023, .T. ) ;
#154422=CARTESIAN_POINT ( 'NONE',  ( -18.39999999999999858, 37.99112772578904895, -261.0419300540664835 ) ) ;
#154424=VECTOR ( 'NONE', #64856, 1000.000000000000000 ) ;
#154444=AXIS2_PLACEMENT_3D ( 'NONE', #191443, #179564, #76584 ) ;
#154450=DIRECTION ( 'NONE',  ( 1.000000000000000000, 0.000000000000000000, 0.000000000000000000 ) ) ;
#154462=ORIENTED_EDGE ( 'NONE', *, *, #95592, .F. ) ;
#154493=DIRECTION ( 'NONE',  ( 0.000000000000000000, 0.9371753822965326330, -0.3488585713686107592 ) ) ;
#154516=FACE_OUTER_BOUND ( 'NONE', #47575, .T. ) ;
#154534=EDGE_LOOP ( 'NONE', ( #10438, #66378, #183492, #196445 ) ) ;
#154630=CARTESIAN_POINT ( 'NONE',  ( 21.05000000000000071, 36.02367271998545561, -235.8812521208699309 ) ) ;
#154651=DIRECTION ( 'NONE',  ( 0.000000000000000000, 0.5273008465187821736, -0.8496786552930323255 ) ) ;
#154654=ORIENTED_EDGE ( 'NONE', *, *, #241766, .T. ) ;
#154725=CARTESIAN_POINT ( 'NONE',  ( -18.43473496883421348, 8.856286808022053592, -245.4294671909037504 ) ) ;
#154728=CARTESIAN_POINT ( 'NONE',  ( -21.02374657821557946, 36.02918351771350558, -236.0543695115171943 ) ) ;
#154735=CARTESIAN_POINT ( 'NONE',  ( 21.07928932188134397, 10.02993822722305062, -228.1074463178676979 ) ) ;
#154741=ORIENTED_EDGE ( 'NONE', *, *, #179901, .F. ) ;
#154811=ORIENTED_EDGE ( 'NONE', *, *, #238648, .T. ) ;
#154852=ORIENTED_EDGE ( 'NONE', *, *, #234052, .T. ) ;
#154886=VECTOR ( 'NONE', #119327, 1000.000000000000000 ) ;
#154911=DIRECTION ( 'NONE',  ( 0.000000000000000000, 0.8814952561688446098, -0.4721928772777316263 ) ) ;
#154913=DIRECTION ( 'NONE',  ( 1.000000000000000000, 0.000000000000000000, 0.000000000000000000 ) ) ;
#154930=CARTESIAN_POINT ( 'NONE',  ( -21.05000000000000071, 18.62343931468261360, -223.9512205031617498 ) ) ;
#154932=ORIENTED_EDGE ( 'NONE', *, *, #101087, .T. ) ;
#154936=EDGE_CURVE ( 'NONE', #189647, #172354, #79601, .T. ) ;
#154949=VERTEX_POINT ( 'NONE', #48661 ) ;
#154950=PLANE ( 'NONE',  #208257 ) ;
#154959=CARTESIAN_POINT ( 'NONE',  ( -21.05000000000000071, 13.71992543034163958, -238.5823796952984992 ) ) ;
#154972=DIRECTION ( 'NONE',  ( 0.000000000000000000, 0.8814952561688444987, -0.4721928772777320149 ) ) ;
#155020=VERTEX_POINT ( 'NONE', #36847 ) ;
#155046=CIRCLE ( 'NONE', #13554, 0.09999999999999986677 ) ;
#155074=EDGE_LOOP ( 'NONE', ( #116525, #187813, #150929, #58238 ) ) ;
#155080=DIRECTION ( 'NONE',  ( 1.000000000000000000, 7.166229603267616255E-16, 4.447280054184918885E-16 ) ) ;
#155156=VERTEX_POINT ( 'NONE', #61517 ) ;
#155173=CARTESIAN_POINT ( 'NONE',  ( -21.05000000000000071, 13.71992543034163958, -238.5823796952984992 ) ) ;
#155176=CARTESIAN_POINT ( 'NONE',  ( 23.14999999999998437, 7.128833340093095217, -233.7327013124392749 ) ) ;
#155183=ADVANCED_FACE ( 'NONE', ( #177639 ), #81049, .T. ) ;
#155207=CIRCLE ( 'NONE', #5293, 4.049999999999994493 ) ;
#155219=DIRECTION ( 'NONE',  ( -0.000000000000000000, -0.8814952561688430555, 0.4721928772777344019 ) ) ;
#155241=VERTEX_POINT ( 'NONE', #23702 ) ;
#155254=ADVANCED_FACE ( 'NONE', ( #120240 ), #21129, .F. ) ;
#155265=CARTESIAN_POINT ( 'NONE',  ( 20.99142135623731065, 36.02918351690956200, -236.0543695120160805 ) ) ;
#155305=CARTESIAN_POINT ( 'NONE',  ( 20.94999999999999929, 40.18490544642472173, -251.4399342103543233 ) ) ;
#155306=DIRECTION ( 'NONE',  ( -3.265361837132812600E-16, 0.4721928772777346239, 0.8814952561688430555 ) ) ;
#155310=EDGE_CURVE ( 'NONE', #253481, #9372, #658, .T. ) ;
#155312=DIRECTION ( 'NONE',  ( -0.000000000000000000, 0.8814952561688430555, -0.4721928772777346239 ) ) ;
#155317=CARTESIAN_POINT ( 'NONE',  ( 21.05000012384647690, 22.88246860595696219, -230.1138889447267957 ) ) ;
#155333=ADVANCED_FACE ( 'NONE', ( #204853 ), #183858, .T. ) ;
#155342=ORIENTED_EDGE ( 'NONE', *, *, #89318, .F. ) ;
#155365=ORIENTED_EDGE ( 'NONE', *, *, #132076, .F. ) ;
#155380=DIRECTION ( 'NONE',  ( 0.000000000000000000, -0.8814952561688430555, 0.4721928772777346239 ) ) ;
#155390=VERTEX_POINT ( 'NONE', #184017 ) ;
#155399=VERTEX_POINT ( 'NONE', #207457 ) ;
#155411=CARTESIAN_POINT ( 'NONE',  ( 20.95224633520496127, 18.81837940936716791, -229.8973978886525913 ) ) ;
#155432=ADVANCED_FACE ( 'NONE', ( #16962 ), #31410, .F. ) ;
#155455=EDGE_CURVE ( 'NONE', #125245, #117081, #142332, .T. ) ;
#155487=DIRECTION ( 'NONE',  ( -1.000000000000000000, 0.000000000000000000, 0.000000000000000000 ) ) ;
#155574=DIRECTION ( 'NONE',  ( -1.000000000000000000, -0.000000000000000000, -0.000000000000000000 ) ) ;
#155590=FACE_OUTER_BOUND ( 'NONE', #236346, .T. ) ;
#155652=EDGE_CURVE ( 'NONE', #82258, #237661, #179962, .T. ) ;
#155697=DIRECTION ( 'NONE',  ( 0.000000000000000000, -0.8814952561688430555, 0.4721928772777346239 ) ) ;
#155701=ORIENTED_EDGE ( 'NONE', *, *, #209888, .T. ) ;
#155705=DIRECTION ( 'NONE',  ( -1.000000000000000000, 0.000000000000000000, 0.000000000000000000 ) ) ;
#155767=DIRECTION ( 'NONE',  ( 1.000000000000000000, 0.000000000000000000, 0.000000000000000000 ) ) ;
#155769=CARTESIAN_POINT ( 'NONE',  ( -21.05000000000000071, 10.30543449102040476, -228.0143625250146329 ) ) ;
#155775=CARTESIAN_POINT ( 'NONE',  ( 18.47654891039377034, 8.940911883994163034, -245.4411313438577054 ) ) ;
#155779=DIRECTION ( 'NONE',  ( 0.000000000000000000, 0.8814952561688438326, -0.4721928772777331251 ) ) ;
#155780=CARTESIAN_POINT ( 'NONE',  ( 21.05000000000000071, 1.658775325992685845, -230.6916041481568982 ) ) ;
#155835=ORIENTED_EDGE ( 'NONE', *, *, #114162, .T. ) ;
#155856=VECTOR ( 'NONE', #202944, 1000.000000000000000 ) ;
#155883=ORIENTED_EDGE ( 'NONE', *, *, #132597, .T. ) ;
#155909=CARTESIAN_POINT ( 'NONE',  ( -18.59999999999999787, 42.15997144203495139, -239.2817429668763793 ) ) ;
#155926=LINE ( 'NONE', #235418, #6032 ) ;
#155932=EDGE_CURVE ( 'NONE', #97404, #98428, #19201, .T. ) ;
#155935=CARTESIAN_POINT ( 'NONE',  ( -18.59999999999999787, 16.44800918141279311, -240.8068063186265135 ) ) ;
#155956=ORIENTED_EDGE ( 'NONE', *, *, #80620, .T. ) ;
#156004=VERTEX_POINT ( 'NONE', #178303 ) ;
#156006=EDGE_LOOP ( 'NONE', ( #25537, #45101, #240168, #140779 ) ) ;
#156007=CARTESIAN_POINT ( 'NONE',  ( -18.59999999999999787, 36.65892442174935439, -249.5511627012433848 ) ) ;
#156016=CARTESIAN_POINT ( 'NONE',  ( 21.11833042828145324, 10.16616178894255107, -228.0475432820529136 ) ) ;
#156022=CARTESIAN_POINT ( 'NONE',  ( 18.57071067811864040, 30.66719544722269220, -234.7938047061825841 ) ) ;
#156040=EDGE_LOOP ( 'NONE', ( #147297, #176105, #154811, #73929, #99813, #58063, #119065, #86538, #82196, #109902 ) ) ;
#156049=LINE ( 'NONE', #235544, #139537 ) ;
#156057=AXIS2_PLACEMENT_3D ( 'NONE', #91771, #34390, #231298 ) ;
#156072=EDGE_CURVE ( 'NONE', #39363, #123093, #176062, .T. ) ;
#156073=CARTESIAN_POINT ( 'NONE',  ( -18.50000000000000000, 7.128833340093095217, -233.7327013124392749 ) ) ;
#156091=CYLINDRICAL_SURFACE ( 'NONE', #47301, 0.1000000000000013933 ) ;
#156126=ORIENTED_EDGE ( 'NONE', *, *, #221851, .F. ) ;
#156132=CIRCLE ( 'NONE', #76391, 0.1000000000000105804 ) ;
#156186=ADVANCED_FACE ( 'NONE', ( #23079 ), #226361, .F. ) ;
#156205=CARTESIAN_POINT ( 'NONE',  ( 21.11345278033269324, 22.11771856871110487, -231.6856372840668428 ) ) ;
#156247=ORIENTED_EDGE ( 'NONE', *, *, #144151, .T. ) ;
#156261=CARTESIAN_POINT ( 'NONE',  ( 18.49999999999999645, 36.65892442174935439, -249.5511627012433848 ) ) ;
#156278=EDGE_CURVE ( 'NONE', #236113, #82258, #254591, .T. ) ;
#156300=ORIENTED_EDGE ( 'NONE', *, *, #66638, .F. ) ;
#156314=AXIS2_PLACEMENT_3D ( 'NONE', #108026, #70205, #153615 ) ;
#156327=CARTESIAN_POINT ( 'NONE',  ( 21.12769345151713196, 22.98650045582965618, -230.0668730597805052 ) ) ;
#156347=CARTESIAN_POINT ( 'NONE',  ( -21.05000000000000071, 28.63831050940605394, -258.0693639473472558 ) ) ;
#156373=EDGE_CURVE ( 'NONE', #79099, #131441, #189161, .T. ) ;
#156411=ORIENTED_EDGE ( 'NONE', *, *, #158627, .T. ) ;
#156438=VERTEX_POINT ( 'NONE', #45839 ) ;
#156439=AXIS2_PLACEMENT_3D ( 'NONE', #19611, #203375, #99106 ) ;
#156446=DIRECTION ( 'NONE',  ( 0.000000000000000000, -0.8814952561688410571, 0.4721928772777385097 ) ) ;
#156449=CIRCLE ( 'NONE', #223216, 0.2000000000000052014 ) ;
#156463=CARTESIAN_POINT ( 'NONE',  ( -18.50000000000000000, 30.36376046184471988, -235.5720385971402493 ) ) ;
#156465=DIRECTION ( 'NONE',  ( 0.000000000000000000, -0.8814952561688430555, 0.4721928772777346239 ) ) ;
#156496=CARTESIAN_POINT ( 'NONE',  ( 20.97224591636398827, 22.94420667656951807, -230.1510067393869576 ) ) ;
#156499=ORIENTED_EDGE ( 'NONE', *, *, #99618, .F. ) ;
#156518=FACE_OUTER_BOUND ( 'NONE', #159547, .T. ) ;
#156528=ORIENTED_EDGE ( 'NONE', *, *, #231237, .T. ) ;
#156535=FACE_OUTER_BOUND ( 'NONE', #99920, .T. ) ;
#156549=DIRECTION ( 'NONE',  ( 0.000000000000000000, -0.3343365196859449662, 0.9424537609900497381 ) ) ;
#156583=ADVANCED_FACE ( 'NONE', ( #156535 ), #236029, .F. ) ;
#156585=VECTOR ( 'NONE', #178960, 1000.000000000000000 ) ;
#156607=CARTESIAN_POINT ( 'NONE',  ( 21.04999999999999716, 22.85780672939456792, -230.1006782354234872 ) ) ;
#156611=CYLINDRICAL_SURFACE ( 'NONE', #94753, 0.09999999999999939493 ) ;
#156692=ORIENTED_EDGE ( 'NONE', *, *, #125289, .F. ) ;
#156710=VERTEX_POINT ( 'NONE', #78231 ) ;
#156718=CARTESIAN_POINT ( 'NONE',  ( 18.49999999999999645, 16.56538529403860238, -240.6448716151659823 ) ) ;
#156754=ORIENTED_EDGE ( 'NONE', *, *, #192949, .T. ) ;
#156850=CARTESIAN_POINT ( 'NONE',  ( -20.85882249326303040, 46.46967969402478360, -243.0849751855955674 ) ) ;
#156864=DIRECTION ( 'NONE',  ( 0.000000000000000000, -0.4721928772777346239, -0.8814952561688430555 ) ) ;
#156865=DIRECTION ( 'NONE',  ( 0.000000000000000000, 0.4721928772777346239, 0.8814952561688430555 ) ) ;
#156870=VERTEX_POINT ( 'NONE', #147201 ) ;
#156885=FACE_OUTER_BOUND ( 'NONE', #208143, .T. ) ;
#156907=AXIS2_PLACEMENT_3D ( 'NONE', #168771, #93023, #209117 ) ;
#156942=EDGE_LOOP ( 'NONE', ( #139349, #150310, #49842, #192867 ) ) ;
#156953=CARTESIAN_POINT ( 'NONE',  ( 23.14999999999999858, 37.65052946403260137, -247.7000226632887916 ) ) ;
#156982=VECTOR ( 'NONE', #150335, 1000.000000000000114 ) ;
#157001=FACE_OUTER_BOUND ( 'NONE', #106608, .T. ) ;
#157003=VECTOR ( 'NONE', #22880, 1000.000000000000000 ) ;
#157055=CARTESIAN_POINT ( 'NONE',  ( 21.05000000000000071, 18.81732247075047937, -230.0377732242114632 ) ) ;
#157063=EDGE_CURVE ( 'NONE', #178909, #135829, #43770, .T. ) ;
#157068=ORIENTED_EDGE ( 'NONE', *, *, #30199, .F. ) ;
#157077=SPHERICAL_SURFACE ( 'NONE', #165994, 0.1000000000000000056 ) ;
#157098=CARTESIAN_POINT ( 'NONE',  ( -18.39999999999999858, -7.667348966301519297, -236.4704904124130280 ) ) ;
#157103=ADVANCED_FACE ( 'NONE', ( #200449 ), #2224, .F. ) ;
#157114=FACE_OUTER_BOUND ( 'NONE', #235219, .T. ) ;
#157125=AXIS2_PLACEMENT_3D ( 'NONE', #4696, #65977, #84191 ) ;
#157169=CARTESIAN_POINT ( 'NONE',  ( -18.59999999999999787, 13.66123737402873495, -238.6633470470287648 ) ) ;
#157222=ORIENTED_EDGE ( 'NONE', *, *, #93247, .F. ) ;
#157287=FACE_OUTER_BOUND ( 'NONE', #162276, .T. ) ;
#157289=CARTESIAN_POINT ( 'NONE',  ( -18.42609945526393034, 8.812905974021688849, -245.4119551042256546 ) ) ;
#157301=CARTESIAN_POINT ( 'NONE',  ( 20.94999999999999929, 36.65892442174935439, -249.5511627012433848 ) ) ;
#157303=AXIS2_PLACEMENT_3D ( 'NONE', #115323, #55321, #216979 ) ;
#157322=EDGE_CURVE ( 'NONE', #15847, #105736, #168733, .T. ) ;
#157381=VERTEX_POINT ( 'NONE', #93324 ) ;
#157387=VERTEX_POINT ( 'NONE', #131168 ) ;
#157397=EDGE_CURVE ( 'NONE', #158507, #184576, #92041, .T. ) ;
#157417=ORIENTED_EDGE ( 'NONE', *, *, #143483, .T. ) ;
#157454=ORIENTED_EDGE ( 'NONE', *, *, #189191, .F. ) ;
#157479=CIRCLE ( 'NONE', #53388, 0.5000000000000008882 ) ;
#157486=AXIS2_PLACEMENT_3D ( 'NONE', #52557, #211665, #133401 ) ;
#157487=CARTESIAN_POINT ( 'NONE',  ( 20.94999999999999929, 28.32080209959243788, -238.8452605374484676 ) ) ;
#157515=CARTESIAN_POINT ( 'NONE',  ( 23.14999999999999858, 36.65892442174935439, -249.5511627012433848 ) ) ;
#157593=DIRECTION ( 'NONE',  ( 1.000000000000000000, 0.000000000000000000, 0.000000000000000000 ) ) ;
#157602=CARTESIAN_POINT ( 'NONE',  ( -21.05000000000000071, 14.77103648604101060, -236.4083752604501001 ) ) ;
#157632=DIRECTION ( 'NONE',  ( -1.000000000000000000, 0.000000000000000000, 0.000000000000000000 ) ) ;
#157635=EDGE_CURVE ( 'NONE', #184466, #54594, #31147, .T. ) ;
#157657=ORIENTED_EDGE ( 'NONE', *, *, #242764, .T. ) ;
#157670=VECTOR ( 'NONE', #152031, 1000.000000000000000 ) ;
#157672=ORIENTED_EDGE ( 'NONE', *, *, #144784, .F. ) ;
#157704=CARTESIAN_POINT ( 'NONE',  ( -20.94999999999999929, 28.15345123516638282, -259.0759448016705733 ) ) ;
#157744=ADVANCED_FACE ( 'NONE', ( #184421 ), #27032, .F. ) ;
#157767=AXIS2_PLACEMENT_3D ( 'NONE', #75690, #96494, #216455 ) ;
#157774=EDGE_LOOP ( 'NONE', ( #256881, #176691, #183486, #218383 ) ) ;
#157794=ORIENTED_EDGE ( 'NONE', *, *, #253872, .F. ) ;
#157809=EDGE_CURVE ( 'NONE', #15834, #16895, #72830, .T. ) ;
#157825=EDGE_CURVE ( 'NONE', #121353, #177802, #176864, .T. ) ;
#157864=DIRECTION ( 'NONE',  ( 0.000000000000000000, -0.4721928772777346239, -0.8814952561688430555 ) ) ;
#157876=CARTESIAN_POINT ( 'NONE',  ( -18.50000000000000000, 46.33035574435032800, -243.0552603638195137 ) ) ;
#157901=ORIENTED_EDGE ( 'NONE', *, *, #94922, .T. ) ;
#157962=CARTESIAN_POINT ( 'NONE',  ( -20.54999999999999716, 36.65892442174935439, -249.5511627012433848 ) ) ;
#157987=ORIENTED_EDGE ( 'NONE', *, *, #188462, .T. ) ;
#157994=EDGE_CURVE ( 'NONE', #155156, #161523, #252038, .T. ) ;
#158030=EDGE_CURVE ( 'NONE', #179549, #182938, #207238, .T. ) ;
#158053=LINE ( 'NONE', #253238, #11244 ) ;
#158134=ADVANCED_FACE ( 'NONE', ( #90010 ), #194286, .F. ) ;
#158153=CARTESIAN_POINT ( 'NONE',  ( -20.54999999999999716, 23.68770167995059595, -252.8127582590406348 ) ) ;
#158176=CARTESIAN_POINT ( 'NONE',  ( 18.49999999999999289, 43.24695311518262031, -245.0026972281755491 ) ) ;
#158180=EDGE_CURVE ( 'NONE', #135829, #216206, #17138, .T. ) ;
#158184=EDGE_CURVE ( 'NONE', #231868, #84289, #85401, .T. ) ;
#158189=CIRCLE ( 'NONE', #8116, 0.1000000000000012546 ) ;
#158195=DIRECTION ( 'NONE',  ( 0.000000000000000000, 0.8814952561688432775, -0.4721928772777344019 ) ) ;
#158212=FACE_OUTER_BOUND ( 'NONE', #83696, .T. ) ;
#158217=FACE_OUTER_BOUND ( 'NONE', #33941, .T. ) ;
#158247=EDGE_LOOP ( 'NONE', ( #99515, #119399, #173252, #205632 ) ) ;
#158271=DIRECTION ( 'NONE',  ( 0.000000000000000000, 0.5868805631290353597, 0.8096735173027127530 ) ) ;
#158276=CARTESIAN_POINT ( 'NONE',  ( -18.46919391072097838, 37.97540340137230430, -261.2271828652933436 ) ) ;
#158295=VERTEX_POINT ( 'NONE', #7833 ) ;
#158317=ORIENTED_EDGE ( 'NONE', *, *, #187171, .F. ) ;
#158320=DIRECTION ( 'NONE',  ( 0.000000000000000000, 0.8814952561688432775, -0.4721928772777345129 ) ) ;
#158337=CARTESIAN_POINT ( 'NONE',  ( -21.05000000000000071, 18.82290990851282331, -233.3604470821920529 ) ) ;
#158340=DIRECTION ( 'NONE',  ( 0.000000000000000000, 0.8814952561688438326, -0.4721928772777331806 ) ) ;
#158346=EDGE_CURVE ( 'NONE', #63327, #153891, #135498, .T. ) ;
#158349=DIRECTION ( 'NONE',  ( -1.387778780781259631E-13, 0.1675535138457220907, -0.9858629823651720026 ) ) ;
#158355=DIRECTION ( 'NONE',  ( 1.000000000000000000, 0.000000000000000000, 0.000000000000000000 ) ) ;
#158382=CYLINDRICAL_SURFACE ( 'NONE', #233935, 0.8750000000000007772 ) ;
#158394=CYLINDRICAL_SURFACE ( 'NONE', #124888, 0.5000000000000008882 ) ;
#158410=FACE_OUTER_BOUND ( 'NONE', #2546, .T. ) ;
#158425=AXIS2_PLACEMENT_3D ( 'NONE', #184025, #101898, #181483 ) ;
#158436=ORIENTED_EDGE ( 'NONE', *, *, #101821, .T. ) ;
#158439=AXIS2_PLACEMENT_3D ( 'NONE', #49617, #91322, #129164 ) ;
#158460=CARTESIAN_POINT ( 'NONE',  ( -20.64999999999999858, 34.98408343502854478, -248.6539962344157004 ) ) ;
#158468=DIRECTION ( 'NONE',  ( 0.000000000000000000, 0.8814952561688434995, -0.4721928772777337913 ) ) ;
#158474=EDGE_CURVE ( 'NONE', #16895, #253739, #163333, .T. ) ;
#158496=DIRECTION ( 'NONE',  ( 0.000000000000000000, -0.8814952561688449428, 0.4721928772777310157 ) ) ;
#158499=FACE_BOUND ( 'NONE', #245131, .T. ) ;
#158502=VERTEX_POINT ( 'NONE', #12983 ) ;
#158507=VERTEX_POINT ( 'NONE', #190327 ) ;
#158513=DIRECTION ( 'NONE',  ( 0.7071067811865485719, 0.6233112732207607420, -0.3338907855510728773 ) ) ;
#158517=ORIENTED_EDGE ( 'NONE', *, *, #153884, .T. ) ;
#158518=EDGE_LOOP ( 'NONE', ( #231011, #230062, #155701, #152642 ) ) ;
#158568=CARTESIAN_POINT ( 'NONE',  ( 21.05000000000000071, 12.62988036037870998, -223.4632815780722410 ) ) ;
#158574=CARTESIAN_POINT ( 'NONE',  ( -18.59999996769639097, 9.038014976666358891, -245.3774329978512014 ) ) ;
#158584=DIRECTION ( 'NONE',  ( 1.000000000000000000, 0.000000000000000000, 0.000000000000000000 ) ) ;
#158585=CIRCLE ( 'NONE', #229310, 11.75000000000000533 ) ;
#158606=CIRCLE ( 'NONE', #196176, 0.2000000000000101419 ) ;
#158627=EDGE_CURVE ( 'NONE', #164610, #248838, #16925, .T. ) ;
#158649=DIRECTION ( 'NONE',  ( 0.000000000000000000, 0.3488585713686311318, 0.9371753822965249725 ) ) ;
#158650=DIRECTION ( 'NONE',  ( 1.000000000000000000, 0.000000000000000000, 0.000000000000000000 ) ) ;
#158654=DIRECTION ( 'NONE',  ( -0.8660254037844515862, -0.4407476280843962146, 0.2360964386388669234 ) ) ;
#158655=DIRECTION ( 'NONE',  ( 0.000000000000000000, 0.8814952561688437216, -0.4721928772777334582 ) ) ;
#158659=ORIENTED_EDGE ( 'NONE', *, *, #205662, .T. ) ;
#158667=CARTESIAN_POINT ( 'NONE',  ( 21.14999999999999503, 7.128833340093095217, -233.7327013124392749 ) ) ;
#158670=ORIENTED_EDGE ( 'NONE', *, *, #34653, .T. ) ;
#158691=ORIENTED_EDGE ( 'NONE', *, *, #197065, .F. ) ;
#158728=CARTESIAN_POINT ( 'NONE',  ( 20.04142135623730070, 31.44980407958351165, -233.5445995079518866 ) ) ;
#158743=CARTESIAN_POINT ( 'NONE',  ( 20.94999999999999929, 30.48727911274996671, -240.1192265702093209 ) ) ;
#158750=CARTESIAN_POINT ( 'NONE',  ( -21.05000000000000071, 18.92285928089247804, -233.3572654221044900 ) ) ;
#158781=CARTESIAN_POINT ( 'NONE',  ( 22.60000000000000142, 7.128833340093095217, -233.7327013124392749 ) ) ;
#158798=ORIENTED_EDGE ( 'NONE', *, *, #102349, .T. ) ;
#158822=FACE_OUTER_BOUND ( 'NONE', #20923, .T. ) ;
#158829=ORIENTED_EDGE ( 'NONE', *, *, #173455, .F. ) ;
#158835=VECTOR ( 'NONE', #167354, 1000.000000000000000 ) ;
#158836=B_SPLINE_CURVE_WITH_KNOTS ( 'NONE', 3,
 ( #123842, #162980, #121305, #24765, #82107, #61293, #22185, #202092, #164257, #178709 ),
 .UNSPECIFIED., .F., .F.,
 ( 4, 2, 2, 2, 4 ),
 ( 0.000000000000000000, 0.0001660831991682130656, 0.0002491247987523196390, 0.0002906455985443753788, 0.0003321663983364311727 ),
 .UNSPECIFIED. ) ;
#158848=EDGE_CURVE ( 'NONE', #149361, #227159, #64955, .T. ) ;
#158864=CARTESIAN_POINT ( 'NONE',  ( -18.43569575749026512, 8.780520186313282238, -245.4165333277510399 ) ) ;
#158874=ORIENTED_EDGE ( 'NONE', *, *, #251499, .T. ) ;
#158897=DIRECTION ( 'NONE',  ( 0.000000000000000000, 0.8814952561688430555, -0.4721928772777346239 ) ) ;
#158909=CARTESIAN_POINT ( 'NONE',  ( 20.86777300164945004, 46.46797214202639026, -243.0846070113367432 ) ) ;
#158919=ORIENTED_EDGE ( 'NONE', *, *, #136132, .F. ) ;
#158927=AXIS2_PLACEMENT_3D ( 'NONE', #82292, #161887, #221806 ) ;
#158955=CYLINDRICAL_SURFACE ( 'NONE', #249681, 0.09999999999998304689 ) ;
#159033=ORIENTED_EDGE ( 'NONE', *, *, #3042, .T. ) ;
#159042=EDGE_CURVE ( 'NONE', #201516, #175441, #3326, .T. ) ;
#159078=DIRECTION ( 'NONE',  ( -1.000000000000000000, 0.000000000000000000, 0.000000000000000000 ) ) ;
#159104=DIRECTION ( 'NONE',  ( -1.000000000000000000, 0.000000000000000000, 0.000000000000000000 ) ) ;
#159123=CARTESIAN_POINT ( 'NONE',  ( -18.54270223418609831, 38.05659262219499794, -261.2177875638973319 ) ) ;
#159146=CYLINDRICAL_SURFACE ( 'NONE', #56200, 0.1000000000000075273 ) ;
#159193=CARTESIAN_POINT ( 'NONE',  ( 20.85000000000000142, 42.92545512184477730, -254.1955779480491344 ) ) ;
#159212=VERTEX_POINT ( 'NONE', #54029 ) ;
#159261=ORIENTED_EDGE ( 'NONE', *, *, #130032, .F. ) ;
#159267=ORIENTED_EDGE ( 'NONE', *, *, #19921, .F. ) ;
#159276=CARTESIAN_POINT ( 'NONE',  ( 20.94999999999999574, 4.184122562697137226, -245.3714803909117279 ) ) ;
#159291=ORIENTED_EDGE ( 'NONE', *, *, #3776, .F. ) ;
#159299=VECTOR ( 'NONE', #194219, 1000.000000000000000 ) ;
#159316=TOROIDAL_SURFACE ( 'NONE', #163396, 0.2000000000000000111, 0.1000000000000000056 ) ;
#159327=EDGE_LOOP ( 'NONE', ( #122729, #115943, #123981 ) ) ;
#159335=( LENGTH_UNIT ( ) NAMED_UNIT ( * ) SI_UNIT ( .MILLI., .METRE. ) );
#159339=EDGE_LOOP ( 'NONE', ( #123804, #255370, #1070, #43094 ) ) ;
#159360=CARTESIAN_POINT ( 'NONE',  ( 22.50000000000000000, -3.092988775432913506, -228.1437074281570858 ) ) ;
#159364=EDGE_LOOP ( 'NONE', ( #2716, #194722, #114994, #150515 ) ) ;
#159365=ORIENTED_EDGE ( 'NONE', *, *, #60620, .T. ) ;
#159430=ORIENTED_EDGE ( 'NONE', *, *, #50486, .T. ) ;
#159468=ADVANCED_FACE ( 'NONE', ( #33901 ), #246782, .T. ) ;
#159472=ADVANCED_FACE ( 'NONE', ( #206389 ), #227224, .T. ) ;
#159506=DIRECTION ( 'NONE',  ( 0.000000000000000000, -0.8814952561688430555, 0.4721928772777346239 ) ) ;
#159517=AXIS2_PLACEMENT_3D ( 'NONE', #23194, #101364, #45301 ) ;
#159519=VERTEX_POINT ( 'NONE', #53411 ) ;
#159531=CARTESIAN_POINT ( 'NONE',  ( 23.14999999999999858, 36.02918351690956200, -236.0543695120161374 ) ) ;
#159547=EDGE_LOOP ( 'NONE', ( #17350, #50850, #48361, #111098 ) ) ;
#159559=CARTESIAN_POINT ( 'NONE',  ( 21.98333005346336577, 0.6286209188979451357, -230.2507154655492343 ) ) ;
#159601=EDGE_CURVE ( 'NONE', #15247, #126382, #27956, .T. ) ;
#159605=CARTESIAN_POINT ( 'NONE',  ( 18.50000000000000000, 26.26588584238432489, -255.7307459359297468 ) ) ;
#159612=ORIENTED_EDGE ( 'NONE', *, *, #15827, .T. ) ;
#159615=ORIENTED_EDGE ( 'NONE', *, *, #34849, .T. ) ;
#159631=CIRCLE ( 'NONE', #192959, 11.90000000000000036 ) ;
#159644=ORIENTED_EDGE ( 'NONE', *, *, #212774, .F. ) ;
#159649=CIRCLE ( 'NONE', #143047, 1.999999999999990452 ) ;
#159665=AXIS2_PLACEMENT_3D ( 'NONE', #153807, #29985, #232026 ) ;
#159720=EDGE_CURVE ( 'NONE', #253241, #155399, #194729, .T. ) ;
#159757=FACE_OUTER_BOUND ( 'NONE', #179892, .T. ) ;
#159788=AXIS2_PLACEMENT_3D ( 'NONE', #244991, #6378, #202023 ) ;
#159813=CARTESIAN_POINT ( 'NONE',  ( -21.05000000000000071, 16.53615870702968138, -240.8540256063542984 ) ) ;
#159817=CARTESIAN_POINT ( 'NONE',  ( 20.94999999999999929, 23.68770167995059239, -252.8127582590406348 ) ) ;
#159831=TOROIDAL_SURFACE ( 'NONE', #172535, 0.6000000000000004219, 0.1000000000000000056 ) ;
#159837=CARTESIAN_POINT ( 'NONE',  ( 22.01447462590973458, 0.7725924869657057048, -230.2154859497122459 ) ) ;
#159842=CIRCLE ( 'NONE', #5866, 0.1000000000000075273 ) ;
#159861=VERTEX_POINT ( 'NONE', #207047 ) ;
#159880=DIRECTION ( 'NONE',  ( 0.000000000000000000, 0.8814952561688429444, -0.4721928772777349015 ) ) ;
#159885=CARTESIAN_POINT ( 'NONE',  ( -21.52071067811865746, 21.68862476185342558, -232.7068767132159621 ) ) ;
#159890=ORIENTED_EDGE ( 'NONE', *, *, #159601, .F. ) ;
#159931=CARTESIAN_POINT ( 'NONE',  ( -20.99142135623731065, 36.02918351690956200, -236.0543695120160805 ) ) ;
#159950=ORIENTED_EDGE ( 'NONE', *, *, #80906, .T. ) ;
#159952=ORIENTED_EDGE ( 'NONE', *, *, #124439, .T. ) ;
#159962=LINE ( 'NONE', #222444, #32766 ) ;
#160015=VECTOR ( 'NONE', #205293, 1000.000000000000000 ) ;
#160043=AXIS2_PLACEMENT_3D ( 'NONE', #570, #175407, #217046 ) ;
#160052=DIRECTION ( 'NONE',  ( -1.000000000000000000, 0.000000000000000000, 0.000000000000000000 ) ) ;
#160067=DIRECTION ( 'NONE',  ( 0.000000000000000000, -0.8814952561685545085, 0.4721928772782730821 ) ) ;
#160094=EDGE_LOOP ( 'NONE', ( #253745, #25036, #91094, #113917 ) ) ;
#160100=ADVANCED_FACE ( 'NONE', ( #103745 ), #223891, .F. ) ;
#160115=ORIENTED_EDGE ( 'NONE', *, *, #215171, .T. ) ;
#160141=AXIS2_PLACEMENT_3D ( 'NONE', #133184, #211433, #171072 ) ;
#160158=DIRECTION ( 'NONE',  ( -1.000000000000000000, 0.000000000000000000, 0.000000000000000000 ) ) ;
#160187=ORIENTED_EDGE ( 'NONE', *, *, #244043, .F. ) ;
#160236=ORIENTED_EDGE ( 'NONE', *, *, #218316, .T. ) ;
#160246=DIRECTION ( 'NONE',  ( 0.000000000000000000, 0.8814952561688430555, -0.4721928772777346239 ) ) ;
#160281=EDGE_LOOP ( 'NONE', ( #199226, #191531, #132122, #158874 ) ) ;
#160327=CARTESIAN_POINT ( 'NONE',  ( 23.14999999999999858, 36.65892442174935439, -249.5511627012433848 ) ) ;
#160337=EDGE_CURVE ( 'NONE', #206320, #213275, #45030, .T. ) ;
#160343=EDGE_CURVE ( 'NONE', #53624, #132943, #221432, .T. ) ;
#160346=AXIS2_PLACEMENT_3D ( 'NONE', #237704, #36967, #59021 ) ;
#160352=CIRCLE ( 'NONE', #47870, 0.5000000000000008882 ) ;
#160360=CIRCLE ( 'NONE', #222662, 0.09999999999998304689 ) ;
#160427=CARTESIAN_POINT ( 'NONE',  ( -18.56579813702276027, 46.46179379974391566, -243.0832762246653544 ) ) ;
#160449=VERTEX_POINT ( 'NONE', #104714 ) ;
#160475=DIRECTION ( 'NONE',  ( 1.000000000000000000, 0.000000000000000000, 0.000000000000000000 ) ) ;
#160478=ORIENTED_EDGE ( 'NONE', *, *, #36252, .T. ) ;
#160495=EDGE_CURVE ( 'NONE', #53791, #95344, #70798, .T. ) ;
#160511=AXIS2_PLACEMENT_3D ( 'NONE', #173233, #190194, #12849 ) ;
#160522=AXIS2_PLACEMENT_3D ( 'NONE', #3304, #63291, #142808 ) ;
#160600=EDGE_LOOP ( 'NONE', ( #87363, #114022, #196683 ) ) ;
#160613=DIRECTION ( 'NONE',  ( 0.7071359030027362103, -0.3338770338704923346, -0.6232856014206863415 ) ) ;
#160616=DIRECTION ( 'NONE',  ( 0.000000000000000000, 0.4721928772777652106, 0.8814952561688266242 ) ) ;
#160624=EDGE_CURVE ( 'NONE', #245180, #199913, #134571, .T. ) ;
#160638=DIRECTION ( 'NONE',  ( 0.000000000000000000, 0.8814952561688437216, -0.4721928772777334582 ) ) ;
#160639=DIRECTION ( 'NONE',  ( 0.000000000000000000, -0.5868805631290353597, -0.8096735173027127530 ) ) ;
#160652=ORIENTED_EDGE ( 'NONE', *, *, #9258, .T. ) ;
#160658=LINE ( 'NONE', #182771, #151123 ) ;
#160659=EDGE_CURVE ( 'NONE', #118730, #102393, #98007, .T. ) ;
#160662=ORIENTED_EDGE ( 'NONE', *, *, #50828, .T. ) ;
#160672=AXIS2_PLACEMENT_3D ( 'NONE', #246047, #106501, #66119 ) ;
#160676=EDGE_LOOP ( 'NONE', ( #252020, #81048, #169644, #49223 ) ) ;
#160677=CARTESIAN_POINT ( 'NONE',  ( 19.75857864376268935, 34.58225676390223668, -235.1091250528070589 ) ) ;
#160688=ORIENTED_EDGE ( 'NONE', *, *, #40307, .F. ) ;
#160742=ORIENTED_EDGE ( 'NONE', *, *, #71658, .F. ) ;
#160749=CARTESIAN_POINT ( 'NONE',  ( -21.45000000000000284, 21.56708615768143034, -232.7219885528102736 ) ) ;
#160790=VERTEX_POINT ( 'NONE', #200996 ) ;
#160825=ORIENTED_EDGE ( 'NONE', *, *, #190126, .T. ) ;
#160850=CARTESIAN_POINT ( 'NONE',  ( 21.05000000000000071, 19.92792862942048870, -235.1286901285539841 ) ) ;
#160865=DIRECTION ( 'NONE',  ( -1.000000000000000000, 0.000000000000000000, 0.000000000000000000 ) ) ;
#160868=VECTOR ( 'NONE', #228062, 1000.000000000000114 ) ;
#160880=EDGE_LOOP ( 'NONE', ( #118093, #87034, #159950, #213677, #253673, #169764, #241528 ) ) ;
#160916=B_SPLINE_CURVE_WITH_KNOTS ( 'NONE', 3,
 ( #49890, #250647, #208966, #132001, #189414, #10775, #231126, #169895 ),
 .UNSPECIFIED., .F., .F.,
 ( 4, 2, 2, 4 ),
 ( 0.000000000000000000, 0.0001306511400391350121, 0.0001959767100587021793, 0.0002613022800782693737 ),
 .UNSPECIFIED. ) ;
#160927=FACE_BOUND ( 'NONE', #142162, .T. ) ;
#160928=LINE ( 'NONE', #4392, #107697 ) ;
#160933=EDGE_CURVE ( 'NONE', #140884, #18374, #204824, .T. ) ;
#160938=CARTESIAN_POINT ( 'NONE',  ( -18.44362607810620958, 8.869041504298024847, -245.4312441985596820 ) ) ;
#160952=CARTESIAN_POINT ( 'NONE',  ( -20.64999999999999858, 23.68770167995059595, -252.8127582590406348 ) ) ;
#160954=EDGE_CURVE ( 'NONE', #153949, #53791, #147437, .T. ) ;
#160975=EDGE_CURVE ( 'NONE', #193742, #11383, #56006, .T. ) ;
#160992=DIRECTION ( 'NONE',  ( 6.938893903907131190E-14, -0.8814952561688476074, 0.4721928772777262417 ) ) ;
#161005=CARTESIAN_POINT ( 'NONE',  ( 20.94999999999999574, 4.260086453440762533, -245.2296700999207246 ) ) ;
#161017=VECTOR ( 'NONE', #144602, 1000.000000000000000 ) ;
#161031=DIRECTION ( 'NONE',  ( 0.000000000000000000, 0.4721928772778128947, 0.8814952561688012000 ) ) ;
#161058=ORIENTED_EDGE ( 'NONE', *, *, #34705, .T. ) ;
#161069=EDGE_CURVE ( 'NONE', #238889, #154195, #66053, .T. ) ;
#161073=ORIENTED_EDGE ( 'NONE', *, *, #48043, .F. ) ;
#161076=EDGE_CURVE ( 'NONE', #18553, #57931, #211822, .T. ) ;
#161081=DIRECTION ( 'NONE',  ( -1.000000000000000000, -1.394253735153569469E-16, -2.602809386958778209E-16 ) ) ;
#161090=VECTOR ( 'NONE', #26752, 1000.000000000000000 ) ;
#161147=CARTESIAN_POINT ( 'NONE',  ( 21.87500000000000355, 30.46448808713892831, -235.1722212069449256 ) ) ;
#161164=DIRECTION ( 'NONE',  ( 1.000000000000000000, 0.000000000000000000, 0.000000000000000000 ) ) ;
#161177=EDGE_CURVE ( 'NONE', #86653, #140654, #170348, .T. ) ;
#161186=DIRECTION ( 'NONE',  ( 0.000000000000000000, -0.8814952561688476074, 0.4721928772777262417 ) ) ;
#161192=AXIS2_PLACEMENT_3D ( 'NONE', #104822, #9609, #168748 ) ;
#161199=AXIS2_PLACEMENT_3D ( 'NONE', #87700, #147699, #93812 ) ;
#161230=DIRECTION ( 'NONE',  ( -1.000000000000000000, 0.000000000000000000, 0.000000000000000000 ) ) ;
#161232=DIRECTION ( 'NONE',  ( -1.000000000000000000, -1.394253735153569469E-16, -2.602809386958778209E-16 ) ) ;
#161287=DIRECTION ( 'NONE',  ( 0.000000000000000000, 0.8814952561688476074, -0.4721928772777262417 ) ) ;
#161320=CARTESIAN_POINT ( 'NONE',  ( 20.95595624212427666, 18.87084431528031914, -227.9704499331523664 ) ) ;
#161347=CIRCLE ( 'NONE', #211404, 0.1000000000000013933 ) ;
#161362=DIRECTION ( 'NONE',  ( 0.000000000000000000, -0.8814952561688425003, 0.4721928772777359007 ) ) ;
#161380=ADVANCED_FACE ( 'NONE', ( #117936 ), #136187, .F. ) ;
#161393=EDGE_CURVE ( 'NONE', #100823, #238889, #17545, .T. ) ;
#161394=AXIS2_PLACEMENT_3D ( 'NONE', #207025, #106610, #145747 ) ;
#161415=ORIENTED_EDGE ( 'NONE', *, *, #187421, .F. ) ;
#161429=SPHERICAL_SURFACE ( 'NONE', #147679, 0.1000000000000000056 ) ;
#161453=ORIENTED_EDGE ( 'NONE', *, *, #129365, .T. ) ;
#161454=VECTOR ( 'NONE', #209250, 1000.000000000000114 ) ;
#161472=CARTESIAN_POINT ( 'NONE',  ( 20.94999027547553894, 46.33166059915855328, -243.0555356998360423 ) ) ;
#161477=CARTESIAN_POINT ( 'NONE',  ( 23.14999999999999858, 36.65892442174935439, -249.5511627012433848 ) ) ;
#161500=ORIENTED_EDGE ( 'NONE', *, *, #81811, .F. ) ;
#161518=DIRECTION ( 'NONE',  ( 0.000000000000000000, -0.8814952561688437216, 0.4721928772777334582 ) ) ;
#161520=DIRECTION ( 'NONE',  ( -1.000000000000000000, -0.000000000000000000, -0.000000000000000000 ) ) ;
#161523=VERTEX_POINT ( 'NONE', #243019 ) ;
#161544=ORIENTED_EDGE ( 'NONE', *, *, #240003, .F. ) ;
#161570=EDGE_CURVE ( 'NONE', #183490, #69221, #195450, .T. ) ;
#161618=VERTEX_POINT ( 'NONE', #161636 ) ;
#161631=AXIS2_PLACEMENT_3D ( 'NONE', #129516, #109936, #30426 ) ;
#161636=CARTESIAN_POINT ( 'NONE',  ( -18.59999999999999787, 42.20719072976272912, -239.1935934412594804 ) ) ;
#161678=DIRECTION ( 'NONE',  ( 0.000000000000000000, 0.9371753822965315228, -0.3488585713686134238 ) ) ;
#161690=AXIS2_PLACEMENT_3D ( 'NONE', #39180, #157864, #237359 ) ;
#161717=CARTESIAN_POINT ( 'NONE',  ( -23.25000000000000000, 3.558777552609281525, -231.8203201594644725 ) ) ;
#161722=CARTESIAN_POINT ( 'NONE',  ( 20.94999999999999929, 16.44800918141279666, -240.8068063186265135 ) ) ;
#161753=AXIS2_PLACEMENT_3D ( 'NONE', #240030, #177520, #23586 ) ;
#161781=CARTESIAN_POINT ( 'NONE',  ( 18.39999999999999858, 37.99112772578902764, -261.0419300540664835 ) ) ;
#161791=AXIS2_PLACEMENT_3D ( 'NONE', #147497, #47086, #227024 ) ;
#161803=EDGE_CURVE ( 'NONE', #235224, #181106, #93627, .T. ) ;
#161806=ORIENTED_EDGE ( 'NONE', *, *, #166621, .F. ) ;
#161820=VERTEX_POINT ( 'NONE', #29833 ) ;
#161828=ORIENTED_EDGE ( 'NONE', *, *, #250214, .F. ) ;
#161834=DIRECTION ( 'NONE',  ( 0.000000000000000000, 0.5341055959866798375, -0.8454177738465836756 ) ) ;
#161845=DIRECTION ( 'NONE',  ( 1.000000000000000000, 1.541880601228652843E-16, 2.878400969107353907E-16 ) ) ;
#161874=ORIENTED_EDGE ( 'NONE', *, *, #107151, .T. ) ;
#161887=DIRECTION ( 'NONE',  ( -1.000000000000000000, -1.541880601228652843E-16, -2.878400969107353907E-16 ) ) ;
#161899=ADVANCED_FACE ( 'NONE', ( #137865 ), #238259, .F. ) ;
#161928=DIRECTION ( 'NONE',  ( 0.000000000000000000, 0.8814952561688432775, -0.4721928772777344019 ) ) ;
#161930=CIRCLE ( 'NONE', #124501, 11.65000000000000924 ) ;
#161948=FACE_OUTER_BOUND ( 'NONE', #232413, .T. ) ;
#161955=AXIS2_PLACEMENT_3D ( 'NONE', #218366, #15397, #174516 ) ;
#161962=CARTESIAN_POINT ( 'NONE',  ( 20.94999999999999929, 23.49882452903949570, -253.1653563615082305 ) ) ;
#161981=CIRCLE ( 'NONE', #161791, 0.1000000000000075273 ) ;
#161985=EDGE_LOOP ( 'NONE', ( #190622, #133013, #107765, #173582 ) ) ;
#161986=VECTOR ( 'NONE', #25201, 1000.000000000000000 ) ;
#161990=CYLINDRICAL_SURFACE ( 'NONE', #162139, 0.1000000000000012546 ) ;
#162010=EDGE_CURVE ( 'NONE', #188452, #132235, #75375, .T. ) ;
#162016=DIRECTION ( 'NONE',  ( -1.836970198721029441E-16, 0.4721928772777346239, 0.8814952561688430555 ) ) ;
#162077=CARTESIAN_POINT ( 'NONE',  ( 20.94999999999999929, 30.92427036846531863, -234.3138941982948040 ) ) ;
#162082=ORIENTED_EDGE ( 'NONE', *, *, #88998, .T. ) ;
#162090=ADVANCED_FACE ( 'NONE', ( #165155 ), #239793, .T. ) ;
#162108=EDGE_LOOP ( 'NONE', ( #252531, #77971, #118780, #99236 ) ) ;
#162139=AXIS2_PLACEMENT_3D ( 'NONE', #44592, #196266, #142393 ) ;
#162146=EDGE_CURVE ( 'NONE', #102393, #18238, #188561, .T. ) ;
#162157=AXIS2_PLACEMENT_3D ( 'NONE', #21055, #45400, #66253 ) ;
#162162=EDGE_CURVE ( 'NONE', #120394, #142601, #120257, .T. ) ;
#162167=DIRECTION ( 'NONE',  ( 0.000000000000000000, -0.8814952561688103039, 0.4721928772777957972 ) ) ;
#162177=DIRECTION ( 'NONE',  ( 0.000000000000000000, -0.8814952561688428334, 0.4721928772777350680 ) ) ;
#162180=CARTESIAN_POINT ( 'NONE',  ( -20.64999999999999858, 21.39147882631411335, -233.2615922652120730 ) ) ;
#162184=TOROIDAL_SURFACE ( 'NONE', #191229, 11.70000000000000107, 0.1000000000000000056 ) ;
#162205=CARTESIAN_POINT ( 'NONE',  ( -21.14999999999999858, 12.71802988599559292, -223.5105008658000258 ) ) ;
#162209=AXIS2_PLACEMENT_3D ( 'NONE', #22274, #40578, #139608 ) ;
#162258=CARTESIAN_POINT ( 'NONE',  ( 23.25000000000000000, 21.10816309994747186, -233.7904894189133813 ) ) ;
#162273=EDGE_LOOP ( 'NONE', ( #112368, #194478, #61767, #41294, #76214, #11701, #89006, #54681, #73042 ) ) ;
#162276=EDGE_LOOP ( 'NONE', ( #228839, #256202 ) ) ;
#162287=CIRCLE ( 'NONE', #195622, 11.79999999999999716 ) ;
#162318=AXIS2_PLACEMENT_3D ( 'NONE', #205478, #183372, #244610 ) ;
#162335=VECTOR ( 'NONE', #34537, 1000.000000000000114 ) ;
#162340=CARTESIAN_POINT ( 'NONE',  ( 18.59999999999999787, 7.128833340093095217, -233.7327013124392749 ) ) ;
#162349=EDGE_LOOP ( 'NONE', ( #21616, #142374, #97279, #153592 ) ) ;
#162380=CARTESIAN_POINT ( 'NONE',  ( -18.59999999999999787, 43.27008861172207332, -245.2265230569236110 ) ) ;
#162422=VERTEX_POINT ( 'NONE', #224493 ) ;
#162432=ORIENTED_EDGE ( 'NONE', *, *, #2647, .F. ) ;
#162433=ADVANCED_FACE ( 'NONE', ( #242765 ), #167128, .F. ) ;
#162439=FACE_OUTER_BOUND ( 'NONE', #10858, .T. ) ;
#162468=DIRECTION ( 'NONE',  ( 1.000000000000000000, 0.000000000000000000, 0.000000000000000000 ) ) ;
#162469=CARTESIAN_POINT ( 'NONE',  ( 22.39999999999999858, 0.3085173699977246109, -229.9658011520297975 ) ) ;
#162477=EDGE_LOOP ( 'NONE', ( #128798, #34913, #83560, #153856 ) ) ;
#162501=ORIENTED_EDGE ( 'NONE', *, *, #125872, .F. ) ;
#162525=LINE ( 'NONE', #142911, #55289 ) ;
#162541=DIRECTION ( 'NONE',  ( 0.000000000000000000, -0.4721928772777346794, -0.8814952561688431665 ) ) ;
#162594=CARTESIAN_POINT ( 'NONE',  ( -21.14999999999999858, 1.611925955256642951, -230.7774450549719916 ) ) ;
#162714=CARTESIAN_POINT ( 'NONE',  ( -22.39999999999999858, 0.3085173699977072914, -229.9658011520297691 ) ) ;
#162741=FACE_OUTER_BOUND ( 'NONE', #55311, .T. ) ;
#162761=VERTEX_POINT ( 'NONE', #242455 ) ;
#162814=DIRECTION ( 'NONE',  ( 0.000000000000000000, -0.8814952561688430555, 0.4721928772777346239 ) ) ;
#162829=FACE_OUTER_BOUND ( 'NONE', #165352, .T. ) ;
#162874=EDGE_CURVE ( 'NONE', #234687, #186652, #183131, .T. ) ;
#162939=DIRECTION ( 'NONE',  ( -1.000000000000000000, -1.541880601228652843E-16, -2.878400969107353907E-16 ) ) ;
#162944=EDGE_CURVE ( 'NONE', #109224, #112914, #70721, .T. ) ;
#162948=TOROIDAL_SURFACE ( 'NONE', #212824, 0.2000000000000000111, 0.1000000000000000056 ) ;
#162965=ORIENTED_EDGE ( 'NONE', *, *, #42323, .F. ) ;
#162967=DIRECTION ( 'NONE',  ( 1.000000000000000000, 0.000000000000000000, 0.000000000000000000 ) ) ;
#162969=LINE ( 'NONE', #41739, #98264 ) ;
#162971=ORIENTED_EDGE ( 'NONE', *, *, #26038, .F. ) ;
#162978=EDGE_CURVE ( 'NONE', #124483, #100546, #245491, .T. ) ;
#162979=CARTESIAN_POINT ( 'NONE',  ( 21.05000000000000071, 10.91926294161915223, -235.7631306847335679 ) ) ;
#162980=CARTESIAN_POINT ( 'NONE',  ( 18.49999999999998934, 38.23184963764531830, -261.0790774497031634 ) ) ;
#162992=DIRECTION ( 'NONE',  ( -0.000000000000000000, 0.8814952561688430555, -0.4721928772777346239 ) ) ;
#162996=DIRECTION ( 'NONE',  ( 0.000000000000000000, 0.4721928772777346239, 0.8814952561688430555 ) ) ;
#163010=CARTESIAN_POINT ( 'NONE',  ( 23.14999999999998437, 3.558777552609279304, -231.8203201594644725 ) ) ;
#163020=VECTOR ( 'NONE', #67652, 1000.000000000000000 ) ;
#163021=LINE ( 'NONE', #221668, #52878 ) ;
#163029=EDGE_LOOP ( 'NONE', ( #200847, #96861, #163738, #111798 ) ) ;
#163033=ADVANCED_FACE ( 'NONE', ( #171960 ), #87243, .T. ) ;
#163040=CARTESIAN_POINT ( 'NONE',  ( 20.95263205890665503, 18.81279984507908409, -229.8998340085670407 ) ) ;
#163049=CIRCLE ( 'NONE', #4773, 7.799999999999993605 ) ;
#163050=FACE_OUTER_BOUND ( 'NONE', #165916, .T. ) ;
#163052=EDGE_CURVE ( 'NONE', #223845, #99386, #162287, .T. ) ;
#163053=EDGE_LOOP ( 'NONE', ( #25054, #198896, #181558, #187757 ) ) ;
#163057=EDGE_CURVE ( 'NONE', #182152, #231868, #83115, .T. ) ;
#163069=ADVANCED_FACE ( 'NONE', ( #75416 ), #154950, .F. ) ;
#163075=CARTESIAN_POINT ( 'NONE',  ( -21.05000000000000071, 7.128833340093095217, -233.7327013124392749 ) ) ;
#163076=ORIENTED_EDGE ( 'NONE', *, *, #226879, .F. ) ;
#163099=CARTESIAN_POINT ( 'NONE',  ( 18.59999999999999076, 2.319530388122574394, -217.8268657444419887 ) ) ;
#163118=CARTESIAN_POINT ( 'NONE',  ( 23.24999999999997513, 35.97645343225767789, -235.9694016464868298 ) ) ;
#163146=AXIS2_PLACEMENT_3D ( 'NONE', #21801, #139132, #240842 ) ;
#163165=DIRECTION ( 'NONE',  ( -1.387778780781259631E-13, 0.1675535138457220907, -0.9858629823651720026 ) ) ;
#163180=EDGE_CURVE ( 'NONE', #140913, #61591, #74998, .T. ) ;
#163187=CARTESIAN_POINT ( 'NONE',  ( -21.05000000000000071, 14.81796439977981272, -236.5325475414793743 ) ) ;
#163190=DIRECTION ( 'NONE',  ( -1.000000000000000000, 0.000000000000000000, 0.000000000000000000 ) ) ;
#163206=CARTESIAN_POINT ( 'NONE',  ( 22.39999999999999503, -3.275978944802467652, -228.2735455795363748 ) ) ;
#163221=CARTESIAN_POINT ( 'NONE',  ( -22.39999999999999858, 10.71943444926882449, -226.8179467668883547 ) ) ;
#163224=CARTESIAN_POINT ( 'NONE',  ( 20.94999999999999574, 7.128833340093095217, -233.7327013124392749 ) ) ;
#163226=CYLINDRICAL_SURFACE ( 'NONE', #11397, 0.1000000000000053763 ) ;
#163247=EDGE_LOOP ( 'NONE', ( #144024, #133883, #58989, #58516 ) ) ;
#163301=DIRECTION ( 'NONE',  ( 0.000000000000000000, 0.8887656589064600876, -0.4583618696494786149 ) ) ;
#163317=DIRECTION ( 'NONE',  ( -1.000000000000000000, 0.000000000000000000, 0.000000000000000000 ) ) ;
#163322=AXIS2_PLACEMENT_3D ( 'NONE', #146688, #188409, #26801 ) ;
#163333=B_SPLINE_CURVE_WITH_KNOTS ( 'NONE', 3,
 ( #170800, #247714, #226862, #230734, #48226, #229442 ),
 .UNSPECIFIED., .F., .F.,
 ( 4, 2, 4 ),
 ( 0.000000000000000000, 0.0001496588209255838274, 0.0002993176418511676548 ),
 .UNSPECIFIED. ) ;
#163396=AXIS2_PLACEMENT_3D ( 'NONE', #146170, #44524, #122789 ) ;
#163465=CARTESIAN_POINT ( 'NONE',  ( -20.15000000000000568, 30.24795051788250433, -235.5764561060020981 ) ) ;
#163494=DIRECTION ( 'NONE',  ( 1.000000000000000000, 0.000000000000000000, 0.000000000000000000 ) ) ;
#163514=DIRECTION ( 'NONE',  ( 0.000000000000000000, -0.8814952561688437216, 0.4721928772777334582 ) ) ;
#163518=ORIENTED_EDGE ( 'NONE', *, *, #223660, .T. ) ;
#163566=EDGE_LOOP ( 'NONE', ( #136378, #222254, #1967, #49435, #213265 ) ) ;
#163584=CARTESIAN_POINT ( 'NONE',  ( 23.14999999999999858, 36.65892442174935439, -249.5511627012433848 ) ) ;
#163594=ORIENTED_EDGE ( 'NONE', *, *, #153972, .F. ) ;
#163621=EDGE_LOOP ( 'NONE', ( #212092, #123363, #189969, #27894 ) ) ;
#163668=EDGE_CURVE ( 'NONE', #144042, #29656, #12631, .T. ) ;
#163674=AXIS2_PLACEMENT_3D ( 'NONE', #188676, #10039, #89564 ) ;
#163703=DIRECTION ( 'NONE',  ( -1.000000000000000000, -3.448943450116723568E-16, -6.438528483529607644E-16 ) ) ;
#163727=TOROIDAL_SURFACE ( 'NONE', #122026, 2.100000000000002309, 0.1000000000000000056 ) ;
#163738=ORIENTED_EDGE ( 'NONE', *, *, #248168, .F. ) ;
#163793=LINE ( 'NONE', #63378, #137763 ) ;
#163811=ORIENTED_EDGE ( 'NONE', *, *, #244230, .T. ) ;
#163830=ORIENTED_EDGE ( 'NONE', *, *, #222391, .F. ) ;
#163846=DIRECTION ( 'NONE',  ( 1.000000000000000000, 0.000000000000000000, 0.000000000000000000 ) ) ;
#163847=AXIS2_PLACEMENT_3D ( 'NONE', #188613, #129917, #131206 ) ;
#163853=DIRECTION ( 'NONE',  ( 0.000000000000000000, -0.03181660087583042251, 0.9994937237965568766 ) ) ;
#163860=CARTESIAN_POINT ( 'NONE',  ( -23.15000000000000213, 11.36448785225375602, -246.7787679937655980 ) ) ;
#163869=CARTESIAN_POINT ( 'NONE',  ( -20.94999999999999929, 18.24178995542692050, -237.7003448530951459 ) ) ;
#163875=CARTESIAN_POINT ( 'NONE',  ( -21.05000000000000071, 10.23276890377598036, -228.1195043774102658 ) ) ;
#163906=CIRCLE ( 'NONE', #51441, 0.09999999999999528710 ) ;
#163914=CARTESIAN_POINT ( 'NONE',  ( -18.59999999999999787, 7.128833340093095217, -233.7327013124392749 ) ) ;
#163932=AXIS2_PLACEMENT_3D ( 'NONE', #210475, #70986, #94355 ) ;
#163937=CARTESIAN_POINT ( 'NONE',  ( 21.05000000000000071, 36.65892442174935439, -249.5511627012433848 ) ) ;
#163951=AXIS2_PLACEMENT_3D ( 'NONE', #105757, #86193, #66668 ) ;
#163969=DIRECTION ( 'NONE',  ( 0.000000000000000000, 0.9446535261619708468, -0.3280696808755038663 ) ) ;
#163997=CARTESIAN_POINT ( 'NONE',  ( 20.94999999999999929, 36.18002604163306302, -236.0784499204090991 ) ) ;
#164007=CARTESIAN_POINT ( 'NONE',  ( -23.25000000000000000, 1.627786319807483340, -244.0021210468063089 ) ) ;
#164044=ORIENTED_EDGE ( 'NONE', *, *, #226605, .T. ) ;
#164056=CARTESIAN_POINT ( 'NONE',  ( 20.94999999999999574, 4.184122562697137226, -245.3714803909117279 ) ) ;
#164069=ORIENTED_EDGE ( 'NONE', *, *, #55510, .T. ) ;
#164071=CARTESIAN_POINT ( 'NONE',  ( -21.05000000000000071, 18.65704504850842227, -226.5784250989226223 ) ) ;
#164097=ORIENTED_EDGE ( 'NONE', *, *, #171447, .F. ) ;
#164112=AXIS2_PLACEMENT_3D ( 'NONE', #205529, #66030, #145561 ) ;
#164211=CIRCLE ( 'NONE', #51730, 0.09999999999999986677 ) ;
#164219=DIRECTION ( 'NONE',  ( -0.000000000000000000, -0.4721928772777330696, -0.8814952561688438326 ) ) ;
#164257=CARTESIAN_POINT ( 'NONE',  ( 18.41416235934318735, 37.99112772578903474, -261.0419300540665404 ) ) ;
#164278=DIRECTION ( 'NONE',  ( -0.000000000000000000, 0.4721928772777345684, 0.8814952561688429444 ) ) ;
#164281=CYLINDRICAL_SURFACE ( 'NONE', #243182, 0.09999999999999939493 ) ;
#164293=DIRECTION ( 'NONE',  ( -0.000000000000000000, 0.8874830700839094755, -0.4608403197577646826 ) ) ;
#164294=CARTESIAN_POINT ( 'NONE',  ( -20.94999999999999929, 7.128833340093095217, -233.7327013124392749 ) ) ;
#164313=CARTESIAN_POINT ( 'NONE',  ( 21.05000000000000071, 18.75470391387417024, -230.0042304569477380 ) ) ;
#164340=CARTESIAN_POINT ( 'NONE',  ( 22.39999999999999503, 10.80758397488569500, -226.8651660546161395 ) ) ;
#164350=CARTESIAN_POINT ( 'NONE',  ( -20.85000000000000142, 45.99141771592758943, -256.5205054824189119 ) ) ;
#164383=DIRECTION ( 'NONE',  ( -1.000000000000000000, -0.000000000000000000, -0.000000000000000000 ) ) ;
#164412=SPHERICAL_SURFACE ( 'NONE', #16159, 0.1000000000000000056 ) ;
#164420=AXIS2_PLACEMENT_3D ( 'NONE', #10292, #151075, #89795 ) ;
#164470=DIRECTION ( 'NONE',  ( 0.000000000000000000, 0.8814952561688429444, -0.4721928772777349015 ) ) ;
#164506=DIRECTION ( 'NONE',  ( -0.000000000000000000, -0.4721928772777330696, -0.8814952561688438326 ) ) ;
#164535=CARTESIAN_POINT ( 'NONE',  ( -21.05000000000000071, 7.128833340093095217, -233.7327013124392749 ) ) ;
#164537=CIRCLE ( 'NONE', #81278, 0.09999999999999681366 ) ;
#164566=ADVANCED_FACE ( 'NONE', ( #239333 ), #176806, .T. ) ;
#164569=ORIENTED_EDGE ( 'NONE', *, *, #237694, .T. ) ;
#164590=ADVANCED_FACE ( 'NONE', ( #137635 ), #238032, .F. ) ;
#164601=CARTESIAN_POINT ( 'NONE',  ( 23.15000000000000213, 12.29073439453116201, -249.8274140313476437 ) ) ;
#164610=VERTEX_POINT ( 'NONE', #46249 ) ;
#164611=VECTOR ( 'NONE', #77241, 1000.000000000000000 ) ;
#164639=ORIENTED_EDGE ( 'NONE', *, *, #236638, .F. ) ;
#164647=ORIENTED_EDGE ( 'NONE', *, *, #128538, .F. ) ;
#164672=CARTESIAN_POINT ( 'NONE',  ( 20.85000000000000142, 43.02787096365918984, -254.3959382439171577 ) ) ;
#164678=ORIENTED_EDGE ( 'NONE', *, *, #135682, .F. ) ;
#164704=TOROIDAL_SURFACE ( 'NONE', #206397, 0.2000000000000000111, 0.1000000000000000056 ) ;
#164709=LINE ( 'NONE', #244218, #7710 ) ;
#164711=ADVANCED_FACE ( 'NONE', ( #69697 ), #4928, .T. ) ;
#164770=CARTESIAN_POINT ( 'NONE',  ( 20.94999999999999929, 19.92792862942048870, -235.1286901285539841 ) ) ;
#164784=DIRECTION ( 'NONE',  ( 0.000000000000000000, 0.8814952561688436106, -0.4721928772777334027 ) ) ;
#164844=AXIS2_PLACEMENT_3D ( 'NONE', #63389, #24302, #202912 ) ;
#164883=AXIS2_PLACEMENT_3D ( 'NONE', #130730, #167319, #188145 ) ;
#164933=ORIENTED_EDGE ( 'NONE', *, *, #43001, .F. ) ;
#164935=VECTOR ( 'NONE', #153146, 1000.000000000000000 ) ;
#164976=CARTESIAN_POINT ( 'NONE',  ( 23.24999999999999289, 21.15538238767524604, -233.7023398932965108 ) ) ;
#164992=CIRCLE ( 'NONE', #102415, 0.1000000000000035444 ) ;
#164997=CARTESIAN_POINT ( 'NONE',  ( 20.94999999999999929, 36.65892442174935439, -249.5511627012433848 ) ) ;
#165034=DIRECTION ( 'NONE',  ( 1.000000000000000000, 0.000000000000000000, 0.000000000000000000 ) ) ;
#165060=ORIENTED_EDGE ( 'NONE', *, *, #22759, .T. ) ;
#165067=DIRECTION ( 'NONE',  ( 0.000000000000000000, 0.8814952561688437216, -0.4721928772777334582 ) ) ;
#165118=DIRECTION ( 'NONE',  ( 1.000000000000000000, 0.000000000000000000, 0.000000000000000000 ) ) ;
#165152=ORIENTED_EDGE ( 'NONE', *, *, #56690, .T. ) ;
#165155=FACE_OUTER_BOUND ( 'NONE', #212767, .T. ) ;
#165190=LINE ( 'NONE', #187338, #149106 ) ;
#165204=CARTESIAN_POINT ( 'NONE',  ( -23.15000000000000213, 26.38661631484795578, -241.7796963509253203 ) ) ;
#165244=ORIENTED_EDGE ( 'NONE', *, *, #165449, .T. ) ;
#165246=CARTESIAN_POINT ( 'NONE',  ( 18.59999999999996945, 46.46967969402478360, -243.0849751855955674 ) ) ;
#165249=ORIENTED_EDGE ( 'NONE', *, *, #230156, .F. ) ;
#165259=ORIENTED_EDGE ( 'NONE', *, *, #244230, .F. ) ;
#165268=CARTESIAN_POINT ( 'NONE',  ( 20.94999999999999929, 36.14042471737574402, -236.0721279892244411 ) ) ;
#165296=DIRECTION ( 'NONE',  ( 0.000000000000000000, -0.8814952561688449428, 0.4721928772777310157 ) ) ;
#165306=EDGE_CURVE ( 'NONE', #74683, #82237, #21734, .T. ) ;
#165349=DIRECTION ( 'NONE',  ( 1.000000000000000000, 0.000000000000000000, 0.000000000000000000 ) ) ;
#165352=EDGE_LOOP ( 'NONE', ( #192681, #30855, #14977, #174086, #118745 ) ) ;
#165374=AXIS2_PLACEMENT_3D ( 'NONE', #9198, #109571, #211256 ) ;
#165377=ADVANCED_FACE ( 'NONE', ( #180053 ), #140926, .T. ) ;
#165382=ORIENTED_EDGE ( 'NONE', *, *, #215171, .F. ) ;
#165386=FACE_OUTER_BOUND ( 'NONE', #89880, .T. ) ;
#165408=VERTEX_POINT ( 'NONE', #40575 ) ;
#165420=EDGE_CURVE ( 'NONE', #5211, #211434, #17146, .T. ) ;
#165449=EDGE_CURVE ( 'NONE', #155241, #179129, #242655, .T. ) ;
#165474=AXIS2_PLACEMENT_3D ( 'NONE', #124712, #25614, #146819 ) ;
#165543=AXIS2_PLACEMENT_3D ( 'NONE', #170871, #228228, #129122 ) ;
#165586=EDGE_CURVE ( 'NONE', #7150, #38262, #255059, .T. ) ;
#165608=EDGE_CURVE ( 'NONE', #53948, #156004, #233318, .T. ) ;
#165634=DIRECTION ( 'NONE',  ( -1.000000000000000000, -0.000000000000000000, -0.000000000000000000 ) ) ;
#165657=ORIENTED_EDGE ( 'NONE', *, *, #162944, .F. ) ;
#165681=AXIS2_PLACEMENT_3D ( 'NONE', #37254, #214574, #15112 ) ;
#165710=CIRCLE ( 'NONE', #111516, 0.1000000000000013933 ) ;
#165755=AXIS2_PLACEMENT_3D ( 'NONE', #7292, #125950, #106376 ) ;
#165787=ORIENTED_EDGE ( 'NONE', *, *, #22693, .F. ) ;
#165818=CARTESIAN_POINT ( 'NONE',  ( 22.49533356619858182, 12.57247511773154258, -223.4325311539369068 ) ) ;
#165819=ORIENTED_EDGE ( 'NONE', *, *, #83952, .F. ) ;
#165820=ORIENTED_EDGE ( 'NONE', *, *, #238648, .F. ) ;
#165885=ORIENTED_EDGE ( 'NONE', *, *, #19837, .T. ) ;
#165916=EDGE_LOOP ( 'NONE', ( #69953, #236495, #147246, #116049 ) ) ;
#165921=EDGE_CURVE ( 'NONE', #95915, #201984, #72175, .T. ) ;
#165936=EDGE_LOOP ( 'NONE', ( #66891, #141075, #138009, #176544, #252921, #241409, #255724 ) ) ;
#165983=ORIENTED_EDGE ( 'NONE', *, *, #237694, .F. ) ;
#165991=ORIENTED_EDGE ( 'NONE', *, *, #45912, .F. ) ;
#165994=AXIS2_PLACEMENT_3D ( 'NONE', #235302, #256091, #200046 ) ;
#166026=VECTOR ( 'NONE', #208616, 1000.000000000000000 ) ;
#166043=CARTESIAN_POINT ( 'NONE',  ( -18.59999999999999787, 16.44800918141279311, -240.8068063186265135 ) ) ;
#166049=VECTOR ( 'NONE', #32673, 1000.000000000000000 ) ;
#166058=ORIENTED_EDGE ( 'NONE', *, *, #244241, .T. ) ;
#166064=CIRCLE ( 'NONE', #154177, 0.1000000000000013933 ) ;
#166071=EDGE_LOOP ( 'NONE', ( #27636, #147566, #102694, #201990 ) ) ;
#166081=CARTESIAN_POINT ( 'NONE',  ( -21.09316766718153247, 1.532113312989072496, -230.6901497882401202 ) ) ;
#166117=DIRECTION ( 'NONE',  ( -0.000000000000000000, 0.4721928772777347905, 0.8814952561688430555 ) ) ;
#166170=DIRECTION ( 'NONE',  ( 1.000000000000000000, 0.000000000000000000, 0.000000000000000000 ) ) ;
#166187=DIRECTION ( 'NONE',  ( 0.000000000000000000, 0.8814952561688476074, -0.4721928772777262417 ) ) ;
#166195=EDGE_CURVE ( 'NONE', #89895, #46953, #234453, .T. ) ;
#166239=VERTEX_POINT ( 'NONE', #227213 ) ;
#166254=DIRECTION ( 'NONE',  ( 4.026293107431335207E-15, -0.8454177738465953329, -0.5341055959866617409 ) ) ;
#166257=AXIS2_PLACEMENT_3D ( 'NONE', #136913, #159078, #255525 ) ;
#166261=DIRECTION ( 'NONE',  ( 1.000000000000000000, 0.000000000000000000, 0.000000000000000000 ) ) ;
#166264=CARTESIAN_POINT ( 'NONE',  ( -18.44448725179915627, 38.02117248346215206, -261.0467725487098392 ) ) ;
#166276=FACE_OUTER_BOUND ( 'NONE', #179835, .T. ) ;
#166282=EDGE_CURVE ( 'NONE', #135784, #156438, #134115, .T. ) ;
#166292=CARTESIAN_POINT ( 'NONE',  ( -23.15000000000000213, 36.65892442174935439, -249.5511627012433848 ) ) ;
#166313=LINE ( 'NONE', #161147, #52521 ) ;
#166359=CIRCLE ( 'NONE', #70864, 0.09999999999999986677 ) ;
#166371=ORIENTED_EDGE ( 'NONE', *, *, #217799, .T. ) ;
#166384=DIRECTION ( 'NONE',  ( -1.000000000000000000, -0.000000000000000000, -0.000000000000000000 ) ) ;
#166403=AXIS2_PLACEMENT_3D ( 'NONE', #12870, #134060, #190210 ) ;
#166467=CARTESIAN_POINT ( 'NONE',  ( -21.05000000000000071, 10.27588520313136300, -228.0695253486332490 ) ) ;
#166479=DIRECTION ( 'NONE',  ( 0.000000000000000000, 0.8034013718071717491, -0.5954378521544919645 ) ) ;
#166489=AXIS2_PLACEMENT_3D ( 'NONE', #145558, #49032, #12502 ) ;
#166492=EDGE_CURVE ( 'NONE', #82377, #7289, #209132, .T. ) ;
#166524=ADVANCED_FACE ( 'NONE', ( #138364 ), #188285, .T. ) ;
#166535=CARTESIAN_POINT ( 'NONE',  ( -20.64999999999999858, 19.28991295610541812, -237.9781866380819793 ) ) ;
#166540=EDGE_LOOP ( 'NONE', ( #140405, #110795, #167918, #49471 ) ) ;
#166561=AXIS2_PLACEMENT_3D ( 'NONE', #249115, #247810, #225646 ) ;
#166563=EDGE_LOOP ( 'NONE', ( #120773, #47099, #223624, #126343, #147557 ) ) ;
#166596=ORIENTED_EDGE ( 'NONE', *, *, #89086, .F. ) ;
#166608=AXIS2_PLACEMENT_3D ( 'NONE', #39067, #238525, #140705 ) ;
#166611=ORIENTED_EDGE ( 'NONE', *, *, #86941, .F. ) ;
#166614=DIRECTION ( 'NONE',  ( -1.000000000000000000, 7.166229603267618227E-16, 4.447280054184918885E-16 ) ) ;
#166615=EDGE_CURVE ( 'NONE', #137667, #137151, #134294, .T. ) ;
#166621=EDGE_CURVE ( 'NONE', #253940, #109684, #208656, .T. ) ;
#166637=CYLINDRICAL_SURFACE ( 'NONE', #135255, 0.1000000000000013933 ) ;
#166656=CARTESIAN_POINT ( 'NONE',  ( -21.37071067811865532, 29.67153963045800324, -236.6525067779183189 ) ) ;
#166663=CARTESIAN_POINT ( 'NONE',  ( -21.14999999999999858, 18.65704504850842227, -226.5784250989226507 ) ) ;
#166700=CYLINDRICAL_SURFACE ( 'NONE', #194870, 0.09999999999999553690 ) ;
#166701=CARTESIAN_POINT ( 'NONE',  ( -23.25000000000000000, 12.67709964810647882, -223.3751320524553705 ) ) ;
#166742=DIRECTION ( 'NONE',  ( 2.465190328815661345E-32, -0.8814952561688430555, 0.4721928772777344574 ) ) ;
#166765=DIRECTION ( 'NONE',  ( 0.000000000000000000, 0.8814952561688437216, -0.4721928772777334582 ) ) ;
#166781=EDGE_CURVE ( 'NONE', #252297, #250592, #91268, .T. ) ;
#166793=ORIENTED_EDGE ( 'NONE', *, *, #203534, .T. ) ;
#166800=EDGE_CURVE ( 'NONE', #206320, #123343, #52114, .T. ) ;
#166815=VECTOR ( 'NONE', #51165, 1000.000000000000000 ) ;
#166822=DIRECTION ( 'NONE',  ( -1.000000000000000000, 0.000000000000000000, 0.000000000000000000 ) ) ;
#166831=CARTESIAN_POINT ( 'NONE',  ( -22.39999999999999858, -3.140208063160686791, -228.2318569537739847 ) ) ;
#166867=DIRECTION ( 'NONE',  ( 0.000000000000000000, 0.8814952561688429444, -0.4721928772777348460 ) ) ;
#166976=EDGE_CURVE ( 'NONE', #189647, #39898, #1056, .T. ) ;
#167002=ORIENTED_EDGE ( 'NONE', *, *, #162944, .T. ) ;
#167018=CIRCLE ( 'NONE', #75421, 0.5000000000000008882 ) ;
#167020=DIRECTION ( 'NONE',  ( -1.000000000000000000, 0.000000000000000000, 0.000000000000000000 ) ) ;
#167021=DIRECTION ( 'NONE',  ( 1.000000000000000000, 1.394253735153569469E-16, 2.602809386958778209E-16 ) ) ;
#167022=VERTEX_POINT ( 'NONE', #128804 ) ;
#167051=LINE ( 'NONE', #71792, #217428 ) ;
#167054=EDGE_CURVE ( 'NONE', #155390, #154949, #139218, .T. ) ;
#167060=DIRECTION ( 'NONE',  ( 1.000000000000000000, 0.000000000000000000, 0.000000000000000000 ) ) ;
#167127=EDGE_CURVE ( 'NONE', #203294, #104543, #101613, .T. ) ;
#167128=PLANE ( 'NONE',  #78681 ) ;
#167145=VERTEX_POINT ( 'NONE', #89650 ) ;
#167276=EDGE_CURVE ( 'NONE', #172562, #2694, #226820, .T. ) ;
#167307=CARTESIAN_POINT ( 'NONE',  ( -18.59999999999999787, 9.783112580922244561, -245.9316685519929422 ) ) ;
#167319=DIRECTION ( 'NONE',  ( -0.000000000000000000, 0.8127272543711080433, -0.5826443254700077734 ) ) ;
#167348=AXIS2_PLACEMENT_3D ( 'NONE', #115173, #96851, #91756 ) ;
#167354=DIRECTION ( 'NONE',  ( 1.000000000000000000, 0.000000000000000000, 0.000000000000000000 ) ) ;
#167358=CARTESIAN_POINT ( 'NONE',  ( -21.08134388332232589, 1.580643611831310302, -230.6746762463788514 ) ) ;
#167359=EDGE_CURVE ( 'NONE', #239499, #71039, #164211, .T. ) ;
#167389=SPHERICAL_SURFACE ( 'NONE', #170286, 0.1000000000000000056 ) ;
#167398=VERTEX_POINT ( 'NONE', #101162 ) ;
#167413=LINE ( 'NONE', #246914, #121652 ) ;
#167420=ADVANCED_FACE ( 'NONE', ( #36129 ), #188551, .T. ) ;
#167489=DIRECTION ( 'NONE',  ( 1.000000000000000000, 0.000000000000000000, 0.000000000000000000 ) ) ;
#167508=CARTESIAN_POINT ( 'NONE',  ( 23.14999999999998792, 12.62988036037870643, -223.4632815780722410 ) ) ;
#167513=CARTESIAN_POINT ( 'NONE',  ( 20.94999999999999574, 18.27574494880468592, -237.6039235467692947 ) ) ;
#167534=ORIENTED_EDGE ( 'NONE', *, *, #196255, .T. ) ;
#167536=ADVANCED_FACE ( 'NONE', ( #150619 ), #21978, .F. ) ;
#167555=CARTESIAN_POINT ( 'NONE',  ( -20.94999999999999929, 4.459011116736869340, -245.2267018908137857 ) ) ;
#167556=VERTEX_POINT ( 'NONE', #231452 ) ;
#167568=FACE_OUTER_BOUND ( 'NONE', #136745, .T. ) ;
#167577=LINE ( 'NONE', #245808, #226454 ) ;
#167613=DIRECTION ( 'NONE',  ( 1.000000000000000000, 1.541880601228652843E-16, 2.878400969107353907E-16 ) ) ;
#167640=CARTESIAN_POINT ( 'NONE',  ( 20.12500000000000000, 30.37633856152204359, -235.1250019192171408 ) ) ;
#167653=CARTESIAN_POINT ( 'NONE',  ( -18.50000000000000000, 30.14024212288317628, -235.5657495473015501 ) ) ;
#167656=FACE_BOUND ( 'NONE', #216738, .T. ) ;
#167675=AXIS2_PLACEMENT_3D ( 'NONE', #163075, #165634, #203466 ) ;
#167704=DIRECTION ( 'NONE',  ( 1.000000000000000000, 0.000000000000000000, 0.000000000000000000 ) ) ;
#167715=ADVANCED_FACE ( 'NONE', ( #24932 ), #241401, .F. ) ;
#167716=CARTESIAN_POINT ( 'NONE',  ( -20.64999999999999858, 38.42191493408704872, -250.4955484557988541 ) ) ;
#167761=CIRCLE ( 'NONE', #26279, 11.75000000000000711 ) ;
#167785=DIRECTION ( 'NONE',  ( 1.000000000000000000, 0.000000000000000000, 0.000000000000000000 ) ) ;
#167789=LINE ( 'NONE', #186041, #70287 ) ;
#167836=CARTESIAN_POINT ( 'NONE',  ( 18.43473516226070075, 8.856315488830345473, -245.4294710645858117 ) ) ;
#167866=AXIS2_PLACEMENT_3D ( 'NONE', #118090, #161081, #240606 ) ;
#167867=LINE ( 'NONE', #107856, #251588 ) ;
#167918=ORIENTED_EDGE ( 'NONE', *, *, #101821, .F. ) ;
#167963=FACE_OUTER_BOUND ( 'NONE', #199903, .T. ) ;
#167965=DIRECTION ( 'NONE',  ( 1.000000000000000000, 0.000000000000000000, 0.000000000000000000 ) ) ;
#168056=DIRECTION ( 'NONE',  ( 1.000000000000000000, 0.000000000000000000, 0.000000000000000000 ) ) ;
#168069=EDGE_CURVE ( 'NONE', #11383, #218506, #113163, .T. ) ;
#168087=CARTESIAN_POINT ( 'NONE',  ( 20.95132126680579532, 18.75531812006552457, -228.0605135901855647 ) ) ;
#168120=DIRECTION ( 'NONE',  ( 1.000000000000000000, 0.000000000000000000, 0.000000000000000000 ) ) ;
#168135=CARTESIAN_POINT ( 'NONE',  ( 20.94999999999999929, 36.65892442174935439, -249.5511627012433848 ) ) ;
#168151=ORIENTED_EDGE ( 'NONE', *, *, #150667, .F. ) ;
#168154=CARTESIAN_POINT ( 'NONE',  ( -23.25000000000000000, 28.00279607545604321, -239.9795148779844283 ) ) ;
#168179=CARTESIAN_POINT ( 'NONE',  ( -1.739115166359751170E-14, 23.42819724844703089, -229.2476443247245186 ) ) ;
#168205=CARTESIAN_POINT ( 'NONE',  ( -20.94999999999999929, 18.18127959618848877, -237.5711165786817389 ) ) ;
#168206=CARTESIAN_POINT ( 'NONE',  ( -23.15000000000000213, 28.42524210734032053, -258.3567845160494585 ) ) ;
#168208=ORIENTED_EDGE ( 'NONE', *, *, #193726, .F. ) ;
#168239=ORIENTED_EDGE ( 'NONE', *, *, #129144, .T. ) ;
#168277=VERTEX_POINT ( 'NONE', #67576 ) ;
#168287=EDGE_CURVE ( 'NONE', #98189, #17866, #104923, .T. ) ;
#168311=EDGE_CURVE ( 'NONE', #158502, #103462, #213282, .T. ) ;
#168386=VERTEX_POINT ( 'NONE', #72749 ) ;
#168397=DIRECTION ( 'NONE',  ( -1.000000000000000000, 0.000000000000000000, 0.000000000000000000 ) ) ;
#168401=ADVANCED_FACE ( 'NONE', ( #192672 ), #138272, .F. ) ;
#168422=CARTESIAN_POINT ( 'NONE',  ( 23.24999999999999289, 31.44980407958351876, -233.5445995079518582 ) ) ;
#168457=EDGE_CURVE ( 'NONE', #203424, #123298, #113345, .T. ) ;
#168563=DIRECTION ( 'NONE',  ( -1.000000000000000000, -8.674042436075353235E-17, -1.619280515896125144E-16 ) ) ;
#168586=ORIENTED_EDGE ( 'NONE', *, *, #107818, .T. ) ;
#168597=CARTESIAN_POINT ( 'NONE',  ( 18.60000000000000142, 38.30077178631847090, -261.1858881914067751 ) ) ;
#168620=VECTOR ( 'NONE', #110733, 1000.000000000000227 ) ;
#168691=FACE_OUTER_BOUND ( 'NONE', #138872, .T. ) ;
#168696=DIRECTION ( 'NONE',  ( 0.000000000000000000, 0.8096735173027155286, -0.5868805631290315850 ) ) ;
#168700=DIRECTION ( 'NONE',  ( -1.000000000000000000, 0.000000000000000000, 0.000000000000000000 ) ) ;
#168722=CARTESIAN_POINT ( 'NONE',  ( -23.15000000000000213, 34.89593390941166007, -248.6067769466879156 ) ) ;
#168723=ORIENTED_EDGE ( 'NONE', *, *, #138827, .T. ) ;
#168726=DIRECTION ( 'NONE',  ( -1.000000000000000000, -0.000000000000000000, -0.000000000000000000 ) ) ;
#168733=CIRCLE ( 'NONE', #56224, 0.1000000000000013933 ) ;
#168734=CARTESIAN_POINT ( 'NONE',  ( 20.85000000000000142, 43.18640298906419162, -245.2812653309023574 ) ) ;
#168741=AXIS2_PLACEMENT_3D ( 'NONE', #166292, #147981, #127126 ) ;
#168744=AXIS2_PLACEMENT_3D ( 'NONE', #219400, #177753, #14830 ) ;
#168748=DIRECTION ( 'NONE',  ( 1.000000000000000000, 0.000000000000000000, 0.000000000000000000 ) ) ;
#168753=CIRCLE ( 'NONE', #226959, 0.1000000000000013933 ) ;
#168756=ORIENTED_EDGE ( 'NONE', *, *, #75206, .T. ) ;
#168771=CARTESIAN_POINT ( 'NONE',  ( -23.15000000000000213, 23.40438595358395091, -253.3416554127419431 ) ) ;
#168775=DIRECTION ( 'NONE',  ( 1.000000000000000000, 0.000000000000000000, 0.000000000000000000 ) ) ;
#168777=DIRECTION ( 'NONE',  ( -0.7070776581709311559, -0.6233369439635936260, 0.3339045366652567126 ) ) ;
#168811=ORIENTED_EDGE ( 'NONE', *, *, #235806, .T. ) ;
#168812=CARTESIAN_POINT ( 'NONE',  ( 21.05000000000000071, 10.27540777873560707, -228.0704167471579069 ) ) ;
#168837=CIRCLE ( 'NONE', #64734, 0.2000000000000027867 ) ;
#168856=PLANE ( 'NONE',  #22233 ) ;
#168907=FACE_OUTER_BOUND ( 'NONE', #322, .T. ) ;
#168948=PLANE ( 'NONE',  #77717 ) ;
#168960=AXIS2_PLACEMENT_3D ( 'NONE', #245135, #122639, #22253 ) ;
#168967=CARTESIAN_POINT ( 'NONE',  ( -21.05000000000000071, 14.72981487416292623, -236.4853282537515895 ) ) ;
#168981=AXIS2_PLACEMENT_3D ( 'NONE', #130138, #71486, #149740 ) ;
#168990=ORIENTED_EDGE ( 'NONE', *, *, #42119, .F. ) ;
#168997=TOROIDAL_SURFACE ( 'NONE', #186089, 0.2000000000000000111, 0.1000000000000000056 ) ;
#169107=DIRECTION ( 'NONE',  ( 0.000000000000000000, -0.8814952561688431665, 0.4721928772777346794 ) ) ;
#169133=CARTESIAN_POINT ( 'NONE',  ( -20.54999999999999716, 21.30332930069722863, -233.2143729774842882 ) ) ;
#169153=DIRECTION ( 'NONE',  ( 0.000000000000000000, 0.8814952561688430555, -0.4721928772777346239 ) ) ;
#169164=EDGE_LOOP ( 'NONE', ( #205422, #246691, #257164, #9886 ) ) ;
#169178=ORIENTED_EDGE ( 'NONE', *, *, #168287, .T. ) ;
#169181=LINE ( 'NONE', #212140, #102380 ) ;
#169255=EDGE_CURVE ( 'NONE', #89738, #226316, #6204, .T. ) ;
#169275=ORIENTED_EDGE ( 'NONE', *, *, #112718, .T. ) ;
#169321=CARTESIAN_POINT ( 'NONE',  ( 21.14999999999999858, 12.71802988599559470, -223.5105008658000258 ) ) ;
#169347=DIRECTION ( 'NONE',  ( 1.000000000000000000, 0.000000000000000000, 0.000000000000000000 ) ) ;
#169366=DIRECTION ( 'NONE',  ( 1.000000000000000000, 2.683427030341247466E-17, -8.429776912874270765E-16 ) ) ;
#169367=CARTESIAN_POINT ( 'NONE',  ( 20.95576188350343116, 18.84758480880311282, -227.9749056404471332 ) ) ;
#169390=CIRCLE ( 'NONE', #56871, 0.09999999999999954758 ) ;
#169400=LINE ( 'NONE', #208505, #129182 ) ;
#169447=EDGE_LOOP ( 'NONE', ( #16648, #191713, #180392 ) ) ;
#169492=ORIENTED_EDGE ( 'NONE', *, *, #243746, .T. ) ;
#169529=EDGE_LOOP ( 'NONE', ( #54352, #153631, #242286, #89108, #64982 ) ) ;
#169530=DIRECTION ( 'NONE',  ( 0.000000000000000000, -0.4721928772777346239, -0.8814952561688430555 ) ) ;
#169541=CARTESIAN_POINT ( 'NONE',  ( -21.06715728752538297, 18.86061765788380740, -226.6874733728450053 ) ) ;
#169554=VECTOR ( 'NONE', #167060, 1000.000000000000000 ) ;
#169555=VECTOR ( 'NONE', #236272, 1000.000000000000114 ) ;
#169571=LINE ( 'NONE', #249080, #3174 ) ;
#169575=LINE ( 'NONE', #127843, #53485 ) ;
#169601=CARTESIAN_POINT ( 'NONE',  ( -21.13422380239047982, 1.404996820536673185, -230.6665987823094781 ) ) ;
#169640=AXIS2_PLACEMENT_3D ( 'NONE', #75184, #94711, #252496 ) ;
#169644=ORIENTED_EDGE ( 'NONE', *, *, #163180, .F. ) ;
#169657=ORIENTED_EDGE ( 'NONE', *, *, #173647, .F. ) ;
#169658=DIRECTION ( 'NONE',  ( 0.000000000000000000, -0.8814952561688476074, 0.4721928772777262417 ) ) ;
#169686=ADVANCED_FACE ( 'NONE', ( #162439 ), #62047, .T. ) ;
#169687=ORIENTED_EDGE ( 'NONE', *, *, #237461, .F. ) ;
#169690=DIRECTION ( 'NONE',  ( 1.000000000000000000, -0.000000000000000000, -0.000000000000000000 ) ) ;
#169714=ORIENTED_EDGE ( 'NONE', *, *, #148438, .T. ) ;
#169732=EDGE_LOOP ( 'NONE', ( #122005, #253837, #152991, #101730 ) ) ;
#169764=ORIENTED_EDGE ( 'NONE', *, *, #43740, .T. ) ;
#169793=CARTESIAN_POINT ( 'NONE',  ( 18.59999999999999076, 36.65892442174935439, -249.5511627012433848 ) ) ;
#169807=ORIENTED_EDGE ( 'NONE', *, *, #167276, .F. ) ;
#169824=DIRECTION ( 'NONE',  ( 0.000000000000000000, 0.8814952561688444987, -0.4721928772777320149 ) ) ;
#169859=CIRCLE ( 'NONE', #94790, 0.09999999999999939493 ) ;
#169889=DIRECTION ( 'NONE',  ( 0.000000000000000000, 0.8814952561689112231, -0.4721928772776075589 ) ) ;
#169895=CARTESIAN_POINT ( 'NONE',  ( 21.07928932188134397, 1.596973512272234830, -230.6572452218043736 ) ) ;
#169936=ORIENTED_EDGE ( 'NONE', *, *, #226605, .F. ) ;
#169942=DIRECTION ( 'NONE',  ( 0.000000000000000000, 0.8814952561688469412, -0.4721928772777276850 ) ) ;
#169955=ORIENTED_EDGE ( 'NONE', *, *, #157809, .F. ) ;
#169970=AXIS2_PLACEMENT_3D ( 'NONE', #36899, #60264, #138495 ) ;
#170010=AXIS2_PLACEMENT_3D ( 'NONE', #51101, #210227, #31605 ) ;
#170022=DIRECTION ( 'NONE',  ( 1.836970198721029441E-16, -0.4721928772777346239, -0.8814952561688430555 ) ) ;
#170025=ORIENTED_EDGE ( 'NONE', *, *, #200216, .T. ) ;
#170031=ORIENTED_EDGE ( 'NONE', *, *, #132076, .T. ) ;
#170053=CARTESIAN_POINT ( 'NONE',  ( -23.15000000000000213, 36.65892442174935439, -249.5511627012433848 ) ) ;
#170080=VECTOR ( 'NONE', #19588, 1000.000000000000000 ) ;
#170089=DIRECTION ( 'NONE',  ( -1.000000000000000000, 0.000000000000000000, 0.000000000000000000 ) ) ;
#170113=ORIENTED_EDGE ( 'NONE', *, *, #139817, .T. ) ;
#170115=AXIS2_PLACEMENT_3D ( 'NONE', #181794, #3129, #80079 ) ;
#170122=ORIENTED_EDGE ( 'NONE', *, *, #162162, .F. ) ;
#170131=CARTESIAN_POINT ( 'NONE',  ( 18.49999999999999645, 16.60731133254646963, -240.9277311905271688 ) ) ;
#170159=CARTESIAN_POINT ( 'NONE',  ( -18.50000000000000000, 38.28679861725831302, -261.0868692510649680 ) ) ;
#170164=ORIENTED_EDGE ( 'NONE', *, *, #68709, .T. ) ;
#170188=ORIENTED_EDGE ( 'NONE', *, *, #9258, .F. ) ;
#170196=AXIS2_PLACEMENT_3D ( 'NONE', #99375, #44568, #178981 ) ;
#170210=CARTESIAN_POINT ( 'NONE',  ( 23.15000000000000213, 24.12844930803501242, -253.0488546976795021 ) ) ;
#170222=DIRECTION ( 'NONE',  ( 0.000000000000000000, -0.4721928772777320149, -0.8814952561688444987 ) ) ;
#170224=CARTESIAN_POINT ( 'NONE',  ( -18.50000000000000000, 10.63601275468165142, -265.6051570720007931 ) ) ;
#170273=VERTEX_POINT ( 'NONE', #27777 ) ;
#170274=ORIENTED_EDGE ( 'NONE', *, *, #161076, .F. ) ;
#170286=AXIS2_PLACEMENT_3D ( 'NONE', #141369, #121830, #220895 ) ;
#170291=AXIS2_PLACEMENT_3D ( 'NONE', #18826, #99620, #254818 ) ;
#170302=ORIENTED_EDGE ( 'NONE', *, *, #201246, .T. ) ;
#170315=DIRECTION ( 'NONE',  ( 1.000000000000000000, 0.000000000000000000, 0.000000000000000000 ) ) ;
#170318=CARTESIAN_POINT ( 'NONE',  ( -21.64999999999999858, 21.39776787615277343, -233.0380739262505472 ) ) ;
#170331=VERTEX_POINT ( 'NONE', #117548 ) ;
#170337=CARTESIAN_POINT ( 'NONE',  ( -22.60000000000080789, -3.206176855256876124, -228.1422739711507859 ) ) ;
#170348=CIRCLE ( 'NONE', #207738, 0.1000000000000015737 ) ;
#170370=DIRECTION ( 'NONE',  ( 0.000000000000000000, 0.5868805631290353597, 0.8096735173027127530 ) ) ;
#170396=CARTESIAN_POINT ( 'NONE',  ( -21.07016717457007005, 1.556953976783240323, -230.7479980709940719 ) ) ;
#170433=CARTESIAN_POINT ( 'NONE',  ( 18.50000324121758055, 46.33100819526736558, -243.0553980158186391 ) ) ;
#170450=CIRCLE ( 'NONE', #116433, 0.1000000000000013933 ) ;
#170454=ORIENTED_EDGE ( 'NONE', *, *, #234905, .T. ) ;
#170477=ADVANCED_FACE ( 'NONE', ( #79687 ), #89477, .F. ) ;
#170485=CIRCLE ( 'NONE', #124651, 0.1000000000000013933 ) ;
#170504=ORIENTED_EDGE ( 'NONE', *, *, #209158, .T. ) ;
#170506=( BOUNDED_SURFACE ( )  B_SPLINE_SURFACE ( 3, 2, ( 
 ( #147419, #152592, #9190 ),
 ( #209974, #88703, #109561 ),
 ( #92567, #69195, #127864 ),
 ( #251655, #249106, #106992 ),
 ( #169601, #148717, #70490 ),
 ( #228252, #186558, #7924 ) ),
 .UNSPECIFIED., .F., .F., .F. ) 
 B_SPLINE_SURFACE_WITH_KNOTS ( ( 4, 2, 4 ),
 ( 3, 3 ),
 ( 0.0001792624049599619591, 0.0003686986002124806685, 0.0005581347954649993779 ),
 ( 0.000000000000000000, 1.000000000000000000 ),
 .UNSPECIFIED. ) 
 GEOMETRIC_REPRESENTATION_ITEM ( )  RATIONAL_B_SPLINE_SURFACE ( (
 ( 1.000000000000000000, 0.9238795325112744150, 1.000000000000000000),
 ( 1.000000000000000000, 0.9229318695233699188, 1.000000000000000000),
 ( 1.000000000000000000, 0.8926288119236824858, 1.000000000000000000),
 ( 1.000000000000000000, 0.8123777807264993545, 1.000000000000000000),
 ( 1.000000000000000000, 0.7629087100935405541, 1.000000000000000000),
 ( 1.000000000000000000, 0.7071067811866220687, 1.000000000000000000) ) ) 
 REPRESENTATION_ITEM ( '' )  SURFACE ( )  );
#170513=ADVANCED_FACE ( 'NONE', ( #103101 ), #19754, .T. ) ;
#170526=AXIS2_PLACEMENT_3D ( 'NONE', #167307, #208972, #30356 ) ;
#170534=VERTEX_POINT ( 'NONE', #26170 ) ;
#170550=CARTESIAN_POINT ( 'NONE',  ( -23.15000000000000213, 1.580567032079710055, -244.0902705724231794 ) ) ;
#170572=CARTESIAN_POINT ( 'NONE',  ( 20.94999999999999929, 19.05165861791954285, -232.6888762659126826 ) ) ;
#170575=CARTESIAN_POINT ( 'NONE',  ( 22.48508240969612260, -3.118744460784280914, -228.1908567849118867 ) ) ;
#170594=EDGE_LOOP ( 'NONE', ( #187666, #225948, #175653, #1878 ) ) ;
#170613=ADVANCED_FACE ( 'NONE', ( #9163 ), #113072, .T. ) ;
#170619=CARTESIAN_POINT ( 'NONE',  ( 23.24999999999999645, 7.128833340093095217, -233.7327013124392749 ) ) ;
#170627=FACE_OUTER_BOUND ( 'NONE', #158247, .T. ) ;
#170652=FACE_OUTER_BOUND ( 'NONE', #70108, .T. ) ;
#170661=CARTESIAN_POINT ( 'NONE',  ( 20.95512828230143398, 22.07647316018445949, -231.6703166944364511 ) ) ;
#170665=CARTESIAN_POINT ( 'NONE',  ( 20.95566103547454517, 18.87012517599244177, -227.9764669589508514 ) ) ;
#170719=ORIENTED_EDGE ( 'NONE', *, *, #46570, .F. ) ;
#170728=VERTEX_POINT ( 'NONE', #96055 ) ;
#170749=DIRECTION ( 'NONE',  ( 0.000000000000000000, -0.8814952561688476074, 0.4721928772777262417 ) ) ;
#170775=VECTOR ( 'NONE', #95631, 1000.000000000000000 ) ;
#170784=ORIENTED_EDGE ( 'NONE', *, *, #95841, .F. ) ;
#170788=ORIENTED_EDGE ( 'NONE', *, *, #12503, .F. ) ;
#170793=AXIS2_PLACEMENT_3D ( 'NONE', #46452, #191142, #249810 ) ;
#170800=CARTESIAN_POINT ( 'NONE',  ( 20.95512820512820440, 22.03025613173517883, -231.6455594930189648 ) ) ;
#170807=ORIENTED_EDGE ( 'NONE', *, *, #119706, .F. ) ;
#170863=ORIENTED_EDGE ( 'NONE', *, *, #257141, .T. ) ;
#170871=CARTESIAN_POINT ( 'NONE',  ( -22.50000000000000000, 12.67709964810648238, -223.3751320524553705 ) ) ;
#170882=DIRECTION ( 'NONE',  ( 0.000000000000000000, 0.8814952561688476074, -0.4721928772777262417 ) ) ;
#170924=EDGE_CURVE ( 'NONE', #178121, #177294, #168837, .T. ) ;
#170926=DIRECTION ( 'NONE',  ( -0.000000000000000000, -0.4721928772777346239, -0.8814952561688430555 ) ) ;
#170954=ORIENTED_EDGE ( 'NONE', *, *, #10721, .F. ) ;
#170955=EDGE_CURVE ( 'NONE', #23820, #123298, #150609, .T. ) ;
#170956=ORIENTED_EDGE ( 'NONE', *, *, #9094, .F. ) ;
#170982=ORIENTED_EDGE ( 'NONE', *, *, #109231, .F. ) ;
#170999=ADVANCED_FACE ( 'NONE', ( #110179, #31963 ), #68502, .F. ) ;
#171008=DIRECTION ( 'NONE',  ( 1.000000000000000000, 1.541880601228652843E-16, 2.878400969107353907E-16 ) ) ;
#171013=EDGE_CURVE ( 'NONE', #63208, #216812, #152060, .T. ) ;
#171033=EDGE_CURVE ( 'NONE', #236989, #239741, #243804, .T. ) ;
#171042=CYLINDRICAL_SURFACE ( 'NONE', #66115, 0.8750000000000007772 ) ;
#171050=CARTESIAN_POINT ( 'NONE',  ( -21.04999999999999716, 8.794517532467699183, -245.5155488533044945 ) ) ;
#171066=ORIENTED_EDGE ( 'NONE', *, *, #48973, .F. ) ;
#171071=ORIENTED_EDGE ( 'NONE', *, *, #252166, .T. ) ;
#171072=DIRECTION ( 'NONE',  ( -1.000000000000000000, 0.000000000000000000, 0.000000000000000000 ) ) ;
#171110=CARTESIAN_POINT ( 'NONE',  ( -23.15000000000000213, 20.01397631055648674, -237.6853859230195098 ) ) ;
#171113=LINE ( 'NONE', #17149, #215863 ) ;
#171119=ORIENTED_EDGE ( 'NONE', *, *, #78223, .T. ) ;
#171133=SPHERICAL_SURFACE ( 'NONE', #196676, 0.1000000000000000056 ) ;
#171137=ADVANCED_FACE ( 'NONE', ( #137434 ), #253534, .T. ) ;
#171160=AXIS2_PLACEMENT_3D ( 'NONE', #151570, #191977, #177564 ) ;
#171164=FACE_OUTER_BOUND ( 'NONE', #219165, .T. ) ;
#171213=EDGE_CURVE ( 'NONE', #188383, #60897, #93958, .T. ) ;
#171228=ORIENTED_EDGE ( 'NONE', *, *, #123355, .T. ) ;
#171256=TOROIDAL_SURFACE ( 'NONE', #179410, 0.2000000000000000111, 0.1000000000000000056 ) ;
#171299=DIRECTION ( 'NONE',  ( 1.000000000000000000, 0.000000000000000000, 0.000000000000000000 ) ) ;
#171330=VERTEX_POINT ( 'NONE', #111178 ) ;
#171398=CARTESIAN_POINT ( 'NONE',  ( -20.54999999999999716, 22.34215363070824623, -231.2750834139128528 ) ) ;
#171433=EDGE_LOOP ( 'NONE', ( #129696, #35925, #83137 ) ) ;
#171447=EDGE_CURVE ( 'NONE', #63327, #214842, #127282, .T. ) ;
#171468=CARTESIAN_POINT ( 'NONE',  ( -18.39999999999999858, 8.780520186313291120, -245.4165333277510115 ) ) ;
#171481=VERTEX_POINT ( 'NONE', #77174 ) ;
#171569=DIRECTION ( 'NONE',  ( 0.000000000000000000, 0.8814952561688430555, -0.4721928772777346239 ) ) ;
#171583=VECTOR ( 'NONE', #155080, 1000.000000000000000 ) ;
#171597=DIRECTION ( 'NONE',  ( 7.304098846218136639E-16, -0.4721928772777346239, -0.8814952561688430555 ) ) ;
#171606=CARTESIAN_POINT ( 'NONE',  ( 21.07964655665547582, 22.04583520435846822, -231.7687797005887091 ) ) ;
#171635=EDGE_CURVE ( 'NONE', #150487, #250267, #24940, .T. ) ;
#171653=CARTESIAN_POINT ( 'NONE',  ( 20.94999999999999574, 16.53615870702968138, -240.8540256063542984 ) ) ;
#171704=DIRECTION ( 'NONE',  ( -1.000000000000000000, -1.394253735153569469E-16, -2.602809386958778209E-16 ) ) ;
#171726=DIRECTION ( 'NONE',  ( -0.000000000000000000, -0.8127272543710951647, 0.5826443254700256480 ) ) ;
#171757=VECTOR ( 'NONE', #213774, 1000.000000000000000 ) ;
#171777=ORIENTED_EDGE ( 'NONE', *, *, #189173, .T. ) ;
#171780=AXIS2_PLACEMENT_3D ( 'NONE', #142971, #244657, #46450 ) ;
#171789=DIRECTION ( 'NONE',  ( -1.000000000000000000, -0.000000000000000000, -0.000000000000000000 ) ) ;
#171790=FACE_OUTER_BOUND ( 'NONE', #232096, .T. ) ;
#171792=DIRECTION ( 'NONE',  ( 2.952720810173288619E-16, -0.4721928772777346239, -0.8814952561688430555 ) ) ;
#171839=LINE ( 'NONE', #11457, #228779 ) ;
#171853=DIRECTION ( 'NONE',  ( 0.000000000000000000, -0.4721928772777346239, -0.8814952561688430555 ) ) ;
#171889=CARTESIAN_POINT ( 'NONE',  ( 21.93340585971088785, 10.58724339642392032, -227.2765004563024434 ) ) ;
#171895=ORIENTED_EDGE ( 'NONE', *, *, #160624, .F. ) ;
#171906=CIRCLE ( 'NONE', #63512, 11.75000000000000000 ) ;
#171911=ORIENTED_EDGE ( 'NONE', *, *, #165608, .F. ) ;
#171935=CARTESIAN_POINT ( 'NONE',  ( 20.95496329884391784, 18.79541830518007473, -227.9940942717060466 ) ) ;
#171960=FACE_OUTER_BOUND ( 'NONE', #153794, .T. ) ;
#171961=LINE ( 'NONE', #126374, #199380 ) ;
#171996=ORIENTED_EDGE ( 'NONE', *, *, #64293, .F. ) ;
#172000=ORIENTED_EDGE ( 'NONE', *, *, #48346, .F. ) ;
#172041=AXIS2_PLACEMENT_3D ( 'NONE', #151742, #112594, #187009 ) ;
#172055=EDGE_LOOP ( 'NONE', ( #147277, #80546, #189854, #30256 ) ) ;
#172084=ORIENTED_EDGE ( 'NONE', *, *, #142953, .T. ) ;
#172107=DIRECTION ( 'NONE',  ( 0.000000000000000000, 0.9698110461157734008, 0.2438576117980102709 ) ) ;
#172153=ADVANCED_FACE ( 'NONE', ( #224077 ), #125005, .T. ) ;
#172156=CARTESIAN_POINT ( 'NONE',  ( -21.05000000000000071, 28.67750504931771616, -258.3094128005139396 ) ) ;
#172167=TOROIDAL_SURFACE ( 'NONE', #59449, 0.2000000000000000111, 0.1000000000000000056 ) ;
#172184=DIRECTION ( 'NONE',  ( 1.000000000000000000, 0.000000000000000000, 0.000000000000000000 ) ) ;
#172214=DIRECTION ( 'NONE',  ( -0.000000000000000000, -0.8814952561688430555, 0.4721928772777346239 ) ) ;
#172228=ORIENTED_EDGE ( 'NONE', *, *, #250710, .T. ) ;
#172239=CARTESIAN_POINT ( 'NONE',  ( -21.14999999999999858, 12.76524917372336709, -223.4223513401831553 ) ) ;
#172267=CARTESIAN_POINT ( 'NONE',  ( 21.05000000000000071, 23.68770167995059239, -252.8127582590406348 ) ) ;
#172275=CARTESIAN_POINT ( 'NONE',  ( 20.94999999999999929, 36.18002604163306302, -236.0784499204090991 ) ) ;
#172318=CARTESIAN_POINT ( 'NONE',  ( 23.14999999999998437, 7.128833340093095217, -233.7327013124392749 ) ) ;
#172328=DIRECTION ( 'NONE',  ( 0.000000000000000000, 0.8814952561688320642, -0.4721928772777551075 ) ) ;
#172354=VERTEX_POINT ( 'NONE', #236925 ) ;
#172372=CARTESIAN_POINT ( 'NONE',  ( 20.53930447207944354, 18.80980900407904599, -229.8058790690892010 ) ) ;
#172407=ORIENTED_EDGE ( 'NONE', *, *, #183283, .T. ) ;
#172410=EDGE_LOOP ( 'NONE', ( #252859, #194089, #164678, #19111 ) ) ;
#172424=AXIS2_PLACEMENT_3D ( 'NONE', #251840, #108483, #227137 ) ;
#172441=CARTESIAN_POINT ( 'NONE',  ( 18.39999999999999858, 38.27493434228539826, -261.1939574891503639 ) ) ;
#172447=CIRCLE ( 'NONE', #64069, 12.97500000000000320 ) ;
#172451=EDGE_CURVE ( 'NONE', #217355, #161618, #125642, .T. ) ;
#172499=EDGE_CURVE ( 'NONE', #223845, #109477, #66951, .T. ) ;
#172505=DIRECTION ( 'NONE',  ( -1.000000000000000000, 0.000000000000000000, 0.000000000000000000 ) ) ;
#172511=AXIS2_PLACEMENT_3D ( 'NONE', #113740, #132022, #96717 ) ;
#172535=AXIS2_PLACEMENT_3D ( 'NONE', #139487, #5090, #224164 ) ;
#172550=CIRCLE ( 'NONE', #43506, 12.87500000000000178 ) ;
#172562=VERTEX_POINT ( 'NONE', #13413 ) ;
#172647=CARTESIAN_POINT ( 'NONE',  ( -18.59999999999999787, 22.43030315632513094, -231.3223027016406093 ) ) ;
#172656=AXIS2_PLACEMENT_3D ( 'NONE', #236045, #216481, #101634 ) ;
#172661=DIRECTION ( 'NONE',  ( -1.000000000000000000, 0.000000000000000000, 0.000000000000000000 ) ) ;
#172672=ORIENTED_EDGE ( 'NONE', *, *, #75887, .T. ) ;
#172673=FACE_OUTER_BOUND ( 'NONE', #197475, .T. ) ;
#172680=DIRECTION ( 'NONE',  ( 1.000000000000000000, 0.000000000000000000, 0.000000000000000000 ) ) ;
#172719=DIRECTION ( 'NONE',  ( 1.000000000000000000, 1.541880601228652843E-16, 2.878400969107353907E-16 ) ) ;
#172752=AXIS2_PLACEMENT_3D ( 'NONE', #163118, #223062, #182679 ) ;
#172759=EDGE_CURVE ( 'NONE', #130702, #105736, #77525, .T. ) ;
#172762=EDGE_LOOP ( 'NONE', ( #24674, #254230, #125669, #180244 ) ) ;
#172768=VECTOR ( 'NONE', #113919, 1000.000000000000000 ) ;
#172843=CIRCLE ( 'NONE', #76924, 0.3999999999999979683 ) ;
#172852=DIRECTION ( 'NONE',  ( 0.000000000000000000, 0.8814952561688438326, -0.4721928772777330696 ) ) ;
#172854=DIRECTION ( 'NONE',  ( 0.000000000000000000, 0.8814952561688437216, -0.4721928772777334582 ) ) ;
#172862=DIRECTION ( 'NONE',  ( 0.000000000000000000, 0.4721928772777351790, 0.8814952561688427224 ) ) ;
#172866=CARTESIAN_POINT ( 'NONE',  ( -21.44999999999999929, 21.39776787615277343, -233.0380739262505472 ) ) ;
#172874=DIRECTION ( 'NONE',  ( 0.000000000000000000, 0.8814952561688476074, -0.4721928772777262417 ) ) ;
#172904=CARTESIAN_POINT ( 'NONE',  ( -22.50485643085238863, -3.265757507883099375, -228.2539816168355742 ) ) ;
#172906=DIRECTION ( 'NONE',  ( -0.000000000000000000, 0.8814952561688430555, -0.4721928772777346239 ) ) ;
#172908=EDGE_LOOP ( 'NONE', ( #85793, #170031, #16649, #135074 ) ) ;
#172930=ORIENTED_EDGE ( 'NONE', *, *, #241327, .F. ) ;
#172931=AXIS2_PLACEMENT_3D ( 'NONE', #33257, #129751, #151910 ) ;
#172954=CARTESIAN_POINT ( 'NONE',  ( -21.53699400387654350, 1.145497594121937190, -230.5275921506975294 ) ) ;
#172975=CARTESIAN_POINT ( 'NONE',  ( -23.25000000000000000, 19.73066058418984170, -238.2142830767208466 ) ) ;
#172981=CARTESIAN_POINT ( 'NONE',  ( 18.54147908293618130, 8.873963602870817979, -245.4029850331302498 ) ) ;
#172985=DIRECTION ( 'NONE',  ( -1.000000000000000000, 0.000000000000000000, 0.000000000000000000 ) ) ;
#173059=CARTESIAN_POINT ( 'NONE',  ( -23.25000000000000000, 36.65892442174935439, -249.5511627012433848 ) ) ;
#173067=AXIS2_PLACEMENT_3D ( 'NONE', #99544, #457, #56562 ) ;
#173221=DIRECTION ( 'NONE',  ( 1.000000000000000000, -0.000000000000000000, -0.000000000000000000 ) ) ;
#173233=CARTESIAN_POINT ( 'NONE',  ( -21.05000000000000071, 7.128833340093095217, -233.7327013124392749 ) ) ;
#173236=CARTESIAN_POINT ( 'NONE',  ( -23.15000000000000213, 23.38726701055792745, -229.1122755113798632 ) ) ;
#173240=CIRCLE ( 'NONE', #248212, 11.80000000000000959 ) ;
#173246=FACE_OUTER_BOUND ( 'NONE', #215808, .T. ) ;
#173252=ORIENTED_EDGE ( 'NONE', *, *, #36735, .F. ) ;
#173254=DIRECTION ( 'NONE',  ( 1.000000000000000000, 0.000000000000000000, 0.000000000000000000 ) ) ;
#173260=CARTESIAN_POINT ( 'NONE',  ( -20.64999999999999858, 20.06933876993645782, -235.7297789824848451 ) ) ;
#173273=ORIENTED_EDGE ( 'NONE', *, *, #117927, .T. ) ;
#173295=VERTEX_POINT ( 'NONE', #179508 ) ;
#173297=EDGE_CURVE ( 'NONE', #149228, #227874, #198360, .T. ) ;
#173306=DIRECTION ( 'NONE',  ( 0.000000000000000000, -0.9941044884914571611, 0.1084263158146499262 ) ) ;
#173315=DIRECTION ( 'NONE',  ( 1.000000000000000000, 0.000000000000000000, 0.000000000000000000 ) ) ;
#173325=CARTESIAN_POINT ( 'NONE',  ( -22.50000000000000000, -3.096576715760142484, -228.1501377515016884 ) ) ;
#173452=VECTOR ( 'NONE', #89329, 1000.000000000000000 ) ;
#173455=EDGE_CURVE ( 'NONE', #204007, #41254, #64668, .T. ) ;
#173521=CARTESIAN_POINT ( 'NONE',  ( -18.59999999999999787, 23.34004772283015328, -229.2004250369967338 ) ) ;
#173545=CARTESIAN_POINT ( 'NONE',  ( -20.64999999999999858, 29.14863708059993286, -237.4168895852561434 ) ) ;
#173582=ORIENTED_EDGE ( 'NONE', *, *, #228544, .T. ) ;
#173585=CARTESIAN_POINT ( 'NONE',  ( 22.59080734064468032, 12.64999392629033359, -223.3606122593135979 ) ) ;
#173600=CARTESIAN_POINT ( 'NONE',  ( 21.05000000000000071, 13.71992543034163958, -238.5823796952984992 ) ) ;
#173630=CYLINDRICAL_SURFACE ( 'NONE', #73515, 12.87500000000000355 ) ;
#173647=EDGE_CURVE ( 'NONE', #253337, #79099, #115333, .T. ) ;
#173655=CARTESIAN_POINT ( 'NONE',  ( 20.46382478191414833, 18.90138345391644847, -228.0154769769863492 ) ) ;
#173663=EDGE_CURVE ( 'NONE', #229490, #227815, #190379, .T. ) ;
#173673=ADVANCED_FACE ( 'NONE', ( #154516 ), #115347, .F. ) ;
#173683=CIRCLE ( 'NONE', #40394, 0.1000000000000013933 ) ;
#173712=EDGE_LOOP ( 'NONE', ( #9156, #132878, #197666, #37664 ) ) ;
#173727=ORIENTED_EDGE ( 'NONE', *, *, #35103, .F. ) ;
#173747=VERTEX_POINT ( 'NONE', #229563 ) ;
#173767=DIRECTION ( 'NONE',  ( 1.000000000000000000, 0.000000000000000000, 0.000000000000000000 ) ) ;
#173791=DIRECTION ( 'NONE',  ( 0.000000000000000000, -0.8814952561688425003, 0.4721928772777359007 ) ) ;
#173793=ORIENTED_EDGE ( 'NONE', *, *, #144813, .F. ) ;
#173806=AXIS2_PLACEMENT_3D ( 'NONE', #81893, #44093, #186176 ) ;
#173822=AXIS2_PLACEMENT_3D ( 'NONE', #231880, #70247, #130170 ) ;
#173846=DIRECTION ( 'NONE',  ( 1.000000000000000000, 0.000000000000000000, 0.000000000000000000 ) ) ;
#173867=CARTESIAN_POINT ( 'NONE',  ( -20.91682497891422798, 46.43483777265581836, -243.0774829958280918 ) ) ;
#173962=EDGE_CURVE ( 'NONE', #172562, #48651, #198724, .T. ) ;
#173995=CARTESIAN_POINT ( 'NONE',  ( -18.44204374631829424, 38.01828962671714862, -261.0463112980073674 ) ) ;
#174015=ADVANCED_FACE ( 'NONE', ( #196831 ), #73861, .T. ) ;
#174040=DIRECTION ( 'NONE',  ( 0.000000000000000000, -0.8814952561688476074, 0.4721928772777262417 ) ) ;
#174053=FACE_OUTER_BOUND ( 'NONE', #141682, .T. ) ;
#174064=EDGE_CURVE ( 'NONE', #181106, #213843, #240427, .T. ) ;
#174069=FACE_OUTER_BOUND ( 'NONE', #40388, .T. ) ;
#174080=CIRCLE ( 'NONE', #61613, 0.5000000000000179856 ) ;
#174086=ORIENTED_EDGE ( 'NONE', *, *, #222075, .F. ) ;
#174091=PRESENTATION_STYLE_ASSIGNMENT (( #252278 ) ) ;
#174095=AXIS2_PLACEMENT_3D ( 'NONE', #226571, #186189, #200614 ) ;
#174152=DIRECTION ( 'NONE',  ( 0.000000000000000000, -0.5954378521545836689, -0.8034013718071036925 ) ) ;
#174156=AXIS2_PLACEMENT_3D ( 'NONE', #174438, #36178, #93559 ) ;
#174158=AXIS2_PLACEMENT_3D ( 'NONE', #219582, #95776, #17528 ) ;
#174164=ORIENTED_EDGE ( 'NONE', *, *, #250821, .F. ) ;
#174176=EDGE_LOOP ( 'NONE', ( #71410, #62029, #165983, #252504, #42384 ) ) ;
#174240=VECTOR ( 'NONE', #154913, 1000.000000000000000 ) ;
#174293=AXIS2_PLACEMENT_3D ( 'NONE', #62840, #141574, #7184 ) ;
#174311=ORIENTED_EDGE ( 'NONE', *, *, #183283, .F. ) ;
#174329=DIRECTION ( 'NONE',  ( 0.000000000000000000, -0.03181660087581671820, 0.9994937237965574317 ) ) ;
#174438=CARTESIAN_POINT ( 'NONE',  ( 20.85000000000000142, 31.15787740146373608, -259.8205824356103903 ) ) ;
#174460=DIRECTION ( 'NONE',  ( 1.000000000000000000, 0.000000000000000000, 0.000000000000000000 ) ) ;
#174508=CARTESIAN_POINT ( 'NONE',  ( -20.94999999999999929, 9.685169582982728897, -235.1020606565447224 ) ) ;
#174516=DIRECTION ( 'NONE',  ( -7.304098846217608103E-16, 0.4721928772776973204, 0.8814952561688629284 ) ) ;
#174522=CARTESIAN_POINT ( 'NONE',  ( 20.95556889135987788, 18.88117369740709961, -227.9781925454673512 ) ) ;
#174543=DIRECTION ( 'NONE',  ( 1.000000000000000000, 0.000000000000000000, 0.000000000000000000 ) ) ;
#174569=CARTESIAN_POINT ( 'NONE',  ( 21.05000000000000071, 9.997527148596393687, -228.1702915402975407 ) ) ;
#174585=SPHERICAL_SURFACE ( 'NONE', #9429, 0.1000000000000000056 ) ;
#174587=EDGE_CURVE ( 'NONE', #226630, #71383, #186641, .T. ) ;
#174611=CARTESIAN_POINT ( 'NONE',  ( -23.25000000000000000, 24.21659883365190069, -253.0960739854072870 ) ) ;
#174671=ORIENTED_EDGE ( 'NONE', *, *, #12069, .T. ) ;
#174730=DIRECTION ( 'NONE',  ( 1.000000000000000000, 0.000000000000000000, 0.000000000000000000 ) ) ;
#174755=CIRCLE ( 'NONE', #187185, 0.1000000000000013933 ) ;
#174779=CARTESIAN_POINT ( 'NONE',  ( -18.39999999999999858, 37.99112772578902764, -261.0419300540664835 ) ) ;
#174785=CARTESIAN_POINT ( 'NONE',  ( -20.94999999999999929, 36.65892442174935439, -249.5511627012433848 ) ) ;
#174837=ORIENTED_EDGE ( 'NONE', *, *, #186639, .F. ) ;
#174865=ORIENTED_EDGE ( 'NONE', *, *, #186006, .T. ) ;
#174866=CARTESIAN_POINT ( 'NONE',  ( -20.94999999999999929, 18.71344899777637494, -226.7788045585494103 ) ) ;
#174907=EDGE_CURVE ( 'NONE', #93493, #153949, #128547, .T. ) ;
#174910=CARTESIAN_POINT ( 'NONE',  ( 18.49999999999999289, 28.91254064196106910, -237.8576372133405528 ) ) ;
#174947=AXIS2_PLACEMENT_3D ( 'NONE', #132752, #111902, #253942 ) ;
#174949=CARTESIAN_POINT ( 'NONE',  ( 20.97438252431638972, 18.81170931721642603, -229.8655759255429700 ) ) ;
#174963=DIRECTION ( 'NONE',  ( 0.000000000000000000, 0.8814952561688476074, -0.4721928772777262417 ) ) ;
#174971=ORIENTED_EDGE ( 'NONE', *, *, #146178, .F. ) ;
#174989=CARTESIAN_POINT ( 'NONE',  ( 20.85000000000000142, 45.99141771592758943, -256.5205054824189119 ) ) ;
#174998=DIRECTION ( 'NONE',  ( 7.589415207398575214E-15, -0.4721928772777346239, -0.8814952561688430555 ) ) ;
#175002=EDGE_CURVE ( 'NONE', #7289, #218161, #28648, .T. ) ;
#175011=CARTESIAN_POINT ( 'NONE',  ( 18.49999999999907985, 33.73043529525261874, -236.3544816891452740 ) ) ;
#175014=ADVANCED_FACE ( 'NONE', ( #145214 ), #167389, .F. ) ;
#175022=EDGE_LOOP ( 'NONE', ( #127704, #135769, #246399, #180124, #105904 ) ) ;
#175040=DIRECTION ( 'NONE',  ( 0.000000000000000000, -0.8774096236503307056, 0.4797419643160112934 ) ) ;
#175089=CARTESIAN_POINT ( 'NONE',  ( -20.94999999999999929, 7.128833340093095217, -233.7327013124392749 ) ) ;
#175169=ORIENTED_EDGE ( 'NONE', *, *, #253117, .T. ) ;
#175268=CARTESIAN_POINT ( 'NONE',  ( -18.47130263965424390, 38.07810181029199015, -261.0557975469300800 ) ) ;
#175271=ORIENTED_EDGE ( 'NONE', *, *, #120677, .F. ) ;
#175277=ORIENTED_EDGE ( 'NONE', *, *, #28417, .T. ) ;
#175304=DIRECTION ( 'NONE',  ( -1.000000000000000000, -1.394253735153569469E-16, -2.602809386958778209E-16 ) ) ;
#175326=CARTESIAN_POINT ( 'NONE',  ( 21.14999999999999858, 17.83900070254454562, -239.4698447713637677 ) ) ;
#175331=DIRECTION ( 'NONE',  ( -0.000000000000000000, 0.4721928772777345684, 0.8814952561688429444 ) ) ;
#175357=EDGE_LOOP ( 'NONE', ( #202383, #243471, #110854, #48252 ) ) ;
#175368=DIRECTION ( 'NONE',  ( 0.000000000000000000, 0.8814952561688430555, -0.4721928772777347350 ) ) ;
#175375=CARTESIAN_POINT ( 'NONE',  ( -18.59999999999999787, 13.63177590472475487, -238.5351604075707144 ) ) ;
#175392=EDGE_CURVE ( 'NONE', #119943, #144042, #74602, .T. ) ;
#175407=DIRECTION ( 'NONE',  ( 1.000000000000000000, 0.000000000000000000, 0.000000000000000000 ) ) ;
#175441=VERTEX_POINT ( 'NONE', #122174 ) ;
#175469=LINE ( 'NONE', #97144, #247217 ) ;
#175485=CARTESIAN_POINT ( 'NONE',  ( -21.05000000000000071, 7.128833340093095217, -233.7327013124392749 ) ) ;
#175503=AXIS2_PLACEMENT_3D ( 'NONE', #10836, #51205, #8274 ) ;
#175512=DIRECTION ( 'NONE',  ( 0.000000000000000000, -0.9371753822965326330, 0.3488585713686107592 ) ) ;
#175556=EDGE_LOOP ( 'NONE', ( #84237, #177814, #115696, #87435 ) ) ;
#175564=CARTESIAN_POINT ( 'NONE',  ( -18.49719636458566896, 8.901920981062144023, -245.3987932648529693 ) ) ;
#175568=CARTESIAN_POINT ( 'NONE',  ( -20.54999999999999716, 26.34635675162282098, -241.8429480539297174 ) ) ;
#175569=ORIENTED_EDGE ( 'NONE', *, *, #32023, .T. ) ;
#175577=EDGE_CURVE ( 'NONE', #235224, #100823, #116271, .T. ) ;
#175588=VECTOR ( 'NONE', #81035, 1000.000000000000000 ) ;
#175638=EDGE_LOOP ( 'NONE', ( #44145, #117269, #232785, #255501 ) ) ;
#175653=ORIENTED_EDGE ( 'NONE', *, *, #166800, .T. ) ;
#175666=ORIENTED_EDGE ( 'NONE', *, *, #160933, .F. ) ;
#175672=EDGE_LOOP ( 'NONE', ( #159267, #74774, #256407, #41211 ) ) ;
#175683=AXIS2_PLACEMENT_3D ( 'NONE', #174785, #73106, #210025 ) ;
#175689=FACE_OUTER_BOUND ( 'NONE', #154534, .T. ) ;
#175693=ORIENTED_EDGE ( 'NONE', *, *, #196282, .T. ) ;
#175713=ORIENTED_EDGE ( 'NONE', *, *, #215305, .T. ) ;
#175731=VECTOR ( 'NONE', #52905, 1000.000000000000000 ) ;
#175757=DIRECTION ( 'NONE',  ( 0.000000000000000000, -0.8814952561688390587, 0.4721928772777421734 ) ) ;
#175763=CARTESIAN_POINT ( 'NONE',  ( 21.05000000000000071, 18.94908112497232011, -227.8991131484155517 ) ) ;
#175767=DIRECTION ( 'NONE',  ( 0.000000000000000000, 0.8814952561688440547, -0.4721928772777327921 ) ) ;
#175779=ORIENTED_EDGE ( 'NONE', *, *, #13722, .T. ) ;
#175810=DIRECTION ( 'NONE',  ( -1.000000000000000000, -1.541880601228652843E-16, -2.878400969107353907E-16 ) ) ;
#175819=CIRCLE ( 'NONE', #96654, 0.1999999999999966804 ) ;
#175852=EDGE_LOOP ( 'NONE', ( #241835, #101072, #232591, #71627 ) ) ;
#175856=DIRECTION ( 'NONE',  ( 1.000000000000000000, 0.000000000000000000, 0.000000000000000000 ) ) ;
#175866=CARTESIAN_POINT ( 'NONE',  ( 20.94999999999999574, 18.74932170447730329, -227.9057176861678613 ) ) ;
#175875=CARTESIAN_POINT ( 'NONE',  ( 21.05193202509564543, 22.92263105335900164, -230.0273867217252075 ) ) ;
#175885=AXIS2_PLACEMENT_3D ( 'NONE', #94236, #212913, #168700 ) ;
#175977=EDGE_LOOP ( 'NONE', ( #113509, #37145, #187526, #252868 ) ) ;
#175978=ORIENTED_EDGE ( 'NONE', *, *, #113230, .T. ) ;
#176020=CARTESIAN_POINT ( 'NONE',  ( 23.14999999999998437, 7.128833340093095217, -233.7327013124392749 ) ) ;
#176045=CARTESIAN_POINT ( 'NONE',  ( -21.05000000000000071, 16.44800918141279311, -240.8068063186265135 ) ) ;
#176052=EDGE_CURVE ( 'NONE', #213843, #239412, #133193, .T. ) ;
#176053=AXIS2_PLACEMENT_3D ( 'NONE', #4714, #145521, #187247 ) ;
#176062=CIRCLE ( 'NONE', #171780, 0.1000000000000013933 ) ;
#176072=CYLINDRICAL_SURFACE ( 'NONE', #102824, 0.5000000000000008882 ) ;
#176105=ORIENTED_EDGE ( 'NONE', *, *, #30021, .T. ) ;
#176135=ORIENTED_EDGE ( 'NONE', *, *, #157635, .T. ) ;
#176183=AXIS2_PLACEMENT_3D ( 'NONE', #38689, #178220, #120813 ) ;
#176188=CIRCLE ( 'NONE', #109513, 0.1000000000000013933 ) ;
#176193=EDGE_CURVE ( 'NONE', #21030, #134482, #204089, .T. ) ;
#176195=EDGE_LOOP ( 'NONE', ( #163518, #13974 ) ) ;
#176196=CARTESIAN_POINT ( 'NONE',  ( 20.12481660106788084, 18.87840997762110007, -229.2195997782433210 ) ) ;
#176204=EDGE_LOOP ( 'NONE', ( #12348, #185315, #254496 ) ) ;
#176212=DIRECTION ( 'NONE',  ( -0.000000000000000000, 0.4721928772777343464, 0.8814952561688431665 ) ) ;
#176252=ORIENTED_EDGE ( 'NONE', *, *, #27834, .T. ) ;
#176273=CYLINDRICAL_SURFACE ( 'NONE', #257044, 0.09999999999999957534 ) ;
#176289=DIRECTION ( 'NONE',  ( 0.000000000000000000, 0.8814952561688476074, -0.4721928772777262417 ) ) ;
#176314=DIRECTION ( 'NONE',  ( 0.000000000000000000, 0.4721928772777346239, 0.8814952561688430555 ) ) ;
#176318=DIRECTION ( 'NONE',  ( 0.000000000000000000, 0.8814952561688430555, -0.4721928772777346239 ) ) ;
#176325=TOROIDAL_SURFACE ( 'NONE', #105522, 0.4000000000000005773, 0.1000000000000000056 ) ;
#176327=VERTEX_POINT ( 'NONE', #38667 ) ;
#176350=DIRECTION ( 'NONE',  ( -0.000000000000000000, 0.8814952561688430555, -0.4721928772777346239 ) ) ;
#176379=CARTESIAN_POINT ( 'NONE',  ( 20.94999999999999929, 19.00443933019177223, -232.7770257915295531 ) ) ;
#176383=ORIENTED_EDGE ( 'NONE', *, *, #8298, .F. ) ;
#176403=CARTESIAN_POINT ( 'NONE',  ( -20.89878130938411616, 46.45193731540633308, -243.0811559066744110 ) ) ;
#176411=CIRCLE ( 'NONE', #68056, 0.1000000000000058481 ) ;
#176441=CIRCLE ( 'NONE', #209736, 0.09999999999999986677 ) ;
#176496=DIRECTION ( 'NONE',  ( -0.000000000000000000, -0.8454177738465993297, -0.5341055959866553016 ) ) ;
#176531=LINE ( 'NONE', #35744, #67052 ) ;
#176544=ORIENTED_EDGE ( 'NONE', *, *, #48973, .T. ) ;
#176590=CIRCLE ( 'NONE', #22480, 0.09999999999999939493 ) ;
#176596=DIRECTION ( 'NONE',  ( -1.000000000000000000, -0.000000000000000000, -0.000000000000000000 ) ) ;
#176602=CIRCLE ( 'NONE', #160043, 0.5999999999999992006 ) ;
#176653=DIRECTION ( 'NONE',  ( 0.000000000000000000, 0.8814952561688407240, -0.4721928772777390093 ) ) ;
#176660=ORIENTED_EDGE ( 'NONE', *, *, #224420, .F. ) ;
#176662=AXIS2_PLACEMENT_3D ( 'NONE', #108121, #226773, #187676 ) ;
#176672=B_SPLINE_CURVE_WITH_KNOTS ( 'NONE', 3,
 ( #103667, #244484, #144085, #222327, #80240, #241911, #240636, #159837, #101071, #119419 ),
 .UNSPECIFIED., .F., .F.,
 ( 4, 3, 3, 4 ),
 ( 1.301042606982605321E-18, 0.0002000000000008467444, 0.001000000000082971845, 0.001967863649483304195 ),
 .UNSPECIFIED. ) ;
#176691=ORIENTED_EDGE ( 'NONE', *, *, #232815, .F. ) ;
#176741=CARTESIAN_POINT ( 'NONE',  ( 21.14999999999999858, 1.627786319807486892, -244.0021210468063089 ) ) ;
#176746=DIRECTION ( 'NONE',  ( 1.000000000000000000, 2.683427030341257327E-17, -8.429776912874271752E-16 ) ) ;
#176749=ORIENTED_EDGE ( 'NONE', *, *, #86801, .T. ) ;
#176767=DIRECTION ( 'NONE',  ( 1.000000000000000000, 0.000000000000000000, 0.000000000000000000 ) ) ;
#176803=VERTEX_POINT ( 'NONE', #49599 ) ;
#176806=SPHERICAL_SURFACE ( 'NONE', #233753, 0.1000000000000000056 ) ;
#176822=CARTESIAN_POINT ( 'NONE',  ( 22.39999999999999858, 10.71943444926881561, -226.8179467668883547 ) ) ;
#176844=CARTESIAN_POINT ( 'NONE',  ( 23.24999999999999289, 12.76524917372336887, -223.4223513401831269 ) ) ;
#176850=ORIENTED_EDGE ( 'NONE', *, *, #91159, .F. ) ;
#176855=DIRECTION ( 'NONE',  ( -1.000000000000000000, 2.775557561562908012E-13, 5.551115123125816024E-13 ) ) ;
#176864=CIRCLE ( 'NONE', #180945, 1.999999999999997335 ) ;
#176875=CARTESIAN_POINT ( 'NONE',  ( 20.94999999999999574, 18.81166555858608902, -229.8642012822692777 ) ) ;
#176897=VERTEX_POINT ( 'NONE', #191711 ) ;
#176908=LINE ( 'NONE', #197721, #13567 ) ;
#176924=DIRECTION ( 'NONE',  ( -1.000000000000000000, -1.541880601228652843E-16, -2.878400969107353907E-16 ) ) ;
#176932=DIRECTION ( 'NONE',  ( 1.000000000000000000, 0.000000000000000000, 0.000000000000000000 ) ) ;
#176936=ORIENTED_EDGE ( 'NONE', *, *, #138214, .F. ) ;
#176945=DIRECTION ( 'NONE',  ( 0.000000000000000000, 0.8814952561688428334, -0.4721928772777350125 ) ) ;
#177003=CIRCLE ( 'NONE', #210303, 0.09999999999999939493 ) ;
#177038=ORIENTED_EDGE ( 'NONE', *, *, #135682, .T. ) ;
#177069=DIRECTION ( 'NONE',  ( -1.000000000000000000, 0.000000000000000000, 0.000000000000000000 ) ) ;
#177092=CARTESIAN_POINT ( 'NONE',  ( 18.58719872626879877, 38.15560524319364077, -261.2056399649021046 ) ) ;
#177096=B_SPLINE_CURVE_WITH_KNOTS ( 'NONE', 3,
 ( #201947, #3735, #83245, #130093, #93538, #192656, #213484, #230494, #148391, #92248, #170575, #133943, #227923, #209642, #250053, #114394 ),
 .UNSPECIFIED., .F., .F.,
 ( 4, 3, 3, 3, 3, 4 ),
 ( 0.000000000000000000, 2.209833635978364789E-05, 5.595056164120505162E-05, 8.979992002657522703E-05, 0.0001236482757199150722, 0.0001574984039363133280 ),
 .UNSPECIFIED. ) ;
#177104=DIRECTION ( 'NONE',  ( -2.978066053179069723E-16, 0.4721928772777349015, 0.8814952561688428334 ) ) ;
#177134=CARTESIAN_POINT ( 'NONE',  ( -23.15000000000000213, 36.65892442174935439, -249.5511627012433848 ) ) ;
#177135=ORIENTED_EDGE ( 'NONE', *, *, #165586, .T. ) ;
#177137=CARTESIAN_POINT ( 'NONE',  ( -18.59999999999999787, 45.93315328338058379, -256.6017782078560003 ) ) ;
#177202=FACE_OUTER_BOUND ( 'NONE', #137621, .T. ) ;
#177208=DIRECTION ( 'NONE',  ( -0.000000000000000000, -0.8814952561688430555, 0.4721928772777346239 ) ) ;
#177240=ORIENTED_EDGE ( 'NONE', *, *, #191899, .T. ) ;
#177294=VERTEX_POINT ( 'NONE', #16605 ) ;
#177318=EDGE_CURVE ( 'NONE', #70602, #237528, #32223, .T. ) ;
#177412=FACE_OUTER_BOUND ( 'NONE', #25825, .T. ) ;
#177442=EDGE_CURVE ( 'NONE', #236989, #208046, #119701, .T. ) ;
#177451=DIRECTION ( 'NONE',  ( -1.000000000000000000, -1.541880601228652843E-16, -2.878400969107353907E-16 ) ) ;
#177455=AXIS2_PLACEMENT_3D ( 'NONE', #172975, #152112, #37293 ) ;
#177463=AXIS2_PLACEMENT_3D ( 'NONE', #186061, #248599, #25704 ) ;
#177467=EDGE_CURVE ( 'NONE', #254486, #246750, #215546, .T. ) ;
#177483=DIRECTION ( 'NONE',  ( -2.952720810173288619E-16, 0.4721928772777346239, 0.8814952561688430555 ) ) ;
#177506=CIRCLE ( 'NONE', #227522, 11.75000000000000178 ) ;
#177507=SPHERICAL_SURFACE ( 'NONE', #27081, 0.1000000000000000056 ) ;
#177520=DIRECTION ( 'NONE',  ( 1.000000000000000000, 0.000000000000000000, 0.000000000000000000 ) ) ;
#177528=ADVANCED_FACE ( 'NONE', ( #26879 ), #24033, .T. ) ;
#177564=DIRECTION ( 'NONE',  ( 0.000000000000000000, -0.5341055959866798375, 0.8454177738465836756 ) ) ;
#177567=ORIENTED_EDGE ( 'NONE', *, *, #53986, .T. ) ;
#177584=CIRCLE ( 'NONE', #2555, 0.09999999999999939493 ) ;
#177599=EDGE_LOOP ( 'NONE', ( #222085, #165787, #147772, #205850 ) ) ;
#177639=FACE_OUTER_BOUND ( 'NONE', #73422, .T. ) ;
#177647=AXIS2_PLACEMENT_3D ( 'NONE', #16855, #96353, #179456 ) ;
#177669=LINE ( 'NONE', #2829, #156585 ) ;
#177713=CARTESIAN_POINT ( 'NONE',  ( 23.15000000000000213, 28.50120599808395028, -258.2149742250584268 ) ) ;
#177723=EDGE_CURVE ( 'NONE', #208046, #246187, #94343, .T. ) ;
#177726=ORIENTED_EDGE ( 'NONE', *, *, #60144, .T. ) ;
#177734=DIRECTION ( 'NONE',  ( 0.000000000000000000, -0.8740096314914906905, 0.4859085964048265316 ) ) ;
#177753=DIRECTION ( 'NONE',  ( 1.000000000000000000, 0.000000000000000000, 0.000000000000000000 ) ) ;
#177759=DIRECTION ( 'NONE',  ( -1.836970198721029441E-16, 0.4721928772777346239, 0.8814952561688430555 ) ) ;
#177793=ORIENTED_EDGE ( 'NONE', *, *, #95951, .F. ) ;
#177794=CYLINDRICAL_SURFACE ( 'NONE', #27847, 0.09999999999999939493 ) ;
#177802=VERTEX_POINT ( 'NONE', #237883 ) ;
#177812=CARTESIAN_POINT ( 'NONE',  ( -23.25000000000000000, 36.65892442174935439, -249.5511627012433848 ) ) ;
#177814=ORIENTED_EDGE ( 'NONE', *, *, #19898, .T. ) ;
#177825=CARTESIAN_POINT ( 'NONE',  ( -18.41809261886955085, 37.95493855205511835, -261.2294694010199692 ) ) ;
#177831=AXIS2_PLACEMENT_3D ( 'NONE', #162205, #5640, #104732 ) ;
#177849=CYLINDRICAL_SURFACE ( 'NONE', #245068, 0.09999999999999939493 ) ;
#177859=DIRECTION ( 'NONE',  ( -1.000000000000000000, 0.000000000000000000, 0.000000000000000000 ) ) ;
#177877=LINE ( 'NONE', #213128, #250867 ) ;
#177898=CARTESIAN_POINT ( 'NONE',  ( 21.09813707148777340, 10.11617798928880063, -228.0894954011192794 ) ) ;
#177936=AXIS2_PLACEMENT_3D ( 'NONE', #242948, #63024, #186857 ) ;
#177939=ORIENTED_EDGE ( 'NONE', *, *, #52197, .F. ) ;
#177978=CIRCLE ( 'NONE', #32438, 0.1000000000000013933 ) ;
#177982=ORIENTED_EDGE ( 'NONE', *, *, #99711, .F. ) ;
#178003=EDGE_CURVE ( 'NONE', #129778, #206320, #189476, .T. ) ;
#178044=CARTESIAN_POINT ( 'NONE',  ( -18.59999999999999787, 45.93315328338058379, -256.6017782078560003 ) ) ;
#178047=ORIENTED_EDGE ( 'NONE', *, *, #191486, .F. ) ;
#178051=FACE_OUTER_BOUND ( 'NONE', #215617, .T. ) ;
#178070=EDGE_CURVE ( 'NONE', #119326, #182152, #108646, .T. ) ;
#178100=EDGE_LOOP ( 'NONE', ( #30317, #52935, #164647, #153861 ) ) ;
#178105=AXIS2_PLACEMENT_3D ( 'NONE', #36977, #371, #138572 ) ;
#178119=CARTESIAN_POINT ( 'NONE',  ( 23.25000000000000000, -7.761787541757068531, -236.6467894636467975 ) ) ;
#178121=VERTEX_POINT ( 'NONE', #139742 ) ;
#178127=( BOUNDED_CURVE ( )  B_SPLINE_CURVE ( 3, ( #88902, #71938, #173655, #70671 ),
 .UNSPECIFIED., .F., .F. ) 
 B_SPLINE_CURVE_WITH_KNOTS ( ( 4, 4 ),
 ( 4.712388980384689674, 6.231880751915386263 ),
 .UNSPECIFIED. ) 
 CURVE ( )  GEOMETRIC_REPRESENTATION_ITEM ( )  RATIONAL_B_SPLINE_CURVE ( ( 1.000000000000000000, 0.8166740347213228279, 0.8166740347213228279, 1.000000000000000000 ) ) 
 REPRESENTATION_ITEM ( '' )  );
#178133=CARTESIAN_POINT ( 'NONE',  ( -18.46946985241266503, 8.797311384861430383, -245.4141716383250866 ) ) ;
#178137=LINE ( 'NONE', #198953, #185388 ) ;
#178144=ORIENTED_EDGE ( 'NONE', *, *, #136276, .T. ) ;
#178182=( LENGTH_UNIT ( ) NAMED_UNIT ( * ) SI_UNIT ( .MILLI., .METRE. ) );
#178212=CARTESIAN_POINT ( 'NONE',  ( -20.94999999999999929, 14.88773611405353314, -236.3451124650200370 ) ) ;
#178220=DIRECTION ( 'NONE',  ( 0.000000000000000000, -0.8814952561688430555, 0.4721928772777346239 ) ) ;
#178246=DIRECTION ( 'NONE',  ( -0.000000000000000000, 0.8814952561688430555, -0.4721928772777346239 ) ) ;
#178303=CARTESIAN_POINT ( 'NONE',  ( -20.94999999999999929, 28.67750504931771616, -258.3094128005139396 ) ) ;
#178364=CYLINDRICAL_SURFACE ( 'NONE', #16121, 0.09999999999999986677 ) ;
#178387=DIRECTION ( 'NONE',  ( -0.000000000000000000, 0.8814952561688430555, -0.4721928772777346239 ) ) ;
#178477=DIRECTION ( 'NONE',  ( 0.000000000000000000, -0.8814952561688430555, 0.4721928772777347350 ) ) ;
#178516=EDGE_LOOP ( 'NONE', ( #154654, #57455, #195687, #84695 ) ) ;
#178535=EDGE_LOOP ( 'NONE', ( #68809, #80494, #9725 ) ) ;
#178544=AXIS2_PLACEMENT_3D ( 'NONE', #37877, #39162, #54830 ) ;
#178558=AXIS2_PLACEMENT_3D ( 'NONE', #48586, #70757, #151580 ) ;
#178562=DIRECTION ( 'NONE',  ( 0.000000000000000000, -0.8814952561688430555, 0.4721928772777346239 ) ) ;
#178578=CARTESIAN_POINT ( 'NONE',  ( -18.59999999999999787, 30.36376046184471988, -235.5720385971402493 ) ) ;
#178593=CIRCLE ( 'NONE', #191049, 3.899999999999993694 ) ;
#178621=ADVANCED_FACE ( 'NONE', ( #29496 ), #148730, .T. ) ;
#178634=FACE_OUTER_BOUND ( 'NONE', #104733, .T. ) ;
#178659=FACE_OUTER_BOUND ( 'NONE', #86415, .T. ) ;
#178676=EDGE_LOOP ( 'NONE', ( #7294, #183915, #43327, #142731 ) ) ;
#178687=CARTESIAN_POINT ( 'NONE',  ( -21.05000000000000071, 7.219003623157315808, -233.4904674204326227 ) ) ;
#178709=CARTESIAN_POINT ( 'NONE',  ( 18.39999999999999858, 37.99112772578902764, -261.0419300540664835 ) ) ;
#178719=CIRCLE ( 'NONE', #257725, 0.09999999999999986677 ) ;
#178726=EDGE_CURVE ( 'NONE', #154195, #218718, #211962, .T. ) ;
#178727=CYLINDRICAL_SURFACE ( 'NONE', #1024, 0.1000000000000013933 ) ;
#178746=AXIS2_PLACEMENT_3D ( 'NONE', #41688, #46786, #225419 ) ;
#178775=DIRECTION ( 'NONE',  ( 0.000000000000000000, 0.8814952561688444987, -0.4721928772777320149 ) ) ;
#178779=VECTOR ( 'NONE', #230598, 1000.000000000000114 ) ;
#178793=CIRCLE ( 'NONE', #212080, 0.1000000000000075273 ) ;
#178823=EDGE_LOOP ( 'NONE', ( #21609, #93791, #116848, #124972 ) ) ;
#178836=AXIS2_PLACEMENT_3D ( 'NONE', #206836, #107728, #148142 ) ;
#178901=CARTESIAN_POINT ( 'NONE',  ( 23.14999999999999858, 34.77015291263840169, -253.0771437259187167 ) ) ;
#178909=VERTEX_POINT ( 'NONE', #180534 ) ;
#178930=AXIS2_PLACEMENT_3D ( 'NONE', #43811, #123350, #142877 ) ;
#178960=DIRECTION ( 'NONE',  ( -1.000000000000000000, 0.000000000000000000, 0.000000000000000000 ) ) ;
#178981=DIRECTION ( 'NONE',  ( 0.000000000000000000, 0.9421926911474418631, -0.3350715337779995862 ) ) ;
#179017=ORIENTED_EDGE ( 'NONE', *, *, #142822, .F. ) ;
#179020=FACE_OUTER_BOUND ( 'NONE', #125783, .T. ) ;
#179041=AXIS2_PLACEMENT_3D ( 'NONE', #105540, #9046, #5161 ) ;
#179051=DIRECTION ( 'NONE',  ( -1.000000000000000000, 0.000000000000000000, -0.000000000000000000 ) ) ;
#179067=ORIENTED_EDGE ( 'NONE', *, *, #148283, .T. ) ;
#179068=EDGE_CURVE ( 'NONE', #240580, #75284, #207355, .T. ) ;
#179081=VERTEX_POINT ( 'NONE', #35612 ) ;
#179129=VERTEX_POINT ( 'NONE', #231232 ) ;
#179154=CARTESIAN_POINT ( 'NONE',  ( -21.64999999999999858, 29.19585636832770348, -237.3287400596392445 ) ) ;
#179161=EDGE_CURVE ( 'NONE', #148418, #226515, #203244, .T. ) ;
#179228=ORIENTED_EDGE ( 'NONE', *, *, #56498, .T. ) ;
#179240=CARTESIAN_POINT ( 'NONE',  ( -23.25000000000000000, 19.84582043097491422, -235.7234899326461743 ) ) ;
#179318=CIRCLE ( 'NONE', #208536, 0.5000000000000008882 ) ;
#179326=EDGE_CURVE ( 'NONE', #64541, #17866, #103267, .T. ) ;
#179355=CARTESIAN_POINT ( 'NONE',  ( 21.05000000000000071, 18.82290990851282331, -233.3604470821920529 ) ) ;
#179375=ORIENTED_EDGE ( 'NONE', *, *, #48994, .F. ) ;
#179410=AXIS2_PLACEMENT_3D ( 'NONE', #48351, #88739, #33977 ) ;
#179426=ORIENTED_EDGE ( 'NONE', *, *, #62120, .T. ) ;
#179451=ORIENTED_EDGE ( 'NONE', *, *, #139898, .T. ) ;
#179456=DIRECTION ( 'NONE',  ( 0.000000000000000000, 0.8814952561688428334, -0.4721928772777349570 ) ) ;
#179508=CARTESIAN_POINT ( 'NONE',  ( 19.97071067811864609, 34.39212750349580006, -235.0405048756463486 ) ) ;
#179545=CARTESIAN_POINT ( 'NONE',  ( -20.94999999999999929, 26.25728039895700050, -243.9792867493661106 ) ) ;
#179549=VERTEX_POINT ( 'NONE', #191805 ) ;
#179557=EDGE_CURVE ( 'NONE', #140913, #78910, #116145, .T. ) ;
#179564=DIRECTION ( 'NONE',  ( 0.000000000000000000, -0.9371753822965316338, 0.3488585713686134793 ) ) ;
#179565=DIRECTION ( 'NONE',  ( -1.000000000000000000, 0.000000000000000000, 0.000000000000000000 ) ) ;
#179589=AXIS2_PLACEMENT_3D ( 'NONE', #33048, #231219, #194673 ) ;
#179605=DIRECTION ( 'NONE',  ( -4.391705002472921695E-16, 0.4721928772777337913, 0.8814952561688434995 ) ) ;
#179644=CARTESIAN_POINT ( 'NONE',  ( 22.47007471830798053, 0.3230635261676697012, -230.0870367350772767 ) ) ;
#179717=CARTESIAN_POINT ( 'NONE',  ( 21.07888907270776002, 22.96605880254024612, -230.0493642421780862 ) ) ;
#179761=CARTESIAN_POINT ( 'NONE',  ( -20.64999999999999858, 23.68770167995059595, -252.8127582590406348 ) ) ;
#179770=ORIENTED_EDGE ( 'NONE', *, *, #177723, .T. ) ;
#179774=ORIENTED_EDGE ( 'NONE', *, *, #47315, .F. ) ;
#179794=AXIS2_PLACEMENT_3D ( 'NONE', #184794, #45293, #42720 ) ;
#179835=EDGE_LOOP ( 'NONE', ( #183526, #109645, #133542, #29870 ) ) ;
#179892=EDGE_LOOP ( 'NONE', ( #58266, #96434, #234561, #36598 ) ) ;
#179901=EDGE_CURVE ( 'NONE', #45529, #71933, #116324, .T. ) ;
#179919=DIRECTION ( 'NONE',  ( 0.000000000000000000, 0.8814952561688430555, -0.4721928772777346239 ) ) ;
#179924=DIRECTION ( 'NONE',  ( 1.000000000000000000, 0.000000000000000000, 0.000000000000000000 ) ) ;
#179939=CARTESIAN_POINT ( 'NONE',  ( -23.15000000000000213, 28.37802281961254636, -258.4449340416662722 ) ) ;
#179951=CYLINDRICAL_SURFACE ( 'NONE', #215537, 0.09999999999999560629 ) ;
#179956=LINE ( 'NONE', #56120, #151639 ) ;
#179958=CARTESIAN_POINT ( 'NONE',  ( -23.15000000000000213, 19.80622355348251418, -246.0044611956074618 ) ) ;
#179962=CIRCLE ( 'NONE', #146598, 12.87500000000000711 ) ;
#179971=CARTESIAN_POINT ( 'NONE',  ( -18.55121869061588669, 46.45193731540634019, -243.0811559066744110 ) ) ;
#179975=AXIS2_PLACEMENT_3D ( 'NONE', #88209, #132506, #187357 ) ;
#180012=FACE_OUTER_BOUND ( 'NONE', #88681, .T. ) ;
#180053=FACE_OUTER_BOUND ( 'NONE', #88263, .T. ) ;
#180064=ORIENTED_EDGE ( 'NONE', *, *, #5201, .F. ) ;
#180079=ORIENTED_EDGE ( 'NONE', *, *, #1029, .F. ) ;
#180098=EDGE_CURVE ( 'NONE', #63775, #48019, #136970, .T. ) ;
#180114=DIRECTION ( 'NONE',  ( 3.265361837132812600E-16, -0.4721928772777346239, -0.8814952561688430555 ) ) ;
#180124=ORIENTED_EDGE ( 'NONE', *, *, #136095, .F. ) ;
#180156=CARTESIAN_POINT ( 'NONE',  ( 22.47071067811865319, 0.3704148268517115650, -229.9999874772931037 ) ) ;
#180177=SURFACE_SIDE_STYLE ('',( #133643 ) ) ;
#180187=DIRECTION ( 'NONE',  ( 0.000000000000000000, 0.8814952561688428334, -0.4721928772777350125 ) ) ;
#180244=ORIENTED_EDGE ( 'NONE', *, *, #33597, .T. ) ;
#180252=AXIS2_PLACEMENT_3D ( 'NONE', #164997, #103710, #107583 ) ;
#180271=TOROIDAL_SURFACE ( 'NONE', #5258, 0.4000000000000009104, 0.1000000000000000056 ) ;
#180276=CIRCLE ( 'NONE', #67833, 0.1999999999999890476 ) ;
#180283=DIRECTION ( 'NONE',  ( 0.000000000000000000, 0.4721928772777551075, 0.8814952561688320642 ) ) ;
#180293=VERTEX_POINT ( 'NONE', #251953 ) ;
#180306=CARTESIAN_POINT ( 'NONE',  ( 21.05000000000000071, 28.56975825374500388, -258.1421690862028413 ) ) ;
#180312=AXIS2_PLACEMENT_3D ( 'NONE', #192598, #11403, #15257 ) ;
#180334=ORIENTED_EDGE ( 'NONE', *, *, #125775, .T. ) ;
#180343=CARTESIAN_POINT ( 'NONE',  ( -20.64999999999999858, 11.43341603104965110, -245.8667934851861787 ) ) ;
#180363=DIRECTION ( 'NONE',  ( 0.000000000000000000, 0.8814952561688437216, -0.4721928772777334582 ) ) ;
#180365=ADVANCED_FACE ( 'NONE', ( #8220 ), #232419, .T. ) ;
#180384=ORIENTED_EDGE ( 'NONE', *, *, #14686, .F. ) ;
#180392=ORIENTED_EDGE ( 'NONE', *, *, #179901, .T. ) ;
#180427=CIRCLE ( 'NONE', #67999, 12.77500000000000036 ) ;
#180453=CARTESIAN_POINT ( 'NONE',  ( 21.08198257630413508, 10.05689443876789468, -228.1127196910771318 ) ) ;
#180534=CARTESIAN_POINT ( 'NONE',  ( -21.05000000000000071, -3.187427350888460076, -228.3200064793908837 ) ) ;
#180574=CARTESIAN_POINT ( 'NONE',  ( -20.54999999999999716, 36.65892442174935439, -249.5511627012433848 ) ) ;
#180608=AXIS2_PLACEMENT_3D ( 'NONE', #139300, #220156, #80605 ) ;
#180699=EDGE_CURVE ( 'NONE', #223089, #83188, #241568, .T. ) ;
#180700=ADVANCED_FACE ( 'NONE', ( #207410 ), #170506, .T. ) ;
#180716=DIRECTION ( 'NONE',  ( -1.000000000000000000, -0.000000000000000000, -0.000000000000000000 ) ) ;
#180732=ORIENTED_EDGE ( 'NONE', *, *, #255995, .F. ) ;
#180763=DIRECTION ( 'NONE',  ( -0.000000000000000000, 0.8814952561688430555, -0.4721928772777346239 ) ) ;
#180783=CIRCLE ( 'NONE', #230684, 0.1000000000000012546 ) ;
#180810=ORIENTED_EDGE ( 'NONE', *, *, #99429, .F. ) ;
#180853=DIRECTION ( 'NONE',  ( 0.000000000000000000, -0.8814952561688430555, 0.4721928772777346239 ) ) ;
#180872=CARTESIAN_POINT ( 'NONE',  ( -21.13435531349824004, 10.19512217334964888, -228.0085169999992161 ) ) ;
#180930=DIRECTION ( 'NONE',  ( 0.000000000000000000, -0.8814952561688429444, 0.4721928772777345684 ) ) ;
#180934=DIRECTION ( 'NONE',  ( 0.000000000000000000, -0.8814952561688437216, 0.4721928772777334582 ) ) ;
#180945=AXIS2_PLACEMENT_3D ( 'NONE', #170053, #207877, #249555 ) ;
#180971=CIRCLE ( 'NONE', #139431, 3.999999999999994671 ) ;
#180978=CARTESIAN_POINT ( 'NONE',  ( -18.59999999999999787, 9.105964803472822666, -245.3658845043482586 ) ) ;
#180998=DIRECTION ( 'NONE',  ( 1.000000000000000000, 0.000000000000000000, 0.000000000000000000 ) ) ;
#181000=EDGE_LOOP ( 'NONE', ( #255291, #87630, #30264 ) ) ;
#181004=CIRCLE ( 'NONE', #68573, 0.1999999999999997335 ) ;
#181035=CARTESIAN_POINT ( 'NONE',  ( 23.14999999999999503, 38.43293829866423295, -234.5626268121764895 ) ) ;
#181045=VERTEX_POINT ( 'NONE', #88395 ) ;
#181058=ORIENTED_EDGE ( 'NONE', *, *, #184387, .T. ) ;
#181061=ORIENTED_EDGE ( 'NONE', *, *, #224420, .T. ) ;
#181062=ORIENTED_EDGE ( 'NONE', *, *, #70450, .T. ) ;
#181069=CARTESIAN_POINT ( 'NONE',  ( -21.05000000000000071, 18.18127959618848166, -237.5711165786817389 ) ) ;
#181075=CARTESIAN_POINT ( 'NONE',  ( -20.94999999999999929, 28.42524210734032053, -258.3567845160494585 ) ) ;
#181090=ORIENTED_EDGE ( 'NONE', *, *, #199747, .T. ) ;
#181106=VERTEX_POINT ( 'NONE', #255140 ) ;
#181127=AXIS2_PLACEMENT_3D ( 'NONE', #60338, #115193, #76059 ) ;
#181154=ADVANCED_FACE ( 'NONE', ( #94833 ), #83502, .F. ) ;
#181208=FACE_OUTER_BOUND ( 'NONE', #202927, .T. ) ;
#181229=CIRCLE ( 'NONE', #214515, 7.800000000000001599 ) ;
#181258=CARTESIAN_POINT ( 'NONE',  ( -23.15000000000000213, 10.78703865319379496, -235.6923017531418623 ) ) ;
#181268=ORIENTED_EDGE ( 'NONE', *, *, #138984, .T. ) ;
#181272=AXIS2_PLACEMENT_3D ( 'NONE', #163584, #181859, #241823 ) ;
#181277=CARTESIAN_POINT ( 'NONE',  ( -20.64999999999999858, 21.43869811404188752, -233.1734427395952025 ) ) ;
#181305=EDGE_LOOP ( 'NONE', ( #95667, #222042, #164097, #179774 ) ) ;
#181306=ADVANCED_FACE ( 'NONE', ( #147769 ), #43534, .T. ) ;
#181329=EDGE_LOOP ( 'NONE', ( #10928, #16491, #170188, #193416 ) ) ;
#181391=EDGE_CURVE ( 'NONE', #24478, #147651, #129514, .T. ) ;
#181474=CARTESIAN_POINT ( 'NONE',  ( 22.60000000000000142, 7.128833340093095217, -233.7327013124392749 ) ) ;
#181483=DIRECTION ( 'NONE',  ( 0.000000000000000000, 0.8814952561688438326, -0.4721928772777330696 ) ) ;
#181498=DIRECTION ( 'NONE',  ( 0.000000000000000000, -0.8814952561688429444, 0.4721928772777349570 ) ) ;
#181529=EDGE_LOOP ( 'NONE', ( #120812, #137651, #191963, #113594 ) ) ;
#181544=CIRCLE ( 'NONE', #198274, 0.1000000000000013933 ) ;
#181558=ORIENTED_EDGE ( 'NONE', *, *, #203792, .F. ) ;
#181614=CARTESIAN_POINT ( 'NONE',  ( 19.94784844284926351, 34.43454196362160502, -235.0718703888029779 ) ) ;
#181663=ADVANCED_FACE ( 'NONE', ( #190462 ), #171256, .T. ) ;
#181686=EDGE_CURVE ( 'NONE', #21708, #142373, #58754, .T. ) ;
#181698=AXIS2_PLACEMENT_3D ( 'NONE', #46117, #43563, #24018 ) ;
#181720=DIRECTION ( 'NONE',  ( 0.000000000000000000, -0.03181660087583042251, 0.9994937237965568766 ) ) ;
#181727=DIRECTION ( 'NONE',  ( 1.000000000000000000, 0.000000000000000000, 0.000000000000000000 ) ) ;
#181745=DIRECTION ( 'NONE',  ( 0.000000000000000000, 0.8814952561688437216, -0.4721928772777334582 ) ) ;
#181791=DIRECTION ( 'NONE',  ( 0.000000000000000000, -0.8096735173027155286, 0.5868805631290315850 ) ) ;
#181794=CARTESIAN_POINT ( 'NONE',  ( -18.59999999999999787, 36.65892442174935439, -249.5511627012433848 ) ) ;
#181800=FACE_OUTER_BOUND ( 'NONE', #243389, .T. ) ;
#181840=EDGE_CURVE ( 'NONE', #1463, #70494, #78173, .T. ) ;
#181841=ORIENTED_EDGE ( 'NONE', *, *, #230586, .T. ) ;
#181859=DIRECTION ( 'NONE',  ( 1.000000000000000000, 1.394253735153569469E-16, 2.602809386958778209E-16 ) ) ;
#181871=CARTESIAN_POINT ( 'NONE',  ( 23.14999999999999858, 28.08470566095357057, -239.2860081655328770 ) ) ;
#181887=DIRECTION ( 'NONE',  ( 0.000000000000000000, 0.5826443254699750218, 0.8127272543711313579 ) ) ;
#181888=FACE_OUTER_BOUND ( 'NONE', #145130, .T. ) ;
#181910=CARTESIAN_POINT ( 'NONE',  ( -23.25000000000000000, 45.93315328338058379, -256.6017782078560003 ) ) ;
#181916=ADVANCED_FACE ( 'NONE', ( #243684 ), #2488, .T. ) ;
#181935=EDGE_LOOP ( 'NONE', ( #31626, #138149, #105141, #214534 ) ) ;
#181940=EDGE_CURVE ( 'NONE', #50036, #82237, #241140, .T. ) ;
#181973=DIRECTION ( 'NONE',  ( 1.000000000000000000, 0.000000000000000000, 0.000000000000000000 ) ) ;
#181985=VERTEX_POINT ( 'NONE', #82004 ) ;
#182017=ORIENTED_EDGE ( 'NONE', *, *, #117153, .F. ) ;
#182021=FACE_OUTER_BOUND ( 'NONE', #222487, .T. ) ;
#182052=VERTEX_POINT ( 'NONE', #22085 ) ;
#182081=CIRCLE ( 'NONE', #94574, 7.900000000000007461 ) ;
#182135=DIRECTION ( 'NONE',  ( 0.000000000000000000, 0.8814952561688437216, -0.4721928772777334582 ) ) ;
#182152=VERTEX_POINT ( 'NONE', #230551 ) ;
#182174=CARTESIAN_POINT ( 'NONE',  ( -20.94999999999999929, 6.977140961446278489, -233.9419795020459389 ) ) ;
#182197=CARTESIAN_POINT ( 'NONE',  ( -18.59999999999999787, 9.105964803472822666, -245.3658845043482586 ) ) ;
#182240=APPLICATION_CONTEXT ( 'automotive_design' ) ;
#182246=ORIENTED_EDGE ( 'NONE', *, *, #166621, .T. ) ;
#182257=CARTESIAN_POINT ( 'NONE',  ( 18.59999999999999787, 16.53615870702968138, -240.8540256063542984 ) ) ;
#182278=AXIS2_PLACEMENT_3D ( 'NONE', #13718, #210638, #150669 ) ;
#182305=DIRECTION ( 'NONE',  ( 1.000000000000000000, 0.000000000000000000, 0.000000000000000000 ) ) ;
#182309=CIRCLE ( 'NONE', #153117, 0.1000000000000013933 ) ;
#182315=CARTESIAN_POINT ( 'NONE',  ( 20.93975676684922504, 46.39397692848788068, -243.0687461883537424 ) ) ;
#182351=VERTEX_POINT ( 'NONE', #38765 ) ;
#182362=CARTESIAN_POINT ( 'NONE',  ( 21.04999999999999716, 18.80863553818519307, -227.8685860884963290 ) ) ;
#182386=DIRECTION ( 'NONE',  ( -3.265361837132814079E-16, 0.4721928772777359007, 0.8814952561688425003 ) ) ;
#182431=CIRCLE ( 'NONE', #232318, 0.09999999999999986677 ) ;
#182435=EDGE_LOOP ( 'NONE', ( #32919, #4755, #94672, #5460 ) ) ;
#182453=DIRECTION ( 'NONE',  ( 0.000000000000000000, 0.8814952561688476074, -0.4721928772777262417 ) ) ;
#182455=DIRECTION ( 'NONE',  ( -1.000000000000000000, -1.394253735153569469E-16, -2.602809386958778209E-16 ) ) ;
#182488=DIRECTION ( 'NONE',  ( -0.000000000000000000, -0.4721928772777346239, -0.8814952561688430555 ) ) ;
#182489=ORIENTED_EDGE ( 'NONE', *, *, #16035, .T. ) ;
#182501=DIRECTION ( 'NONE',  ( 2.952720810173288126E-16, -0.4721928772777345684, -0.8814952561688429444 ) ) ;
#182508=EDGE_CURVE ( 'NONE', #172354, #57307, #188725, .T. ) ;
#182510=AXIS2_PLACEMENT_3D ( 'NONE', #162340, #31833, #9666 ) ;
#182551=DIRECTION ( 'NONE',  ( 0.000000000000000000, 0.4721928772776973204, 0.8814952561688629284 ) ) ;
#182618=EDGE_CURVE ( 'NONE', #155020, #53624, #247216, .T. ) ;
#182652=DIRECTION ( 'NONE',  ( 1.000000000000000000, 0.000000000000000000, 0.000000000000000000 ) ) ;
#182679=DIRECTION ( 'NONE',  ( 0.000000000000000000, -0.4721928772776973204, -0.8814952561688629284 ) ) ;
#182699=DIRECTION ( 'NONE',  ( 0.000000000000000000, 0.4721928772777351790, 0.8814952561688427224 ) ) ;
#182719=CARTESIAN_POINT ( 'NONE',  ( -21.76363531954647357, 0.9937110212123942965, -230.3339729431867511 ) ) ;
#182745=AXIS2_PLACEMENT_3D ( 'NONE', #120424, #62976, #199943 ) ;
#182752=CARTESIAN_POINT ( 'NONE',  ( 18.59999999999999076, 43.08613539620618837, -254.3146655184800409 ) ) ;
#182767=CARTESIAN_POINT ( 'NONE',  ( -21.44999999999999929, 21.48591740176965814, -233.0852932139783036 ) ) ;
#182771=CARTESIAN_POINT ( 'NONE',  ( 23.25000000000000000, 12.29073439453116201, -249.8274140313476437 ) ) ;
#182781=DIRECTION ( 'NONE',  ( 0.000000000000000000, 0.8814952561688430555, -0.4721928772777344574 ) ) ;
#182782=CARTESIAN_POINT ( 'NONE',  ( -20.94999999999999929, 16.53615870702968138, -240.8540256063542984 ) ) ;
#182816=CIRCLE ( 'NONE', #41157, 11.65000000000000391 ) ;
#182818=CARTESIAN_POINT ( 'NONE',  ( 21.97500000000000497, 22.61918030723622408, -230.9697045991730988 ) ) ;
#182826=CARTESIAN_POINT ( 'NONE',  ( -23.25000000000000000, 2.319530388122572617, -217.8268657444419887 ) ) ;
#182866=ORIENTED_EDGE ( 'NONE', *, *, #112718, .F. ) ;
#182885=CARTESIAN_POINT ( 'NONE',  ( -23.15000000000000213, 23.45160524131172508, -253.2535058871250726 ) ) ;
#182904=AXIS2_PLACEMENT_3D ( 'NONE', #222548, #86884, #166479 ) ;
#182925=CIRCLE ( 'NONE', #211967, 0.1000000000000108025 ) ;
#182929=EDGE_LOOP ( 'NONE', ( #152481, #29857, #36176, #118384 ) ) ;
#182938=VERTEX_POINT ( 'NONE', #128269 ) ;
#182960=EDGE_LOOP ( 'NONE', ( #2021, #233264, #248340, #15546 ) ) ;
#182987=DIRECTION ( 'NONE',  ( 0.000000000000000000, -0.2438576117979363023, 0.9698110461157920525 ) ) ;
#182989=EDGE_CURVE ( 'NONE', #222451, #105736, #207834, .T. ) ;
#182990=CIRCLE ( 'NONE', #58046, 4.000000000000010658 ) ;
#183013=EDGE_CURVE ( 'NONE', #60388, #48459, #75684, .T. ) ;
#183016=VERTEX_POINT ( 'NONE', #78221 ) ;
#183020=FACE_OUTER_BOUND ( 'NONE', #70926, .T. ) ;
#183028=CARTESIAN_POINT ( 'NONE',  ( 21.05000000000000071, 36.65892442174935439, -249.5511627012433848 ) ) ;
#183131=CIRCLE ( 'NONE', #153953, 0.1999999999999987899 ) ;
#183142=DIRECTION ( 'NONE',  ( -1.000000000000000000, 0.000000000000000000, 0.000000000000000000 ) ) ;
#183228=ADVANCED_FACE ( 'NONE', ( #84601 ), #137849, .T. ) ;
#183265=CYLINDRICAL_SURFACE ( 'NONE', #103166, 0.1000000000000075273 ) ;
#183280=DIRECTION ( 'NONE',  ( 0.000000000000000000, 0.8814952561688430555, -0.4721928772777346239 ) ) ;
#183283=EDGE_CURVE ( 'NONE', #89895, #171481, #49382, .T. ) ;
#183295=ADVANCED_FACE ( 'NONE', ( #147188 ), #151055, .T. ) ;
#183300=ORIENTED_EDGE ( 'NONE', *, *, #150187, .F. ) ;
#183301=DIRECTION ( 'NONE',  ( -1.000000000000000000, 0.000000000000000000, 0.000000000000000000 ) ) ;
#183335=ORIENTED_EDGE ( 'NONE', *, *, #39002, .T. ) ;
#183355=DIRECTION ( 'NONE',  ( -1.000000000000000000, 3.448943450116721596E-16, 6.438528483529608630E-16 ) ) ;
#183362=DIRECTION ( 'NONE',  ( 0.000000000000000000, -0.8814952561688430555, 0.4721928772777346239 ) ) ;
#183372=DIRECTION ( 'NONE',  ( 0.000000000000000000, 0.03181660087583048496, -0.9994937237965570986 ) ) ;
#183378=ORIENTED_EDGE ( 'NONE', *, *, #221293, .F. ) ;
#183438=CARTESIAN_POINT ( 'NONE',  ( -21.04999999999958149, 10.11179281909484828, -228.1329080630113140 ) ) ;
#183463=AXIS2_PLACEMENT_3D ( 'NONE', #182767, #161928, #43248 ) ;
#183481=DIRECTION ( 'NONE',  ( 1.000000000000000000, 0.000000000000000000, 0.000000000000000000 ) ) ;
#183486=ORIENTED_EDGE ( 'NONE', *, *, #179161, .F. ) ;
#183490=VERTEX_POINT ( 'NONE', #71975 ) ;
#183492=ORIENTED_EDGE ( 'NONE', *, *, #4276, .F. ) ;
#183495=DIRECTION ( 'NONE',  ( 1.000000000000000000, 0.000000000000000000, 0.000000000000000000 ) ) ;
#183512=EDGE_CURVE ( 'NONE', #203844, #41248, #54828, .T. ) ;
#183526=ORIENTED_EDGE ( 'NONE', *, *, #69283, .T. ) ;
#183545=CARTESIAN_POINT ( 'NONE',  ( -18.52139480978222608, 8.843916517143410871, -245.4074197334283838 ) ) ;
#183558=CARTESIAN_POINT ( 'NONE',  ( 20.95000000000002416, 36.22724532936084074, -235.9903003947922002 ) ) ;
#183682=CIRCLE ( 'NONE', #8887, 0.2000000000000027867 ) ;
#183695=DIRECTION ( 'NONE',  ( -6.938893903907220489E-15, 0.4721928772777343464, 0.8814952561688431665 ) ) ;
#183716=DIRECTION ( 'NONE',  ( -1.000000000000000000, -0.000000000000000000, -0.000000000000000000 ) ) ;
#183721=CARTESIAN_POINT ( 'NONE',  ( 23.14999999999999858, 36.65892442174935439, -249.5511627012433848 ) ) ;
#183754=LINE ( 'NONE', #203317, #103654 ) ;
#183778=AXIS2_PLACEMENT_3D ( 'NONE', #114344, #150900, #93484 ) ;
#183785=DIRECTION ( 'NONE',  ( -0.7071067811865708874, 0.3338907855511046296, 0.6233112732207185536 ) ) ;
#183823=ORIENTED_EDGE ( 'NONE', *, *, #34716, .F. ) ;
#183827=ADVANCED_FACE ( 'NONE', ( #242579 ), #186478, .T. ) ;
#183858=TOROIDAL_SURFACE ( 'NONE', #34057, 0.2000000000000000111, 0.1000000000000000056 ) ;
#183868=ADVANCED_FACE ( 'NONE', ( #251572 ), #252851, .T. ) ;
#183892=AXIS2_PLACEMENT_3D ( 'NONE', #125100, #245031, #45550 ) ;
#183915=ORIENTED_EDGE ( 'NONE', *, *, #76498, .T. ) ;
#183933=DIRECTION ( 'NONE',  ( 0.000000000000000000, 0.8814952561688437216, -0.4721928772777331806 ) ) ;
#183961=ORIENTED_EDGE ( 'NONE', *, *, #160624, .T. ) ;
#183982=DIRECTION ( 'NONE',  ( 1.000000000000000000, 0.000000000000000000, 0.000000000000000000 ) ) ;
#183989=DIRECTION ( 'NONE',  ( 1.000000000000000000, 0.000000000000000000, 0.000000000000000000 ) ) ;
#184005=DIRECTION ( 'NONE',  ( -0.000000000000000000, -0.8814952561688430555, 0.4721928772777346239 ) ) ;
#184010=FACE_OUTER_BOUND ( 'NONE', #126526, .T. ) ;
#184017=CARTESIAN_POINT ( 'NONE',  ( -20.07928932188135107, 22.36925365942468957, -231.4362706255523108 ) ) ;
#184025=CARTESIAN_POINT ( 'NONE',  ( 21.05000000000000071, 36.65892442174935439, -249.5511627012433848 ) ) ;
#184045=LINE ( 'NONE', #100623, #16046 ) ;
#184053=DIRECTION ( 'NONE',  ( 0.000000000000000000, 0.8814952561688428334, -0.4721928772777349570 ) ) ;
#184069=EDGE_CURVE ( 'NONE', #124845, #71933, #37692, .T. ) ;
#184096=ORIENTED_EDGE ( 'NONE', *, *, #19921, .T. ) ;
#184136=ORIENTED_EDGE ( 'NONE', *, *, #13854, .T. ) ;
#184161=CYLINDRICAL_SURFACE ( 'NONE', #7677, 0.09999999999999939493 ) ;
#184183=DIRECTION ( 'NONE',  ( 0.000000000000000000, 0.8814952561688476074, -0.4721928772777262417 ) ) ;
#184188=SPHERICAL_SURFACE ( 'NONE', #257607, 0.1000000000000000056 ) ;
#184198=EDGE_CURVE ( 'NONE', #73105, #138276, #28074, .T. ) ;
#184273=DIRECTION ( 'NONE',  ( 0.000000000000000000, 0.8814952561688476074, -0.4721928772777262417 ) ) ;
#184292=ORIENTED_EDGE ( 'NONE', *, *, #165921, .T. ) ;
#184340=ADVANCED_FACE ( 'NONE', ( #254746, #157001 ), #13621, .T. ) ;
#184346=DIRECTION ( 'NONE',  ( -1.000000000000000000, -1.394253735153569469E-16, -2.602809386958778209E-16 ) ) ;
#184369=AXIS2_PLACEMENT_3D ( 'NONE', #193874, #230425, #131319 ) ;
#184378=CYLINDRICAL_SURFACE ( 'NONE', #108396, 0.09999999999999939493 ) ;
#184383=VERTEX_POINT ( 'NONE', #56558 ) ;
#184387=EDGE_CURVE ( 'NONE', #116858, #72339, #155207, .T. ) ;
#184397=ORIENTED_EDGE ( 'NONE', *, *, #144784, .T. ) ;
#184399=ORIENTED_EDGE ( 'NONE', *, *, #79285, .F. ) ;
#184421=FACE_OUTER_BOUND ( 'NONE', #236156, .T. ) ;
#184427=DIRECTION ( 'NONE',  ( 1.000000000000000000, 1.394253735153569469E-16, 2.602809386958778209E-16 ) ) ;
#184466=VERTEX_POINT ( 'NONE', #160850 ) ;
#184487=CIRCLE ( 'NONE', #246847, 0.1000000000000075273 ) ;
#184489=ORIENTED_EDGE ( 'NONE', *, *, #115460, .T. ) ;
#184492=DIRECTION ( 'NONE',  ( -1.000000000000000000, -0.000000000000000000, -0.000000000000000000 ) ) ;
#184529=FACE_OUTER_BOUND ( 'NONE', #221723, .T. ) ;
#184576=VERTEX_POINT ( 'NONE', #145105 ) ;
#184589=EDGE_LOOP ( 'NONE', ( #154462, #246628, #105899, #196292 ) ) ;
#184614=FILL_AREA_STYLE ('',( #201610 ) ) ;
#184618=TOROIDAL_SURFACE ( 'NONE', #251245, 0.4000000000000012990, 0.1000000000000000056 ) ;
#184665=ADVANCED_FACE ( 'NONE', ( #66869 ), #146379, .T. ) ;
#184668=CARTESIAN_POINT ( 'NONE',  ( 21.93642651522410603, 10.58866904893262095, -227.2738390313130878 ) ) ;
#184670=ADVANCED_FACE ( 'NONE', ( #227219 ), #163727, .T. ) ;
#184689=AXIS2_PLACEMENT_3D ( 'NONE', #233050, #54385, #133917 ) ;
#184693=EDGE_CURVE ( 'NONE', #231948, #182351, #5479, .T. ) ;
#184696=EDGE_LOOP ( 'NONE', ( #90597, #109937, #108473, #250570 ) ) ;
#184739=CARTESIAN_POINT ( 'NONE',  ( 20.94999999999999574, 4.436385504674529301, -245.3241086753762659 ) ) ;
#184744=FACE_OUTER_BOUND ( 'NONE', #25057, .T. ) ;
#184770=CARTESIAN_POINT ( 'NONE',  ( 18.59999999999999432, 14.81796439977981272, -236.5325475414793743 ) ) ;
#184771=DIRECTION ( 'NONE',  ( 0.000000000000000000, 0.4721928772778128947, 0.8814952561688012000 ) ) ;
#184775=DIRECTION ( 'NONE',  ( 0.000000000000000000, 0.8814952561688476074, -0.4721928772777262417 ) ) ;
#184794=CARTESIAN_POINT ( 'NONE',  ( -21.05000000000000071, 4.436385504674529301, -245.3241086753762659 ) ) ;
#184798=AXIS2_PLACEMENT_3D ( 'NONE', #128070, #90197, #108498 ) ;
#184824=CARTESIAN_POINT ( 'NONE',  ( 20.85000000000000142, 36.22724532936083364, -235.9903003947922002 ) ) ;
#184826=ORIENTED_EDGE ( 'NONE', *, *, #172759, .T. ) ;
#184841=ADVANCED_FACE ( 'NONE', ( #97955 ), #137117, .F. ) ;
#184862=TOROIDAL_SURFACE ( 'NONE', #251505, 4.149999999999999467, 0.1000000000000000056 ) ;
#184905=VECTOR ( 'NONE', #242108, 1000.000000000000000 ) ;
#184942=DIRECTION ( 'NONE',  ( 0.000000000000000000, -0.4721928772777332917, -0.8814952561688437216 ) ) ;
#184952=AXIS2_PLACEMENT_3D ( 'NONE', #56901, #132635, #212181 ) ;
#184959=DIRECTION ( 'NONE',  ( 0.000000000000000000, 0.8814952561688476074, -0.4721928772777262417 ) ) ;
#185023=DIRECTION ( 'NONE',  ( -1.000000000000000000, 0.000000000000000000, 0.000000000000000000 ) ) ;
#185031=CARTESIAN_POINT ( 'NONE',  ( -18.59999999999999787, 18.18127959618848166, -237.5711165786817389 ) ) ;
#185041=AXIS2_PLACEMENT_3D ( 'NONE', #27163, #187506, #107944 ) ;
#185128=DIRECTION ( 'NONE',  ( -1.000000000000000000, -0.000000000000000000, -0.000000000000000000 ) ) ;
#185137=CIRCLE ( 'NONE', #218418, 0.3999999999999973022 ) ;
#185147=CARTESIAN_POINT ( 'NONE',  ( 21.05000000000000071, 18.71397270169369875, -229.9382605683272232 ) ) ;
#185166=ORIENTED_EDGE ( 'NONE', *, *, #196277, .T. ) ;
#185172=VERTEX_POINT ( 'NONE', #114681 ) ;
#185173=DIRECTION ( 'NONE',  ( -0.000000000000000000, -0.03181660087583042251, 0.9994937237965568766 ) ) ;
#185182=ORIENTED_EDGE ( 'NONE', *, *, #102572, .F. ) ;
#185183=ORIENTED_EDGE ( 'NONE', *, *, #38217, .F. ) ;
#185184=DIRECTION ( 'NONE',  ( 0.000000000000000000, -0.8454177738465993297, -0.5341055959866553016 ) ) ;
#185189=EDGE_LOOP ( 'NONE', ( #194710, #257526, #61444, #81128 ) ) ;
#185243=AXIS2_PLACEMENT_3D ( 'NONE', #71399, #214731, #16553 ) ;
#185266=ORIENTED_EDGE ( 'NONE', *, *, #160343, .F. ) ;
#185270=ORIENTED_EDGE ( 'NONE', *, *, #98565, .F. ) ;
#185274=CARTESIAN_POINT ( 'NONE',  ( -21.95218792049438861, 0.8274991115115355456, -230.2449076364474081 ) ) ;
#185288=FACE_OUTER_BOUND ( 'NONE', #222748, .T. ) ;
#185309=DIRECTION ( 'NONE',  ( 0.000000000000000000, 0.9371753822965315228, -0.3488585713686133682 ) ) ;
#185313=ADVANCED_FACE ( 'NONE', ( #62415 ), #41587, .T. ) ;
#185315=ORIENTED_EDGE ( 'NONE', *, *, #201347, .F. ) ;
#185325=CIRCLE ( 'NONE', #135422, 0.1000000000000012546 ) ;
#185355=CARTESIAN_POINT ( 'NONE',  ( 20.95512820512820440, 18.90192396791319851, -227.9871466877642661 ) ) ;
#185366=CARTESIAN_POINT ( 'NONE',  ( -22.39999999999999858, 12.67709964810648238, -223.3751320524553705 ) ) ;
#185388=VECTOR ( 'NONE', #76435, 1000.000000000000000 ) ;
#185426=ORIENTED_EDGE ( 'NONE', *, *, #240704, .F. ) ;
#185443=DIRECTION ( 'NONE',  ( 0.000000000000000000, 0.8814952561688430555, -0.4721928772777346239 ) ) ;
#185456=DIRECTION ( 'NONE',  ( 1.000000000000000000, 8.674042436075324885E-17, 1.619280515896126624E-16 ) ) ;
#185476=AXIS2_PLACEMENT_3D ( 'NONE', #171050, #71910, #111022 ) ;
#185485=AXIS2_PLACEMENT_3D ( 'NONE', #153746, #217488, #98807 ) ;
#185508=EDGE_LOOP ( 'NONE', ( #106066, #143496, #8852, #108532 ) ) ;
#185509=ORIENTED_EDGE ( 'NONE', *, *, #160975, .T. ) ;
#185527=EDGE_CURVE ( 'NONE', #11913, #186847, #133926, .T. ) ;
#185546=ORIENTED_EDGE ( 'NONE', *, *, #230080, .T. ) ;
#185583=AXIS2_PLACEMENT_3D ( 'NONE', #152101, #72557, #93375 ) ;
#185611=CARTESIAN_POINT ( 'NONE',  ( -23.25000000000000000, 43.08613539620618837, -254.3146655184800409 ) ) ;
#185631=AXIS2_PLACEMENT_3D ( 'NONE', #151534, #188069, #210210 ) ;
#185656=B_SPLINE_CURVE_WITH_KNOTS ( 'NONE', 3,
 ( #10021, #28340, #170433, #205636, #68716, #50403, #49139, #187390, #51682, #227779, #248630, #208241, #129946, #29616, #110396, #66144, #70020, #30903, #165246 ),
 .UNSPECIFIED., .F., .F.,
 ( 4, 3, 3, 3, 3, 3, 4 ),
 ( -2.000416914664862515E-06, 0.000000000000000000, 4.714008503747113684E-05, 9.979203887778935727E-05, 0.0001372215519229636642, 0.0001635031576221091139, 0.0001900083748504286928 ),
 .UNSPECIFIED. ) ;
#185718=AXIS2_PLACEMENT_3D ( 'NONE', #236385, #60306, #120340 ) ;
#185731=CIRCLE ( 'NONE', #48350, 0.1000000000000013933 ) ;
#185774=EDGE_LOOP ( 'NONE', ( #199910, #25546, #238081, #127022 ) ) ;
#185783=CARTESIAN_POINT ( 'NONE',  ( -18.59999999999999787, 43.24695311518262031, -245.0026972281755491 ) ) ;
#185788=VECTOR ( 'NONE', #1287, 1000.000000000000000 ) ;
#185791=DIRECTION ( 'NONE',  ( 0.000000000000000000, 0.8814952561688439436, -0.4721928772777332362 ) ) ;
#185814=CIRCLE ( 'NONE', #6759, 0.1000000000000013933 ) ;
#185836=CARTESIAN_POINT ( 'NONE',  ( 21.05000000000000071, 7.128833340093095217, -233.7327013124392749 ) ) ;
#185851=AXIS2_PLACEMENT_3D ( 'NONE', #77535, #137518, #217052 ) ;
#185862=DIRECTION ( 'NONE',  ( -1.000000000000000000, 0.000000000000000000, 0.000000000000000000 ) ) ;
#185882=CIRCLE ( 'NONE', #19296, 0.1999999999999997335 ) ;
#185883=AXIS2_PLACEMENT_3D ( 'NONE', #120825, #239469, #216031 ) ;
#185956=DIRECTION ( 'NONE',  ( -7.304098846218132695E-16, 0.4721928772777346794, 0.8814952561688431665 ) ) ;
#185976=CARTESIAN_POINT ( 'NONE',  ( 20.94999999999999574, 4.296375042184049420, -245.1619261326362391 ) ) ;
#185982=AXIS2_PLACEMENT_3D ( 'NONE', #211852, #33239, #174040 ) ;
#186004=DIRECTION ( 'NONE',  ( -0.000000000000000000, 0.4721928772777346239, 0.8814952561688430555 ) ) ;
#186006=EDGE_CURVE ( 'NONE', #184576, #210749, #81044, .T. ) ;
#186021=AXIS2_PLACEMENT_3D ( 'NONE', #136363, #94698, #135098 ) ;
#186032=DIRECTION ( 'NONE',  ( 1.000000000000000000, -0.000000000000000000, -0.000000000000000000 ) ) ;
#186041=CARTESIAN_POINT ( 'NONE',  ( -21.05000000000000071, -3.187805682001703556, -228.3198038177705484 ) ) ;
#186061=CARTESIAN_POINT ( 'NONE',  ( 20.94999999999999574, 4.136903274969363942, -245.4596299165286268 ) ) ;
#186089=AXIS2_PLACEMENT_3D ( 'NONE', #246873, #224736, #164784 ) ;
#186096=DIRECTION ( 'NONE',  ( 1.000000000000000000, -0.000000000000000000, -0.000000000000000000 ) ) ;
#186136=AXIS2_PLACEMENT_3D ( 'NONE', #131949, #103071, #182652 ) ;
#186165=ORIENTED_EDGE ( 'NONE', *, *, #4664, .F. ) ;
#186176=DIRECTION ( 'NONE',  ( 0.000000000000000000, -0.8814952561688476074, 0.4721928772777262417 ) ) ;
#186189=DIRECTION ( 'NONE',  ( 0.000000000000000000, 0.8814952561688430555, -0.4721928772777346239 ) ) ;
#186216=ORIENTED_EDGE ( 'NONE', *, *, #133059, .F. ) ;
#186223=VERTEX_POINT ( 'NONE', #223103 ) ;
#186248=CARTESIAN_POINT ( 'NONE',  ( -20.94999999999999929, 7.219003623157315808, -233.4904674204326227 ) ) ;
#186296=LINE ( 'NONE', #108038, #15600 ) ;
#186309=EDGE_LOOP ( 'NONE', ( #241939, #38305, #36767, #116549 ) ) ;
#186356=CARTESIAN_POINT ( 'NONE',  ( -21.59142135623730852, 29.56732162031123323, -236.8470621936657210 ) ) ;
#186368=CARTESIAN_POINT ( 'NONE',  ( -21.14999999999999858, 12.62988036037870998, -223.4632815780722410 ) ) ;
#186431=DIRECTION ( 'NONE',  ( -1.000000000000000000, 0.000000000000000000, 0.000000000000000000 ) ) ;
#186444=CYLINDRICAL_SURFACE ( 'NONE', #118406, 0.1000000000000013933 ) ;
#186477=VERTEX_POINT ( 'NONE', #152601 ) ;
#186478=CYLINDRICAL_SURFACE ( 'NONE', #84183, 0.09999999999999939493 ) ;
#186480=VERTEX_POINT ( 'NONE', #130428 ) ;
#186501=ORIENTED_EDGE ( 'NONE', *, *, #160495, .T. ) ;
#186515=( BOUNDED_SURFACE ( )  B_SPLINE_SURFACE ( 3, 2, ( 
 ( #224985, #86763, #72379 ),
 ( #253550, #94479, #191051 ),
 ( #231451, #153217, #71094 ),
 ( #131044, #52779, #111488 ),
 ( #235273, #93197, #12411 ),
 ( #33274, #132327, #155780 ) ),
 .UNSPECIFIED., .F., .F., .F. ) 
 B_SPLINE_SURFACE_WITH_KNOTS ( ( 4, 2, 4 ),
 ( 3, 3 ),
 ( 0.0001300404313046743976, 0.0003183318589266739113, 0.0005066232865486734521 ),
 ( 0.000000000000000000, 1.000000000000000000 ),
 .UNSPECIFIED. ) 
 GEOMETRIC_REPRESENTATION_ITEM ( )  RATIONAL_B_SPLINE_SURFACE ( (
 ( 1.000000000000000000, 0.7071067811866340591, 1.000000000000000000),
 ( 1.000000000000000000, 0.7625113560533209878, 1.000000000000000000),
 ( 1.000000000000000000, 0.8126073484696791915, 1.000000000000000000),
 ( 1.000000000000000000, 0.8923049332723984595, 1.000000000000000000),
 ( 1.000000000000000000, 0.9231914937775878016, 1.000000000000000000),
 ( 1.000000000000000000, 0.9238795325112881818, 1.000000000000000000) ) ) 
 REPRESENTATION_ITEM ( '' )  SURFACE ( )  );
#186527=FACE_OUTER_BOUND ( 'NONE', #243149, .T. ) ;
#186547=AXIS2_PLACEMENT_3D ( 'NONE', #195111, #171704, #135088 ) ;
#186556=LINE ( 'NONE', #147417, #214074 ) ;
#186558=CARTESIAN_POINT ( 'NONE',  ( -21.05000000000002203, 1.363275264940673859, -230.6442496871288483 ) ) ;
#186626=ORIENTED_EDGE ( 'NONE', *, *, #22388, .T. ) ;
#186627=EDGE_LOOP ( 'NONE', ( #154932, #171895, #254003, #38653 ) ) ;
#186633=DIRECTION ( 'NONE',  ( 0.000000000000000000, 0.4721928772777820860, 0.8814952561688176313 ) ) ;
#186639=EDGE_CURVE ( 'NONE', #229490, #61591, #143265, .T. ) ;
#186641=CIRCLE ( 'NONE', #153351, 0.09999999999999939493 ) ;
#186652=VERTEX_POINT ( 'NONE', #106691 ) ;
#186699=ORIENTED_EDGE ( 'NONE', *, *, #186901, .F. ) ;
#186707=DIRECTION ( 'NONE',  ( -1.000000000000000000, 0.000000000000000000, 0.000000000000000000 ) ) ;
#186718=AXIS2_PLACEMENT_3D ( 'NONE', #172239, #251728, #152660 ) ;
#186738=DIRECTION ( 'NONE',  ( 0.000000000000000000, 0.8814952561688437216, -0.4721928772777334582 ) ) ;
#186739=ORIENTED_EDGE ( 'NONE', *, *, #132456, .F. ) ;
#186740=CIRCLE ( 'NONE', #28555, 12.87500000000000355 ) ;
#186754=CARTESIAN_POINT ( 'NONE',  ( 21.05000000000000071, 22.90266353732884497, -230.0169390150674076 ) ) ;
#186774=ORIENTED_EDGE ( 'NONE', *, *, #27000, .T. ) ;
#186809=DIRECTION ( 'NONE',  ( -1.000000000000000000, 3.448943450116728005E-16, 6.438528483529605672E-16 ) ) ;
#186810=ADVANCED_FACE ( 'NONE', ( #92272 ), #115400, .F. ) ;
#186811=ORIENTED_EDGE ( 'NONE', *, *, #102477, .F. ) ;
#186847=VERTEX_POINT ( 'NONE', #251344 ) ;
#186857=DIRECTION ( 'NONE',  ( 0.000000000000000000, 0.8814952561688476074, -0.4721928772777262417 ) ) ;
#186901=EDGE_CURVE ( 'NONE', #38568, #159861, #2965, .T. ) ;
#186903=DIRECTION ( 'NONE',  ( 0.000000000000000000, 0.8814952561688438326, -0.4721928772777331251 ) ) ;
#186904=EDGE_LOOP ( 'NONE', ( #30581, #81716, #62998, #58069 ) ) ;
#186953=CARTESIAN_POINT ( 'NONE',  ( 18.59999999999996945, 43.35377423437995503, -245.1717807829448930 ) ) ;
#186961=AXIS2_PLACEMENT_3D ( 'NONE', #183028, #146431, #224690 ) ;
#186962=CARTESIAN_POINT ( 'NONE',  ( 23.14999999999999858, 30.43677443282724937, -239.5249545687858870 ) ) ;
#187006=CYLINDRICAL_SURFACE ( 'NONE', #41442, 0.09999999999999939493 ) ;
#187009=DIRECTION ( 'NONE',  ( 0.000000000000000000, -0.8814952561687088295, 0.4721928772779852013 ) ) ;
#187065=ORIENTED_EDGE ( 'NONE', *, *, #235109, .F. ) ;
#187094=AXIS2_PLACEMENT_3D ( 'NONE', #127526, #167965, #52775 ) ;
#187137=AXIS2_PLACEMENT_3D ( 'NONE', #254516, #176318, #155487 ) ;
#187165=DIRECTION ( 'NONE',  ( 1.000000000000000000, -7.930164461608253340E-15, 0.000000000000000000 ) ) ;
#187171=EDGE_CURVE ( 'NONE', #9313, #67371, #148031, .T. ) ;
#187185=AXIS2_PLACEMENT_3D ( 'NONE', #248534, #92024, #13779 ) ;
#187194=DIRECTION ( 'NONE',  ( 2.952720810173290098E-16, -0.4721928772777333472, -0.8814952561688437216 ) ) ;
#187211=ADVANCED_FACE ( 'NONE', ( #23882 ), #97931, .F. ) ;
#187247=DIRECTION ( 'NONE',  ( 0.000000000000000000, 0.4721928772777343464, 0.8814952561688431665 ) ) ;
#187321=EDGE_CURVE ( 'NONE', #41664, #81229, #206304, .T. ) ;
#187338=CARTESIAN_POINT ( 'NONE',  ( 20.94999999999999929, 36.12913288928921673, -236.0511878519285176 ) ) ;
#187357=DIRECTION ( 'NONE',  ( 0.000000000000000000, 0.8814952561688476074, -0.4721928772777262417 ) ) ;
#187360=DIRECTION ( 'NONE',  ( 1.000000000000000000, 0.000000000000000000, 0.000000000000000000 ) ) ;
#187368=AXIS2_PLACEMENT_3D ( 'NONE', #127236, #67256, #106360 ) ;
#187372=CARTESIAN_POINT ( 'NONE',  ( 20.94999999999999929, 18.71171618620643429, -229.8673829423568691 ) ) ;
#187384=CARTESIAN_POINT ( 'NONE',  ( 18.50000000000000000, 9.122720154857365316, -245.4644708025848274 ) ) ;
#187390=CARTESIAN_POINT ( 'NONE',  ( 18.51024323315077069, 46.39397692848790200, -243.0687461883537708 ) ) ;
#187398=EDGE_CURVE ( 'NONE', #253739, #125839, #247983, .T. ) ;
#187410=CYLINDRICAL_SURFACE ( 'NONE', #134432, 0.5000000000000008882 ) ;
#187421=EDGE_CURVE ( 'NONE', #83188, #257030, #252037, .T. ) ;
#187422=DIRECTION ( 'NONE',  ( -1.000000000000000000, 0.000000000000000000, 0.000000000000000000 ) ) ;
#187423=DIRECTION ( 'NONE',  ( 0.000000000000000000, -0.8814952561688430555, 0.4721928772777346239 ) ) ;
#187446=EDGE_CURVE ( 'NONE', #121060, #239691, #6374, .T. ) ;
#187448=LINE ( 'NONE', #8798, #112786 ) ;
#187467=CYLINDRICAL_SURFACE ( 'NONE', #17156, 0.1000000000000053763 ) ;
#187496=CARTESIAN_POINT ( 'NONE',  ( -21.03922262424668688, 18.66391577654005829, -226.7251572270064912 ) ) ;
#187506=DIRECTION ( 'NONE',  ( -0.7071067811865474617, -0.3338907855510734324, -0.6233112732207618523 ) ) ;
#187526=ORIENTED_EDGE ( 'NONE', *, *, #35882, .F. ) ;
#187536=FACE_OUTER_BOUND ( 'NONE', #182435, .T. ) ;
#187598=CARTESIAN_POINT ( 'NONE',  ( 23.14999999999999858, 35.97645343225767789, -235.9694016464868298 ) ) ;
#187609=ORIENTED_EDGE ( 'NONE', *, *, #132456, .T. ) ;
#187618=DIRECTION ( 'NONE',  ( 1.000000000000000000, 0.000000000000000000, 0.000000000000000000 ) ) ;
#187635=AXIS2_PLACEMENT_3D ( 'NONE', #2811, #245299, #66661 ) ;
#187643=EDGE_CURVE ( 'NONE', #217845, #129019, #207013, .T. ) ;
#187661=DIRECTION ( 'NONE',  ( 0.000000000000000000, -0.5826443254699606999, -0.8127272543711416830 ) ) ;
#187666=ORIENTED_EDGE ( 'NONE', *, *, #17488, .T. ) ;
#187676=DIRECTION ( 'NONE',  ( 0.000000000000000000, 0.8814952561688428334, -0.4721928772777350125 ) ) ;
#187682=EDGE_CURVE ( 'NONE', #170534, #208884, #25010, .T. ) ;
#187698=ORIENTED_EDGE ( 'NONE', *, *, #19018, .T. ) ;
#187704=EDGE_CURVE ( 'NONE', #246187, #239741, #106487, .T. ) ;
#187732=DIRECTION ( 'NONE',  ( 0.000000000000000000, -0.4721928772777352346, -0.8814952561688428334 ) ) ;
#187757=ORIENTED_EDGE ( 'NONE', *, *, #39632, .F. ) ;
#187762=DIRECTION ( 'NONE',  ( 0.000000000000000000, 0.8814952561688476074, -0.4721928772777262417 ) ) ;
#187798=ORIENTED_EDGE ( 'NONE', *, *, #192949, .F. ) ;
#187812=ORIENTED_EDGE ( 'NONE', *, *, #12986, .F. ) ;
#187813=ORIENTED_EDGE ( 'NONE', *, *, #171447, .T. ) ;
#187827=DIRECTION ( 'NONE',  ( 0.000000000000000000, 0.4721928772777330696, 0.8814952561688438326 ) ) ;
#187858=ORIENTED_EDGE ( 'NONE', *, *, #66330, .T. ) ;
#187860=CARTESIAN_POINT ( 'NONE',  ( -21.07928932188134041, 1.596973512272247042, -230.6572452218044020 ) ) ;
#187871=DIRECTION ( 'NONE',  ( -0.000000000000000000, -0.8814952561688430555, 0.4721928772777346239 ) ) ;
#187879=EDGE_CURVE ( 'NONE', #201767, #92552, #102567, .T. ) ;
#187891=FACE_OUTER_BOUND ( 'NONE', #18346, .T. ) ;
#187918=AXIS2_PLACEMENT_3D ( 'NONE', #20488, #16634, #96134 ) ;
#187928=CARTESIAN_POINT ( 'NONE',  ( 23.14999999999999503, 28.95347087985017609, -237.9930060266852081 ) ) ;
#187934=CARTESIAN_POINT ( 'NONE',  ( 22.59066674512260064, 12.65021040783260275, -223.3607282225494544 ) ) ;
#187940=ORIENTED_EDGE ( 'NONE', *, *, #80906, .F. ) ;
#187941=DIRECTION ( 'NONE',  ( 1.000000000000000000, 0.000000000000000000, 0.000000000000000000 ) ) ;
#187960=LINE ( 'NONE', #84963, #53557 ) ;
#187968=EDGE_CURVE ( 'NONE', #34543, #74336, #60899, .T. ) ;
#187973=ORIENTED_EDGE ( 'NONE', *, *, #246333, .F. ) ;
#187997=CIRCLE ( 'NONE', #137897, 0.1000000000000013933 ) ;
#188008=DIRECTION ( 'NONE',  ( 1.000000000000000000, 0.000000000000000000, 0.000000000000000000 ) ) ;
#188027=DIRECTION ( 'NONE',  ( 1.000000000000000000, 5.204170427930452838E-14, 0.000000000000000000 ) ) ;
#188031=CARTESIAN_POINT ( 'NONE',  ( 21.14999999999999858, 10.21728496540352360, -227.9671432372868765 ) ) ;
#188069=DIRECTION ( 'NONE',  ( 0.000000000000000000, -0.8814952561688430555, 0.4721928772777346239 ) ) ;
#188094=ADVANCED_FACE ( 'NONE', ( #105123 ), #89446, .F. ) ;
#188145=DIRECTION ( 'NONE',  ( 0.000000000000000000, 0.5826443254699606999, 0.8127272543711416830 ) ) ;
#188164=ORIENTED_EDGE ( 'NONE', *, *, #15827, .F. ) ;
#188200=ORIENTED_EDGE ( 'NONE', *, *, #240302, .T. ) ;
#188210=DIRECTION ( 'NONE',  ( 0.000000000000000000, -0.8814952561688476074, 0.4721928772777262417 ) ) ;
#188222=LINE ( 'NONE', #229918, #246177 ) ;
#188245=CARTESIAN_POINT ( 'NONE',  ( -23.15000000000000213, -1.269135479188211013, -224.5262296913251987 ) ) ;
#188254=DIRECTION ( 'NONE',  ( -0.000000000000000000, 0.8814952561688430555, -0.4721928772777346239 ) ) ;
#188273=CARTESIAN_POINT ( 'NONE',  ( -21.05000000000000071, 18.27574494880468592, -237.6039235467692947 ) ) ;
#188285=TOROIDAL_SURFACE ( 'NONE', #100762, 0.2000000000000000111, 0.1000000000000000056 ) ;
#188293=AXIS2_PLACEMENT_3D ( 'NONE', #71680, #229454, #110778 ) ;
#188308=CARTESIAN_POINT ( 'NONE',  ( 21.05000000000000071, 22.92579362702542412, -230.0293291570564520 ) ) ;
#188319=EDGE_CURVE ( 'NONE', #138276, #213072, #231807, .T. ) ;
#188322=AXIS2_PLACEMENT_3D ( 'NONE', #244591, #201620, #225013 ) ;
#188377=LINE ( 'NONE', #89266, #131413 ) ;
#188380=CARTESIAN_POINT ( 'NONE',  ( 18.39999999999999858, 37.95493834378066111, -261.2294694241335264 ) ) ;
#188383=VERTEX_POINT ( 'NONE', #80123 ) ;
#188398=EDGE_LOOP ( 'NONE', ( #112342, #215263, #159890, #252951 ) ) ;
#188401=CARTESIAN_POINT ( 'NONE',  ( -22.57320508075686760, 12.67709964810650902, -223.3751320524553705 ) ) ;
#188408=CARTESIAN_POINT ( 'NONE',  ( 23.15000000000000213, 23.40438595358394736, -253.3416554127419431 ) ) ;
#188409=DIRECTION ( 'NONE',  ( 4.504528286903030855E-15, 0.8127272543710891695, -0.5826443254700338636 ) ) ;
#188423=ORIENTED_EDGE ( 'NONE', *, *, #42594, .F. ) ;
#188432=DIRECTION ( 'NONE',  ( 0.000000000000000000, -0.8814952561688476074, 0.4721928772777262417 ) ) ;
#188442=DIRECTION ( 'NONE',  ( 0.000000000000000000, 0.8454177738465993297, 0.5341055959866553016 ) ) ;
#188452=VERTEX_POINT ( 'NONE', #240529 ) ;
#188460=CYLINDRICAL_SURFACE ( 'NONE', #202557, 0.09999999999999986677 ) ;
#188462=EDGE_CURVE ( 'NONE', #241914, #233103, #136079, .T. ) ;
#188468=ORIENTED_EDGE ( 'NONE', *, *, #196421, .F. ) ;
#188486=VERTEX_POINT ( 'NONE', #100959 ) ;
#188551=TOROIDAL_SURFACE ( 'NONE', #138462, 3.899999999999999467, 0.1000000000000000056 ) ;
#188560=DIRECTION ( 'NONE',  ( 0.000000000000000000, 0.8814952561688442767, -0.4721928772777324035 ) ) ;
#188561=LINE ( 'NONE', #209405, #157670 ) ;
#188563=CARTESIAN_POINT ( 'NONE',  ( 21.05543885634738643, 22.01316703130699182, -231.7502803265042246 ) ) ;
#188613=CARTESIAN_POINT ( 'NONE',  ( -22.39999999999999858, 0.3085173699977072914, -229.9658011520297691 ) ) ;
#188647=DIRECTION ( 'NONE',  ( 1.301042606982683102E-14, -0.8496786552930133407, -0.5273008465188128158 ) ) ;
#188648=EDGE_CURVE ( 'NONE', #226630, #15834, #231260, .T. ) ;
#188676=CARTESIAN_POINT ( 'NONE',  ( -20.94999999999999929, 38.43293829866423295, -234.5626268121764895 ) ) ;
#188707=DIRECTION ( 'NONE',  ( -0.000000000000000000, 0.03181660087583042251, -0.9994937237965568766 ) ) ;
#188709=DIRECTION ( 'NONE',  ( 1.000000000000000000, 0.000000000000000000, 0.000000000000000000 ) ) ;
#188725=( BOUNDED_CURVE ( )  B_SPLINE_CURVE ( 3, ( #248508, #245954, #210666, #8623 ),
 .UNSPECIFIED., .F., .F. ) 
 B_SPLINE_CURVE_WITH_KNOTS ( ( 4, 4 ),
 ( 0.06456096931748313283, 3.077031684272310219 ),
 .UNSPECIFIED. ) 
 CURVE ( )  GEOMETRIC_REPRESENTATION_ITEM ( )  RATIONAL_B_SPLINE_CURVE ( ( 1.000000000000000000, 0.3763440860215094830, 0.3763440860215094830, 1.000000000000000000 ) ) 
 REPRESENTATION_ITEM ( '' )  );
#188728=EDGE_LOOP ( 'NONE', ( #99912, #114548, #201846, #113657 ) ) ;
#188751=CARTESIAN_POINT ( 'NONE',  ( -20.94999999999999929, 18.70793820085226500, -226.6056871674032323 ) ) ;
#188760=DIRECTION ( 'NONE',  ( 0.000000000000000000, -0.8814952561688476074, 0.4721928772777262417 ) ) ;
#188790=CARTESIAN_POINT ( 'NONE',  ( 18.59999999999999432, -2.275048162540885155, -230.1697641654749305 ) ) ;
#188793=CARTESIAN_POINT ( 'NONE',  ( -22.24259225415828212, 10.57914693326955735, -227.0818154154764841 ) ) ;
#188794=EDGE_LOOP ( 'NONE', ( #137073, #20967, #90008, #250690 ) ) ;
#188826=DIRECTION ( 'NONE',  ( 1.000000000000000000, 0.000000000000000000, 0.000000000000000000 ) ) ;
#188830=VERTEX_POINT ( 'NONE', #240242 ) ;
#188856=DIRECTION ( 'NONE',  ( 0.000000000000000000, 0.8814952561688444987, -0.4721928772777320149 ) ) ;
#188871=EDGE_LOOP ( 'NONE', ( #220309, #234908, #151830, #35718 ) ) ;
#188879=CIRCLE ( 'NONE', #255466, 2.000000000000006661 ) ;
#188891=ORIENTED_EDGE ( 'NONE', *, *, #175577, .T. ) ;
#188963=ORIENTED_EDGE ( 'NONE', *, *, #236578, .T. ) ;
#188969=CARTESIAN_POINT ( 'NONE',  ( -18.50000000000000000, 31.49702336731128582, -233.4564499823349877 ) ) ;
#188991=DIRECTION ( 'NONE',  ( -1.000000000000000000, 0.000000000000000000, 0.000000000000000000 ) ) ;
#188994=AXIS2_PLACEMENT_3D ( 'NONE', #239717, #21961, #101429 ) ;
#189004=FACE_OUTER_BOUND ( 'NONE', #18385, .T. ) ;
#189047=ORIENTED_EDGE ( 'NONE', *, *, #170924, .T. ) ;
#189050=CARTESIAN_POINT ( 'NONE',  ( -21.65000000000000213, 21.65523568329831505, -232.7692078405380300 ) ) ;
#189062=CARTESIAN_POINT ( 'NONE',  ( -22.57320508075687115, 12.67709964810647882, -223.3751320524553705 ) ) ;
#189065=DIRECTION ( 'NONE',  ( 0.000000000000000000, 0.8814952561688429444, -0.4721928772777348460 ) ) ;
#189093=CARTESIAN_POINT ( 'NONE',  ( 23.24999999999999645, 35.66731937946609321, -251.4023027391979497 ) ) ;
#189107=EDGE_CURVE ( 'NONE', #218397, #97404, #90101, .T. ) ;
#189157=CIRCLE ( 'NONE', #222432, 0.09999999999999983902 ) ;
#189161=CIRCLE ( 'NONE', #55852, 0.4999999999999970024 ) ;
#189173=EDGE_CURVE ( 'NONE', #97016, #249890, #256854, .T. ) ;
#189179=CIRCLE ( 'NONE', #39359, 0.1000000000000013933 ) ;
#189191=EDGE_CURVE ( 'NONE', #203844, #186652, #162969, .T. ) ;
#189192=AXIS2_PLACEMENT_3D ( 'NONE', #157602, #72923, #55856 ) ;
#189203=EDGE_LOOP ( 'NONE', ( #254297, #1462, #229719, #159430 ) ) ;
#189238=DIRECTION ( 'NONE',  ( 0.000000000000000000, 0.8814952561688476074, -0.4721928772777262417 ) ) ;
#189269=ADVANCED_FACE ( 'NONE', ( #122555 ), #23473, .T. ) ;
#189275=EDGE_CURVE ( 'NONE', #138714, #124845, #29886, .T. ) ;
#189294=CARTESIAN_POINT ( 'NONE',  ( -21.05000000000000071, 14.81796439977981272, -236.5325475414793743 ) ) ;
#189297=CARTESIAN_POINT ( 'NONE',  ( 21.14999999999999858, 10.30543449102040654, -228.0143625250146329 ) ) ;
#189372=ORIENTED_EDGE ( 'NONE', *, *, #230080, .F. ) ;
#189380=EDGE_CURVE ( 'NONE', #103462, #98749, #7737, .T. ) ;
#189382=CARTESIAN_POINT ( 'NONE',  ( -23.15000000000000213, 28.56975825374500388, -258.1421690862028413 ) ) ;
#189395=DIRECTION ( 'NONE',  ( -2.557131231893036492E-16, 0.8496786552930076786, 0.5273008465188220306 ) ) ;
#189396=CARTESIAN_POINT ( 'NONE',  ( 18.41832399655350727, 37.95493863640855636, -261.2294693916588244 ) ) ;
#189414=CARTESIAN_POINT ( 'NONE',  ( 21.09610168723073187, 1.521674863716753423, -230.6909948682581444 ) ) ;
#189454=EDGE_LOOP ( 'NONE', ( #146619, #69287, #40738, #36413 ) ) ;
#189476=LINE ( 'NONE', #13412, #119311 ) ;
#189514=CARTESIAN_POINT ( 'NONE',  ( 20.94999999999999929, 43.35377423437995503, -245.1717807829448930 ) ) ;
#189522=DIRECTION ( 'NONE',  ( 0.000000000000000000, 0.8814952561688430555, -0.4721928772777346239 ) ) ;
#189544=ORIENTED_EDGE ( 'NONE', *, *, #186006, .F. ) ;
#189581=ADVANCED_FACE ( 'NONE', ( #79224 ), #202716, .F. ) ;
#189597=VECTOR ( 'NONE', #145823, 1000.000000000000000 ) ;
#189608=PLANE ( 'NONE',  #130457 ) ;
#189613=CIRCLE ( 'NONE', #156314, 0.1000000000000012546 ) ;
#189637=ORIENTED_EDGE ( 'NONE', *, *, #190461, .F. ) ;
#189647=VERTEX_POINT ( 'NONE', #249571 ) ;
#189664=ORIENTED_EDGE ( 'NONE', *, *, #1437, .T. ) ;
#189676=ORIENTED_EDGE ( 'NONE', *, *, #232919, .T. ) ;
#189681=ORIENTED_EDGE ( 'NONE', *, *, #216873, .T. ) ;
#189699=CARTESIAN_POINT ( 'NONE',  ( 20.94999999999999929, 36.65892442174935439, -249.5511627012433848 ) ) ;
#189701=CIRCLE ( 'NONE', #73210, 0.1000000000000019901 ) ;
#189733=ORIENTED_EDGE ( 'NONE', *, *, #42323, .T. ) ;
#189752=VECTOR ( 'NONE', #128081, 1000.000000000000000 ) ;
#189776=AXIS2_PLACEMENT_3D ( 'NONE', #214733, #255091, #130387 ) ;
#189845=CARTESIAN_POINT ( 'NONE',  ( 23.24999999999999289, 2.319530388122574394, -217.8268657444419887 ) ) ;
#189851=CARTESIAN_POINT ( 'NONE',  ( 21.10710606213542206, 22.06360055159736788, -231.7760222370280303 ) ) ;
#189854=ORIENTED_EDGE ( 'NONE', *, *, #174587, .F. ) ;
#189875=ORIENTED_EDGE ( 'NONE', *, *, #223610, .T. ) ;
#189877=PLANE ( 'NONE',  #210000 ) ;
#189954=EDGE_LOOP ( 'NONE', ( #207613, #17253, #237476 ) ) ;
#189968=FACE_OUTER_BOUND ( 'NONE', #185774, .T. ) ;
#189969=ORIENTED_EDGE ( 'NONE', *, *, #40060, .F. ) ;
#189979=CARTESIAN_POINT ( 'NONE',  ( -20.94999999999999929, 36.14042471737580087, -236.0721279892244411 ) ) ;
#189982=CARTESIAN_POINT ( 'NONE',  ( -18.50000000000000000, 18.11150788191476124, -237.7585516551410478 ) ) ;
#189986=AXIS2_PLACEMENT_3D ( 'NONE', #22710, #40992, #239163 ) ;
#189998=DIRECTION ( 'NONE',  ( 0.000000000000000000, 0.8814952561688476074, -0.4721928772777262417 ) ) ;
#190030=CARTESIAN_POINT ( 'NONE',  ( 21.14999999999999503, -3.275978944802464099, -228.2735455795363748 ) ) ;
#190031=FACE_OUTER_BOUND ( 'NONE', #15745, .T. ) ;
#190060=DIRECTION ( 'NONE',  ( 0.7071067811865474617, 0.3338907855510732658, 0.6233112732207619633 ) ) ;
#190080=DIRECTION ( 'NONE',  ( 1.000000000000000000, -0.000000000000000000, -0.000000000000000000 ) ) ;
#190083=CARTESIAN_POINT ( 'NONE',  ( -21.07016717456945898, 10.11353658153798918, -228.1608219491300531 ) ) ;
#190116=FACE_OUTER_BOUND ( 'NONE', #129266, .T. ) ;
#190126=EDGE_CURVE ( 'NONE', #3876, #231732, #230993, .T. ) ;
#190131=ORIENTED_EDGE ( 'NONE', *, *, #163668, .F. ) ;
#190172=CARTESIAN_POINT ( 'NONE',  ( 20.94999999999999929, 28.51339163295720525, -258.4040038037771865 ) ) ;
#190183=FACE_OUTER_BOUND ( 'NONE', #33942, .T. ) ;
#190194=DIRECTION ( 'NONE',  ( 1.000000000000000000, 0.000000000000000000, 0.000000000000000000 ) ) ;
#190196=LINE ( 'NONE', #55764, #255931 ) ;
#190197=ADVANCED_FACE ( 'NONE', ( #77023 ), #156611, .T. ) ;
#190204=DIRECTION ( 'NONE',  ( 0.000000000000000000, 0.5826443254699606999, 0.8127272543711416830 ) ) ;
#190206=CIRCLE ( 'NONE', #156907, 0.09999999999999939493 ) ;
#190210=DIRECTION ( 'NONE',  ( -1.000000000000000000, 0.000000000000000000, 0.000000000000000000 ) ) ;
#190233=DIRECTION ( 'NONE',  ( -1.000000000000000000, -1.394253735153569469E-16, -2.602809386958778209E-16 ) ) ;
#190256=DIRECTION ( 'NONE',  ( -1.000000000000000000, -0.000000000000000000, -0.000000000000000000 ) ) ;
#190261=DIRECTION ( 'NONE',  ( 1.000000000000000000, 3.448943450116727019E-16, 6.438528483529604686E-16 ) ) ;
#190267=DIRECTION ( 'NONE',  ( 0.000000000000000000, -0.4721928772777346239, -0.8814952561688430555 ) ) ;
#190272=VERTEX_POINT ( 'NONE', #163010 ) ;
#190306=DIRECTION ( 'NONE',  ( -1.000000000000000000, 0.000000000000000000, 0.000000000000000000 ) ) ;
#190327=CARTESIAN_POINT ( 'NONE',  ( 18.59999999999999076, 28.86532135423329493, -237.9457867389574517 ) ) ;
#190348=PRODUCT_DEFINITION ( 'UNKNOWN', '', #211277, #235731 ) ;
#190355=ORIENTED_EDGE ( 'NONE', *, *, #31537, .F. ) ;
#190358=ORIENTED_EDGE ( 'NONE', *, *, #50486, .F. ) ;
#190371=ORIENTED_EDGE ( 'NONE', *, *, #47248, .T. ) ;
#190379=CIRCLE ( 'NONE', #52781, 0.1999999999999905742 ) ;
#190392=DIRECTION ( 'NONE',  ( 1.000000000000000000, 0.000000000000000000, 0.000000000000000000 ) ) ;
#190430=CYLINDRICAL_SURFACE ( 'NONE', #166561, 0.09999999999999939493 ) ;
#190439=DIRECTION ( 'NONE',  ( -1.000000000000000000, -0.000000000000000000, -0.000000000000000000 ) ) ;
#190459=CARTESIAN_POINT ( 'NONE',  ( 23.14999999999999503, 31.44980407958351876, -233.5445995079518582 ) ) ;
#190461=EDGE_CURVE ( 'NONE', #182938, #240363, #232343, .T. ) ;
#190462=FACE_OUTER_BOUND ( 'NONE', #32955, .T. ) ;
#190464=DIRECTION ( 'NONE',  ( -3.265361837132814079E-16, 0.4721928772777359007, 0.8814952561688425003 ) ) ;
#190487=DIRECTION ( 'NONE',  ( -1.000000000000000000, 0.000000000000000000, 0.000000000000000000 ) ) ;
#190517=DIRECTION ( 'NONE',  ( 0.000000000000000000, -0.8814952561688437216, 0.4721928772777334582 ) ) ;
#190518=CARTESIAN_POINT ( 'NONE',  ( -21.05000000000000071, 14.09264586382695938, -237.4630250429333671 ) ) ;
#190521=ORIENTED_EDGE ( 'NONE', *, *, #15294, .T. ) ;
#190525=CARTESIAN_POINT ( 'NONE',  ( 22.47071067811865319, 10.68684811775432664, -226.8807012965928323 ) ) ;
#190558=EDGE_CURVE ( 'NONE', #254810, #22846, #215729, .T. ) ;
#190569=EDGE_CURVE ( 'NONE', #193742, #203294, #165710, .T. ) ;
#190586=CIRCLE ( 'NONE', #19894, 0.1000000000000042383 ) ;
#190611=FACE_OUTER_BOUND ( 'NONE', #172908, .T. ) ;
#190622=ORIENTED_EDGE ( 'NONE', *, *, #230156, .T. ) ;
#190624=CARTESIAN_POINT ( 'NONE',  ( 20.54374330479345545, 18.89937786101421580, -228.1205973389425594 ) ) ;
#190638=ORIENTED_EDGE ( 'NONE', *, *, #54050, .T. ) ;
#190689=AXIS2_PLACEMENT_3D ( 'NONE', #25316, #66985, #27899 ) ;
#190723=ORIENTED_EDGE ( 'NONE', *, *, #35554, .F. ) ;
#190735=CARTESIAN_POINT ( 'NONE',  ( 18.58685178364169488, 8.967183825920946205, -245.3887925020941907 ) ) ;
#190748=CYLINDRICAL_SURFACE ( 'NONE', #148647, 0.1000000000000013933 ) ;
#190761=EDGE_CURVE ( 'NONE', #50959, #81287, #244972, .T. ) ;
#190766=ORIENTED_EDGE ( 'NONE', *, *, #25672, .F. ) ;
#190767=EDGE_CURVE ( 'NONE', #89629, #31578, #244765, .T. ) ;
#190826=CARTESIAN_POINT ( 'NONE',  ( -20.64999999999999858, 23.49882452903949925, -253.1653563615082305 ) ) ;
#190897=AXIS2_PLACEMENT_3D ( 'NONE', #207326, #108213, #187762 ) ;
#190914=CARTESIAN_POINT ( 'NONE',  ( -20.54999999999999716, 36.65892442174935439, -249.5511627012433848 ) ) ;
#190943=EDGE_LOOP ( 'NONE', ( #58096, #231435, #32900, #254200 ) ) ;
#190957=CARTESIAN_POINT ( 'NONE',  ( -18.39999999999999858, 37.99112772578902764, -261.0419300540664835 ) ) ;
#190988=AXIS2_PLACEMENT_3D ( 'NONE', #161722, #164278, #122587 ) ;
#190999=AXIS2_PLACEMENT_3D ( 'NONE', #65384, #144903, #224451 ) ;
#191000=FACE_OUTER_BOUND ( 'NONE', #98088, .T. ) ;
#191016=AXIS2_PLACEMENT_3D ( 'NONE', #204108, #85413, #2047 ) ;
#191020=( NAMED_UNIT ( * ) PLANE_ANGLE_UNIT ( ) SI_UNIT ( $, .RADIAN. ) );
#191021=DIRECTION ( 'NONE',  ( 0.000000000000000000, -0.9371753822965326330, 0.3488585713686107592 ) ) ;
#191032=EDGE_CURVE ( 'NONE', #257480, #142373, #236759, .T. ) ;
#191043=DIRECTION ( 'NONE',  ( 0.000000000000000000, 0.3488585713686311318, 0.9371753822965249725 ) ) ;
#191049=AXIS2_PLACEMENT_3D ( 'NONE', #245011, #3839, #225428 ) ;
#191051=CARTESIAN_POINT ( 'NONE',  ( 21.05000000000000071, 1.371218861927975929, -230.7619483865794621 ) ) ;
#191074=DIRECTION ( 'NONE',  ( 0.000000000000000000, -0.8774096236503307056, 0.4797419643160112934 ) ) ;
#191099=DIRECTION ( 'NONE',  ( 0.000000000000000000, -0.8814952561688438326, 0.4721928772777334582 ) ) ;
#191105=CARTESIAN_POINT ( 'NONE',  ( -18.59999999999999787, 16.53615870702968138, -240.8540256063542984 ) ) ;
#191142=DIRECTION ( 'NONE',  ( -1.000000000000000000, 0.000000000000000000, 0.000000000000000000 ) ) ;
#191159=CARTESIAN_POINT ( 'NONE',  ( 21.05281448260627641, 22.00373637783006586, -231.7449573266841583 ) ) ;
#191168=AXIS2_PLACEMENT_3D ( 'NONE', #153132, #113951, #232648 ) ;
#191229=AXIS2_PLACEMENT_3D ( 'NONE', #71601, #91139, #212389 ) ;
#191264=EDGE_CURVE ( 'NONE', #75744, #234336, #61999, .T. ) ;
#191265=FACE_OUTER_BOUND ( 'NONE', #148973, .T. ) ;
#191304=ORIENTED_EDGE ( 'NONE', *, *, #86413, .T. ) ;
#191343=CYLINDRICAL_SURFACE ( 'NONE', #24070, 0.09999999999999939493 ) ;
#191361=CARTESIAN_POINT ( 'NONE',  ( 21.05000000000000071, 38.42191493408704872, -250.4955484557988541 ) ) ;
#191390=DIRECTION ( 'NONE',  ( 0.000000000000000000, 0.8814952561688476074, -0.4721928772777262417 ) ) ;
#191396=CARTESIAN_POINT ( 'NONE',  ( -22.00356870141395049, 10.55423491370564726, -227.3381210828049177 ) ) ;
#191436=AXIS2_PLACEMENT_3D ( 'NONE', #10801, #229844, #51173 ) ;
#191441=EDGE_CURVE ( 'NONE', #207618, #200406, #211847, .T. ) ;
#191443=CARTESIAN_POINT ( 'NONE',  ( -18.59999999999999787, -4.963776450181787148, -229.1688993039521449 ) ) ;
#191470=CIRCLE ( 'NONE', #229037, 0.1000000000000035444 ) ;
#191486=EDGE_CURVE ( 'NONE', #237528, #35657, #16399, .T. ) ;
#191490=CARTESIAN_POINT ( 'NONE',  ( 20.95575313997065336, 18.85908140503239494, -227.9747421143725887 ) ) ;
#191494=DIRECTION ( 'NONE',  ( 0.000000000000000000, 0.9994937237965569876, 0.03181660087583042945 ) ) ;
#191508=CARTESIAN_POINT ( 'NONE',  ( 23.24999999999999645, 36.65892442174935439, -249.5511627012433848 ) ) ;
#191531=ORIENTED_EDGE ( 'NONE', *, *, #241636, .T. ) ;
#191609=DIRECTION ( 'NONE',  ( 0.000000000000000000, -0.8814952561688430555, 0.4721928772777348460 ) ) ;
#191651=CIRCLE ( 'NONE', #241680, 11.80000000000000604 ) ;
#191654=ORIENTED_EDGE ( 'NONE', *, *, #58668, .T. ) ;
#191675=AXIS2_PLACEMENT_3D ( 'NONE', #77280, #76009, #198520 ) ;
#191683=VERTEX_POINT ( 'NONE', #83204 ) ;
#191699=DIRECTION ( 'NONE',  ( 0.000000000000000000, 0.8814952561688438326, -0.4721928772777334582 ) ) ;
#191711=CARTESIAN_POINT ( 'NONE',  ( 18.59999999999996945, 46.46967969402478360, -243.0849751855955674 ) ) ;
#191713=ORIENTED_EDGE ( 'NONE', *, *, #242373, .T. ) ;
#191732=DIRECTION ( 'NONE',  ( 1.000000000000000000, 0.000000000000000000, 0.000000000000000000 ) ) ;
#191747=ADVANCED_FACE ( 'NONE', ( #147047 ), #241268, .F. ) ;
#191796=ORIENTED_EDGE ( 'NONE', *, *, #6477, .F. ) ;
#191805=CARTESIAN_POINT ( 'NONE',  ( -22.47071067811865319, 0.3704148268516976872, -229.9999874772930752 ) ) ;
#191806=DIRECTION ( 'NONE',  ( 0.000000000000000000, 0.4721928772777346239, 0.8814952561688430555 ) ) ;
#191818=CARTESIAN_POINT ( 'NONE',  ( -21.45000000000000284, 29.41239393758413811, -236.9245051605820720 ) ) ;
#191862=AXIS2_PLACEMENT_3D ( 'NONE', #132407, #69884, #231516 ) ;
#191873=CARTESIAN_POINT ( 'NONE',  ( -20.00857864376270001, 22.43030315632513094, -231.3223027016406093 ) ) ;
#191874=ORIENTED_EDGE ( 'NONE', *, *, #161570, .T. ) ;
#191877=CARTESIAN_POINT ( 'NONE',  ( 18.59999999999999076, 18.24178995542692050, -237.7003448530951459 ) ) ;
#191890=EDGE_CURVE ( 'NONE', #52358, #75284, #141457, .T. ) ;
#191896=ORIENTED_EDGE ( 'NONE', *, *, #190767, .T. ) ;
#191899=EDGE_CURVE ( 'NONE', #34148, #248047, #49880, .T. ) ;
#191905=AXIS2_PLACEMENT_3D ( 'NONE', #207754, #249443, #169942 ) ;
#191918=CARTESIAN_POINT ( 'NONE',  ( 20.97217846901852312, 18.81354558019653211, -229.9232606961761860 ) ) ;
#191963=ORIENTED_EDGE ( 'NONE', *, *, #131381, .T. ) ;
#191977=DIRECTION ( 'NONE',  ( 0.000000000000000000, 0.8454177738465993297, 0.5341055959866553016 ) ) ;
#191988=CARTESIAN_POINT ( 'NONE',  ( 18.50000000000000355, 38.30077178631847801, -261.1858881914067183 ) ) ;
#192040=DIRECTION ( 'NONE',  ( 1.000000000000000000, 0.000000000000000000, 0.000000000000000000 ) ) ;
#192052=CARTESIAN_POINT ( 'NONE',  ( -20.85000000000000142, 43.08613539620618837, -254.3146655184800409 ) ) ;
#192053=CARTESIAN_POINT ( 'NONE',  ( -23.25000000000000000, 36.65892442174935439, -249.5511627012433848 ) ) ;
#192111=EDGE_CURVE ( 'NONE', #70952, #4561, #108165, .T. ) ;
#192162=EDGE_CURVE ( 'NONE', #67785, #110689, #112095, .T. ) ;
#192166=ADVANCED_FACE ( 'NONE', ( #74945 ), #133597, .T. ) ;
#192243=VERTEX_POINT ( 'NONE', #138697 ) ;
#192281=ADVANCED_FACE ( 'NONE', ( #183020 ), #60470, .F. ) ;
#192306=ADVANCED_FACE ( 'NONE', ( #222098 ), #43502, .F. ) ;
#192307=LINE ( 'NONE', #170224, #61645 ) ;
#192385=CARTESIAN_POINT ( 'NONE',  ( 23.14999999999999503, 2.319530388122574394, -217.8268657444419887 ) ) ;
#192391=DIRECTION ( 'NONE',  ( 0.000000000000000000, 0.4721928772777346794, 0.8814952561688431665 ) ) ;
#192404=FACE_OUTER_BOUND ( 'NONE', #102878, .T. ) ;
#192418=ORIENTED_EDGE ( 'NONE', *, *, #10400, .T. ) ;
#192421=DIRECTION ( 'NONE',  ( -1.000000000000000000, -0.000000000000000000, -0.000000000000000000 ) ) ;
#192441=EDGE_CURVE ( 'NONE', #24478, #21030, #227259, .T. ) ;
#192505=CARTESIAN_POINT ( 'NONE',  ( 18.47073956224749480, 8.922622944725832284, -245.4386566365344322 ) ) ;
#192513=EDGE_CURVE ( 'NONE', #176327, #210749, #140689, .T. ) ;
#192532=VERTEX_POINT ( 'NONE', #100252 ) ;
#192549=DIRECTION ( 'NONE',  ( 0.000000000000000000, 0.8814952561688476074, -0.4721928772777262417 ) ) ;
#192557=CARTESIAN_POINT ( 'NONE',  ( -22.39999999999999858, -3.275978944802464987, -228.2735455795363748 ) ) ;
#192559=CARTESIAN_POINT ( 'NONE',  ( 21.05000000000000071, 1.658775325997237315, -230.6916041481598540 ) ) ;
#192560=EDGE_LOOP ( 'NONE', ( #18731, #245396, #122712, #196873, #116278 ) ) ;
#192579=FACE_OUTER_BOUND ( 'NONE', #172762, .T. ) ;
#192598=CARTESIAN_POINT ( 'NONE',  ( -22.39999999999999858, 7.176052627820866725, -233.6445517868224044 ) ) ;
#192610=DIRECTION ( 'NONE',  ( 1.000000000000000000, 0.000000000000000000, 0.000000000000000000 ) ) ;
#192612=AXIS2_PLACEMENT_3D ( 'NONE', #1519, #101888, #160639 ) ;
#192626=ORIENTED_EDGE ( 'NONE', *, *, #188648, .F. ) ;
#192631=CARTESIAN_POINT ( 'NONE',  ( -21.05000000000000071, 30.48950451747912993, -239.6099224343151946 ) ) ;
#192656=CARTESIAN_POINT ( 'NONE',  ( 22.44352723754029810, -3.135960183319440375, -228.2236081556235376 ) ) ;
#192668=LINE ( 'NONE', #248791, #250173 ) ;
#192672=FACE_OUTER_BOUND ( 'NONE', #957, .T. ) ;
#192681=ORIENTED_EDGE ( 'NONE', *, *, #223574, .T. ) ;
#192706=CIRCLE ( 'NONE', #146873, 0.1000000000000075273 ) ;
#192733=EDGE_CURVE ( 'NONE', #117242, #230514, #192668, .T. ) ;
#192761=DIRECTION ( 'NONE',  ( -1.000000000000000000, -1.394253735153569469E-16, -2.602809386958778209E-16 ) ) ;
#192791=ORIENTED_EDGE ( 'NONE', *, *, #129870, .F. ) ;
#192801=FACE_OUTER_BOUND ( 'NONE', #149055, .T. ) ;
#192812=ORIENTED_EDGE ( 'NONE', *, *, #100972, .F. ) ;
#192847=CARTESIAN_POINT ( 'NONE',  ( -22.47886152344871036, -3.122868706952835360, -228.1986027551170935 ) ) ;
#192867=ORIENTED_EDGE ( 'NONE', *, *, #163052, .F. ) ;
#192915=LINE ( 'NONE', #74278, #159299 ) ;
#192949=EDGE_CURVE ( 'NONE', #143721, #48376, #122111, .T. ) ;
#192959=AXIS2_PLACEMENT_3D ( 'NONE', #228803, #172719, #115262 ) ;
#192968=ORIENTED_EDGE ( 'NONE', *, *, #235707, .F. ) ;
#192983=ORIENTED_EDGE ( 'NONE', *, *, #191486, .T. ) ;
#193003=CIRCLE ( 'NONE', #34794, 0.09999999999999939493 ) ;
#193029=ADVANCED_FACE ( 'NONE', ( #25583 ), #242043, .T. ) ;
#193061=EDGE_LOOP ( 'NONE', ( #113667, #135700, #218116, #110776 ) ) ;
#193137=ORIENTED_EDGE ( 'NONE', *, *, #53108, .T. ) ;
#193159=DIRECTION ( 'NONE',  ( 1.000000000000000000, -0.000000000000000000, -0.000000000000000000 ) ) ;
#193183=AXIS2_PLACEMENT_3D ( 'NONE', #94731, #174329, #75199 ) ;
#193190=ORIENTED_EDGE ( 'NONE', *, *, #189275, .F. ) ;
#193231=DIRECTION ( 'NONE',  ( -1.000000000000000000, -3.448943450116723568E-16, -6.438528483529607644E-16 ) ) ;
#193248=CARTESIAN_POINT ( 'NONE',  ( 18.49999999999999289, 33.98796489282362643, -236.2185561567993091 ) ) ;
#193256=AXIS2_PLACEMENT_3D ( 'NONE', #22200, #162996, #5151 ) ;
#193266=FACE_OUTER_BOUND ( 'NONE', #12303, .T. ) ;
#193267=CARTESIAN_POINT ( 'NONE',  ( -20.94999999999999929, 42.90983634497242605, -254.2202269430244996 ) ) ;
#193270=ORIENTED_EDGE ( 'NONE', *, *, #198602, .F. ) ;
#193299=DIRECTION ( 'NONE',  ( -0.000000000000000000, 0.8454177738465993297, 0.5341055959866553016 ) ) ;
#193302=EDGE_CURVE ( 'NONE', #227126, #33556, #137514, .T. ) ;
#193311=CARTESIAN_POINT ( 'NONE',  ( 21.07928932188134397, 7.128833340093095217, -233.7327013124392749 ) ) ;
#193375=FACE_OUTER_BOUND ( 'NONE', #153138, .T. ) ;
#193403=VECTOR ( 'NONE', #151011, 1000.000000000000114 ) ;
#193406=ADVANCED_FACE ( 'NONE', ( #104762 ), #86486, .T. ) ;
#193416=ORIENTED_EDGE ( 'NONE', *, *, #93580, .F. ) ;
#193420=CARTESIAN_POINT ( 'NONE',  ( -21.05000000000000071, 14.72981487416292623, -236.4853282537515895 ) ) ;
#193435=CIRCLE ( 'NONE', #110189, 0.09999999999999939493 ) ;
#193467=DIRECTION ( 'NONE',  ( 0.000000000000000000, -0.4721928772777346794, -0.8814952561688431665 ) ) ;
#193471=DIRECTION ( 'NONE',  ( -0.000000000000000000, -0.8814952561688430555, 0.4721928772777346239 ) ) ;
#193504=DIRECTION ( 'NONE',  ( 0.7070776581709138364, -0.3339045366652431679, -0.6233369439636203824 ) ) ;
#193540=AXIS2_PLACEMENT_3D ( 'NONE', #18757, #215660, #177859 ) ;
#193542=ORIENTED_EDGE ( 'NONE', *, *, #726, .F. ) ;
#193552=CARTESIAN_POINT ( 'NONE',  ( -22.49533356619859603, 12.57247511773151061, -223.4325311539369352 ) ) ;
#193580=CARTESIAN_POINT ( 'NONE',  ( -21.10257677756357353, 10.12810965763892668, -228.0807765930105973 ) ) ;
#193591=CARTESIAN_POINT ( 'NONE',  ( 18.44364597020194196, 8.869066854935326205, -245.4312477487408728 ) ) ;
#193607=CARTESIAN_POINT ( 'NONE',  ( 20.94999999999999929, 16.44800918141279666, -240.8068063186265135 ) ) ;
#193610=EDGE_CURVE ( 'NONE', #160790, #53948, #150038, .T. ) ;
#193629=DIRECTION ( 'NONE',  ( 0.000000000000000000, -0.8814952561688423893, 0.4721928772777357897 ) ) ;
#193648=CIRCLE ( 'NONE', #6182, 6.258578643762700011 ) ;
#193674=ORIENTED_EDGE ( 'NONE', *, *, #104245, .T. ) ;
#193690=CARTESIAN_POINT ( 'NONE',  ( -23.25000000000000000, 2.319530388122572617, -217.8268657444419887 ) ) ;
#193726=EDGE_CURVE ( 'NONE', #188486, #44729, #40708, .T. ) ;
#193742=VERTEX_POINT ( 'NONE', #221840 ) ;
#193766=CARTESIAN_POINT ( 'NONE',  ( -18.50000000000000000, 2.319530388122570841, -217.8268657444419887 ) ) ;
#193769=ORIENTED_EDGE ( 'NONE', *, *, #167054, .T. ) ;
#193807=ORIENTED_EDGE ( 'NONE', *, *, #162146, .T. ) ;
#193832=CARTESIAN_POINT ( 'NONE',  ( -18.58693740092109081, 8.967674985626857165, -245.3887142130325287 ) ) ;
#193855=CIRCLE ( 'NONE', #97968, 0.3999999999999994671 ) ;
#193873=VERTEX_POINT ( 'NONE', #10538 ) ;
#193874=CARTESIAN_POINT ( 'NONE',  ( 20.94999999999999929, 36.65892442174935439, -249.5511627012433848 ) ) ;
#193926=CARTESIAN_POINT ( 'NONE',  ( 21.05000000000000071, 23.68770167995059239, -252.8127582590406348 ) ) ;
#193948=DIRECTION ( 'NONE',  ( -0.000000000000000000, 0.4721928772777347350, 0.8814952561688429444 ) ) ;
#193983=ORIENTED_EDGE ( 'NONE', *, *, #27153, .T. ) ;
#194005=ORIENTED_EDGE ( 'NONE', *, *, #197065, .T. ) ;
#194006=ORIENTED_EDGE ( 'NONE', *, *, #158180, .T. ) ;
#194012=DIRECTION ( 'NONE',  ( 1.441126678808780685E-14, 0.3280696808754172689, 0.9446535261620007118 ) ) ;
#194089=ORIENTED_EDGE ( 'NONE', *, *, #213544, .F. ) ;
#194093=CARTESIAN_POINT ( 'NONE',  ( 20.94999999999999929, 28.08470566095357057, -239.2860081655328770 ) ) ;
#194113=ADVANCED_FACE ( 'NONE', ( #230881 ), #4607, .F. ) ;
#194119=ADVANCED_FACE ( 'NONE', ( #102877 ), #42072, .T. ) ;
#194123=AXIS2_PLACEMENT_3D ( 'NONE', #238841, #201002, #58890 ) ;
#194150=TOROIDAL_SURFACE ( 'NONE', #235809, 12.97499999999999609, 0.1000000000000000056 ) ;
#194154=FACE_OUTER_BOUND ( 'NONE', #239359, .T. ) ;
#194180=CARTESIAN_POINT ( 'NONE',  ( 20.89878130938411616, 46.45193731540633308, -243.0811559066744110 ) ) ;
#194219=DIRECTION ( 'NONE',  ( 1.000000000000000000, 0.000000000000000000, 0.000000000000000000 ) ) ;
#194236=DIRECTION ( 'NONE',  ( 0.000000000000000000, -0.8814952561688437216, 0.4721928772777334582 ) ) ;
#194242=ORIENTED_EDGE ( 'NONE', *, *, #58381, .F. ) ;
#194260=EDGE_CURVE ( 'NONE', #122934, #97226, #230227, .T. ) ;
#194264=ORIENTED_EDGE ( 'NONE', *, *, #116414, .F. ) ;
#194275=CIRCLE ( 'NONE', #98332, 0.1999999999999905742 ) ;
#194286=CYLINDRICAL_SURFACE ( 'NONE', #97883, 0.1000000000000013933 ) ;
#194296=DIRECTION ( 'NONE',  ( 0.000000000000000000, 0.8814952561688438326, -0.4721928772777332362 ) ) ;
#194300=EDGE_CURVE ( 'NONE', #105344, #173747, #250509, .T. ) ;
#194301=CARTESIAN_POINT ( 'NONE',  ( -23.15000000000000213, 38.51006445970392633, -250.5427677435266389 ) ) ;
#194314=CIRCLE ( 'NONE', #2732, 0.1000000000000001027 ) ;
#194332=ORIENTED_EDGE ( 'NONE', *, *, #196716, .T. ) ;
#194345=ORIENTED_EDGE ( 'NONE', *, *, #165608, .T. ) ;
#194394=ORIENTED_EDGE ( 'NONE', *, *, #141500, .F. ) ;
#194423=DIRECTION ( 'NONE',  ( 0.000000000000000000, -0.8814952561688444987, 0.4721928772777320149 ) ) ;
#194447=ORIENTED_EDGE ( 'NONE', *, *, #48335, .F. ) ;
#194469=DIRECTION ( 'NONE',  ( 0.000000000000000000, -0.8814952561688430555, 0.4721928772777346239 ) ) ;
#194478=ORIENTED_EDGE ( 'NONE', *, *, #121730, .T. ) ;
#194489=VERTEX_POINT ( 'NONE', #253622 ) ;
#194512=VERTEX_POINT ( 'NONE', #189382 ) ;
#194525=EDGE_LOOP ( 'NONE', ( #105181, #96207, #94714, #67758 ) ) ;
#194531=VERTEX_POINT ( 'NONE', #232375 ) ;
#194571=DIRECTION ( 'NONE',  ( 0.000000000000000000, 0.8096735173027155286, -0.5868805631290315850 ) ) ;
#194578=ORIENTED_EDGE ( 'NONE', *, *, #59382, .F. ) ;
#194602=DIRECTION ( 'NONE',  ( 0.000000000000000000, 0.8814952561688437216, -0.4721928772777331806 ) ) ;
#194627=EDGE_CURVE ( 'NONE', #257602, #50106, #217356, .T. ) ;
#194636=CARTESIAN_POINT ( 'NONE',  ( -23.15000000000000213, 36.65892442174935439, -249.5511627012433848 ) ) ;
#194663=EDGE_CURVE ( 'NONE', #213275, #87394, #88162, .T. ) ;
#194669=AXIS2_PLACEMENT_3D ( 'NONE', #141990, #41642, #199431 ) ;
#194673=DIRECTION ( 'NONE',  ( 0.000000000000000000, 0.8814952561688428334, -0.4721928772777349570 ) ) ;
#194704=DIRECTION ( 'NONE',  ( -1.000000000000000000, 0.000000000000000000, 0.000000000000000000 ) ) ;
#194710=ORIENTED_EDGE ( 'NONE', *, *, #144151, .F. ) ;
#194722=ORIENTED_EDGE ( 'NONE', *, *, #145789, .F. ) ;
#194729=CIRCLE ( 'NONE', #140505, 0.09999999999999986677 ) ;
#194740=VECTOR ( 'NONE', #85890, 1000.000000000000114 ) ;
#194767=EDGE_CURVE ( 'NONE', #70426, #63775, #13385, .T. ) ;
#194786=FACE_OUTER_BOUND ( 'NONE', #211897, .T. ) ;
#194803=AXIS2_PLACEMENT_3D ( 'NONE', #128456, #191021, #50181 ) ;
#194807=DIRECTION ( 'NONE',  ( 0.000000000000000000, 0.8814952561688436106, -0.4721928772777336247 ) ) ;
#194819=CARTESIAN_POINT ( 'NONE',  ( -18.46154800491024517, 38.05094987613883717, -261.0515204261999997 ) ) ;
#194838=ORIENTED_EDGE ( 'NONE', *, *, #83795, .T. ) ;
#194839=EDGE_CURVE ( 'NONE', #193873, #245180, #120885, .T. ) ;
#194840=AXIS2_PLACEMENT_3D ( 'NONE', #96117, #135246, #41326 ) ;
#194860=DIRECTION ( 'NONE',  ( 2.952720810173289605E-16, -0.4721928772777352346, -0.8814952561688427224 ) ) ;
#194870=AXIS2_PLACEMENT_3D ( 'NONE', #188790, #67562, #209643 ) ;
#194911=CARTESIAN_POINT ( 'NONE',  ( 23.24999999999999289, 2.319530388122574394, -217.8268657444419887 ) ) ;
#194921=FACE_OUTER_BOUND ( 'NONE', #52689, .T. ) ;
#194935=CARTESIAN_POINT ( 'NONE',  ( -23.25000000000000000, -8.777002227904194598, -238.5420042644097975 ) ) ;
#194943=FACE_OUTER_BOUND ( 'NONE', #237947, .T. ) ;
#194972=EDGE_CURVE ( 'NONE', #123343, #56714, #216658, .T. ) ;
#195017=AXIS2_PLACEMENT_3D ( 'NONE', #141071, #241455, #221854 ) ;
#195034=DIRECTION ( 'NONE',  ( 0.000000000000000000, 0.8814952561688430555, -0.4721928772777346239 ) ) ;
#195086=AXIS2_PLACEMENT_3D ( 'NONE', #10767, #90278, #169889 ) ;
#195111=CARTESIAN_POINT ( 'NONE',  ( 23.14999999999999858, 36.65892442174935439, -249.5511627012433848 ) ) ;
#195150=CARTESIAN_POINT ( 'NONE',  ( 23.14999999999999503, 23.34004772283015683, -229.2004250369967338 ) ) ;
#195166=LINE ( 'NONE', #131303, #140392 ) ;
#195168=EDGE_CURVE ( 'NONE', #170534, #13871, #196702, .T. ) ;
#195177=DIRECTION ( 'NONE',  ( -1.000000000000000000, 0.000000000000000000, 0.000000000000000000 ) ) ;
#195181=ADVANCED_FACE ( 'NONE', ( #93273 ), #146807, .T. ) ;
#195238=CARTESIAN_POINT ( 'NONE',  ( -20.54999999999999716, 20.06933876993645782, -235.7297789824848451 ) ) ;
#195254=COLOUR_RGB ( '', 0.31764706, 0.68627451, 0.89019608) ;
#195267=DIRECTION ( 'NONE',  ( 1.000000000000000000, 0.000000000000000000, 0.000000000000000000 ) ) ;
#195274=AXIS2_PLACEMENT_3D ( 'NONE', #205498, #127260, #107686 ) ;
#195289=ORIENTED_EDGE ( 'NONE', *, *, #208238, .F. ) ;
#195294=TOROIDAL_SURFACE ( 'NONE', #248872, 4.149999999999999467, 0.1000000000000000056 ) ;
#195343=CARTESIAN_POINT ( 'NONE',  ( -18.50000000000000000, 43.08613539620618837, -254.3146655184800409 ) ) ;
#195359=FACE_OUTER_BOUND ( 'NONE', #35733, .T. ) ;
#195378=DIRECTION ( 'NONE',  ( 1.000000000000000000, 0.000000000000000000, 0.000000000000000000 ) ) ;
#195383=DIRECTION ( 'NONE',  ( 0.000000000000000000, 0.8814952561688476074, -0.4721928772777262417 ) ) ;
#195393=VERTEX_POINT ( 'NONE', #243057 ) ;
#195417=CYLINDRICAL_SURFACE ( 'NONE', #92122, 0.09999999999999986677 ) ;
#195421=ORIENTED_EDGE ( 'NONE', *, *, #6324, .T. ) ;
#195429=EDGE_LOOP ( 'NONE', ( #103042, #47537, #3835, #229542 ) ) ;
#195442=DIRECTION ( 'NONE',  ( 1.000000000000000000, 0.000000000000000000, 0.000000000000000000 ) ) ;
#195450=CIRCLE ( 'NONE', #116338, 0.09999999999999939493 ) ;
#195463=AXIS2_PLACEMENT_3D ( 'NONE', #41941, #22377, #163165 ) ;
#195479=VERTEX_POINT ( 'NONE', #120571 ) ;
#195486=CARTESIAN_POINT ( 'NONE',  ( 20.95000000000000284, 36.02918351690956200, -236.0543695120161090 ) ) ;
#195502=DIRECTION ( 'NONE',  ( 0.000000000000000000, 0.8814952561688476074, -0.4721928772777262417 ) ) ;
#195507=DIRECTION ( 'NONE',  ( 0.000000000000000000, -0.4721928772777346239, -0.8814952561688430555 ) ) ;
#195560=AXIS2_PLACEMENT_3D ( 'NONE', #154959, #117093, #17974 ) ;
#195581=CIRCLE ( 'NONE', #33271, 0.1000000000000013933 ) ;
#195613=VERTEX_POINT ( 'NONE', #115114 ) ;
#195622=AXIS2_PLACEMENT_3D ( 'NONE', #255246, #200469, #41413 ) ;
#195637=CARTESIAN_POINT ( 'NONE',  ( -20.05000000000000426, 30.22839164850006455, -235.6129688350293350 ) ) ;
#195687=ORIENTED_EDGE ( 'NONE', *, *, #230843, .F. ) ;
#195766=CARTESIAN_POINT ( 'NONE',  ( 20.77526135991734080, 18.81146737447475203, -229.8579754828443811 ) ) ;
#195851=ORIENTED_EDGE ( 'NONE', *, *, #75402, .F. ) ;
#195967=VERTEX_POINT ( 'NONE', #88796 ) ;
#196008=ADVANCED_FACE ( 'NONE', ( #214854 ), #53927, .F. ) ;
#196017=VECTOR ( 'NONE', #98964, 1000.000000000000000 ) ;
#196027=CARTESIAN_POINT ( 'NONE',  ( 21.05000000000000071, 28.60154115857409352, -258.4512230915049713 ) ) ;
#196081=CARTESIAN_POINT ( 'NONE',  ( -18.52309608778585570, 38.02470060592907686, -261.2215444011879981 ) ) ;
#196126=VERTEX_POINT ( 'NONE', #205543 ) ;
#196141=CARTESIAN_POINT ( 'NONE',  ( -21.07928932188134041, 10.02993822722303818, -228.1074463178677263 ) ) ;
#196156=CARTESIAN_POINT ( 'NONE',  ( 21.12757541349815682, 10.18096795049375025, -228.0240099581621109 ) ) ;
#196176=AXIS2_PLACEMENT_3D ( 'NONE', #174910, #177451, #219094 ) ;
#196177=CIRCLE ( 'NONE', #254416, 0.09999999999999036049 ) ;
#196179=TOROIDAL_SURFACE ( 'NONE', #8748, 7.800000000000000711, 0.1000000000000000056 ) ;
#196227=DIRECTION ( 'NONE',  ( 0.000000000000000000, 0.8034013718071717491, -0.5954378521544919645 ) ) ;
#196235=ORIENTED_EDGE ( 'NONE', *, *, #49995, .T. ) ;
#196236=ORIENTED_EDGE ( 'NONE', *, *, #138707, .T. ) ;
#196252=DIRECTION ( 'NONE',  ( -1.000000000000000000, -0.000000000000000000, -0.000000000000000000 ) ) ;
#196255=EDGE_CURVE ( 'NONE', #67785, #20946, #193648, .T. ) ;
#196265=DIRECTION ( 'NONE',  ( 0.000000000000000000, -0.8814952561688476074, 0.4721928772777262417 ) ) ;
#196266=DIRECTION ( 'NONE',  ( -2.827886303505248766E-16, -0.03181660087583048496, 0.9994937237965570986 ) ) ;
#196277=EDGE_CURVE ( 'NONE', #256947, #42982, #202020, .T. ) ;
#196282=EDGE_CURVE ( 'NONE', #92552, #30609, #31192, .T. ) ;
#196291=EDGE_CURVE ( 'NONE', #15834, #125839, #147837, .T. ) ;
#196292=ORIENTED_EDGE ( 'NONE', *, *, #157322, .F. ) ;
#196337=EDGE_CURVE ( 'NONE', #92509, #1130, #31372, .T. ) ;
#196353=PLANE ( 'NONE',  #252111 ) ;
#196366=ORIENTED_EDGE ( 'NONE', *, *, #233858, .F. ) ;
#196391=CARTESIAN_POINT ( 'NONE',  ( 21.14999999999999858, 10.21728496540352893, -227.9671432372868765 ) ) ;
#196421=EDGE_CURVE ( 'NONE', #239691, #156870, #117825, .T. ) ;
#196423=VERTEX_POINT ( 'NONE', #60598 ) ;
#196424=CARTESIAN_POINT ( 'NONE',  ( -20.64999999999999858, 18.47808476326694915, -239.8121846073901224 ) ) ;
#196445=ORIENTED_EDGE ( 'NONE', *, *, #188319, .F. ) ;
#196449=AXIS2_PLACEMENT_3D ( 'NONE', #202962, #148132, #163846 ) ;
#196471=ORIENTED_EDGE ( 'NONE', *, *, #240121, .F. ) ;
#196494=CIRCLE ( 'NONE', #84014, 0.1999999999999997335 ) ;
#196523=ORIENTED_EDGE ( 'NONE', *, *, #202262, .F. ) ;
#196529=CARTESIAN_POINT ( 'NONE',  ( -22.48970261584618058, 12.58107241917856456, -223.4371365001174752 ) ) ;
#196570=CARTESIAN_POINT ( 'NONE',  ( -23.25000000000000000, 18.38993523765007154, -239.7649653196623376 ) ) ;
#196576=FACE_OUTER_BOUND ( 'NONE', #24770, .T. ) ;
#196584=DIRECTION ( 'NONE',  ( 0.000000000000000000, -0.5868805631290353597, -0.8096735173027127530 ) ) ;
#196601=FACE_OUTER_BOUND ( 'NONE', #127286, .T. ) ;
#196605=EDGE_CURVE ( 'NONE', #186477, #81287, #1293, .T. ) ;
#196608=CARTESIAN_POINT ( 'NONE',  ( -21.05000000000000071, 13.66123737402873495, -238.6633470470287648 ) ) ;
#196614=CARTESIAN_POINT ( 'NONE',  ( 22.47071067811864964, 0.3704148268517156728, -229.9999874772931037 ) ) ;
#196639=ORIENTED_EDGE ( 'NONE', *, *, #76212, .T. ) ;
#196647=CARTESIAN_POINT ( 'NONE',  ( 19.88284271247461632, 34.46644681994002468, -235.1135425616689076 ) ) ;
#196648=ORIENTED_EDGE ( 'NONE', *, *, #153557, .F. ) ;
#196676=AXIS2_PLACEMENT_3D ( 'NONE', #210230, #112407, #49846 ) ;
#196683=ORIENTED_EDGE ( 'NONE', *, *, #9019, .F. ) ;
#196702=CIRCLE ( 'NONE', #26044, 0.1000000000000013933 ) ;
#196711=ORIENTED_EDGE ( 'NONE', *, *, #210720, .T. ) ;
#196716=EDGE_CURVE ( 'NONE', #202898, #107904, #109628, .T. ) ;
#196724=CYLINDRICAL_SURFACE ( 'NONE', #180608, 0.1000000000000013933 ) ;
#196808=ORIENTED_EDGE ( 'NONE', *, *, #228526, .F. ) ;
#196824=CYLINDRICAL_SURFACE ( 'NONE', #58041, 0.09999999999999939493 ) ;
#196831=FACE_OUTER_BOUND ( 'NONE', #236080, .T. ) ;
#196849=VERTEX_POINT ( 'NONE', #94294 ) ;
#196873=ORIENTED_EDGE ( 'NONE', *, *, #234639, .F. ) ;
#196880=DIRECTION ( 'NONE',  ( 0.000000000000000000, -0.8814952561688444987, 0.4721928772777320149 ) ) ;
#196926=ORIENTED_EDGE ( 'NONE', *, *, #145877, .F. ) ;
#196930=DIRECTION ( 'NONE',  ( 0.000000000000000000, -0.5273008465188072647, 0.8496786552930167824 ) ) ;
#196979=DIRECTION ( 'NONE',  ( -0.7071067811865474617, -0.3338907855510734324, -0.6233112732207618523 ) ) ;
#196991=LINE ( 'NONE', #18371, #124334 ) ;
#197048=CARTESIAN_POINT ( 'NONE',  ( 23.24999999999999289, 29.08883969319483498, -237.9520757887960940 ) ) ;
#197058=EDGE_LOOP ( 'NONE', ( #156528, #190355, #141501, #41708, #64670 ) ) ;
#197065=EDGE_CURVE ( 'NONE', #234543, #97016, #13971, .T. ) ;
#197136=ORIENTED_EDGE ( 'NONE', *, *, #139807, .T. ) ;
#197137=LINE ( 'NONE', #13387, #169555 ) ;
#197156=CARTESIAN_POINT ( 'NONE',  ( -20.54999999999999716, 11.60058429089262333, -246.3380203656811887 ) ) ;
#197220=CARTESIAN_POINT ( 'NONE',  ( -20.94983749550516450, 46.34703458179515678, -243.0587802416264651 ) ) ;
#197226=AXIS2_PLACEMENT_3D ( 'NONE', #74449, #154001, #135649 ) ;
#197233=LINE ( 'NONE', #19900, #30099 ) ;
#197235=CARTESIAN_POINT ( 'NONE',  ( -20.64999999999999858, 34.89593390941166007, -248.6067769466879156 ) ) ;
#197260=VERTEX_POINT ( 'NONE', #162979 ) ;
#197265=ORIENTED_EDGE ( 'NONE', *, *, #67586, .T. ) ;
#197296=CARTESIAN_POINT ( 'NONE',  ( -20.94999999999999929, 36.65892442174935439, -249.5511627012433848 ) ) ;
#197315=FACE_OUTER_BOUND ( 'NONE', #93927, .T. ) ;
#197330=EDGE_CURVE ( 'NONE', #104319, #155390, #89149, .T. ) ;
#197346=AXIS2_PLACEMENT_3D ( 'NONE', #37683, #97595, #232354 ) ;
#197348=CARTESIAN_POINT ( 'NONE',  ( -18.37151313414626586, 38.14841574062842966, -261.2067459223885635 ) ) ;
#197388=CIRCLE ( 'NONE', #147518, 0.4999999999999902855 ) ;
#197393=EDGE_CURVE ( 'NONE', #77718, #92509, #30928, .T. ) ;
#197411=AXIS2_PLACEMENT_3D ( 'NONE', #216244, #37646, #117168 ) ;
#197416=CARTESIAN_POINT ( 'NONE',  ( -21.07946286933444568, 10.04976323809818162, -228.1174753750304660 ) ) ;
#197431=CARTESIAN_POINT ( 'NONE',  ( -20.00857864376270001, 22.33586458086958615, -231.4986017528744071 ) ) ;
#197475=EDGE_LOOP ( 'NONE', ( #117017, #93019, #48773, #169275 ) ) ;
#197482=DIRECTION ( 'NONE',  ( 0.000000000000000000, 0.8034013718071717491, -0.5954378521544919645 ) ) ;
#197493=EDGE_CURVE ( 'NONE', #159212, #155020, #22729, .T. ) ;
#197494=DIRECTION ( 'NONE',  ( 1.000000000000000000, 0.000000000000000000, 0.000000000000000000 ) ) ;
#197511=VECTOR ( 'NONE', #1314, 1000.000000000000000 ) ;
#197525=ORIENTED_EDGE ( 'NONE', *, *, #152050, .F. ) ;
#197549=AXIS2_PLACEMENT_3D ( 'NONE', #151111, #89827, #48143 ) ;
#197562=ORIENTED_EDGE ( 'NONE', *, *, #142319, .F. ) ;
#197564=ADVANCED_FACE ( 'NONE', ( #213630 ), #94961, .F. ) ;
#197581=AXIS2_PLACEMENT_3D ( 'NONE', #123144, #64452, #24057 ) ;
#197583=DIRECTION ( 'NONE',  ( 1.000000000000000000, 1.541880601228652843E-16, 2.878400969107353907E-16 ) ) ;
#197604=AXIS2_PLACEMENT_3D ( 'NONE', #189699, #128442, #249678 ) ;
#197611=DIRECTION ( 'NONE',  ( 0.000000000000000000, -0.3343365196859449662, 0.9424537609900497381 ) ) ;
#197616=CIRCLE ( 'NONE', #118548, 4.299999999999952749 ) ;
#197628=ORIENTED_EDGE ( 'NONE', *, *, #189275, .T. ) ;
#197653=DIRECTION ( 'NONE',  ( -5.603264701231742896E-32, 0.8814952561688431665, -0.4721928772777344574 ) ) ;
#197664=DIRECTION ( 'NONE',  ( 0.000000000000000000, -0.8814952561688423893, 0.4721928772777359007 ) ) ;
#197666=ORIENTED_EDGE ( 'NONE', *, *, #81576, .T. ) ;
#197673=CARTESIAN_POINT ( 'NONE',  ( 21.05000000000000071, 10.30543449102041187, -228.0143625250146329 ) ) ;
#197675=ORIENTED_EDGE ( 'NONE', *, *, #232309, .T. ) ;
#197721=CARTESIAN_POINT ( 'NONE',  ( -23.25000000000000000, 43.27008861172207332, -245.2265230569236110 ) ) ;
#197729=ORIENTED_EDGE ( 'NONE', *, *, #15256, .F. ) ;
#197746=CARTESIAN_POINT ( 'NONE',  ( -20.94999999999999574, 36.09166453643263850, -236.0643439437599511 ) ) ;
#197825=ORIENTED_EDGE ( 'NONE', *, *, #39648, .T. ) ;
#197853=CARTESIAN_POINT ( 'NONE',  ( 20.94999999999999929, 18.75483929237739389, -228.0790484105328630 ) ) ;
#197871=ADVANCED_FACE ( 'NONE', ( #119052 ), #201963, .T. ) ;
#197894=LINE ( 'NONE', #38845, #76105 ) ;
#197895=FACE_OUTER_BOUND ( 'NONE', #76285, .T. ) ;
#197922=( BOUNDED_SURFACE ( )  B_SPLINE_SURFACE ( 3, 2, ( 
 ( #76431, #95987, #257582 ),
 ( #77705, #157289, #236785 ),
 ( #154725, #119434, #178133 ),
 ( #115563, #78974, #724 ),
 ( #16490, #175564, #215933 ),
 ( #60710, #140244, #193832 ),
 ( #37335, #19032, #158574 ),
 ( #238073, #75186, #255011 ) ),
 .UNSPECIFIED., .F., .F., .F. ) 
 B_SPLINE_SURFACE_WITH_KNOTS ( ( 4, 2, 2, 4 ),
 ( 3, 3 ),
 ( 0.0001723339234021435316, 0.0002782939632049939412, 0.0003842540030078444050, 0.0005961740826135453327 ),
 ( 0.000000000000000000, 1.000000000000000000 ),
 .UNSPECIFIED. ) 
 GEOMETRIC_REPRESENTATION_ITEM ( )  RATIONAL_B_SPLINE_SURFACE ( (
 ( 1.000000000000000000, 0.9504532311154613167, 1.000000000000000000),
 ( 1.000000000000000000, 0.9506023220703098131, 1.000000000000000000),
 ( 1.000000000000000000, 0.9395774818190307798, 1.000000000000000000),
 ( 1.000000000000000000, 0.9079328464638727336, 1.000000000000000000),
 ( 1.000000000000000000, 0.8875702416201843858, 1.000000000000000000),
 ( 1.000000000000000000, 0.8205919608046280400, 1.000000000000000000),
 ( 1.000000000000000000, 0.7666842783593341704, 1.000000000000000000),
 ( 1.000000000000000000, 0.7071067811864559793, 1.000000000000000000) ) ) 
 REPRESENTATION_ITEM ( '' )  SURFACE ( )  );
#197930=VECTOR ( 'NONE', #97168, 1000.000000000000000 ) ;
#197933=ADVANCED_FACE ( 'NONE', ( #367 ), #56477, .F. ) ;
#197946=CIRCLE ( 'NONE', #6413, 11.70000000000001172 ) ;
#197957=EDGE_LOOP ( 'NONE', ( #70718, #36697, #67118, #73959 ) ) ;
#197975=CARTESIAN_POINT ( 'NONE',  ( 21.05000000000000071, 22.90266353732884497, -230.0169390150674076 ) ) ;
#197987=CARTESIAN_POINT ( 'NONE',  ( -21.14999999999999858, 12.62988036037870465, -223.4632815780722694 ) ) ;
#198000=CARTESIAN_POINT ( 'NONE',  ( 21.87500000000000355, 30.37633856152204359, -235.1250019192171408 ) ) ;
#198003=VERTEX_POINT ( 'NONE', #125472 ) ;
#198021=AXIS2_PLACEMENT_3D ( 'NONE', #58139, #42450, #201523 ) ;
#198027=ADVANCED_FACE ( 'NONE', ( #103311 ), #139389, .T. ) ;
#198090=CIRCLE ( 'NONE', #114890, 0.1000000000000091649 ) ;
#198117=CARTESIAN_POINT ( 'NONE',  ( -20.64999999999999858, 19.93396995659180249, -235.7707092203739307 ) ) ;
#198123=EDGE_CURVE ( 'NONE', #188383, #204007, #85383, .T. ) ;
#198211=DIRECTION ( 'NONE',  ( 0.7071067811865474617, 0.3338907855510734324, 0.6233112732207618523 ) ) ;
#198254=ORIENTED_EDGE ( 'NONE', *, *, #126329, .F. ) ;
#198274=AXIS2_PLACEMENT_3D ( 'NONE', #101781, #82216, #83505 ) ;
#198344=ORIENTED_EDGE ( 'NONE', *, *, #211549, .F. ) ;
#198347=ORIENTED_EDGE ( 'NONE', *, *, #166492, .T. ) ;
#198351=ORIENTED_EDGE ( 'NONE', *, *, #207604, .F. ) ;
#198360=CIRCLE ( 'NONE', #185883, 0.1000000000000013933 ) ;
#198405=ORIENTED_EDGE ( 'NONE', *, *, #138827, .F. ) ;
#198415=VERTEX_POINT ( 'NONE', #122464 ) ;
#198448=DIRECTION ( 'NONE',  ( 0.000000000000000000, -0.8814952561688429444, 0.4721928772777349570 ) ) ;
#198458=CARTESIAN_POINT ( 'NONE',  ( 23.24999999999997513, 36.02367271998545561, -235.8812521208699309 ) ) ;
#198483=CARTESIAN_POINT ( 'NONE',  ( 20.04142135623730070, 34.40595771266846725, -235.0146864773515176 ) ) ;
#198520=DIRECTION ( 'NONE',  ( -1.000000000000000000, 0.000000000000000000, 0.000000000000000000 ) ) ;
#198540=CARTESIAN_POINT ( 'NONE',  ( -22.50000000000000000, 7.128833340093095217, -233.7327013124392749 ) ) ;
#198566=ADVANCED_FACE ( 'NONE', ( #208434 ), #135667, .T. ) ;
#198584=ADVANCED_FACE ( 'NONE', ( #170627 ), #8990, .F. ) ;
#198602=EDGE_CURVE ( 'NONE', #189647, #20661, #74070, .T. ) ;
#198615=ORIENTED_EDGE ( 'NONE', *, *, #38713, .T. ) ;
#198638=CARTESIAN_POINT ( 'NONE',  ( -18.40904629823862848, 37.99112787675455394, -261.0419301349346028 ) ) ;
#198671=DIRECTION ( 'NONE',  ( 1.000000000000000000, 0.000000000000000000, 0.000000000000000000 ) ) ;
#198679=TOROIDAL_SURFACE ( 'NONE', #215254, 11.65000000000000036, 0.1000000000000000056 ) ;
#198689=ORIENTED_EDGE ( 'NONE', *, *, #150667, .T. ) ;
#198724=CIRCLE ( 'NONE', #194669, 0.1000000000000013933 ) ;
#198751=DIRECTION ( 'NONE',  ( 0.000000000000000000, 0.9740678456249560746, -0.2262561206234139088 ) ) ;
#198753=CARTESIAN_POINT ( 'NONE',  ( 18.59999999999999076, 18.90448995781211750, -232.7802074516171444 ) ) ;
#198756=CARTESIAN_POINT ( 'NONE',  ( 23.14999999999999858, -8.777002227904191045, -238.5420042644097975 ) ) ;
#198823=CIRCLE ( 'NONE', #23895, 0.09999999999999441280 ) ;
#198870=EDGE_CURVE ( 'NONE', #17591, #39875, #133385, .T. ) ;
#198871=DIRECTION ( 'NONE',  ( 1.000000000000000000, 0.000000000000000000, 0.000000000000000000 ) ) ;
#198896=ORIENTED_EDGE ( 'NONE', *, *, #16202, .T. ) ;
#198947=VERTEX_POINT ( 'NONE', #23733 ) ;
#198953=CARTESIAN_POINT ( 'NONE',  ( -22.50000000000000000, 7.040683814476209612, -233.6854820247115185 ) ) ;
#198988=EDGE_CURVE ( 'NONE', #231806, #43771, #97673, .T. ) ;
#198996=EDGE_CURVE ( 'NONE', #97044, #254141, #75126, .T. ) ;
#198997=CARTESIAN_POINT ( 'NONE',  ( -23.15000000000000213, 39.47455543563931002, -237.7297955216985201 ) ) ;
#199014=SPHERICAL_SURFACE ( 'NONE', #69, 0.1000000000000000056 ) ;
#199051=AXIS2_PLACEMENT_3D ( 'NONE', #124580, #25480, #48875 ) ;
#199052=CIRCLE ( 'NONE', #11628, 0.1000000000000013933 ) ;
#199110=ADVANCED_FACE ( 'NONE', ( #90072 ), #105773, .T. ) ;
#199117=AXIS2_PLACEMENT_3D ( 'NONE', #150436, #188254, #109993 ) ;
#199132=FACE_OUTER_BOUND ( 'NONE', #224325, .T. ) ;
#199138=AXIS2_PLACEMENT_3D ( 'NONE', #174508, #97441, #257775 ) ;
#199169=DIRECTION ( 'NONE',  ( 0.000000000000000000, -0.8814952561688476074, 0.4721928772777262417 ) ) ;
#199181=AXIS2_PLACEMENT_3D ( 'NONE', #86512, #227335, #145221 ) ;
#199190=LINE ( 'NONE', #196608, #249339 ) ;
#199198=ORIENTED_EDGE ( 'NONE', *, *, #57117, .F. ) ;
#199200=CARTESIAN_POINT ( 'NONE',  ( 18.54286124688535153, 38.05691696594434603, -261.2177481181072949 ) ) ;
#199226=ORIENTED_EDGE ( 'NONE', *, *, #159601, .T. ) ;
#199233=DIRECTION ( 'NONE',  ( 0.000000000000000000, -0.4721928772776434191, -0.8814952561688919053 ) ) ;
#199260=CARTESIAN_POINT ( 'NONE',  ( -22.42253884134832020, -3.139326375914578193, -228.2301371206982026 ) ) ;
#199273=CARTESIAN_POINT ( 'NONE',  ( 20.99780126800925473, 36.04544038259444250, -236.0569647481119091 ) ) ;
#199275=CARTESIAN_POINT ( 'NONE',  ( 21.05000000000000071, 22.91252772851732189, -230.0222229922490271 ) ) ;
#199326=DIRECTION ( 'NONE',  ( 0.000000000000000000, 0.8814952561688437216, -0.4721928772777334582 ) ) ;
#199335=VERTEX_POINT ( 'NONE', #40427 ) ;
#199374=CIRCLE ( 'NONE', #82776, 0.1000000000000134115 ) ;
#199380=VECTOR ( 'NONE', #168120, 1000.000000000000000 ) ;
#199387=CIRCLE ( 'NONE', #224299, 0.1000000000000013933 ) ;
#199415=EDGE_LOOP ( 'NONE', ( #83787, #199992, #71375, #104961 ) ) ;
#199430=TOROIDAL_SURFACE ( 'NONE', #157767, 6.258578643762700899, 0.1000000000000000056 ) ;
#199431=DIRECTION ( 'NONE',  ( 0.000000000000000000, 0.8814952561688476074, -0.4721928772777262417 ) ) ;
#199441=CIRCLE ( 'NONE', #86950, 0.09999999999998464284 ) ;
#199458=DIRECTION ( 'NONE',  ( 0.000000000000000000, -0.8814952561688431665, 0.4721928772777346794 ) ) ;
#199469=ADVANCED_FACE ( 'NONE', ( #238587 ), #63805, .T. ) ;
#199472=ORIENTED_EDGE ( 'NONE', *, *, #103695, .F. ) ;
#199519=FACE_OUTER_BOUND ( 'NONE', #79316, .T. ) ;
#199529=EDGE_LOOP ( 'NONE', ( #249503, #254978, #155956, #2620 ) ) ;
#199534=EDGE_LOOP ( 'NONE', ( #63137, #38597, #230050, #7086 ) ) ;
#199548=EDGE_CURVE ( 'NONE', #71417, #108268, #164537, .T. ) ;
#199564=CARTESIAN_POINT ( 'NONE',  ( 23.24999999999999289, 2.272311100394802885, -217.9150152700588592 ) ) ;
#199581=VERTEX_POINT ( 'NONE', #209738 ) ;
#199596=EDGE_LOOP ( 'NONE', ( #83591, #242131 ) ) ;
#199638=DIRECTION ( 'NONE',  ( 1.000000000000000000, 0.000000000000000000, 0.000000000000000000 ) ) ;
#199681=CARTESIAN_POINT ( 'NONE',  ( 21.00000000000000000, 22.61918030723622408, -230.9697045991730988 ) ) ;
#199702=ORIENTED_EDGE ( 'NONE', *, *, #8782, .F. ) ;
#199705=ADVANCED_FACE ( 'NONE', ( #196576 ), #247348, .F. ) ;
#199736=CIRCLE ( 'NONE', #24953, 0.1000000000000013933 ) ;
#199747=EDGE_CURVE ( 'NONE', #248047, #183490, #43925, .T. ) ;
#199759=DIRECTION ( 'NONE',  ( 1.000000000000000000, 0.000000000000000000, 0.000000000000000000 ) ) ;
#199826=ADVANCED_FACE ( 'NONE', ( #122196 ), #164704, .F. ) ;
#199833=CARTESIAN_POINT ( 'NONE',  ( 22.48970261584622321, 12.58107241917856634, -223.4371365001174752 ) ) ;
#199847=ORIENTED_EDGE ( 'NONE', *, *, #102568, .T. ) ;
#199854=CIRCLE ( 'NONE', #233174, 0.3999999999999994671 ) ;
#199886=EDGE_CURVE ( 'NONE', #107706, #78910, #126020, .T. ) ;
#199903=EDGE_LOOP ( 'NONE', ( #126786, #68259, #185182, #107507 ) ) ;
#199904=AXIS2_PLACEMENT_3D ( 'NONE', #66387, #162939, #121267 ) ;
#199910=ORIENTED_EDGE ( 'NONE', *, *, #192441, .F. ) ;
#199913=VERTEX_POINT ( 'NONE', #127317 ) ;
#199920=CARTESIAN_POINT ( 'NONE',  ( 23.25000000000000000, 24.26958830762006514, -252.6664436919618879 ) ) ;
#199938=CYLINDRICAL_SURFACE ( 'NONE', #1401, 11.74999999999999112 ) ;
#199943=DIRECTION ( 'NONE',  ( 0.000000000000000000, 0.8814952561688444987, -0.4721928772777320149 ) ) ;
#199978=CARTESIAN_POINT ( 'NONE',  ( -20.64999999999999858, 26.18196512540240661, -241.1028522842020152 ) ) ;
#199992=ORIENTED_EDGE ( 'NONE', *, *, #40442, .F. ) ;
#200012=AXIS2_PLACEMENT_3D ( 'NONE', #151615, #215405, #137156 ) ;
#200023=CARTESIAN_POINT ( 'NONE',  ( -21.05000000000000071, 7.128833340093095217, -233.7327013124392749 ) ) ;
#200046=DIRECTION ( 'NONE',  ( 0.000000000000000000, 0.8814952561688437216, -0.4721928772777334582 ) ) ;
#200120=ORIENTED_EDGE ( 'NONE', *, *, #31213, .F. ) ;
#200134=ORIENTED_EDGE ( 'NONE', *, *, #67657, .T. ) ;
#200145=LINE ( 'NONE', #201415, #112956 ) ;
#200158=CIRCLE ( 'NONE', #37685, 0.5000000000000008882 ) ;
#200216=EDGE_CURVE ( 'NONE', #229996, #143721, #177584, .T. ) ;
#200221=DIRECTION ( 'NONE',  ( -1.000000000000000000, 0.000000000000000000, 0.000000000000000000 ) ) ;
#200230=DIRECTION ( 'NONE',  ( 5.603264701231743991E-32, -0.8814952561688430555, 0.4721928772777344019 ) ) ;
#200246=DIRECTION ( 'NONE',  ( -1.000000000000000000, 0.000000000000000000, 0.000000000000000000 ) ) ;
#200272=DIRECTION ( 'NONE',  ( 0.000000000000000000, 0.8814952561688430555, -0.4721928772777344574 ) ) ;
#200290=EDGE_CURVE ( 'NONE', #156870, #158295, #56697, .T. ) ;
#200323=ORIENTED_EDGE ( 'NONE', *, *, #217178, .F. ) ;
#200388=ORIENTED_EDGE ( 'NONE', *, *, #151891, .F. ) ;
#200406=VERTEX_POINT ( 'NONE', #43635 ) ;
#200411=VECTOR ( 'NONE', #117364, 1000.000000000000000 ) ;
#200414=CARTESIAN_POINT ( 'NONE',  ( 19.99999999999998934, 34.58225676390223668, -235.1091250528070589 ) ) ;
#200438=EDGE_CURVE ( 'NONE', #136977, #140654, #123170, .T. ) ;
#200445=EDGE_CURVE ( 'NONE', #48459, #21732, #190206, .T. ) ;
#200449=FACE_OUTER_BOUND ( 'NONE', #45509, .T. ) ;
#200469=DIRECTION ( 'NONE',  ( 1.000000000000000000, -0.000000000000000000, -0.000000000000000000 ) ) ;
#200491=DIRECTION ( 'NONE',  ( 0.000000000000000000, 0.4721928772777346239, 0.8814952561688430555 ) ) ;
#200511=ORIENTED_EDGE ( 'NONE', *, *, #135902, .F. ) ;
#200529=CARTESIAN_POINT ( 'NONE',  ( 18.52928932188133970, 33.71149860592453251, -236.3111109633099716 ) ) ;
#200544=CARTESIAN_POINT ( 'NONE',  ( 21.04386569057668410, 36.16263438457939117, -235.9556900804371082 ) ) ;
#200575=FACE_OUTER_BOUND ( 'NONE', #194525, .T. ) ;
#200589=AXIS2_PLACEMENT_3D ( 'NONE', #30283, #10712, #152822 ) ;
#200593=EDGE_CURVE ( 'NONE', #3876, #71987, #202662, .T. ) ;
#200600=CARTESIAN_POINT ( 'NONE',  ( 20.94999999999999929, 23.68770167995059239, -252.8127582590406348 ) ) ;
#200614=DIRECTION ( 'NONE',  ( -1.000000000000000000, 0.000000000000000000, 0.000000000000000000 ) ) ;
#200644=VECTOR ( 'NONE', #142451, 1000.000000000000000 ) ;
#200666=ORIENTED_EDGE ( 'NONE', *, *, #194767, .T. ) ;
#200746=FACE_OUTER_BOUND ( 'NONE', #225823, .T. ) ;
#200751=PLANE ( 'NONE',  #238890 ) ;
#200772=ORIENTED_EDGE ( 'NONE', *, *, #19837, .F. ) ;
#200791=ORIENTED_EDGE ( 'NONE', *, *, #160954, .T. ) ;
#200809=CARTESIAN_POINT ( 'NONE',  ( -18.50000972452446035, 46.33166059915856039, -243.0555356998360423 ) ) ;
#200833=FACE_OUTER_BOUND ( 'NONE', #185508, .T. ) ;
#200847=ORIENTED_EDGE ( 'NONE', *, *, #69356, .F. ) ;
#200853=ORIENTED_EDGE ( 'NONE', *, *, #127434, .T. ) ;
#200876=ORIENTED_EDGE ( 'NONE', *, *, #161177, .F. ) ;
#200896=CARTESIAN_POINT ( 'NONE',  ( 21.05000000000000071, 36.02918351690956200, -236.0543695120161090 ) ) ;
#200898=B_SPLINE_CURVE_WITH_KNOTS ( 'NONE', 3,
 ( #197975, #199275, #175875, #255335, #20651, #100134, #217527, #179717, #2331, #76745, #1030, #237115, #156327, #98843, #55875, #136711 ),
 .UNSPECIFIED., .F., .F.,
 ( 4, 3, 3, 3, 3, 4 ),
 ( 0.000000000000000000, 3.357088238233614221E-05, 6.714213034887457252E-05, 0.0001007408646120896615, 0.0001343627955914202031, 0.0001573956632895978950 ),
 .UNSPECIFIED. ) ;
#200918=ORIENTED_EDGE ( 'NONE', *, *, #207808, .F. ) ;
#200934=ORIENTED_EDGE ( 'NONE', *, *, #85190, .F. ) ;
#200943=FACE_OUTER_BOUND ( 'NONE', #152596, .T. ) ;
#200960=CARTESIAN_POINT ( 'NONE',  ( -20.64999999999999858, 27.82649702422227733, -239.8850763025288870 ) ) ;
#200996=CARTESIAN_POINT ( 'NONE',  ( -20.85000000000000142, 28.55432187084631224, -258.5393726171218418 ) ) ;
#201002=DIRECTION ( 'NONE',  ( 0.000000000000000000, -0.8814952561688430555, 0.4721928772777346239 ) ) ;
#201078=FACE_BOUND ( 'NONE', #123706, .T. ) ;
#201126=ADVANCED_FACE ( 'NONE', ( #78905 ), #152815, .T. ) ;
#201186=ORIENTED_EDGE ( 'NONE', *, *, #105413, .F. ) ;
#201188=CARTESIAN_POINT ( 'NONE',  ( -21.44999999999999929, 29.14863708059993286, -237.4168895852561434 ) ) ;
#201193=TOROIDAL_SURFACE ( 'NONE', #159517, 0.2000000000000000111, 0.1000000000000000056 ) ;
#201198=DIRECTION ( 'NONE',  ( 0.000000000000000000, 0.8814952561688437216, -0.4721928772777331806 ) ) ;
#201246=EDGE_CURVE ( 'NONE', #41556, #91231, #40574, .T. ) ;
#201277=VECTOR ( 'NONE', #160475, 1000.000000000000000 ) ;
#201323=EDGE_CURVE ( 'NONE', #221081, #253337, #148883, .T. ) ;
#201330=VERTEX_POINT ( 'NONE', #230003 ) ;
#201347=EDGE_CURVE ( 'NONE', #105209, #142016, #190586, .T. ) ;
#201348=CARTESIAN_POINT ( 'NONE',  ( -21.05000000000000071, 6.977140961446278489, -233.9419795020459389 ) ) ;
#201408=EDGE_CURVE ( 'NONE', #210749, #118204, #56484, .T. ) ;
#201415=CARTESIAN_POINT ( 'NONE',  ( -22.50000000000000000, 7.176052627820866725, -233.6445517868224044 ) ) ;
#201440=DIRECTION ( 'NONE',  ( -4.391705002472921695E-16, 0.4721928772777337913, 0.8814952561688434995 ) ) ;
#201476=ADVANCED_FACE ( 'NONE', ( #158217 ), #100724, .T. ) ;
#201508=CYLINDRICAL_SURFACE ( 'NONE', #89912, 0.09999999999998304689 ) ;
#201516=VERTEX_POINT ( 'NONE', #73095 ) ;
#201523=DIRECTION ( 'NONE',  ( 0.000000000000000000, 0.6855225566104692358, 0.7280513885559494192 ) ) ;
#201529=DIRECTION ( 'NONE',  ( 0.000000000000000000, -0.4721928772776568528, -0.8814952561688845778 ) ) ;
#201547=VECTOR ( 'NONE', #167489, 1000.000000000000000 ) ;
#201548=CARTESIAN_POINT ( 'NONE',  ( 22.40000000000020819, -3.275978944803190185, -228.2735455795370854 ) ) ;
#201577=ORIENTED_EDGE ( 'NONE', *, *, #171213, .F. ) ;
#201581=CARTESIAN_POINT ( 'NONE',  ( 21.05000000000000071, 18.82290990851281975, -233.3604470821920529 ) ) ;
#201610=FILL_AREA_STYLE_COLOUR ( '', #102525 ) ;
#201620=DIRECTION ( 'NONE',  ( -1.000000000000000000, -1.394253735153569469E-16, -2.602809386958778209E-16 ) ) ;
#201622=DIRECTION ( 'NONE',  ( 1.000000000000000000, 0.000000000000000000, 0.000000000000000000 ) ) ;
#201663=ORIENTED_EDGE ( 'NONE', *, *, #236638, .T. ) ;
#201668=CARTESIAN_POINT ( 'NONE',  ( 21.51976009735019346, 10.39190259496836433, -227.6411649781647384 ) ) ;
#201672=AXIS2_PLACEMENT_3D ( 'NONE', #215408, #216694, #13370 ) ;
#201692=LINE ( 'NONE', #200414, #113530 ) ;
#201731=CARTESIAN_POINT ( 'NONE',  ( -21.05000000000000071, 28.50120599808395028, -258.2149742250584268 ) ) ;
#201762=LINE ( 'NONE', #83063, #20841 ) ;
#201767=VERTEX_POINT ( 'NONE', #109510 ) ;
#201789=DIRECTION ( 'NONE',  ( 1.000000000000000000, 0.000000000000000000, 0.000000000000000000 ) ) ;
#201792=CARTESIAN_POINT ( 'NONE',  ( -20.85000000000000497, 36.10799525571641766, -235.9264213948819702 ) ) ;
#201798=CIRCLE ( 'NONE', #160141, 0.09999999999999939493 ) ;
#201807=CARTESIAN_POINT ( 'NONE',  ( 21.30000000000002558, 7.128833340093095217, -233.7327013124392749 ) ) ;
#201812=AXIS2_PLACEMENT_3D ( 'NONE', #59630, #101301, #20564 ) ;
#201828=CARTESIAN_POINT ( 'NONE',  ( 20.96428641293828576, 36.19089144327175944, -235.9708266132240055 ) ) ;
#201841=FACE_OUTER_BOUND ( 'NONE', #189954, .T. ) ;
#201846=ORIENTED_EDGE ( 'NONE', *, *, #166492, .F. ) ;
#201920=DIRECTION ( 'NONE',  ( 0.000000000000000000, -0.4646089985449268767, -0.8855159391400474478 ) ) ;
#201927=CARTESIAN_POINT ( 'NONE',  ( -21.93642651522410247, 10.58866904893262628, -227.2738390313130878 ) ) ;
#201947=CARTESIAN_POINT ( 'NONE',  ( 22.39999999999999503, -3.140208063160686791, -228.2318569537739847 ) ) ;
#201963=TOROIDAL_SURFACE ( 'NONE', #226888, 0.2000000000000000111, 0.1000000000000000056 ) ;
#201984=VERTEX_POINT ( 'NONE', #105319 ) ;
#201990=ORIENTED_EDGE ( 'NONE', *, *, #55814, .F. ) ;
#201997=DIRECTION ( 'NONE',  ( 1.000000000000000000, 0.000000000000000000, 0.000000000000000000 ) ) ;
#202009=CARTESIAN_POINT ( 'NONE',  ( -21.05000000000000071, 18.18127959618848166, -237.5711165786817389 ) ) ;
#202020=CIRCLE ( 'NONE', #214476, 0.09999999999999507894 ) ;
#202023=DIRECTION ( 'NONE',  ( 2.952720810173290098E-16, -0.4721928772777354011, -0.8814952561688427224 ) ) ;
#202079=CARTESIAN_POINT ( 'NONE',  ( -18.59999999999999787, 38.30077178631846380, -261.1858881914067751 ) ) ;
#202092=CARTESIAN_POINT ( 'NONE',  ( 18.42636655943170965, 38.00040813105046311, -261.0434348347492914 ) ) ;
#202094=CARTESIAN_POINT ( 'NONE',  ( -18.55807992284872299, 46.45729338110134421, -243.0823073233429170 ) ) ;
#202112=DIRECTION ( 'NONE',  ( 0.5000000000001139089, 0.7633972851576313889, -0.4089310272085548981 ) ) ;
#202151=ORIENTED_EDGE ( 'NONE', *, *, #239956, .F. ) ;
#202163=VERTEX_POINT ( 'NONE', #210879 ) ;
#202167=EDGE_CURVE ( 'NONE', #72339, #116858, #240820, .T. ) ;
#202168=ORIENTED_EDGE ( 'NONE', *, *, #239089, .F. ) ;
#202189=CIRCLE ( 'NONE', #98101, 0.1000000000000075273 ) ;
#202207=ORIENTED_EDGE ( 'NONE', *, *, #188319, .T. ) ;
#202220=ORIENTED_EDGE ( 'NONE', *, *, #43001, .T. ) ;
#202262=EDGE_CURVE ( 'NONE', #195967, #251749, #111826, .T. ) ;
#202308=DIRECTION ( 'NONE',  ( -1.000000000000000000, 0.000000000000000000, 0.000000000000000000 ) ) ;
#202328=FACE_OUTER_BOUND ( 'NONE', #53890, .T. ) ;
#202339=FACE_OUTER_BOUND ( 'NONE', #129327, .T. ) ;
#202361=DIRECTION ( 'NONE',  ( -0.000000000000000000, -0.4721928772777351790, -0.8814952561688427224 ) ) ;
#202383=ORIENTED_EDGE ( 'NONE', *, *, #103873, .T. ) ;
#202417=ORIENTED_EDGE ( 'NONE', *, *, #76212, .F. ) ;
#202434=DIRECTION ( 'NONE',  ( 0.7071067811865473507, 0.3338907855510733769, 0.6233112732207618523 ) ) ;
#202453=EDGE_CURVE ( 'NONE', #140654, #52463, #70348, .T. ) ;
#202469=ORIENTED_EDGE ( 'NONE', *, *, #100672, .F. ) ;
#202474=CARTESIAN_POINT ( 'NONE',  ( -21.14999999999999858, 12.76524917372336709, -223.4223513401831553 ) ) ;
#202478=ORIENTED_EDGE ( 'NONE', *, *, #147802, .F. ) ;
#202479=EDGE_LOOP ( 'NONE', ( #174865, #85960, #140186, #203530 ) ) ;
#202549=ADVANCED_FACE ( 'NONE', ( #174053 ), #215682, .T. ) ;
#202557=AXIS2_PLACEMENT_3D ( 'NONE', #231461, #52790, #9827 ) ;
#202567=ORIENTED_EDGE ( 'NONE', *, *, #222075, .T. ) ;
#202586=ORIENTED_EDGE ( 'NONE', *, *, #187879, .F. ) ;
#202596=CIRCLE ( 'NONE', #206693, 7.900000000000014566 ) ;
#202607=DIRECTION ( 'NONE',  ( 0.000000000000000000, -0.8814952561688431665, 0.4721928772777346794 ) ) ;
#202640=DIRECTION ( 'NONE',  ( 1.000000000000000000, 0.000000000000000000, 0.000000000000000000 ) ) ;
#202662=CIRCLE ( 'NONE', #106793, 0.09999999999999507894 ) ;
#202684=EDGE_CURVE ( 'NONE', #240363, #161820, #51394, .T. ) ;
#202713=CIRCLE ( 'NONE', #248516, 0.09999999999999986677 ) ;
#202716=TOROIDAL_SURFACE ( 'NONE', #236043, 12.97499999999999787, 0.1000000000000000056 ) ;
#202810=EDGE_LOOP ( 'NONE', ( #23629, #101124, #212875, #235801 ) ) ;
#202821=DIRECTION ( 'NONE',  ( -1.000000000000000000, 0.000000000000000000, 0.000000000000000000 ) ) ;
#202825=ORIENTED_EDGE ( 'NONE', *, *, #234905, .F. ) ;
#202835=CARTESIAN_POINT ( 'NONE',  ( -23.15000000000000213, 36.65892442174935439, -249.5511627012433848 ) ) ;
#202876=AXIS2_PLACEMENT_3D ( 'NONE', #232071, #74296, #5584 ) ;
#202877=DIRECTION ( 'NONE',  ( 0.000000000000000000, 0.8814952561688437216, -0.4721928772777334582 ) ) ;
#202889=AXIS2_PLACEMENT_3D ( 'NONE', #38737, #19159, #96113 ) ;
#202898=VERTEX_POINT ( 'NONE', #257049 ) ;
#202900=ORIENTED_EDGE ( 'NONE', *, *, #40981, .T. ) ;
#202903=CARTESIAN_POINT ( 'NONE',  ( -20.94999999999999929, 4.348235979057646361, -245.2768893876484810 ) ) ;
#202912=DIRECTION ( 'NONE',  ( -1.000000000000000000, 0.000000000000000000, 0.000000000000000000 ) ) ;
#202927=EDGE_LOOP ( 'NONE', ( #254129, #129885, #208808, #73282 ) ) ;
#202930=ORIENTED_EDGE ( 'NONE', *, *, #230843, .T. ) ;
#202933=PLANE ( 'NONE',  #57346 ) ;
#202941=ADVANCED_FACE ( 'NONE', ( #215401 ), #78450, .T. ) ;
#202944=DIRECTION ( 'NONE',  ( -0.000000000000000000, -0.8814952561688430555, 0.4721928772777346239 ) ) ;
#202962=CARTESIAN_POINT ( 'NONE',  ( 18.59999999999999076, 19.00443933019177578, -232.7770257915295531 ) ) ;
#202973=EDGE_CURVE ( 'NONE', #256102, #136922, #70525, .T. ) ;
#202984=DIRECTION ( 'NONE',  ( 0.000000000000000000, -0.8814952561688430555, 0.4721928772777346239 ) ) ;
#203047=DIRECTION ( 'NONE',  ( 1.000000000000000000, 0.000000000000000000, 0.000000000000000000 ) ) ;
#203048=DIRECTION ( 'NONE',  ( -0.000000000000000000, 0.8814952561688430555, -0.4721928772777346239 ) ) ;
#203058=ORIENTED_EDGE ( 'NONE', *, *, #140857, .F. ) ;
#203082=CARTESIAN_POINT ( 'NONE',  ( 21.05000000000000071, 18.71396320652088718, -229.9379713345707614 ) ) ;
#203085=CIRCLE ( 'NONE', #174095, 0.09999999999999939493 ) ;
#203120=CYLINDRICAL_SURFACE ( 'NONE', #81573, 11.75000000000000533 ) ;
#203136=LINE ( 'NONE', #104011, #14947 ) ;
#203152=ORIENTED_EDGE ( 'NONE', *, *, #192162, .F. ) ;
#203166=ORIENTED_EDGE ( 'NONE', *, *, #13681, .F. ) ;
#203188=DIRECTION ( 'NONE',  ( 0.000000000000000000, -0.8454177738465993297, -0.5341055959866553016 ) ) ;
#203198=DIRECTION ( 'NONE',  ( 1.000000000000000000, 0.000000000000000000, 0.000000000000000000 ) ) ;
#203227=ORIENTED_EDGE ( 'NONE', *, *, #42869, .T. ) ;
#203244=CIRCLE ( 'NONE', #157486, 0.09999999999999939493 ) ;
#203281=CARTESIAN_POINT ( 'NONE',  ( -20.54999999999999716, 20.06933876993645782, -235.7297789824848451 ) ) ;
#203284=ADVANCED_FACE ( 'NONE', ( #87437 ), #190430, .T. ) ;
#203285=DIRECTION ( 'NONE',  ( 0.000000000000000000, -0.7960711469212456981, 0.6052030477777622375 ) ) ;
#203294=VERTEX_POINT ( 'NONE', #150019 ) ;
#203317=CARTESIAN_POINT ( 'NONE',  ( -20.94999999999999929, 28.56975825374500388, -258.1421690862028413 ) ) ;
#203342=ORIENTED_EDGE ( 'NONE', *, *, #120677, .T. ) ;
#203353=LINE ( 'NONE', #178687, #229121 ) ;
#203357=CARTESIAN_POINT ( 'NONE',  ( 21.30000000000002558, 7.128833340093095217, -233.7327013124392749 ) ) ;
#203359=DIRECTION ( 'NONE',  ( 0.000000000000000000, 0.3488585713686159218, 0.9371753822965306346 ) ) ;
#203371=ORIENTED_EDGE ( 'NONE', *, *, #140396, .T. ) ;
#203375=DIRECTION ( 'NONE',  ( -0.000000000000000000, -0.8814952561688430555, 0.4721928772777346239 ) ) ;
#203418=CYLINDRICAL_SURFACE ( 'NONE', #96915, 0.1000000000000013933 ) ;
#203424=VERTEX_POINT ( 'NONE', #92573 ) ;
#203435=CARTESIAN_POINT ( 'NONE',  ( 21.05000000000000071, 28.50120599808395028, -258.2149742250584268 ) ) ;
#203466=DIRECTION ( 'NONE',  ( 0.000000000000000000, 0.8814952561688449428, -0.4721928772777311267 ) ) ;
#203483=EDGE_LOOP ( 'NONE', ( #52073, #30781 ) ) ;
#203492=CARTESIAN_POINT ( 'NONE',  ( -23.15000000000000213, 28.42524210734032053, -258.3567845160494585 ) ) ;
#203493=CARTESIAN_POINT ( 'NONE',  ( 18.59999999999999432, 38.30077178631847801, -261.1858881914067751 ) ) ;
#203513=DIRECTION ( 'NONE',  ( 1.000000000000000000, 0.000000000000000000, 0.000000000000000000 ) ) ;
#203530=ORIENTED_EDGE ( 'NONE', *, *, #43740, .F. ) ;
#203534=EDGE_CURVE ( 'NONE', #229996, #104319, #127232, .T. ) ;
#203571=VECTOR ( 'NONE', #145185, 1000.000000000000000 ) ;
#203584=CARTESIAN_POINT ( 'NONE',  ( 21.05000000000000071, 23.68770167995059239, -252.8127582590406348 ) ) ;
#203613=DIRECTION ( 'NONE',  ( 1.000000000000000000, 0.000000000000000000, 0.000000000000000000 ) ) ;
#203637=AXIS2_PLACEMENT_3D ( 'NONE', #35535, #95464, #194602 ) ;
#203639=VERTEX_POINT ( 'NONE', #9846 ) ;
#203685=ADVANCED_FACE ( 'NONE', ( #76224 ), #157077, .T. ) ;
#203691=ADVANCED_FACE ( 'NONE', ( #55350 ), #236580, .T. ) ;
#203710=CARTESIAN_POINT ( 'NONE',  ( -20.64999999999999858, 7.128833340093095217, -233.7327013124392749 ) ) ;
#203732=EDGE_CURVE ( 'NONE', #243045, #148687, #160928, .T. ) ;
#203733=CARTESIAN_POINT ( 'NONE',  ( 19.96984138294287092, 34.47169263967519726, -235.0498988782159131 ) ) ;
#203762=DIRECTION ( 'NONE',  ( 1.000000000000000000, 0.000000000000000000, 0.000000000000000000 ) ) ;
#203778=CARTESIAN_POINT ( 'NONE',  ( 20.94999999999999929, 19.09887790564731702, -232.6007267402957837 ) ) ;
#203792=EDGE_CURVE ( 'NONE', #103016, #199581, #257663, .T. ) ;
#203794=VECTOR ( 'NONE', #98335, 1000.000000000000000 ) ;
#203806=FACE_OUTER_BOUND ( 'NONE', #189203, .T. ) ;
#203814=DIRECTION ( 'NONE',  ( -6.938893903907221278E-15, 0.4721928772777346239, 0.8814952561688430555 ) ) ;
#203819=EDGE_CURVE ( 'NONE', #184466, #60897, #224721, .T. ) ;
#203844=VERTEX_POINT ( 'NONE', #244286 ) ;
#203864=ORIENTED_EDGE ( 'NONE', *, *, #209350, .T. ) ;
#203869=B_SPLINE_CURVE_WITH_KNOTS ( 'NONE', 3,
 ( #62519, #123779, #19549, #238582, #99044, #41685 ),
 .UNSPECIFIED., .F., .F.,
 ( 4, 2, 4 ),
 ( 4.336808689942017736E-19, 0.0001569047307838686138, 0.0003138094615677367938 ),
 .UNSPECIFIED. ) ;
#203883=ORIENTED_EDGE ( 'NONE', *, *, #187446, .F. ) ;
#203911=VECTOR ( 'NONE', #61900, 1000.000000000000000 ) ;
#203962=ORIENTED_EDGE ( 'NONE', *, *, #216324, .F. ) ;
#203989=ADVANCED_FACE ( 'NONE', ( #70830 ), #152943, .T. ) ;
#204000=ORIENTED_EDGE ( 'NONE', *, *, #221851, .T. ) ;
#204007=VERTEX_POINT ( 'NONE', #73400 ) ;
#204036=CARTESIAN_POINT ( 'NONE',  ( -18.50000000000000000, 30.09302283515540211, -235.6538990729184491 ) ) ;
#204089=CIRCLE ( 'NONE', #191675, 0.09999999999999939493 ) ;
#204091=CARTESIAN_POINT ( 'NONE',  ( 23.24999999999999289, 23.34004772283015683, -229.2004250369967338 ) ) ;
#204108=CARTESIAN_POINT ( 'NONE',  ( -23.15000000000000213, 31.44980407958350455, -233.5445995079518866 ) ) ;
#204136=DIRECTION ( 'NONE',  ( 1.000000000000000000, 0.000000000000000000, 0.000000000000000000 ) ) ;
#204196=B_SPLINE_CURVE_WITH_KNOTS ( 'NONE', 3,
 ( #11348, #208276, #33523, #8780, #12652, #10058, #68759, #192559 ),
 .UNSPECIFIED., .F., .F.,
 ( 4, 2, 2, 4 ),
 ( 0.000000000000000000, 0.0001881495939909263277, 0.0002822243909863877704, 0.0003762991879818492402 ),
 .UNSPECIFIED. ) ;
#204211=CARTESIAN_POINT ( 'NONE',  ( -21.05000000000000071, 13.59055429284667404, -238.6121134008722038 ) ) ;
#204216=EDGE_CURVE ( 'NONE', #241914, #103462, #91338, .T. ) ;
#204229=PLANE ( 'NONE',  #136164 ) ;
#204276=VECTOR ( 'NONE', #163853, 1000.000000000000114 ) ;
#204280=EDGE_CURVE ( 'NONE', #221081, #95915, #245276, .T. ) ;
#204281=ADVANCED_FACE ( 'NONE', ( #219288 ), #45793, .T. ) ;
#204284=SPHERICAL_SURFACE ( 'NONE', #77409, 0.1000000000000000056 ) ;
#204289=DIRECTION ( 'NONE',  ( 0.000000000000000000, -0.03181660087583042251, 0.9994937237965568766 ) ) ;
#204300=DIRECTION ( 'NONE',  ( -0.000000000000000000, -0.8814952561688430555, 0.4721928772777346239 ) ) ;
#204327=LINE ( 'NONE', #62265, #206126 ) ;
#204372=CARTESIAN_POINT ( 'NONE',  ( -20.64999999999999858, 21.39147882631411335, -233.2615922652120730 ) ) ;
#204383=CARTESIAN_POINT ( 'NONE',  ( 20.87155475150661132, 36.12098300858676936, -235.9333785785471775 ) ) ;
#204397=CIRCLE ( 'NONE', #221153, 1.900000000000002132 ) ;
#204400=ORIENTED_EDGE ( 'NONE', *, *, #227696, .T. ) ;
#204411=CARTESIAN_POINT ( 'NONE',  ( 20.94403535211772294, 46.37740828070795374, -243.0652246697500800 ) ) ;
#204424=ORIENTED_EDGE ( 'NONE', *, *, #106749, .T. ) ;
#204437=DIRECTION ( 'NONE',  ( 0.000000000000000000, 0.8814952561688431665, -0.4721928772777344574 ) ) ;
#204442=DIRECTION ( 'NONE',  ( -1.000000000000000000, 0.000000000000000000, 0.000000000000000000 ) ) ;
#204486=DIRECTION ( 'NONE',  ( 1.000000000000000000, -0.000000000000000000, -0.000000000000000000 ) ) ;
#204496=ORIENTED_EDGE ( 'NONE', *, *, #92980, .F. ) ;
#204501=ORIENTED_EDGE ( 'NONE', *, *, #28417, .F. ) ;
#204544=CARTESIAN_POINT ( 'NONE',  ( -20.54999999999999716, 25.94586868676353575, -241.5435999122864530 ) ) ;
#204555=TOROIDAL_SURFACE ( 'NONE', #138087, 0.2000000000000000111, 0.1000000000000000056 ) ;
#204603=EDGE_CURVE ( 'NONE', #156438, #34617, #84564, .T. ) ;
#204612=DIRECTION ( 'NONE',  ( 0.000000000000000000, -0.8814952561688431665, 0.4721928772777346794 ) ) ;
#204620=DIRECTION ( 'NONE',  ( 0.000000000000000000, 0.8814952561688434995, -0.4721928772777335137 ) ) ;
#204630=CARTESIAN_POINT ( 'NONE',  ( -20.94999999999999929, 30.48950451747912993, -239.6099224343151946 ) ) ;
#204646=FACE_OUTER_BOUND ( 'NONE', #34212, .T. ) ;
#204673=SPHERICAL_SURFACE ( 'NONE', #138614, 0.1000000000000000056 ) ;
#204684=CARTESIAN_POINT ( 'NONE',  ( -18.59999999999999787, 42.99798587058931076, -254.2674462307522560 ) ) ;
#204715=ORIENTED_EDGE ( 'NONE', *, *, #143483, .F. ) ;
#204769=DIRECTION ( 'NONE',  ( 1.000000000000000000, -0.000000000000000000, -0.000000000000000000 ) ) ;
#204778=CARTESIAN_POINT ( 'NONE',  ( -20.64999999999999858, 27.82649702422227733, -239.8850763025288870 ) ) ;
#204783=DIRECTION ( 'NONE',  ( 0.000000000000000000, 0.8814952561688444987, -0.4721928772777320149 ) ) ;
#204815=CARTESIAN_POINT ( 'NONE',  ( -22.32929514600008503, 0.4950742925550095652, -230.0667831724111068 ) ) ;
#204824=LINE ( 'NONE', #207429, #116154 ) ;
#204849=ORIENTED_EDGE ( 'NONE', *, *, #31623, .T. ) ;
#204853=FACE_OUTER_BOUND ( 'NONE', #151415, .T. ) ;
#204884=TOROIDAL_SURFACE ( 'NONE', #221441, 0.2000000000000000111, 0.1000000000000000056 ) ;
#204904=CARTESIAN_POINT ( 'NONE',  ( 22.49544290803734725, 12.61946619309020790, -223.3444065952062942 ) ) ;
#204915=LINE ( 'NONE', #185366, #251798 ) ;
#204916=AXIS2_PLACEMENT_3D ( 'NONE', #208397, #25899, #184959 ) ;
#204937=DIRECTION ( 'NONE',  ( 0.000000000000000000, 0.8127272543710951647, -0.5826443254700256480 ) ) ;
#204954=ADVANCED_FACE ( 'NONE', ( #72792 ), #41644, .T. ) ;
#204959=VECTOR ( 'NONE', #91027, 1000.000000000000000 ) ;
#205013=ORIENTED_EDGE ( 'NONE', *, *, #173297, .F. ) ;
#205052=DIRECTION ( 'NONE',  ( 0.000000000000000000, -0.4721928772777346239, -0.8814952561688430555 ) ) ;
#205064=CARTESIAN_POINT ( 'NONE',  ( 21.05000000000000071, 33.04479387145709524, -247.6151719044046899 ) ) ;
#205081=EDGE_CURVE ( 'NONE', #52463, #176327, #139105, .T. ) ;
#205094=EDGE_LOOP ( 'NONE', ( #131611, #16451, #80039 ) ) ;
#205132=CARTESIAN_POINT ( 'NONE',  ( 23.14999999999999858, 40.18490544642472884, -251.4399342103543233 ) ) ;
#205149=AXIS2_PLACEMENT_3D ( 'NONE', #193311, #92902, #233726 ) ;
#205178=VERTEX_POINT ( 'NONE', #111262 ) ;
#205186=DIRECTION ( 'NONE',  ( 0.000000000000000000, -0.4721928772777346239, -0.8814952561688430555 ) ) ;
#205203=FACE_OUTER_BOUND ( 'NONE', #219702, .T. ) ;
#205210=VECTOR ( 'NONE', #53917, 1000.000000000000000 ) ;
#205263=FACE_OUTER_BOUND ( 'NONE', #141663, .T. ) ;
#205268=EDGE_CURVE ( 'NONE', #253940, #208884, #46069, .T. ) ;
#205272=DIRECTION ( 'NONE',  ( 0.000000000000000000, 0.8814952561688430555, -0.4721928772777347905 ) ) ;
#205286=DIRECTION ( 'NONE',  ( 0.000000000000000000, 0.8814952561688429444, -0.4721928772777345684 ) ) ;
#205293=DIRECTION ( 'NONE',  ( -1.000000000000000000, 0.000000000000000000, 0.000000000000000000 ) ) ;
#205353=DIRECTION ( 'NONE',  ( -0.000000000000000000, 0.8814952561688430555, -0.4721928772777346239 ) ) ;
#205377=CARTESIAN_POINT ( 'NONE',  ( 21.05000000000000071, 36.65892442174935439, -249.5511627012433848 ) ) ;
#205380=CIRCLE ( 'NONE', #92981, 12.87500000000000355 ) ;
#205404=CIRCLE ( 'NONE', #197604, 1.900000000000002132 ) ;
#205422=ORIENTED_EDGE ( 'NONE', *, *, #209290, .T. ) ;
#205457=VERTEX_POINT ( 'NONE', #116681 ) ;
#205463=DIRECTION ( 'NONE',  ( 0.000000000000000000, 0.8814952561688429444, -0.4721928772777345684 ) ) ;
#205478=CARTESIAN_POINT ( 'NONE',  ( -18.59999999999999787, 19.09764897702175546, -235.7051342141560042 ) ) ;
#205498=CARTESIAN_POINT ( 'NONE',  ( 20.94999999999999574, 13.71992543034163958, -238.5823796952984992 ) ) ;
#205529=CARTESIAN_POINT ( 'NONE',  ( 20.85000000000000142, 36.18002604163306302, -236.0784499204090991 ) ) ;
#205543=CARTESIAN_POINT ( 'NONE',  ( 20.94999999999999929, 42.15997144203495139, -239.2817429668763793 ) ) ;
#205546=AXIS2_PLACEMENT_3D ( 'NONE', #157515, #237018, #92361 ) ;
#205552=CARTESIAN_POINT ( 'NONE',  ( -21.05000000000000071, 13.66123737402873495, -238.6633470470287648 ) ) ;
#205582=AXIS2_PLACEMENT_3D ( 'NONE', #153314, #232834, #133706 ) ;
#205599=VERTEX_POINT ( 'NONE', #146503 ) ;
#205604=EDGE_CURVE ( 'NONE', #5002, #190272, #132104, .T. ) ;
#205618=DIRECTION ( 'NONE',  ( -3.265361837132813586E-16, 0.4721928772777346239, 0.8814952561688430555 ) ) ;
#205629=CARTESIAN_POINT ( 'NONE',  ( -18.50000000000000000, 16.44800918141279311, -240.8068063186265135 ) ) ;
#205632=ORIENTED_EDGE ( 'NONE', *, *, #194972, .F. ) ;
#205636=CARTESIAN_POINT ( 'NONE',  ( 18.50000972452444969, 46.33166059915859591, -243.0555356998358718 ) ) ;
#205639=CARTESIAN_POINT ( 'NONE',  ( 21.05000000000000071, 18.81732247075047937, -230.0377732242114632 ) ) ;
#205662=EDGE_CURVE ( 'NONE', #31578, #32586, #188222, .T. ) ;
#205684=ADVANCED_FACE ( 'NONE', ( #129539 ), #21344, .T. ) ;
#205722=CIRCLE ( 'NONE', #64089, 4.149999999999996803 ) ;
#205796=DIRECTION ( 'NONE',  ( 0.000000000000000000, 0.9371753822965315228, -0.3488585713686134238 ) ) ;
#205800=EDGE_CURVE ( 'NONE', #221637, #254141, #118970, .T. ) ;
#205821=CIRCLE ( 'NONE', #47576, 0.09999999999999939493 ) ;
#205840=CARTESIAN_POINT ( 'NONE',  ( -18.50000000000000000, 30.18746141061095045, -235.4776000216846796 ) ) ;
#205850=ORIENTED_EDGE ( 'NONE', *, *, #204603, .F. ) ;
#205853=ORIENTED_EDGE ( 'NONE', *, *, #139782, .F. ) ;
#205943=VERTEX_POINT ( 'NONE', #220630 ) ;
#205975=FACE_OUTER_BOUND ( 'NONE', #116236, .T. ) ;
#205994=CARTESIAN_POINT ( 'NONE',  ( -23.25000000000000000, 31.11065811373596190, -259.9087319612273177 ) ) ;
#206008=CIRCLE ( 'NONE', #118546, 0.09999999999999986677 ) ;
#206019=EDGE_CURVE ( 'NONE', #226316, #225564, #80192, .T. ) ;
#206048=AXIS2_PLACEMENT_3D ( 'NONE', #117316, #101564, #140724 ) ;
#206084=CARTESIAN_POINT ( 'NONE',  ( -21.05000000000000071, 7.128833340093095217, -233.7327013124392749 ) ) ;
#206089=DIRECTION ( 'NONE',  ( 0.000000000000000000, -0.8814952561688266242, 0.4721928772777652106 ) ) ;
#206126=VECTOR ( 'NONE', #243462, 1000.000000000000000 ) ;
#206127=ORIENTED_EDGE ( 'NONE', *, *, #145977, .T. ) ;
#206161=FACE_OUTER_BOUND ( 'NONE', #137891, .T. ) ;
#206205=CARTESIAN_POINT ( 'NONE',  ( 22.57320508075689247, 12.67709964810646817, -223.3751320524553705 ) ) ;
#206214=DIRECTION ( 'NONE',  ( 0.000000000000000000, 0.8814952561688444987, -0.4721928772777320149 ) ) ;
#206271=CARTESIAN_POINT ( 'NONE',  ( -23.25000000000000000, 36.65892442174935439, -249.5511627012433848 ) ) ;
#206304=CIRCLE ( 'NONE', #43977, 0.09999999999999997780 ) ;
#206320=VERTEX_POINT ( 'NONE', #239894 ) ;
#206331=ORIENTED_EDGE ( 'NONE', *, *, #5405, .F. ) ;
#206350=ADVANCED_FACE ( 'NONE', ( #125082 ), #62532, .T. ) ;
#206368=VECTOR ( 'NONE', #185173, 1000.000000000000114 ) ;
#206384=CARTESIAN_POINT ( 'NONE',  ( -18.50000000000000000, 23.34004772283015328, -229.2004250369967338 ) ) ;
#206389=FACE_OUTER_BOUND ( 'NONE', #31247, .T. ) ;
#206396=ORIENTED_EDGE ( 'NONE', *, *, #99999, .F. ) ;
#206397=AXIS2_PLACEMENT_3D ( 'NONE', #137872, #160052, #17939 ) ;
#206421=ORIENTED_EDGE ( 'NONE', *, *, #255911, .F. ) ;
#206441=LINE ( 'NONE', #83877, #156982 ) ;
#206530=FACE_OUTER_BOUND ( 'NONE', #19066, .T. ) ;
#206539=EDGE_CURVE ( 'NONE', #73105, #63327, #71363, .T. ) ;
#206558=AXIS2_PLACEMENT_3D ( 'NONE', #193926, #55643, #136477 ) ;
#206574=ORIENTED_EDGE ( 'NONE', *, *, #244384, .F. ) ;
#206608=AXIS2_PLACEMENT_3D ( 'NONE', #48710, #245640, #46148 ) ;
#206693=AXIS2_PLACEMENT_3D ( 'NONE', #253439, #12299, #250871 ) ;
#206773=EDGE_CURVE ( 'NONE', #71417, #186223, #253369, .T. ) ;
#206779=ORIENTED_EDGE ( 'NONE', *, *, #68709, .F. ) ;
#206782=CIRCLE ( 'NONE', #123574, 0.09999999999999986677 ) ;
#206810=DIRECTION ( 'NONE',  ( 0.000000000000000000, 0.4721928772780015771, 0.8814952561687000587 ) ) ;
#206822=ORIENTED_EDGE ( 'NONE', *, *, #16825, .T. ) ;
#206836=CARTESIAN_POINT ( 'NONE',  ( 23.15000000000000213, 28.42524210734032408, -258.3567845160494585 ) ) ;
#206851=ORIENTED_EDGE ( 'NONE', *, *, #207604, .T. ) ;
#206868=AXIS2_PLACEMENT_3D ( 'NONE', #156953, #213043, #38273 ) ;
#206887=DIRECTION ( 'NONE',  ( -1.836970198721029441E-16, 0.4721928772777346239, 0.8814952561688430555 ) ) ;
#206895=ORIENTED_EDGE ( 'NONE', *, *, #158184, .T. ) ;
#206953=CARTESIAN_POINT ( 'NONE',  ( 20.94999999999999929, 36.65892442174935439, -249.5511627012433848 ) ) ;
#206965=DIRECTION ( 'NONE',  ( -1.000000000000000000, 0.000000000000000000, -0.000000000000000000 ) ) ;
#206980=CARTESIAN_POINT ( 'NONE',  ( 20.94999999999999929, 20.02733907826963033, -235.1395327601354666 ) ) ;
#206996=LINE ( 'NONE', #109158, #106557 ) ;
#207013=( BOUNDED_CURVE ( )  B_SPLINE_CURVE ( 3, ( #198483, #137226, #257125, #160677 ),
 .UNSPECIFIED., .F., .F. ) 
 B_SPLINE_CURVE_WITH_KNOTS ( ( 4, 4 ),
 ( 0.000000000000000000, 1.570796326794908992 ),
 .UNSPECIFIED. ) 
 CURVE ( )  GEOMETRIC_REPRESENTATION_ITEM ( )  RATIONAL_B_SPLINE_CURVE ( ( 1.000000000000000000, 0.8047378541243619399, 0.8047378541243619399, 1.000000000000000000 ) ) 
 REPRESENTATION_ITEM ( '' )  );
#207025=CARTESIAN_POINT ( 'NONE',  ( 20.94999999999999929, 36.65892442174935439, -249.5511627012433848 ) ) ;
#207032=DIRECTION ( 'NONE',  ( 0.000000000000000000, -0.8814952561688437216, 0.4721928772777334582 ) ) ;
#207047=CARTESIAN_POINT ( 'NONE',  ( 23.14999999999999503, 31.36165455396662693, -233.4973802202241018 ) ) ;
#207086=DIRECTION ( 'NONE',  ( -1.000000000000000000, 0.000000000000000000, 0.000000000000000000 ) ) ;
#207094=TOROIDAL_SURFACE ( 'NONE', #7144, 11.65000000000000036, 0.1000000000000000056 ) ;
#207118=DIRECTION ( 'NONE',  ( 0.000000000000000000, 0.4721928772776973204, 0.8814952561688629284 ) ) ;
#207134=CARTESIAN_POINT ( 'NONE',  ( -23.25000000000000000, 31.36165455396662693, -233.4973802202241302 ) ) ;
#207177=DIRECTION ( 'NONE',  ( 0.000000000000000000, 0.8814952561688476074, -0.4721928772777262417 ) ) ;
#207182=AXIS2_PLACEMENT_3D ( 'NONE', #163937, #229050, #50373 ) ;
#207195=DIRECTION ( 'NONE',  ( 0.000000000000000000, 0.8814952561688429444, -0.4721928772777348460 ) ) ;
#207208=VECTOR ( 'NONE', #17081, 1000.000000000000000 ) ;
#207232=CARTESIAN_POINT ( 'NONE',  ( -22.39999999999999858, 0.2612980822699374484, -230.0539506776466681 ) ) ;
#207238=B_SPLINE_CURVE_WITH_KNOTS ( 'NONE', 3,
 ( #125303, #126583, #69202, #204815, #124024, #185274, #182719, #108308, #228261, #187860 ),
 .UNSPECIFIED., .F., .F.,
 ( 4, 3, 3, 4 ),
 ( 4.504661056180557620E-18, 0.0002000000000002871876, 0.001000000000045109336, 0.001967863649472136479 ),
 .UNSPECIFIED. ) ;
#207249=DIRECTION ( 'NONE',  ( 0.000000000000000000, 0.8814952561688430555, -0.4721928772777346239 ) ) ;
#207252=CIRCLE ( 'NONE', #28199, 0.1000000000000012546 ) ;
#207279=CARTESIAN_POINT ( 'NONE',  ( -20.64999999999999858, 27.82649702422227733, -239.8850763025288870 ) ) ;
#207326=CARTESIAN_POINT ( 'NONE',  ( 20.94999999999999929, 43.08613539620618837, -254.3146655184800409 ) ) ;
#207335=CARTESIAN_POINT ( 'NONE',  ( 20.85000000000000142, 31.15787740146373963, -259.8205824356103903 ) ) ;
#207352=DIRECTION ( 'NONE',  ( -1.000000000000000000, -0.000000000000000000, -0.000000000000000000 ) ) ;
#207355=CIRCLE ( 'NONE', #94895, 0.2000000000000150546 ) ;
#207366=VERTEX_POINT ( 'NONE', #204630 ) ;
#207405=FACE_OUTER_BOUND ( 'NONE', #169732, .T. ) ;
#207410=FACE_OUTER_BOUND ( 'NONE', #22216, .T. ) ;
#207429=CARTESIAN_POINT ( 'NONE',  ( -21.05000000000000071, 4.348235979057646361, -245.2768893876484810 ) ) ;
#207457=CARTESIAN_POINT ( 'NONE',  ( -21.05000000000000071, 13.54362637910787370, -238.4879411198429580 ) ) ;
#207501=DIRECTION ( 'NONE',  ( -2.840903330521632269E-16, 0.8454177738465993297, 0.5341055959866553016 ) ) ;
#207558=ORIENTED_EDGE ( 'NONE', *, *, #26038, .T. ) ;
#207568=FACE_OUTER_BOUND ( 'NONE', #230925, .T. ) ;
#207584=CARTESIAN_POINT ( 'NONE',  ( -23.15000000000000213, 23.68770167995059595, -252.8127582590406348 ) ) ;
#207603=VERTEX_POINT ( 'NONE', #139199 ) ;
#207604=EDGE_CURVE ( 'NONE', #205178, #50106, #184487, .T. ) ;
#207613=ORIENTED_EDGE ( 'NONE', *, *, #252166, .F. ) ;
#207618=VERTEX_POINT ( 'NONE', #23155 ) ;
#207657=ORIENTED_EDGE ( 'NONE', *, *, #246573, .F. ) ;
#207659=DIRECTION ( 'NONE',  ( 0.000000000000000000, 0.8814952561688431665, -0.4721928772777345129 ) ) ;
#207688=CARTESIAN_POINT ( 'NONE',  ( 21.07928932188134397, 10.02993822722304351, -228.1074463178677263 ) ) ;
#207690=CARTESIAN_POINT ( 'NONE',  ( 18.46163235739464881, 38.05111684352567636, -261.0515469419265742 ) ) ;
#207738=AXIS2_PLACEMENT_3D ( 'NONE', #223755, #46403, #20783 ) ;
#207754=CARTESIAN_POINT ( 'NONE',  ( 21.05000000000000071, 11.60058429089262333, -246.3380203656811887 ) ) ;
#207798=CYLINDRICAL_SURFACE ( 'NONE', #77340, 0.09999999999999970024 ) ;
#207808=EDGE_CURVE ( 'NONE', #110056, #179549, #1325, .T. ) ;
#207834=LINE ( 'NONE', #152666, #63022 ) ;
#207864=ORIENTED_EDGE ( 'NONE', *, *, #90833, .F. ) ;
#207877=DIRECTION ( 'NONE',  ( -1.000000000000000000, -0.000000000000000000, -0.000000000000000000 ) ) ;
#207905=DIRECTION ( 'NONE',  ( 0.000000000000000000, 0.8814952561688429444, -0.4721928772777348460 ) ) ;
#207926=CARTESIAN_POINT ( 'NONE',  ( 23.14999999999999858, 7.128833340093095217, -233.7327013124392749 ) ) ;
#207938=CARTESIAN_POINT ( 'NONE',  ( 18.52928932188133970, 30.80256426056735108, -234.7528744682934700 ) ) ;
#207950=CARTESIAN_POINT ( 'NONE',  ( 20.85000000000000142, 43.27008861172207332, -245.2265230569236110 ) ) ;
#208000=CIRCLE ( 'NONE', #57930, 0.09999999999999939493 ) ;
#208034=AXIS2_PLACEMENT_3D ( 'NONE', #209286, #69802, #228861 ) ;
#208038=AXIS2_PLACEMENT_3D ( 'NONE', #97678, #178562, #134248 ) ;
#208046=VERTEX_POINT ( 'NONE', #99764 ) ;
#208064=LINE ( 'NONE', #90646, #1032 ) ;
#208120=DIRECTION ( 'NONE',  ( 0.000000000000000000, 0.4721928772776973204, 0.8814952561688629284 ) ) ;
#208130=ORIENTED_EDGE ( 'NONE', *, *, #173962, .T. ) ;
#208132=VECTOR ( 'NONE', #98772, 1000.000000000000000 ) ;
#208143=EDGE_LOOP ( 'NONE', ( #77881, #222184, #34878, #40673 ) ) ;
#208163=CARTESIAN_POINT ( 'NONE',  ( -23.15000000000000213, 40.09675592080784412, -251.3927149226265385 ) ) ;
#208172=CIRCLE ( 'NONE', #87335, 0.1000000000000013933 ) ;
#208181=ORIENTED_EDGE ( 'NONE', *, *, #232485, .T. ) ;
#208182=DIRECTION ( 'NONE',  ( 0.000000000000000000, 0.4721928772777551075, 0.8814952561688320642 ) ) ;
#208183=FACE_OUTER_BOUND ( 'NONE', #1438, .T. ) ;
#208217=ORIENTED_EDGE ( 'NONE', *, *, #47847, .F. ) ;
#208236=EDGE_LOOP ( 'NONE', ( #213748, #81502, #160478, #62927 ) ) ;
#208238=EDGE_CURVE ( 'NONE', #32586, #19570, #64064, .T. ) ;
#208241=CARTESIAN_POINT ( 'NONE',  ( 18.54148534481893762, 46.44433919924418319, -243.0795225066946159 ) ) ;
#208257=AXIS2_PLACEMENT_3D ( 'NONE', #17964, #59634, #58355 ) ;
#208276=CARTESIAN_POINT ( 'NONE',  ( 21.05000000000000426, 1.372128392831997390, -230.7624356707774496 ) ) ;
#208314=ORIENTED_EDGE ( 'NONE', *, *, #107403, .F. ) ;
#208326=ORIENTED_EDGE ( 'NONE', *, *, #91159, .T. ) ;
#208345=CARTESIAN_POINT ( 'NONE',  ( -21.00250684356849362, 18.86061765621301234, -226.6874733719499488 ) ) ;
#208358=ADVANCED_FACE ( 'NONE', ( #93587 ), #16632, .T. ) ;
#208359=ORIENTED_EDGE ( 'NONE', *, *, #179068, .F. ) ;
#208362=EDGE_CURVE ( 'NONE', #180293, #35579, #1512, .T. ) ;
#208371=AXIS2_PLACEMENT_3D ( 'NONE', #214117, #236239, #175040 ) ;
#208378=DIRECTION ( 'NONE',  ( -1.000000000000000000, 0.000000000000000000, 0.000000000000000000 ) ) ;
#208384=CARTESIAN_POINT ( 'NONE',  ( -21.17356465864818205, 10.07444543872610154, -228.0243256418613385 ) ) ;
#208397=CARTESIAN_POINT ( 'NONE',  ( 21.05000000000000071, 24.04029978241812771, -253.0016354099517457 ) ) ;
#208434=FACE_OUTER_BOUND ( 'NONE', #220879, .T. ) ;
#208438=CARTESIAN_POINT ( 'NONE',  ( -23.25000000000000000, 46.01276039807270024, -256.6622985126337539 ) ) ;
#208442=FACE_OUTER_BOUND ( 'NONE', #163053, .T. ) ;
#208474=CYLINDRICAL_SURFACE ( 'NONE', #219573, 0.09999999999998304689 ) ;
#208484=EDGE_CURVE ( 'NONE', #71383, #117652, #7455, .T. ) ;
#208502=CARTESIAN_POINT ( 'NONE',  ( -23.15000000000000213, 7.128833340093095217, -233.7327013124392749 ) ) ;
#208505=CARTESIAN_POINT ( 'NONE',  ( -23.25000000000000000, 30.38404434817536881, -239.4399867032565794 ) ) ;
#208536=AXIS2_PLACEMENT_3D ( 'NONE', #27185, #49273, #150951 ) ;
#208577=CARTESIAN_POINT ( 'NONE',  ( -20.94999999999999929, 14.85285025691667293, -236.4388300032497057 ) ) ;
#208616=DIRECTION ( 'NONE',  ( -2.952720810173288619E-16, 0.4721928772777346239, 0.8814952561688430555 ) ) ;
#208627=EDGE_CURVE ( 'NONE', #63775, #185172, #128555, .T. ) ;
#208656=LINE ( 'NONE', #144791, #9404 ) ;
#208784=VERTEX_POINT ( 'NONE', #54685 ) ;
#208787=CARTESIAN_POINT ( 'NONE',  ( 18.39999999999999858, 38.26833061496694199, -261.1904200532067648 ) ) ;
#208798=AXIS2_PLACEMENT_3D ( 'NONE', #229914, #31749, #209066 ) ;
#208808=ORIENTED_EDGE ( 'NONE', *, *, #92437, .T. ) ;
#208836=DIRECTION ( 'NONE',  ( 1.000000000000000000, 0.000000000000000000, 0.000000000000000000 ) ) ;
#208852=DIRECTION ( 'NONE',  ( 0.000000000000000000, -0.4721928772777346239, -0.8814952561688430555 ) ) ;
#208884=VERTEX_POINT ( 'NONE', #80650 ) ;
#208954=CARTESIAN_POINT ( 'NONE',  ( 18.39999999999999858, 37.95493834378066822, -261.2294694241335264 ) ) ;
#208960=ORIENTED_EDGE ( 'NONE', *, *, #257784, .T. ) ;
#208966=CARTESIAN_POINT ( 'NONE',  ( 21.12230431290519661, 1.438979023680419633, -230.6788918746589161 ) ) ;
#208972=DIRECTION ( 'NONE',  ( 0.000000000000000000, -0.4721928772777346239, -0.8814952561688430555 ) ) ;
#208997=CIRCLE ( 'NONE', #75738, 0.09999999999999986677 ) ;
#209010=ADVANCED_FACE ( 'NONE', ( #44117 ), #47653, .T. ) ;
#209022=ADVANCED_FACE ( 'NONE', ( #49240 ), #60750, .T. ) ;
#209026=CARTESIAN_POINT ( 'NONE',  ( -21.14250536705909411, 1.383095487280965763, -230.6548668376462672 ) ) ;
#209066=DIRECTION ( 'NONE',  ( 0.000000000000000000, 0.8814952561688437216, -0.4721928772777331806 ) ) ;
#209070=CARTESIAN_POINT ( 'NONE',  ( -23.25000000000000000, 3.558777552609281525, -231.8203201594644725 ) ) ;
#209117=DIRECTION ( 'NONE',  ( 1.000000000000000000, 0.000000000000000000, 0.000000000000000000 ) ) ;
#209125=CARTESIAN_POINT ( 'NONE',  ( 20.94999999999999929, 23.68770167995059239, -252.8127582590406348 ) ) ;
#209126=EDGE_CURVE ( 'NONE', #76756, #81287, #153533, .T. ) ;
#209132=CIRCLE ( 'NONE', #255453, 0.09999999999999031886 ) ;
#209146=LINE ( 'NONE', #110050, #247657 ) ;
#209158=EDGE_CURVE ( 'NONE', #208884, #75744, #39526, .T. ) ;
#209225=CARTESIAN_POINT ( 'NONE',  ( -23.15000000000000213, 23.42819724844703444, -229.2476443247244902 ) ) ;
#209230=VERTEX_POINT ( 'NONE', #201581 ) ;
#209250=DIRECTION ( 'NONE',  ( -0.000000000000000000, -0.8814952561688430555, 0.4721928772777344574 ) ) ;
#209253=AXIS2_PLACEMENT_3D ( 'NONE', #23068, #98682, #161287 ) ;
#209255=DIRECTION ( 'NONE',  ( -1.836970198721029441E-16, 0.4721928772777346239, 0.8814952561688430555 ) ) ;
#209286=CARTESIAN_POINT ( 'NONE',  ( -23.15000000000000213, 25.94586868676353575, -241.5435999122864530 ) ) ;
#209290=EDGE_CURVE ( 'NONE', #89936, #147651, #88971, .T. ) ;
#209326=CARTESIAN_POINT ( 'NONE',  ( 18.59999999999998366, 43.35377423437995503, -245.1717807829448930 ) ) ;
#209340=VECTOR ( 'NONE', #77876, 1000.000000000000000 ) ;
#209348=ORIENTED_EDGE ( 'NONE', *, *, #107306, .T. ) ;
#209350=EDGE_CURVE ( 'NONE', #56882, #186477, #123344, .T. ) ;
#209365=ORIENTED_EDGE ( 'NONE', *, *, #140023, .T. ) ;
#209378=LINE ( 'NONE', #88115, #231567 ) ;
#209399=ORIENTED_EDGE ( 'NONE', *, *, #139898, .F. ) ;
#209405=CARTESIAN_POINT ( 'NONE',  ( -20.64999999999999858, 29.28400589394459530, -237.3759593473670293 ) ) ;
#209407=CARTESIAN_POINT ( 'NONE',  ( 21.12802099929860589, 22.07166910013054917, -231.7761939280465526 ) ) ;
#209482=CARTESIAN_POINT ( 'NONE',  ( -20.54999999999999716, 23.45160524131172508, -253.2535058871250726 ) ) ;
#209500=ORIENTED_EDGE ( 'NONE', *, *, #69170, .T. ) ;
#209560=CARTESIAN_POINT ( 'NONE',  ( 21.14999999999999858, 23.34004772283015328, -229.2004250369967338 ) ) ;
#209579=ORIENTED_EDGE ( 'NONE', *, *, #19889, .T. ) ;
#209589=ORIENTED_EDGE ( 'NONE', *, *, #79309, .F. ) ;
#209616=DIRECTION ( 'NONE',  ( -1.000000000000000000, 0.000000000000000000, 0.000000000000000000 ) ) ;
#209625=DIRECTION ( 'NONE',  ( 0.000000000000000000, 0.8814952561688476074, -0.4721928772777262417 ) ) ;
#209639=DIRECTION ( 'NONE',  ( 0.000000000000000000, 0.8814952561688476074, -0.4721928772777262417 ) ) ;
#209640=DIRECTION ( 'NONE',  ( 0.000000000000000000, -0.8814952561685545085, 0.4721928772782730821 ) ) ;
#209642=CARTESIAN_POINT ( 'NONE',  ( 22.49806830649814060, -3.103911027125945132, -228.1634219689893825 ) ) ;
#209643=DIRECTION ( 'NONE',  ( 0.000000000000000000, 0.3488585713686273571, 0.9371753822965264158 ) ) ;
#209658=CARTESIAN_POINT ( 'NONE',  ( -21.05000000000000071, 7.128833340093095217, -233.7327013124392749 ) ) ;
#209722=VERTEX_POINT ( 'NONE', #2753 ) ;
#209736=AXIS2_PLACEMENT_3D ( 'NONE', #12673, #110459, #28403 ) ;
#209738=CARTESIAN_POINT ( 'NONE',  ( -21.44999999999999929, 29.19585636832770703, -237.3287400596392445 ) ) ;
#209739=CARTESIAN_POINT ( 'NONE',  ( 20.94999999999999929, 33.13294339707397995, -247.6623911921324463 ) ) ;
#209744=CIRCLE ( 'NONE', #214020, 0.09999999999999986677 ) ;
#209761=AXIS2_PLACEMENT_3D ( 'NONE', #211779, #193504, #14874 ) ;
#209784=ORIENTED_EDGE ( 'NONE', *, *, #217702, .F. ) ;
#209804=DIRECTION ( 'NONE',  ( -0.000000000000000000, -0.8814952561688430555, 0.4721928772777346239 ) ) ;
#209833=LINE ( 'NONE', #168179, #32175 ) ;
#209850=CIRCLE ( 'NONE', #97371, 0.09999999999999939493 ) ;
#209888=EDGE_CURVE ( 'NONE', #35113, #12130, #186556, .T. ) ;
#209911=CARTESIAN_POINT ( 'NONE',  ( -20.54999999999999716, 25.30967299857549691, -243.4716794062925374 ) ) ;
#209913=ORIENTED_EDGE ( 'NONE', *, *, #121618, .T. ) ;
#209974=CARTESIAN_POINT ( 'NONE',  ( -21.07954763557448175, 1.580699497018342559, -230.6859858789673297 ) ) ;
#210000=AXIS2_PLACEMENT_3D ( 'NONE', #11245, #106454, #204289 ) ;
#210020=EDGE_CURVE ( 'NONE', #117081, #125245, #243280, .T. ) ;
#210025=DIRECTION ( 'NONE',  ( 0.000000000000000000, -0.8814952561688437216, 0.4721928772777331806 ) ) ;
#210028=ORIENTED_EDGE ( 'NONE', *, *, #133779, .T. ) ;
#210042=AXIS2_PLACEMENT_3D ( 'NONE', #176822, #257561, #132551 ) ;
#210083=ORIENTED_EDGE ( 'NONE', *, *, #230098, .T. ) ;
#210097=TOROIDAL_SURFACE ( 'NONE', #39422, 0.2000000000000000111, 0.1000000000000000056 ) ;
#210100=DIRECTION ( 'NONE',  ( -0.000000000000000000, 0.4721928772777345684, 0.8814952561688429444 ) ) ;
#210106=CARTESIAN_POINT ( 'NONE',  ( 22.59999999999999432, 12.61936297652653138, -223.3443501630868298 ) ) ;
#210112=DIRECTION ( 'NONE',  ( 1.000000000000000000, 0.000000000000000000, 0.000000000000000000 ) ) ;
#210176=ADVANCED_FACE ( 'NONE', ( #27201 ), #88393, .F. ) ;
#210179=CARTESIAN_POINT ( 'NONE',  ( 20.22483756094572271, 18.79053017939081016, -229.2002498143492346 ) ) ;
#210185=DIRECTION ( 'NONE',  ( -2.940209281316618057E-16, 0.4721928772777342354, 0.8814952561688433885 ) ) ;
#210189=EDGE_LOOP ( 'NONE', ( #236894, #197136, #4505, #70842 ) ) ;
#210210=DIRECTION ( 'NONE',  ( 1.000000000000000000, 0.000000000000000000, 0.000000000000000000 ) ) ;
#210227=DIRECTION ( 'NONE',  ( 1.000000000000000000, -0.000000000000000000, -0.000000000000000000 ) ) ;
#210230=CARTESIAN_POINT ( 'NONE',  ( -20.94999999999999929, 18.18127959618848877, -237.5711165786817389 ) ) ;
#210258=TOROIDAL_SURFACE ( 'NONE', #231114, 0.4000000000000003553, 0.1000000000000000056 ) ;
#210290=LINE ( 'NONE', #31672, #69652 ) ;
#210303=AXIS2_PLACEMENT_3D ( 'NONE', #191818, #32754, #112266 ) ;
#210307=CARTESIAN_POINT ( 'NONE',  ( 21.05000000000000071, 20.97908333644147660, -233.6079013178409411 ) ) ;
#210335=ORIENTED_EDGE ( 'NONE', *, *, #134734, .T. ) ;
#210336=ADVANCED_FACE ( 'NONE', ( #71447 ), #152272, .F. ) ;
#210436=DIRECTION ( 'NONE',  ( 1.000000000000000000, 0.000000000000000000, 0.000000000000000000 ) ) ;
#210475=CARTESIAN_POINT ( 'NONE',  ( -20.64999999999999858, 36.65892442174935439, -249.5511627012433848 ) ) ;
#210489=ORIENTED_EDGE ( 'NONE', *, *, #102572, .T. ) ;
#210518=ORIENTED_EDGE ( 'NONE', *, *, #135594, .F. ) ;
#210559=AXIS2_PLACEMENT_3D ( 'NONE', #53702, #133246, #92819 ) ;
#210578=ORIENTED_EDGE ( 'NONE', *, *, #128919, .T. ) ;
#210638=DIRECTION ( 'NONE',  ( -0.000000000000000000, 0.5474227397873200340, -0.8368562265788217491 ) ) ;
#210643=DIRECTION ( 'NONE',  ( 1.000000000000000000, 0.000000000000000000, 0.000000000000000000 ) ) ;
#210645=AXIS2_PLACEMENT_3D ( 'NONE', #43844, #82928, #141649 ) ;
#210662=EDGE_LOOP ( 'NONE', ( #206331, #191896, #158659, #73380, #25698, #51347, #52272, #143113, #208217, #135603, #216271, #45252 ) ) ;
#210666=CARTESIAN_POINT ( 'NONE',  ( 19.58285714285715073, 18.80841834337416074, -229.7621925467414883 ) ) ;
#210674=FACE_OUTER_BOUND ( 'NONE', #111973, .T. ) ;
#210695=CARTESIAN_POINT ( 'NONE',  ( -22.59999999999999787, -3.180729737797944434, -228.0957332317254895 ) ) ;
#210696=CARTESIAN_POINT ( 'NONE',  ( 23.25000000000000000, 23.68770167995059239, -252.8127582590406348 ) ) ;
#210710=AXIS2_PLACEMENT_3D ( 'NONE', #248691, #72641, #29672 ) ;
#210717=ORIENTED_EDGE ( 'NONE', *, *, #177318, .F. ) ;
#210720=EDGE_CURVE ( 'NONE', #137100, #251749, #106707, .T. ) ;
#210731=CARTESIAN_POINT ( 'NONE',  ( -20.00857864376270001, 22.24771505525269788, -231.4513824651465939 ) ) ;
#210732=EDGE_CURVE ( 'NONE', #254141, #13152, #147815, .T. ) ;
#210749=VERTEX_POINT ( 'NONE', #198753 ) ;
#210751=CARTESIAN_POINT ( 'NONE',  ( -22.39999999999999503, 0.2612980822699338401, -230.0539506776466681 ) ) ;
#210811=DIRECTION ( 'NONE',  ( 1.000000000000000000, 0.000000000000000000, 0.000000000000000000 ) ) ;
#210813=DIRECTION ( 'NONE',  ( -1.000000000000000000, 0.000000000000000000, 0.000000000000000000 ) ) ;
#210879=CARTESIAN_POINT ( 'NONE',  ( -20.94999999999999929, 13.66123737402873495, -238.6633470470287648 ) ) ;
#210951=ORIENTED_EDGE ( 'NONE', *, *, #78408, .F. ) ;
#210960=ORIENTED_EDGE ( 'NONE', *, *, #228413, .F. ) ;
#210965=AXIS2_PLACEMENT_3D ( 'NONE', #39941, #115592, #135139 ) ;
#210973=CYLINDRICAL_SURFACE ( 'NONE', #154444, 0.09999999999999568956 ) ;
#211021=CARTESIAN_POINT ( 'NONE',  ( 21.04999999999997229, 22.02795578261032716, -231.6498538120116280 ) ) ;
#211023=CARTESIAN_POINT ( 'NONE',  ( 20.95520789717937404, 18.80512403970892166, -227.9885191826238895 ) ) ;
#211049=FACE_OUTER_BOUND ( 'NONE', #24739, .T. ) ;
#211054=DIRECTION ( 'NONE',  ( -0.000000000000000000, 0.8814952561688430555, -0.4721928772777346239 ) ) ;
#211074=DIRECTION ( 'NONE',  ( 0.000000000000000000, -0.8814952561688430555, 0.4721928772777346239 ) ) ;
#211081=TOROIDAL_SURFACE ( 'NONE', #127703, 0.2000000000000000111, 0.1000000000000000056 ) ;
#211128=AXIS2_PLACEMENT_3D ( 'NONE', #86460, #143889, #181745 ) ;
#211136=ORIENTED_EDGE ( 'NONE', *, *, #86201, .T. ) ;
#211138=DIRECTION ( 'NONE',  ( 0.000000000000000000, 0.8814952561688429444, -0.4721928772777347350 ) ) ;
#211165=ORIENTED_EDGE ( 'NONE', *, *, #13213, .T. ) ;
#211172=EDGE_CURVE ( 'NONE', #140599, #59542, #222987, .T. ) ;
#211173=ORIENTED_EDGE ( 'NONE', *, *, #145877, .T. ) ;
#211187=CARTESIAN_POINT ( 'NONE',  ( -21.14999999999999858, 18.77629512215284535, -226.6423040988329092 ) ) ;
#211206=CARTESIAN_POINT ( 'NONE',  ( 21.14999999999999503, 12.67709964810648238, -223.3751320524553705 ) ) ;
#211217=CARTESIAN_POINT ( 'NONE',  ( -20.64999999999999858, 36.65892442174935439, -249.5511627012433848 ) ) ;
#211231=ORIENTED_EDGE ( 'NONE', *, *, #33807, .F. ) ;
#211256=DIRECTION ( 'NONE',  ( 0.000000000000000000, 0.8814952561688476074, -0.4721928772777262417 ) ) ;
#211277=PRODUCT_DEFINITION_FORMATION_WITH_SPECIFIED_SOURCE ( 'ANY', '', #249281, .NOT_KNOWN. ) ;
#211282=CARTESIAN_POINT ( 'NONE',  ( 20.94999999999999574, 16.50669723772569952, -240.7258389668962479 ) ) ;
#211326=DIRECTION ( 'NONE',  ( 0.000000000000000000, -0.8814952561688476074, 0.4721928772777262417 ) ) ;
#211339=ORIENTED_EDGE ( 'NONE', *, *, #171635, .T. ) ;
#211360=EDGE_CURVE ( 'NONE', #86653, #123093, #85771, .T. ) ;
#211370=CARTESIAN_POINT ( 'NONE',  ( 20.94999999999999929, 11.46684968301824625, -245.9610388612851750 ) ) ;
#211392=ORIENTED_EDGE ( 'NONE', *, *, #36718, .F. ) ;
#211393=DIRECTION ( 'NONE',  ( 0.000000000000000000, 0.8814952561688430555, -0.4721928772777346239 ) ) ;
#211399=CYLINDRICAL_SURFACE ( 'NONE', #239802, 0.5000000000000008882 ) ;
#211404=AXIS2_PLACEMENT_3D ( 'NONE', #148483, #182488, #28587 ) ;
#211433=DIRECTION ( 'NONE',  ( 0.000000000000000000, 0.8814952561688430555, -0.4721928772777346239 ) ) ;
#211434=VERTEX_POINT ( 'NONE', #80405 ) ;
#211466=ORIENTED_EDGE ( 'NONE', *, *, #157825, .T. ) ;
#211476=ORIENTED_EDGE ( 'NONE', *, *, #49658, .T. ) ;
#211503=ADVANCED_FACE ( 'NONE', ( #119597 ), #44124, .F. ) ;
#211505=AXIS2_PLACEMENT_3D ( 'NONE', #49274, #204486, #246200 ) ;
#211507=ORIENTED_EDGE ( 'NONE', *, *, #147958, .T. ) ;
#211528=CARTESIAN_POINT ( 'NONE',  ( 22.42357213249528769, 10.66459267205035388, -226.9222596543260977 ) ) ;
#211531=CARTESIAN_POINT ( 'NONE',  ( 18.44208962362734638, 38.17972036805543468, -261.2023309164682701 ) ) ;
#211533=CARTESIAN_POINT ( 'NONE',  ( 18.49999999999999289, 33.90972941529384599, -236.3646070729083988 ) ) ;
#211549=EDGE_CURVE ( 'NONE', #239741, #67400, #209378, .T. ) ;
#211552=CARTESIAN_POINT ( 'NONE',  ( -21.05000000000000071, 18.26942912180536638, -237.6183358664095238 ) ) ;
#211555=ORIENTED_EDGE ( 'NONE', *, *, #134450, .T. ) ;
#211646=DIRECTION ( 'NONE',  ( 0.000000000000000000, 0.8814952561688444987, -0.4721928772777320149 ) ) ;
#211665=DIRECTION ( 'NONE',  ( 0.000000000000000000, -0.8814952561688430555, 0.4721928772777346239 ) ) ;
#211668=ORIENTED_EDGE ( 'NONE', *, *, #95798, .F. ) ;
#211730=CIRCLE ( 'NONE', #190897, 0.2000000000000027867 ) ;
#211755=AXIS2_PLACEMENT_3D ( 'NONE', #65094, #144613, #175767 ) ;
#211779=CARTESIAN_POINT ( 'NONE',  ( -22.39999999999999503, 10.71943444926882449, -226.8179467668883547 ) ) ;
#211787=DIRECTION ( 'NONE',  ( 1.000000000000000000, 0.000000000000000000, 0.000000000000000000 ) ) ;
#211822=CIRCLE ( 'NONE', #103630, 4.149999999999996803 ) ;
#211827=DIRECTION ( 'NONE',  ( 0.000000000000000000, 0.3343365196859449662, -0.9424537609900497381 ) ) ;
#211839=CIRCLE ( 'NONE', #178544, 0.09999999999999711897 ) ;
#211847=CIRCLE ( 'NONE', #132924, 12.87500000000000178 ) ;
#211848=ORIENTED_EDGE ( 'NONE', *, *, #181686, .T. ) ;
#211852=CARTESIAN_POINT ( 'NONE',  ( -18.59999999999999787, 23.34004772283014972, -229.2004250369967338 ) ) ;
#211869=AXIS2_PLACEMENT_3D ( 'NONE', #27344, #211074, #32471 ) ;
#211897=EDGE_LOOP ( 'NONE', ( #136082, #9673, #146829, #55989 ) ) ;
#211901=ADVANCED_FACE ( 'NONE', ( #123131 ), #143957, .T. ) ;
#211961=DIRECTION ( 'NONE',  ( -1.000000000000000000, -5.641646265808601873E-14, 4.044497296483820071E-14 ) ) ;
#211962=LINE ( 'NONE', #192385, #98778 ) ;
#211967=AXIS2_PLACEMENT_3D ( 'NONE', #156347, #38946, #57183 ) ;
#212004=CARTESIAN_POINT ( 'NONE',  ( 20.94999999999999929, 28.40523720341322544, -239.6697522603257937 ) ) ;
#212036=EDGE_LOOP ( 'NONE', ( #209365, #25207, #190131, #185183 ) ) ;
#212068=ORIENTED_EDGE ( 'NONE', *, *, #205268, .T. ) ;
#212080=AXIS2_PLACEMENT_3D ( 'NONE', #187598, #149756, #53196 ) ;
#212092=ORIENTED_EDGE ( 'NONE', *, *, #152698, .T. ) ;
#212106=FACE_OUTER_BOUND ( 'NONE', #83758, .T. ) ;
#212109=ORIENTED_EDGE ( 'NONE', *, *, #228544, .F. ) ;
#212136=ORIENTED_EDGE ( 'NONE', *, *, #248185, .F. ) ;
#212140=CARTESIAN_POINT ( 'NONE',  ( 21.14999999999999858, 12.37888392014804495, -249.8746333190754569 ) ) ;
#212169=EDGE_CURVE ( 'NONE', #119326, #207618, #19556, .T. ) ;
#212181=DIRECTION ( 'NONE',  ( 1.000000000000000000, 0.000000000000000000, 0.000000000000000000 ) ) ;
#212182=ORIENTED_EDGE ( 'NONE', *, *, #137221, .T. ) ;
#212195=CIRCLE ( 'NONE', #49854, 0.9750000000000036415 ) ;
#212223=CARTESIAN_POINT ( 'NONE',  ( -21.05000000000000071, 16.52766025697963315, -240.8672687545768270 ) ) ;
#212229=CARTESIAN_POINT ( 'NONE',  ( -21.00023020733437562, 10.14655627732183873, -228.0991803899404431 ) ) ;
#212233=CARTESIAN_POINT ( 'NONE',  ( -21.12642695952773764, 10.05219176827227123, -228.0658859103580767 ) ) ;
#212258=EDGE_CURVE ( 'NONE', #62371, #138714, #2778, .T. ) ;
#212272=DIRECTION ( 'NONE',  ( 0.000000000000000000, -0.4721928772777334582, -0.8814952561688437216 ) ) ;
#212297=ADVANCED_FACE ( 'NONE', ( #192801 ), #211081, .T. ) ;
#212310=CYLINDRICAL_SURFACE ( 'NONE', #94634, 0.09999999999999939493 ) ;
#212330=EDGE_CURVE ( 'NONE', #34617, #227159, #137932, .T. ) ;
#212333=CARTESIAN_POINT ( 'NONE',  ( -20.64999999999999858, 21.30332930069722863, -233.2143729774842882 ) ) ;
#212356=CARTESIAN_POINT ( 'NONE',  ( 20.85000000000000142, 42.96960653111219131, -254.4772109693542745 ) ) ;
#212379=AXIS2_PLACEMENT_3D ( 'NONE', #31151, #72832, #248878 ) ;
#212382=CIRCLE ( 'NONE', #116675, 0.1000000000000076522 ) ;
#212389=DIRECTION ( 'NONE',  ( 0.000000000000000000, -0.8814952561688429444, 0.4721928772777349570 ) ) ;
#212403=DIRECTION ( 'NONE',  ( 0.000000000000000000, 0.4721928772777346239, 0.8814952561688430555 ) ) ;
#212422=LINE ( 'NONE', #175866, #74343 ) ;
#212451=EDGE_CURVE ( 'NONE', #54600, #114424, #107195, .T. ) ;
#212458=CARTESIAN_POINT ( 'NONE',  ( -18.50000000000000000, 43.18640298906419162, -245.2812653309023574 ) ) ;
#212495=VERTEX_POINT ( 'NONE', #222591 ) ;
#212501=EDGE_CURVE ( 'NONE', #156710, #72605, #2953, .T. ) ;
#212507=ADVANCED_FACE ( 'NONE', ( #103925 ), #40613, .F. ) ;
#212516=DIRECTION ( 'NONE',  ( 1.000000000000000000, 0.000000000000000000, 0.000000000000000000 ) ) ;
#212593=ORIENTED_EDGE ( 'NONE', *, *, #81811, .T. ) ;
#212630=ADVANCED_FACE ( 'NONE', ( #225160 ), #69631, .F. ) ;
#212668=CARTESIAN_POINT ( 'NONE',  ( 22.60000000000000142, 12.58798907299599179, -223.3278890275437050 ) ) ;
#212701=CARTESIAN_POINT ( 'NONE',  ( 21.12400247839537926, 22.98976051637114182, -230.0661232092074329 ) ) ;
#212716=ADVANCED_FACE ( 'NONE', ( #97178 ), #13848, .F. ) ;
#212767=EDGE_LOOP ( 'NONE', ( #239705, #234854, #97040, #170113 ) ) ;
#212774=EDGE_CURVE ( 'NONE', #35062, #182351, #119900, .T. ) ;
#212800=ORIENTED_EDGE ( 'NONE', *, *, #116414, .T. ) ;
#212801=EDGE_CURVE ( 'NONE', #120394, #209230, #78918, .T. ) ;
#212824=AXIS2_PLACEMENT_3D ( 'NONE', #85813, #31053, #107986 ) ;
#212841=AXIS2_PLACEMENT_3D ( 'NONE', #226482, #90830, #110402 ) ;
#212855=DIRECTION ( 'NONE',  ( 1.000000000000000000, 0.000000000000000000, 0.000000000000000000 ) ) ;
#212856=AXIS2_PLACEMENT_3D ( 'NONE', #88183, #47783, #43953 ) ;
#212875=ORIENTED_EDGE ( 'NONE', *, *, #175002, .F. ) ;
#212899=CARTESIAN_POINT ( 'NONE',  ( 18.59999999999999076, 18.18127959618848166, -237.5711165786817389 ) ) ;
#212903=VECTOR ( 'NONE', #239846, 1000.000000000000000 ) ;
#212905=ORIENTED_EDGE ( 'NONE', *, *, #114913, .F. ) ;
#212913=DIRECTION ( 'NONE',  ( -0.000000000000000000, -0.8814952561688430555, 0.4721928772777346239 ) ) ;
#212915=CARTESIAN_POINT ( 'NONE',  ( -20.54999999999999716, 30.27561093622783517, -235.5248193094124645 ) ) ;
#212926=AXIS2_PLACEMENT_3D ( 'NONE', #112852, #192391, #172874 ) ;
#212956=DIRECTION ( 'NONE',  ( -0.000000000000000000, 0.7280513885559045661, -0.6855225566105168644 ) ) ;
#212966=CARTESIAN_POINT ( 'NONE',  ( -23.15000000000000213, 34.80778438379478246, -248.5595576589601592 ) ) ;
#213037=ORIENTED_EDGE ( 'NONE', *, *, #125107, .F. ) ;
#213043=DIRECTION ( 'NONE',  ( 2.465190328815661345E-32, -0.8814952561688430555, 0.4721928772777344574 ) ) ;
#213064=ORIENTED_EDGE ( 'NONE', *, *, #11494, .F. ) ;
#213072=VERTEX_POINT ( 'NONE', #111356 ) ;
#213128=CARTESIAN_POINT ( 'NONE',  ( -23.25000000000000000, 46.46967969402478360, -243.0849751855955674 ) ) ;
#213129=( BOUNDED_SURFACE ( )  B_SPLINE_SURFACE ( 3, 2, ( 
 ( #21922, #25761, #102699 ),
 ( #3617, #66171, #122298 ),
 ( #199273, #200544, #63597 ),
 ( #83122, #105253, #204383 ),
 ( #165268, #201828, #243520 ),
 ( #163997, #183558, #184824 ) ),
 .UNSPECIFIED., .F., .F., .F. ) 
 B_SPLINE_SURFACE_WITH_KNOTS ( ( 4, 2, 4 ),
 ( 3, 3 ),
 ( -1.776356839400250465E-15, 0.7853981633974468357, 1.570796326794895448 ),
 ( 0.000000000000000000, 1.000000000000000000 ),
 .UNSPECIFIED. ) 
 GEOMETRIC_REPRESENTATION_ITEM ( )  RATIONAL_B_SPLINE_SURFACE ( (
 ( 1.000000000000000000, 0.4999999999999739098, 1.000000000000000000),
 ( 1.000000000000000000, 0.4993418825349509316, 1.000000000000000000),
 ( 1.000000000000000000, 0.5278258667037128982, 1.000000000000000000),
 ( 1.000000000000000000, 0.6092287576717151376, 1.000000000000000000),
 ( 1.000000000000000000, 0.6611148371763631015, 1.000000000000000000),
 ( 1.000000000000000000, 0.7071067811864732988, 1.000000000000000000) ) ) 
 REPRESENTATION_ITEM ( '' )  SURFACE ( )  );
#213138=CARTESIAN_POINT ( 'NONE',  ( -18.59999999999999787, 14.81796439977981272, -236.5325475414793743 ) ) ;
#213140=DIRECTION ( 'NONE',  ( 0.000000000000000000, 0.8814952561688438326, -0.4721928772777334582 ) ) ;
#213146=FACE_OUTER_BOUND ( 'NONE', #240343, .T. ) ;
#213175=ORIENTED_EDGE ( 'NONE', *, *, #130555, .T. ) ;
#213207=DIRECTION ( 'NONE',  ( 1.000000000000000000, 0.000000000000000000, 0.000000000000000000 ) ) ;
#213223=CARTESIAN_POINT ( 'NONE',  ( -22.50000000000000000, -3.140208063160686791, -228.2318569537739847 ) ) ;
#213245=DIRECTION ( 'NONE',  ( -1.000000000000000000, 0.000000000000000000, 0.000000000000000000 ) ) ;
#213252=CARTESIAN_POINT ( 'NONE',  ( -22.57848426163147693, -3.230800903051896267, -228.1881664583613656 ) ) ;
#213253=CARTESIAN_POINT ( 'NONE',  ( 21.04999999999908411, 21.99007072299442100, -231.7373276070881616 ) ) ;
#213265=ORIENTED_EDGE ( 'NONE', *, *, #251922, .F. ) ;
#213267=DIRECTION ( 'NONE',  ( 0.000000000000000000, -0.8814952561688430555, 0.4721928772777346239 ) ) ;
#213275=VERTEX_POINT ( 'NONE', #109752 ) ;
#213282=CIRCLE ( 'NONE', #204916, 0.1000000000000013933 ) ;
#213353=EDGE_CURVE ( 'NONE', #65641, #88893, #49315, .T. ) ;
#213363=ORIENTED_EDGE ( 'NONE', *, *, #196337, .F. ) ;
#213364=CARTESIAN_POINT ( 'NONE',  ( 21.05000000000000071, 34.89593390941166007, -248.6067769466879156 ) ) ;
#213370=ADVANCED_FACE ( 'NONE', ( #14545 ), #49115, .T. ) ;
#213392=EDGE_LOOP ( 'NONE', ( #120914, #5555, #140211, #64959 ) ) ;
#213394=DIRECTION ( 'NONE',  ( -0.000000000000000000, 0.4721928772777346239, 0.8814952561688430555 ) ) ;
#213397=CARTESIAN_POINT ( 'NONE',  ( 20.94999999999999929, 45.93315328338058379, -256.6017782078560003 ) ) ;
#213477=ORIENTED_EDGE ( 'NONE', *, *, #6850, .T. ) ;
#213484=CARTESIAN_POINT ( 'NONE',  ( 22.45301702632625762, -3.133220771888840073, -228.2183440840713047 ) ) ;
#213485=CARTESIAN_POINT ( 'NONE',  ( 20.94999999999999929, 23.45160524131172153, -253.2535058871250726 ) ) ;
#213511=ORIENTED_EDGE ( 'NONE', *, *, #143561, .F. ) ;
#213530=CARTESIAN_POINT ( 'NONE',  ( 21.53699400380535423, 10.33394250185612684, -227.7493655665005576 ) ) ;
#213544=EDGE_CURVE ( 'NONE', #257030, #225564, #196991, .T. ) ;
#213557=DIRECTION ( 'NONE',  ( 2.715809747126120452E-16, -0.4721928772777324035, -0.8814952561688441657 ) ) ;
#213559=ORIENTED_EDGE ( 'NONE', *, *, #116741, .T. ) ;
#213585=DIRECTION ( 'NONE',  ( 2.915501640297155269E-16, -0.4721928772777346239, -0.8814952561688430555 ) ) ;
#213603=VECTOR ( 'NONE', #215150, 1000.000000000000000 ) ;
#213618=ORIENTED_EDGE ( 'NONE', *, *, #13213, .F. ) ;
#213625=EDGE_CURVE ( 'NONE', #62371, #89738, #16200, .T. ) ;
#213630=FACE_OUTER_BOUND ( 'NONE', #113137, .T. ) ;
#213677=ORIENTED_EDGE ( 'NONE', *, *, #151648, .T. ) ;
#213716=CARTESIAN_POINT ( 'NONE',  ( 20.89192007715127986, 46.45729338110133710, -243.0823073233429170 ) ) ;
#213723=ORIENTED_EDGE ( 'NONE', *, *, #34338, .T. ) ;
#213724=EDGE_CURVE ( 'NONE', #97226, #253940, #118116, .T. ) ;
#213746=CARTESIAN_POINT ( 'NONE',  ( -23.15000000000000213, 27.86742726211138788, -240.0204451158735708 ) ) ;
#213748=ORIENTED_EDGE ( 'NONE', *, *, #46197, .F. ) ;
#213774=DIRECTION ( 'NONE',  ( -0.000000000000000000, -0.4721928772777351790, -0.8814952561688427224 ) ) ;
#213779=ORIENTED_EDGE ( 'NONE', *, *, #116491, .F. ) ;
#213830=FACE_OUTER_BOUND ( 'NONE', #181935, .T. ) ;
#213843=VERTEX_POINT ( 'NONE', #137655 ) ;
#213862=EDGE_CURVE ( 'NONE', #44729, #17866, #223876, .T. ) ;
#213902=ORIENTED_EDGE ( 'NONE', *, *, #88581, .T. ) ;
#213967=CARTESIAN_POINT ( 'NONE',  ( -20.85000000000000142, 43.62273694548321856, -253.2814864317374770 ) ) ;
#213977=CARTESIAN_POINT ( 'NONE',  ( 20.94999999999999929, 28.08470566095357057, -239.2860081655328770 ) ) ;
#213979=CARTESIAN_POINT ( 'NONE',  ( 21.08804281139617487, 23.03085422597683163, -230.2011867825314653 ) ) ;
#213980=CARTESIAN_POINT ( 'NONE',  ( -20.64999999999999858, 11.41170713998152841, -246.6906184681487559 ) ) ;
#213981=ORIENTED_EDGE ( 'NONE', *, *, #179161, .T. ) ;
#213986=DIRECTION ( 'NONE',  ( 0.000000000000000000, 0.8814952561688434995, -0.4721928772777335137 ) ) ;
#214001=VECTOR ( 'NONE', #147040, 1000.000000000000114 ) ;
#214020=AXIS2_PLACEMENT_3D ( 'NONE', #125841, #202821, #28070 ) ;
#214024=CARTESIAN_POINT ( 'NONE',  ( 20.86036036209913647, 18.90186385150083836, -227.9902976072726233 ) ) ;
#214025=EDGE_LOOP ( 'NONE', ( #142974, #40890, #135384, #158517 ) ) ;
#214030=ADVANCED_FACE ( 'NONE', ( #106230 ), #136976, .T. ) ;
#214052=CARTESIAN_POINT ( 'NONE',  ( -21.05000000000000071, 36.65892442174935439, -249.5511627012433848 ) ) ;
#214068=EDGE_CURVE ( 'NONE', #19594, #167556, #103067, .T. ) ;
#214074=VECTOR ( 'NONE', #167020, 1000.000000000000000 ) ;
#214076=EDGE_CURVE ( 'NONE', #94319, #257480, #233991, .T. ) ;
#214117=CARTESIAN_POINT ( 'NONE',  ( -22.59999999999999787, -3.092988775432913506, -228.1437074281570858 ) ) ;
#214125=CARTESIAN_POINT ( 'NONE',  ( 18.60000000000001563, 9.036467987174443550, -245.3776959182873156 ) ) ;
#214186=EDGE_CURVE ( 'NONE', #109477, #212495, #45397, .T. ) ;
#214195=CARTESIAN_POINT ( 'NONE',  ( -18.59999999999999787, 30.22839164850006455, -235.6129688350293350 ) ) ;
#214219=CARTESIAN_POINT ( 'NONE',  ( -18.50000000000000000, 43.35377423437995503, -245.1717807829448930 ) ) ;
#214241=CARTESIAN_POINT ( 'NONE',  ( 20.94999999999999929, 16.44800918141279666, -240.8068063186265135 ) ) ;
#214260=CARTESIAN_POINT ( 'NONE',  ( -20.94999999999999929, 18.18127959618848521, -237.5711165786817389 ) ) ;
#214299=CIRCLE ( 'NONE', #139443, 0.1999999999999966804 ) ;
#214308=CARTESIAN_POINT ( 'NONE',  ( -22.48660254037843487, 12.58580559757028183, -223.4396719342083770 ) ) ;
#214320=ADVANCED_FACE ( 'NONE', ( #100768 ), #40876, .F. ) ;
#214345=DIRECTION ( 'NONE',  ( 8.673617379884085959E-15, -0.8814952561688430555, 0.4721928772777346239 ) ) ;
#214355=CARTESIAN_POINT ( 'NONE',  ( 20.12500000000000000, 30.46448808713892831, -235.1722212069449256 ) ) ;
#214369=ORIENTED_EDGE ( 'NONE', *, *, #200290, .F. ) ;
#214405=VECTOR ( 'NONE', #187423, 1000.000000000000000 ) ;
#214407=AXIS2_PLACEMENT_3D ( 'NONE', #45923, #122908, #4216 ) ;
#214424=DIRECTION ( 'NONE',  ( 0.000000000000000000, 0.4721928772777343464, 0.8814952561688431665 ) ) ;
#214456=CARTESIAN_POINT ( 'NONE',  ( -20.94999999999999929, 36.65892442174935439, -249.5511627012433848 ) ) ;
#214463=AXIS2_PLACEMENT_3D ( 'NONE', #242145, #186032, #42665 ) ;
#214475=CARTESIAN_POINT ( 'NONE',  ( -20.94999999999999929, 36.65892442174935439, -249.5511627012433848 ) ) ;
#214476=AXIS2_PLACEMENT_3D ( 'NONE', #232851, #54181, #11221 ) ;
#214484=AXIS2_PLACEMENT_3D ( 'NONE', #103928, #220059, #43984 ) ;
#214510=EDGE_CURVE ( 'NONE', #25443, #2987, #157479, .T. ) ;
#214511=CIRCLE ( 'NONE', #185485, 0.1000000000000081657 ) ;
#214515=AXIS2_PLACEMENT_3D ( 'NONE', #6821, #4234, #47210 ) ;
#214534=ORIENTED_EDGE ( 'NONE', *, *, #157397, .F. ) ;
#214542=DIRECTION ( 'NONE',  ( 1.000000000000000000, 0.000000000000000000, 0.000000000000000000 ) ) ;
#214570=CARTESIAN_POINT ( 'NONE',  ( -23.25000000000000000, 35.97645343225766368, -235.9694016464868298 ) ) ;
#214574=DIRECTION ( 'NONE',  ( 1.000000000000000000, 0.000000000000000000, 0.000000000000000000 ) ) ;
#214579=DIRECTION ( 'NONE',  ( 0.000000000000000000, 0.8814952561688476074, -0.4721928772777262417 ) ) ;
#214587=CARTESIAN_POINT ( 'NONE',  ( 22.50000000000000000, 10.70017861337865916, -226.8538937894029743 ) ) ;
#214614=EDGE_CURVE ( 'NONE', #42982, #34543, #171113, .T. ) ;
#214626=FACE_OUTER_BOUND ( 'NONE', #44936, .T. ) ;
#214627=AXIS2_PLACEMENT_3D ( 'NONE', #257896, #240959, #42754 ) ;
#214659=FACE_OUTER_BOUND ( 'NONE', #252498, .T. ) ;
#214663=DIRECTION ( 'NONE',  ( 0.000000000000000000, -0.4721928772777346239, -0.8814952561688430555 ) ) ;
#214668=CARTESIAN_POINT ( 'NONE',  ( -22.50000000000088463, -3.119615478075010717, -228.1914279391694720 ) ) ;
#214670=CARTESIAN_POINT ( 'NONE',  ( 21.04999999999958149, 10.11149931895240606, -228.1331641884628141 ) ) ;
#214675=DIRECTION ( 'NONE',  ( 0.000000000000000000, -0.8814952561688430555, 0.4721928772777346239 ) ) ;
#214687=DIRECTION ( 'NONE',  ( 0.000000000000000000, 0.4859085964047519801, 0.8740096314915323239 ) ) ;
#214701=VERTEX_POINT ( 'NONE', #78368 ) ;
#214704=ADVANCED_FACE ( 'NONE', ( #43112 ), #121401, .F. ) ;
#214731=DIRECTION ( 'NONE',  ( -1.000000000000000000, -0.000000000000000000, -0.000000000000000000 ) ) ;
#214733=CARTESIAN_POINT ( 'NONE',  ( 23.14999999999999503, 23.34004772283015683, -229.2004250369967338 ) ) ;
#214741=VECTOR ( 'NONE', #99954, 1000.000000000000000 ) ;
#214746=CARTESIAN_POINT ( 'NONE',  ( 23.15000000000000213, 28.56975825374500388, -258.1421690862028413 ) ) ;
#214788=ADVANCED_FACE ( 'NONE', ( #99203 ), #90986, .F. ) ;
#214842=VERTEX_POINT ( 'NONE', #164350 ) ;
#214845=EDGE_CURVE ( 'NONE', #65949, #146046, #20267, .T. ) ;
#214854=FACE_OUTER_BOUND ( 'NONE', #113722, .T. ) ;
#214857=CARTESIAN_POINT ( 'NONE',  ( 23.15000000000000213, 28.42524210734032408, -258.3567845160494585 ) ) ;
#214866=DIRECTION ( 'NONE',  ( -1.000000000000000000, 0.000000000000000000, 0.000000000000000000 ) ) ;
#214875=AXIS2_PLACEMENT_3D ( 'NONE', #110716, #190267, #93717 ) ;
#214883=EDGE_CURVE ( 'NONE', #183016, #159861, #69105, .T. ) ;
#214917=CARTESIAN_POINT ( 'NONE',  ( -20.94999999999999929, 4.184122562697133674, -245.3714803909117279 ) ) ;
#214931=CARTESIAN_POINT ( 'NONE',  ( -18.59999999999999787, 13.71992543034163958, -238.5823796952984992 ) ) ;
#214939=B_SPLINE_CURVE_WITH_KNOTS ( 'NONE', 3,
 ( #237041, #60956, #177092, #199200, #256539, #79222, #40153, #100061 ),
 .UNSPECIFIED., .F., .F.,
 ( 4, 2, 2, 4 ),
 ( 0.000000000000000000, 0.0002181133598168967676, 0.0003271700397253451379, 0.0004362267196337935352 ),
 .UNSPECIFIED. ) ;
#214973=CARTESIAN_POINT ( 'NONE',  ( 23.14999999999999503, 31.44980407958351876, -233.5445995079518582 ) ) ;
#214987=ORIENTED_EDGE ( 'NONE', *, *, #100831, .T. ) ;
#215008=DIRECTION ( 'NONE',  ( 0.000000000000000000, 0.8814952561688444987, -0.4721928772777320149 ) ) ;
#215018=AXIS2_PLACEMENT_3D ( 'NONE', #238323, #200491, #180930 ) ;
#215045=VERTEX_POINT ( 'NONE', #254126 ) ;
#215052=ORIENTED_EDGE ( 'NONE', *, *, #212774, .T. ) ;
#215056=ORIENTED_EDGE ( 'NONE', *, *, #120297, .F. ) ;
#215061=DIRECTION ( 'NONE',  ( 1.000000000000000000, 0.000000000000000000, 0.000000000000000000 ) ) ;
#215064=FACE_OUTER_BOUND ( 'NONE', #160880, .T. ) ;
#215097=EDGE_CURVE ( 'NONE', #170728, #64541, #241007, .T. ) ;
#215111=CYLINDRICAL_SURFACE ( 'NONE', #216836, 0.09999999999999216460 ) ;
#215150=DIRECTION ( 'NONE',  ( -0.000000000000000000, 0.8096735173027155286, -0.5868805631290315850 ) ) ;
#215154=ORIENTED_EDGE ( 'NONE', *, *, #71512, .F. ) ;
#215171=EDGE_CURVE ( 'NONE', #50106, #257602, #112037, .T. ) ;
#215190=ORIENTED_EDGE ( 'NONE', *, *, #86016, .T. ) ;
#215230=DIRECTION ( 'NONE',  ( 0.000000000000000000, 0.8814952561688437216, -0.4721928772777334582 ) ) ;
#215238=DIRECTION ( 'NONE',  ( 0.000000000000000000, 0.8814952561688437216, -0.4721928772777334582 ) ) ;
#215241=ORIENTED_EDGE ( 'NONE', *, *, #208484, .F. ) ;
#215254=AXIS2_PLACEMENT_3D ( 'NONE', #246202, #49275, #247479 ) ;
#215257=ORIENTED_EDGE ( 'NONE', *, *, #34728, .T. ) ;
#215258=CARTESIAN_POINT ( 'NONE',  ( 18.59999999999999076, 33.89981536720673461, -236.1713368690715527 ) ) ;
#215263=ORIENTED_EDGE ( 'NONE', *, *, #10618, .F. ) ;
#215264=AXIS2_PLACEMENT_3D ( 'NONE', #189050, #169530, #91241 ) ;
#215274=CARTESIAN_POINT ( 'NONE',  ( 21.05000000000000071, 28.43730376342110944, -239.4748853164439879 ) ) ;
#215296=CARTESIAN_POINT ( 'NONE',  ( 20.59588692710267921, 18.75868443233201077, -228.1998404859263303 ) ) ;
#215305=EDGE_CURVE ( 'NONE', #105344, #148418, #91174, .T. ) ;
#215306=CARTESIAN_POINT ( 'NONE',  ( 20.94999999999999929, 18.18127959618848877, -237.5711165786817389 ) ) ;
#215323=ORIENTED_EDGE ( 'NONE', *, *, #158474, .F. ) ;
#215335=EDGE_CURVE ( 'NONE', #26083, #1255, #161930, .T. ) ;
#215360=ORIENTED_EDGE ( 'NONE', *, *, #118099, .F. ) ;
#215362=CARTESIAN_POINT ( 'NONE',  ( 18.49999999999999289, 33.78452921692649369, -236.3958672130747800 ) ) ;
#215401=FACE_OUTER_BOUND ( 'NONE', #163621, .T. ) ;
#215405=DIRECTION ( 'NONE',  ( 0.000000000000000000, -0.8454177738465953329, -0.5341055959866617409 ) ) ;
#215408=CARTESIAN_POINT ( 'NONE',  ( 21.05000000000000071, 34.10258817885969052, -248.1818033571379658 ) ) ;
#215489=CARTESIAN_POINT ( 'NONE',  ( -21.05000000000000071, 1.316055977212913009, -230.7323992127457473 ) ) ;
#215537=AXIS2_PLACEMENT_3D ( 'NONE', #140815, #198211, #62565 ) ;
#215539=ORIENTED_EDGE ( 'NONE', *, *, #115460, .F. ) ;
#215546=CIRCLE ( 'NONE', #157125, 3.900000000000020783 ) ;
#215551=EDGE_CURVE ( 'NONE', #227951, #41664, #200158, .T. ) ;
#215573=AXIS2_PLACEMENT_3D ( 'NONE', #20737, #221457, #123677 ) ;
#215585=CARTESIAN_POINT ( 'NONE',  ( 18.59999999999999432, 13.63177590472475487, -238.5351604075707144 ) ) ;
#215598=EDGE_CURVE ( 'NONE', #149301, #35579, #241841, .T. ) ;
#215617=EDGE_LOOP ( 'NONE', ( #170807, #10956, #157901, #149790 ) ) ;
#215619=CARTESIAN_POINT ( 'NONE',  ( 21.05000000000000071, 28.52545328903799415, -239.5221046041717443 ) ) ;
#215624=CARTESIAN_POINT ( 'NONE',  ( -18.33981767444368671, 38.15129771152390248, -261.2066580151159769 ) ) ;
#215660=DIRECTION ( 'NONE',  ( 0.000000000000000000, -0.8814952561688430555, 0.4721928772777346239 ) ) ;
#215667=CARTESIAN_POINT ( 'NONE',  ( 22.39999999999999858, 7.128833340093095217, -233.7327013124392749 ) ) ;
#215682=CYLINDRICAL_SURFACE ( 'NONE', #24537, 0.1000000000000013933 ) ;
#215698=FACE_OUTER_BOUND ( 'NONE', #122041, .T. ) ;
#215699=AXIS2_PLACEMENT_3D ( 'NONE', #53648, #194469, #229717 ) ;
#215720=AXIS2_PLACEMENT_3D ( 'NONE', #58320, #2206, #20528 ) ;
#215729=CIRCLE ( 'NONE', #115791, 0.2000000000000027867 ) ;
#215750=EDGE_LOOP ( 'NONE', ( #209348, #221586, #23595, #137435, #25725, #150750, #104353, #110956, #70148, #204000, #96378, #91607, #221403, #112284, #98163, #244901, #36099, #111660, #196235, #229225, #153477, #18342, #20398, #250010, #257278 ) ) ;
#215751=EDGE_LOOP ( 'NONE', ( #158691, #213175, #179375 ) ) ;
#215788=CARTESIAN_POINT ( 'NONE',  ( 23.15000000000000213, 28.37802281961254991, -258.4449340416662722 ) ) ;
#215794=CARTESIAN_POINT ( 'NONE',  ( -21.14999999999999858, 18.60615189616458309, -226.5511630304420976 ) ) ;
#215802=CARTESIAN_POINT ( 'NONE',  ( -18.59999999999999787, 36.65892442174935439, -249.5511627012433848 ) ) ;
#215808=EDGE_LOOP ( 'NONE', ( #166371, #190766, #200511, #168208 ) ) ;
#215819=VECTOR ( 'NONE', #207501, 1000.000000000000000 ) ;
#215850=FACE_OUTER_BOUND ( 'NONE', #1632, .T. ) ;
#215863=VECTOR ( 'NONE', #131934, 1000.000000000000000 ) ;
#215870=DIRECTION ( 'NONE',  ( 0.000000000000000000, -0.3488585713686311318, -0.9371753822965249725 ) ) ;
#215891=EDGE_CURVE ( 'NONE', #41254, #201767, #146166, .T. ) ;
#215909=AXIS2_PLACEMENT_3D ( 'NONE', #35613, #98081, #96799 ) ;
#215922=ORIENTED_EDGE ( 'NONE', *, *, #252970, .T. ) ;
#215923=DIRECTION ( 'NONE',  ( 0.000000000000000000, 0.9698110461157734008, 0.2438576117980102709 ) ) ;
#215933=CARTESIAN_POINT ( 'NONE',  ( -18.54159361262961525, 8.874177542791873208, -245.4029526999691200 ) ) ;
#215938=CARTESIAN_POINT ( 'NONE',  ( 20.85000000000000142, 36.22724532936083364, -235.9903003947922286 ) ) ;
#215957=CARTESIAN_POINT ( 'NONE',  ( 18.49999999999999289, 28.81810206650552075, -238.0339362645743222 ) ) ;
#215969=DIRECTION ( 'NONE',  ( 0.000000000000000000, 0.8814952561688444987, -0.4721928772777320149 ) ) ;
#216031=DIRECTION ( 'NONE',  ( 0.000000000000000000, 0.8814952561688476074, -0.4721928772777262417 ) ) ;
#216064=CARTESIAN_POINT ( 'NONE',  ( 20.94999999999999929, 34.10258817885969052, -248.1818033571379658 ) ) ;
#216073=ORIENTED_EDGE ( 'NONE', *, *, #34551, .F. ) ;
#216101=CONICAL_SURFACE ( 'NONE', #166257, 4.049999999999996270, 0.7853981633974604915 ) ;
#216150=EDGE_CURVE ( 'NONE', #147651, #237661, #90848, .T. ) ;
#216156=ADVANCED_FACE ( 'NONE', ( #212106 ), #251199, .F. ) ;
#216185=DIRECTION ( 'NONE',  ( -1.000000000000000000, -0.000000000000000000, -0.000000000000000000 ) ) ;
#216191=CARTESIAN_POINT ( 'NONE',  ( -23.25000000000000000, 28.37802281961254636, -258.4449340416662722 ) ) ;
#216206=VERTEX_POINT ( 'NONE', #153451 ) ;
#216219=ORIENTED_EDGE ( 'NONE', *, *, #217790, .T. ) ;
#216221=DIRECTION ( 'NONE',  ( 0.000000000000000000, -0.8814952561688476074, 0.4721928772777262417 ) ) ;
#216234=CARTESIAN_POINT ( 'NONE',  ( 23.14999999999999858, 36.65892442174935439, -249.5511627012433848 ) ) ;
#216244=CARTESIAN_POINT ( 'NONE',  ( 23.14999999999999503, 35.97645343225767789, -235.9694016464868298 ) ) ;
#216270=ORIENTED_EDGE ( 'NONE', *, *, #19477, .F. ) ;
#216271=ORIENTED_EDGE ( 'NONE', *, *, #235354, .F. ) ;
#216324=EDGE_CURVE ( 'NONE', #218203, #59200, #176672, .T. ) ;
#216345=AXIS2_PLACEMENT_3D ( 'NONE', #226690, #31109, #166765 ) ;
#216374=AXIS2_PLACEMENT_3D ( 'NONE', #28291, #45249, #161362 ) ;
#216377=ORIENTED_EDGE ( 'NONE', *, *, #253740, .T. ) ;
#216388=CARTESIAN_POINT ( 'NONE',  ( 18.49999999999999289, 2.272311100394801109, -217.9150152700588592 ) ) ;
#216389=DIRECTION ( 'NONE',  ( -0.000000000000000000, -0.8814952561688430555, 0.4721928772777346239 ) ) ;
#216393=AXIS2_PLACEMENT_3D ( 'NONE', #134981, #109010, #188560 ) ;
#216455=DIRECTION ( 'NONE',  ( 0.000000000000000000, 0.8814952561688433885, -0.4721928772777338468 ) ) ;
#216461=EDGE_CURVE ( 'NONE', #248473, #253739, #151112, .T. ) ;
#216481=DIRECTION ( 'NONE',  ( 1.000000000000000000, -0.000000000000000000, -0.000000000000000000 ) ) ;
#216497=ORIENTED_EDGE ( 'NONE', *, *, #154248, .F. ) ;
#216532=FACE_OUTER_BOUND ( 'NONE', #137233, .T. ) ;
#216535=CARTESIAN_POINT ( 'NONE',  ( 21.04116576186301302, 23.01330991368982382, -230.1885797082096303 ) ) ;
#216546=LINE ( 'NONE', #233561, #144362 ) ;
#216562=CARTESIAN_POINT ( 'NONE',  ( -20.85000000000000142, 43.30036367478129478, -245.0872390055602352 ) ) ;
#216579=ORIENTED_EDGE ( 'NONE', *, *, #104260, .T. ) ;
#216658=B_SPLINE_CURVE_WITH_KNOTS ( 'NONE', 3,
 ( #105101, #221218, #201668, #3461, #184668, #47718, #43887 ),
 .UNSPECIFIED., .F., .F.,
 ( 4, 3, 4 ),
 ( 0.000000000000000000, 0.0007844235214594253575, 0.001767853679404338563 ),
 .UNSPECIFIED. ) ;
#216694=DIRECTION ( 'NONE',  ( 0.000000000000000000, -0.4721928772777346239, -0.8814952561688430555 ) ) ;
#216704=CYLINDRICAL_SURFACE ( 'NONE', #194123, 0.09999999999999939493 ) ;
#216738=EDGE_LOOP ( 'NONE', ( #30600, #53822 ) ) ;
#216755=DIRECTION ( 'NONE',  ( 1.000000000000000000, 0.000000000000000000, 0.000000000000000000 ) ) ;
#216779=LINE ( 'NONE', #38167, #84337 ) ;
#216791=AXIS2_PLACEMENT_3D ( 'NONE', #106393, #185956, #167704 ) ;
#216812=VERTEX_POINT ( 'NONE', #212458 ) ;
#216836=AXIS2_PLACEMENT_3D ( 'NONE', #254218, #79431, #59861 ) ;
#216838=EDGE_CURVE ( 'NONE', #180293, #193873, #13919, .T. ) ;
#216860=DIRECTION ( 'NONE',  ( 0.000000000000000000, 0.8814952561688429444, -0.4721928772777345684 ) ) ;
#216872=CARTESIAN_POINT ( 'NONE',  ( 20.94999999999999574, 4.348235979057646361, -245.2768893876484810 ) ) ;
#216873=EDGE_CURVE ( 'NONE', #186223, #253241, #9113, .T. ) ;
#216879=CYLINDRICAL_SURFACE ( 'NONE', #147210, 12.87500000000000178 ) ;
#216908=CARTESIAN_POINT ( 'NONE',  ( -18.50000000000000000, 38.30077178631847801, -261.1858881914067751 ) ) ;
#216948=EDGE_CURVE ( 'NONE', #216206, #201516, #39070, .T. ) ;
#216979=DIRECTION ( 'NONE',  ( -3.469446951953618606E-14, -0.8814952561688437216, 0.4721928772777334582 ) ) ;
#216984=DIRECTION ( 'NONE',  ( -1.000000000000000000, -1.394253735153569469E-16, -2.602809386958778209E-16 ) ) ;
#217023=CARTESIAN_POINT ( 'NONE',  ( -22.39999999999999858, 12.58895012248959766, -223.3279127647276141 ) ) ;
#217044=CARTESIAN_POINT ( 'NONE',  ( -23.25000000000000000, 36.65892442174935439, -249.5511627012433848 ) ) ;
#217046=DIRECTION ( 'NONE',  ( 0.000000000000000000, 0.8814952561688437216, -0.4721928772777334582 ) ) ;
#217052=DIRECTION ( 'NONE',  ( 1.000000000000000000, 0.000000000000000000, 0.000000000000000000 ) ) ;
#217082=ORIENTED_EDGE ( 'NONE', *, *, #8096, .T. ) ;
#217178=EDGE_CURVE ( 'NONE', #132943, #237152, #176441, .T. ) ;
#217192=PLANE ( 'NONE',  #103310 ) ;
#217193=ORIENTED_EDGE ( 'NONE', *, *, #183013, .T. ) ;
#217203=ORIENTED_EDGE ( 'NONE', *, *, #139614, .F. ) ;
#217212=PLANE ( 'NONE',  #169640 ) ;
#217223=CARTESIAN_POINT ( 'NONE',  ( -22.50875500270931795, -3.275978733247508323, -228.2735451763257402 ) ) ;
#217225=CARTESIAN_POINT ( 'NONE',  ( 21.13422380239121168, 10.19493587022274106, -228.0088647928831733 ) ) ;
#217245=CARTESIAN_POINT ( 'NONE',  ( 22.50046968638144307, -3.207446843257450109, -228.1445966768302469 ) ) ;
#217257=VECTOR ( 'NONE', #135300, 1000.000000000000000 ) ;
#217308=ORIENTED_EDGE ( 'NONE', *, *, #139817, .F. ) ;
#217322=VERTEX_POINT ( 'NONE', #17760 ) ;
#217326=ORIENTED_EDGE ( 'NONE', *, *, #172499, .F. ) ;
#217332=ORIENTED_EDGE ( 'NONE', *, *, #158627, .F. ) ;
#217355=VERTEX_POINT ( 'NONE', #76460 ) ;
#217356=CIRCLE ( 'NONE', #121561, 4.150000000000009237 ) ;
#217394=DIRECTION ( 'NONE',  ( 0.000000000000000000, -0.8814952561688430555, 0.4721928772777346239 ) ) ;
#217407=CARTESIAN_POINT ( 'NONE',  ( 21.05000000000000071, 18.88692293749142337, -227.8658170387887481 ) ) ;
#217428=VECTOR ( 'NONE', #226987, 1000.000000000000000 ) ;
#217436=CARTESIAN_POINT ( 'NONE',  ( -21.07928932188134041, 10.02993822722303818, -228.1074463178677263 ) ) ;
#217447=ADVANCED_FACE ( 'NONE', ( #82849 ), #106280, .T. ) ;
#217464=CARTESIAN_POINT ( 'NONE',  ( -21.05000000000000071, 28.46617234522943107, -258.4921533293940570 ) ) ;
#217468=VECTOR ( 'NONE', #64125, 1000.000000000000114 ) ;
#217488=DIRECTION ( 'NONE',  ( 0.000000000000000000, 0.8887656589064600876, -0.4583618696494786149 ) ) ;
#217492=EDGE_CURVE ( 'NONE', #2987, #62655, #172550, .T. ) ;
#217506=CARTESIAN_POINT ( 'NONE',  ( -22.50000000000000000, -3.092988775432913506, -228.1437074281570858 ) ) ;
#217511=DIRECTION ( 'NONE',  ( -1.000000000000000000, -1.394253735153569469E-16, -2.602809386958778209E-16 ) ) ;
#217527=CARTESIAN_POINT ( 'NONE',  ( 21.07189867249812210, 22.95831064513460973, -230.0453146669910325 ) ) ;
#217540=CYLINDRICAL_SURFACE ( 'NONE', #109590, 0.09999999999999939493 ) ;
#217592=ORIENTED_EDGE ( 'NONE', *, *, #148378, .T. ) ;
#217601=DIRECTION ( 'NONE',  ( -1.000000000000000000, 0.000000000000000000, 0.000000000000000000 ) ) ;
#217634=AXIS2_PLACEMENT_3D ( 'NONE', #110155, #209255, #14929 ) ;
#217651=EDGE_CURVE ( 'NONE', #168386, #30609, #205821, .T. ) ;
#217656=VECTOR ( 'NONE', #249199, 1000.000000000000000 ) ;
#217688=DIRECTION ( 'NONE',  ( 0.000000000000000000, 0.8009761297185381546, -0.5986962832865355688 ) ) ;
#217702=EDGE_CURVE ( 'NONE', #70602, #114510, #205404, .T. ) ;
#217734=DIRECTION ( 'NONE',  ( 1.000000000000000000, 1.541880601228652843E-16, 2.878400969107353907E-16 ) ) ;
#217774=ADVANCED_FACE ( 'NONE', ( #54033 ), #18563, .T. ) ;
#217787=LINE ( 'NONE', #82119, #100907 ) ;
#217790=EDGE_CURVE ( 'NONE', #145739, #245180, #126319, .T. ) ;
#217799=EDGE_CURVE ( 'NONE', #188486, #72511, #39437, .T. ) ;
#217844=ADVANCED_FACE ( 'NONE', ( #240387 ), #222064, .F. ) ;
#217845=VERTEX_POINT ( 'NONE', #64311 ) ;
#217853=CIRCLE ( 'NONE', #109538, 0.1000000000000013933 ) ;
#217855=CARTESIAN_POINT ( 'NONE',  ( -21.05000000000000071, 4.272272088314018390, -245.4186996786394843 ) ) ;
#217856=ADVANCED_FACE ( 'NONE', ( #23929 ), #223367, .F. ) ;
#217886=CARTESIAN_POINT ( 'NONE',  ( 20.95289811251229750, 18.82242866597310282, -229.9079097911970280 ) ) ;
#217893=ORIENTED_EDGE ( 'NONE', *, *, #93580, .T. ) ;
#217903=ORIENTED_EDGE ( 'NONE', *, *, #144131, .F. ) ;
#217907=CARTESIAN_POINT ( 'NONE',  ( -20.54999999999999716, 36.65892442174935439, -249.5511627012433848 ) ) ;
#217965=VECTOR ( 'NONE', #185456, 1000.000000000000000 ) ;
#217998=CYLINDRICAL_SURFACE ( 'NONE', #21047, 0.09999999999999986677 ) ;
#218011=AXIS2_PLACEMENT_3D ( 'NONE', #220621, #218022, #121552 ) ;
#218022=DIRECTION ( 'NONE',  ( 0.000000000000000000, -0.03181660087583042945, 0.9994937237965569876 ) ) ;
#218034=LINE ( 'NONE', #161962, #217468 ) ;
#218053=CIRCLE ( 'NONE', #55715, 0.1000000000000081657 ) ;
#218065=SPHERICAL_SURFACE ( 'NONE', #23844, 0.1000000000000000056 ) ;
#218073=AXIS2_PLACEMENT_3D ( 'NONE', #12953, #135427, #231997 ) ;
#218096=CARTESIAN_POINT ( 'NONE',  ( 22.39999999999999858, 0.3085173699977246109, -229.9658011520297975 ) ) ;
#218116=ORIENTED_EDGE ( 'NONE', *, *, #152698, .F. ) ;
#218124=EDGE_CURVE ( 'NONE', #91231, #95344, #227538, .T. ) ;
#218128=PLANE ( 'NONE',  #218185 ) ;
#218153=VERTEX_POINT ( 'NONE', #134534 ) ;
#218161=VERTEX_POINT ( 'NONE', #117559 ) ;
#218185=AXIS2_PLACEMENT_3D ( 'NONE', #197296, #172661, #216860 ) ;
#218203=VERTEX_POINT ( 'NONE', #236220 ) ;
#218229=DIRECTION ( 'NONE',  ( 1.000000000000000000, 0.000000000000000000, 0.000000000000000000 ) ) ;
#218241=ORIENTED_EDGE ( 'NONE', *, *, #201347, .T. ) ;
#218260=CARTESIAN_POINT ( 'NONE',  ( 18.42555734704281889, 8.849919995194017730, -245.4285591738437802 ) ) ;
#218283=DIRECTION ( 'NONE',  ( 0.000000000000000000, 0.4721928772777345129, 0.8814952561688431665 ) ) ;
#218299=DIRECTION ( 'NONE',  ( -1.000000000000000000, -0.000000000000000000, -0.000000000000000000 ) ) ;
#218302=DIRECTION ( 'NONE',  ( -1.000000000000000000, -8.674042436075353235E-17, -1.619280515896125144E-16 ) ) ;
#218316=EDGE_CURVE ( 'NONE', #188486, #53873, #176590, .T. ) ;
#218329=LINE ( 'NONE', #16325, #14301 ) ;
#218354=CYLINDRICAL_SURFACE ( 'NONE', #222353, 0.1000000000000075273 ) ;
#218366=CARTESIAN_POINT ( 'NONE',  ( -1.739115166359751170E-14, 34.53503747617445185, -235.1972745784239578 ) ) ;
#218369=ORIENTED_EDGE ( 'NONE', *, *, #142713, .T. ) ;
#218383=ORIENTED_EDGE ( 'NONE', *, *, #146406, .F. ) ;
#218397=VERTEX_POINT ( 'NONE', #49250 ) ;
#218399=LINE ( 'NONE', #39817, #154886 ) ;
#218418=AXIS2_PLACEMENT_3D ( 'NONE', #54056, #34522, #150604 ) ;
#218421=DIRECTION ( 'NONE',  ( 0.000000000000000000, 0.8814952561688425003, -0.4721928772777359007 ) ) ;
#218478=ORIENTED_EDGE ( 'NONE', *, *, #67020, .F. ) ;
#218491=ORIENTED_EDGE ( 'NONE', *, *, #104950, .F. ) ;
#218497=VERTEX_POINT ( 'NONE', #111806 ) ;
#218503=CARTESIAN_POINT ( 'NONE',  ( 21.05000000000000071, 9.997527148596399016, -228.1702915402975407 ) ) ;
#218505=ORIENTED_EDGE ( 'NONE', *, *, #184387, .F. ) ;
#218506=VERTEX_POINT ( 'NONE', #231755 ) ;
#218533=FACE_OUTER_BOUND ( 'NONE', #36290, .T. ) ;
#218542=CIRCLE ( 'NONE', #39552, 0.1000000000000013933 ) ;
#218580=CARTESIAN_POINT ( 'NONE',  ( 18.49999999999999289, 19.81721122307411420, -227.1998943584050039 ) ) ;
#218607=DIRECTION ( 'NONE',  ( 0.000000000000000000, -0.4721928772777350125, -0.8814952561688429444 ) ) ;
#218630=CARTESIAN_POINT ( 'NONE',  ( -18.59999999999999787, 2.319530388122570841, -217.8268657444419887 ) ) ;
#218651=CARTESIAN_POINT ( 'NONE',  ( -22.49436431346200038, 12.57088205413893434, -223.4317334472834489 ) ) ;
#218652=DIRECTION ( 'NONE',  ( -0.7071067811865217045, 0.3338907855512895928, 0.6233112732206752549 ) ) ;
#218656=ORIENTED_EDGE ( 'NONE', *, *, #253117, .F. ) ;
#218664=EDGE_LOOP ( 'NONE', ( #189681, #19255, #250469, #237148 ) ) ;
#218680=ORIENTED_EDGE ( 'NONE', *, *, #235354, .T. ) ;
#218710=CARTESIAN_POINT ( 'NONE',  ( 18.59999999999999076, 30.76917518201224055, -234.8152055956155380 ) ) ;
#218718=VERTEX_POINT ( 'NONE', #232736 ) ;
#218726=AXIS2_PLACEMENT_3D ( 'NONE', #28059, #47573, #181973 ) ;
#218775=AXIS2_PLACEMENT_3D ( 'NONE', #185783, #166254, #245764 ) ;
#218794=FACE_OUTER_BOUND ( 'NONE', #186904, .T. ) ;
#218796=UNCERTAINTY_MEASURE_WITH_UNIT (LENGTH_MEASURE( 1.000000000000000082E-05 ), #159335, 'distance_accuracy_value', 'NONE');
#218849=DIRECTION ( 'NONE',  ( 0.000000000000000000, -0.4721928772777334582, -0.8814952561688437216 ) ) ;
#218886=VECTOR ( 'NONE', #117116, 1000.000000000000000 ) ;
#218892=ORIENTED_EDGE ( 'NONE', *, *, #94470, .T. ) ;
#218904=ADVANCED_FACE ( 'NONE', ( #215698 ), #115327, .F. ) ;
#218940=ADVANCED_FACE ( 'NONE', ( #235271 ), #210097, .F. ) ;
#218943=VECTOR ( 'NONE', #113185, 1000.000000000000000 ) ;
#218965=ORIENTED_EDGE ( 'NONE', *, *, #99782, .T. ) ;
#218982=VERTEX_POINT ( 'NONE', #23964 ) ;
#218983=CARTESIAN_POINT ( 'NONE',  ( -20.94999999999999929, 28.58935552370083144, -258.2621935127861548 ) ) ;
#218987=CARTESIAN_POINT ( 'NONE',  ( 21.03670563405601968, 23.01071051840566284, -230.1870050808868768 ) ) ;
#219019=ORIENTED_EDGE ( 'NONE', *, *, #248643, .F. ) ;
#219044=CARTESIAN_POINT ( 'NONE',  ( -18.50000000000000000, 18.37021030142088662, -237.6367305148568221 ) ) ;
#219056=AXIS2_PLACEMENT_3D ( 'NONE', #122989, #8174, #121713 ) ;
#219061=ORIENTED_EDGE ( 'NONE', *, *, #8237, .T. ) ;
#219063=CARTESIAN_POINT ( 'NONE',  ( -20.00857864376270001, 22.33586458086958615, -231.4986017528744071 ) ) ;
#219094=DIRECTION ( 'NONE',  ( 0.000000000000000000, 0.4721928772776568528, 0.8814952561688845778 ) ) ;
#219165=EDGE_LOOP ( 'NONE', ( #202900, #219817, #28716, #56681, #122158 ) ) ;
#219215=FACE_OUTER_BOUND ( 'NONE', #113835, .T. ) ;
#219229=CARTESIAN_POINT ( 'NONE',  ( -18.50000000000000355, 43.02787096365918984, -254.3959382439171577 ) ) ;
#219288=FACE_OUTER_BOUND ( 'NONE', #82521, .T. ) ;
#219308=AXIS2_PLACEMENT_3D ( 'NONE', #5737, #22791, #60587 ) ;
#219338=EDGE_LOOP ( 'NONE', ( #59237, #163830, #72976, #101762 ) ) ;
#219350=AXIS2_PLACEMENT_3D ( 'NONE', #200600, #75542, #199326 ) ;
#219362=DIRECTION ( 'NONE',  ( -0.000000000000000000, 0.4721928772777345684, 0.8814952561688429444 ) ) ;
#219368=ORIENTED_EDGE ( 'NONE', *, *, #233065, .F. ) ;
#219377=ORIENTED_EDGE ( 'NONE', *, *, #138970, .T. ) ;
#219392=DIRECTION ( 'NONE',  ( 0.000000000000000000, -0.5341055959867045955, 0.8454177738465681324 ) ) ;
#219400=CARTESIAN_POINT ( 'NONE',  ( 18.39999999999999858, 37.94390843806124991, -261.1300795796834109 ) ) ;
#219419=CARTESIAN_POINT ( 'NONE',  ( 21.13461538461538325, 23.02743022372036918, -230.2075788195831763 ) ) ;
#219439=ORIENTED_EDGE ( 'NONE', *, *, #82897, .F. ) ;
#219446=ORIENTED_EDGE ( 'NONE', *, *, #151648, .F. ) ;
#219455=EDGE_CURVE ( 'NONE', #256947, #117242, #71629, .T. ) ;
#219484=DIRECTION ( 'NONE',  ( 0.000000000000000000, -0.8814952561688423893, 0.4721928772777359007 ) ) ;
#219497=EDGE_LOOP ( 'NONE', ( #90212, #33552, #127600, #254208 ) ) ;
#219507=CARTESIAN_POINT ( 'NONE',  ( 22.39999999999999503, 0.2612980822699583205, -230.0539506776466681 ) ) ;
#219561=ORIENTED_EDGE ( 'NONE', *, *, #208362, .F. ) ;
#219562=EDGE_CURVE ( 'NONE', #16612, #44305, #97990, .T. ) ;
#219573=AXIS2_PLACEMENT_3D ( 'NONE', #50638, #31139, #29844 ) ;
#219580=VECTOR ( 'NONE', #151782, 1000.000000000000114 ) ;
#219582=CARTESIAN_POINT ( 'NONE',  ( -21.05000000000000071, 28.24160076078326753, -259.1231640893983581 ) ) ;
#219594=CARTESIAN_POINT ( 'NONE',  ( -18.47653818581420637, 8.940896014627114141, -245.4411290137018113 ) ) ;
#219597=EDGE_CURVE ( 'NONE', #176803, #167022, #118884, .T. ) ;
#219692=SPHERICAL_SURFACE ( 'NONE', #238233, 0.1000000000000000056 ) ;
#219700=CIRCLE ( 'NONE', #128332, 11.80000000000001137 ) ;
#219702=EDGE_LOOP ( 'NONE', ( #124803, #50424, #52382, #219765 ) ) ;
#219718=CARTESIAN_POINT ( 'NONE',  ( 20.85000000000000142, 43.35377423437995503, -245.1717807829448930 ) ) ;
#219723=EDGE_CURVE ( 'NONE', #202898, #62992, #189613, .T. ) ;
#219735=EDGE_CURVE ( 'NONE', #131441, #82237, #23210, .T. ) ;
#219736=FACE_OUTER_BOUND ( 'NONE', #232636, .T. ) ;
#219740=CIRCLE ( 'NONE', #57429, 0.09999999999999681366 ) ;
#219741=ORIENTED_EDGE ( 'NONE', *, *, #86016, .F. ) ;
#219751=CARTESIAN_POINT ( 'NONE',  ( 22.50000000000000000, 7.128833340093095217, -233.7327013124392749 ) ) ;
#219765=ORIENTED_EDGE ( 'NONE', *, *, #198870, .F. ) ;
#219775=LINE ( 'NONE', #86665, #56999 ) ;
#219776=LINE ( 'NONE', #178119, #11968 ) ;
#219804=CARTESIAN_POINT ( 'NONE',  ( -20.54999999999999716, 19.93396995659180249, -235.7707092203739307 ) ) ;
#219817=ORIENTED_EDGE ( 'NONE', *, *, #173297, .T. ) ;
#219842=AXIS2_PLACEMENT_3D ( 'NONE', #31966, #154493, #191043 ) ;
#219870=DIRECTION ( 'NONE',  ( 0.000000000000000000, 0.8814952561688418342, -0.4721928772777367889 ) ) ;
#219879=EDGE_LOOP ( 'NONE', ( #89937, #28438, #233648, #175277 ) ) ;
#219910=CYLINDRICAL_SURFACE ( 'NONE', #164844, 0.09999999999999939493 ) ;
#219952=CARTESIAN_POINT ( 'NONE',  ( 21.14999999999999503, -3.187427350888460076, -228.3200064793908837 ) ) ;
#220006=ADVANCED_FACE ( 'NONE', ( #46118 ), #207798, .T. ) ;
#220026=ORIENTED_EDGE ( 'NONE', *, *, #192111, .F. ) ;
#220037=CARTESIAN_POINT ( 'NONE',  ( 22.00411653889213071, 0.7817229495155295638, -230.2203756341537257 ) ) ;
#220059=DIRECTION ( 'NONE',  ( -0.000000000000000000, 0.8814952561688430555, -0.4721928772777346239 ) ) ;
#220083=CIRCLE ( 'NONE', #78427, 0.1000000000000015737 ) ;
#220089=FACE_OUTER_BOUND ( 'NONE', #195429, .T. ) ;
#220099=CARTESIAN_POINT ( 'NONE',  ( -22.46246831459151494, -3.130120236468494355, -228.2124027741761552 ) ) ;
#220100=EDGE_CURVE ( 'NONE', #144042, #72959, #12164, .T. ) ;
#220146=TOROIDAL_SURFACE ( 'NONE', #182745, 0.4000000000000009104, 0.1000000000000000056 ) ;
#220156=DIRECTION ( 'NONE',  ( 1.000000000000000000, 0.000000000000000000, 0.000000000000000000 ) ) ;
#220157=EDGE_LOOP ( 'NONE', ( #174311, #24075, #75778, #102706, #123959 ) ) ;
#220179=ORIENTED_EDGE ( 'NONE', *, *, #134150, .F. ) ;
#220233=CARTESIAN_POINT ( 'NONE',  ( 18.50000000000000000, 9.122720154857379526, -245.4644708025848558 ) ) ;
#220247=CARTESIAN_POINT ( 'NONE',  ( -21.05000000000000071, 18.90448995781211750, -232.7802074516171444 ) ) ;
#220279=ORIENTED_EDGE ( 'NONE', *, *, #155455, .F. ) ;
#220309=ORIENTED_EDGE ( 'NONE', *, *, #120297, .T. ) ;
#220389=VERTEX_POINT ( 'NONE', #182782 ) ;
#220415=SPHERICAL_SURFACE ( 'NONE', #44463, 0.1000000000000000056 ) ;
#220420=CIRCLE ( 'NONE', #162157, 0.2000000000000027867 ) ;
#220468=CIRCLE ( 'NONE', #153876, 0.5000000000000008882 ) ;
#220470=DIRECTION ( 'NONE',  ( 0.000000000000000000, -0.8814952561688429444, 0.4721928772777349570 ) ) ;
#220483=ORIENTED_EDGE ( 'NONE', *, *, #202973, .F. ) ;
#220499=VERTEX_POINT ( 'NONE', #13126 ) ;
#220561=CARTESIAN_POINT ( 'NONE',  ( -23.25000000000000000, 27.82649702422227733, -239.8850763025288870 ) ) ;
#220617=CYLINDRICAL_SURFACE ( 'NONE', #257355, 0.09999999999999986677 ) ;
#220621=CARTESIAN_POINT ( 'NONE',  ( -20.94999999999999929, 18.82290990851282331, -233.3604470821920529 ) ) ;
#220630=CARTESIAN_POINT ( 'NONE',  ( -23.25000000000000000, 19.16534496950139399, -238.0132401564540032 ) ) ;
#220684=AXIS2_PLACEMENT_3D ( 'NONE', #252256, #14961, #138699 ) ;
#220717=ORIENTED_EDGE ( 'NONE', *, *, #105413, .T. ) ;
#220721=ADVANCED_FACE ( 'NONE', ( #39122 ), #176072, .F. ) ;
#220728=ORIENTED_EDGE ( 'NONE', *, *, #160933, .T. ) ;
#220748=DIRECTION ( 'NONE',  ( 1.000000000000000000, 0.000000000000000000, 0.000000000000000000 ) ) ;
#220783=ORIENTED_EDGE ( 'NONE', *, *, #36107, .T. ) ;
#220793=ORIENTED_EDGE ( 'NONE', *, *, #8782, .T. ) ;
#220815=DIRECTION ( 'NONE',  ( -1.000000000000000000, 0.000000000000000000, 0.000000000000000000 ) ) ;
#220850=CARTESIAN_POINT ( 'NONE',  ( 21.10320863425824811, 10.12894173882548365, -228.0790718293079067 ) ) ;
#220868=LINE ( 'NONE', #244281, #96884 ) ;
#220872=DIRECTION ( 'NONE',  ( 1.000000000000000000, 0.000000000000000000, 0.000000000000000000 ) ) ;
#220879=EDGE_LOOP ( 'NONE', ( #256185, #220026, #251825, #209913, #12696 ) ) ;
#220887=ORIENTED_EDGE ( 'NONE', *, *, #44279, .T. ) ;
#220894=DIRECTION ( 'NONE',  ( 0.000000000000000000, -0.8814952561688430555, 0.4721928772777345684 ) ) ;
#220895=DIRECTION ( 'NONE',  ( 1.000000000000000000, 0.000000000000000000, 0.000000000000000000 ) ) ;
#220976=ADVANCED_FACE ( 'NONE', ( #170652 ), #207094, .T. ) ;
#221006=EDGE_CURVE ( 'NONE', #141753, #252297, #152955, .T. ) ;
#221008=CARTESIAN_POINT ( 'NONE',  ( 23.14999999999999858, 28.08470566095357057, -239.2860081655328770 ) ) ;
#221014=ADVANCED_FACE ( 'NONE', ( #132777 ), #212310, .F. ) ;
#221048=CARTESIAN_POINT ( 'NONE',  ( -20.54999999999999716, 16.34561257290783942, -251.9995012668252343 ) ) ;
#221081=VERTEX_POINT ( 'NONE', #196570 ) ;
#221089=CIRCLE ( 'NONE', #100281, 0.1999999999999905742 ) ;
#221103=LINE ( 'NONE', #4619, #231823 ) ;
#221115=ORIENTED_EDGE ( 'NONE', *, *, #254348, .T. ) ;
#221142=ORIENTED_EDGE ( 'NONE', *, *, #187682, .F. ) ;
#221153=AXIS2_PLACEMENT_3D ( 'NONE', #248457, #28149, #88060 ) ;
#221169=ADVANCED_FACE ( 'NONE', ( #84270 ), #19658, .F. ) ;
#221175=CARTESIAN_POINT ( 'NONE',  ( 18.59999999999999432, 13.66123737402873495, -238.6633470470287648 ) ) ;
#221209=DIRECTION ( 'NONE',  ( 1.000000000000000000, 0.000000000000000000, 0.000000000000000000 ) ) ;
#221218=CARTESIAN_POINT ( 'NONE',  ( 21.33487959338958362, 10.30459399514276519, -227.8041537064418947 ) ) ;
#221252=CARTESIAN_POINT ( 'NONE',  ( -21.05000000000000071, 10.12484234394027816, -228.1850061131911218 ) ) ;
#221293=EDGE_CURVE ( 'NONE', #250267, #136073, #140816, .T. ) ;
#221323=CARTESIAN_POINT ( 'NONE',  ( 23.14999999999999147, 7.128833340093095217, -233.7327013124392749 ) ) ;
#221334=FACE_OUTER_BOUND ( 'NONE', #104391, .T. ) ;
#221354=CARTESIAN_POINT ( 'NONE',  ( -18.60000000000000497, 9.036460724854876503, -245.3776971525634565 ) ) ;
#221403=ORIENTED_EDGE ( 'NONE', *, *, #31623, .F. ) ;
#221406=DIRECTION ( 'NONE',  ( -1.000000000000000000, -1.394253735153569469E-16, -2.602809386958778209E-16 ) ) ;
#221432=B_SPLINE_CURVE_WITH_KNOTS ( 'NONE', 3,
 ( #35817, #95745, #76190, #155775, #38368, #59166, #193591, #218260, #34536, #117890 ),
 .UNSPECIFIED., .F., .F.,
 ( 4, 2, 2, 2, 4 ),
 ( 0.000000000000000000, 0.0001584437871625069168, 0.0002376656807437669617, 0.0002772766275343895438, 0.0003168875743250120988 ),
 .UNSPECIFIED. ) ;
#221441=AXIS2_PLACEMENT_3D ( 'NONE', #37579, #195378, #256548 ) ;
#221444=DIRECTION ( 'NONE',  ( -1.000000000000000000, 0.000000000000000000, 0.000000000000000000 ) ) ;
#221457=DIRECTION ( 'NONE',  ( 0.000000000000000000, 0.4721928772777346239, 0.8814952561688430555 ) ) ;
#221473=CARTESIAN_POINT ( 'NONE',  ( 18.59999999999999076, 18.18127959618848166, -237.5711165786817389 ) ) ;
#221514=DIRECTION ( 'NONE',  ( 7.304098846218132695E-16, -0.4721928772777346794, -0.8814952561688431665 ) ) ;
#221578=DIRECTION ( 'NONE',  ( -1.000000000000000000, -1.394253735153568729E-16, -2.602809386958776729E-16 ) ) ;
#221586=ORIENTED_EDGE ( 'NONE', *, *, #235707, .T. ) ;
#221591=DIRECTION ( 'NONE',  ( 0.000000000000000000, -0.8814952561685701626, 0.4721928772782442163 ) ) ;
#221609=CARTESIAN_POINT ( 'NONE',  ( -23.25000000000000000, -3.187427350888460076, -228.3200064793908837 ) ) ;
#221623=AXIS2_PLACEMENT_3D ( 'NONE', #252601, #132677, #209639 ) ;
#221624=CARTESIAN_POINT ( 'NONE',  ( -18.59999999999999787, 46.46967969402478360, -243.0849751855955674 ) ) ;
#221636=CARTESIAN_POINT ( 'NONE',  ( 20.85000000000000142, 42.20719072976272912, -239.1935934412594804 ) ) ;
#221637=VERTEX_POINT ( 'NONE', #226077 ) ;
#221642=DIRECTION ( 'NONE',  ( 0.000000000000000000, 0.8814952561688476074, -0.4721928772777262417 ) ) ;
#221668=CARTESIAN_POINT ( 'NONE',  ( 20.94999999999999574, 4.384524567800934136, -245.2091454203640239 ) ) ;
#221703=ORIENTED_EDGE ( 'NONE', *, *, #27667, .T. ) ;
#221707=DIRECTION ( 'NONE',  ( 0.000000000000000000, -0.8814952561688429444, 0.4721928772777350680 ) ) ;
#221723=EDGE_LOOP ( 'NONE', ( #110006, #95722, #19666, #2759 ) ) ;
#221729=ORIENTED_EDGE ( 'NONE', *, *, #50259, .F. ) ;
#221749=CARTESIAN_POINT ( 'NONE',  ( -18.59999999999999787, 43.35377423437995503, -245.1717807829448930 ) ) ;
#221770=VECTOR ( 'NONE', #151248, 1000.000000000000000 ) ;
#221806=DIRECTION ( 'NONE',  ( -2.940209281316618057E-16, 0.4721928772777340688, 0.8814952561688433885 ) ) ;
#221840=CARTESIAN_POINT ( 'NONE',  ( 18.49999999999999289, 34.53503747617446606, -235.1972745784239578 ) ) ;
#221848=AXIS2_PLACEMENT_3D ( 'NONE', #248436, #14972, #151926 ) ;
#221851=EDGE_CURVE ( 'NONE', #251749, #257480, #18287, .T. ) ;
#221854=DIRECTION ( 'NONE',  ( 0.000000000000000000, -0.3488585713686159218, -0.9371753822965306346 ) ) ;
#221866=DIRECTION ( 'NONE',  ( 1.000000000000000000, 0.000000000000000000, 0.000000000000000000 ) ) ;
#221869=CYLINDRICAL_SURFACE ( 'NONE', #218011, 0.1000000000000012546 ) ;
#221874=DIRECTION ( 'NONE',  ( 1.000000000000000000, -0.000000000000000000, -0.000000000000000000 ) ) ;
#221908=CARTESIAN_POINT ( 'NONE',  ( 22.39999999999999503, 0.3085173699977246109, -229.9658011520297975 ) ) ;
#221911=DIRECTION ( 'NONE',  ( 0.000000000000000000, -0.8814952561688476074, 0.4721928772777262417 ) ) ;
#221997=ORIENTED_EDGE ( 'NONE', *, *, #85734, .F. ) ;
#222039=ORIENTED_EDGE ( 'NONE', *, *, #210020, .T. ) ;
#222042=ORIENTED_EDGE ( 'NONE', *, *, #76498, .F. ) ;
#222050=CARTESIAN_POINT ( 'NONE',  ( -21.05000000000000071, 4.384524567800934136, -245.2091454203640239 ) ) ;
#222054=CARTESIAN_POINT ( 'NONE',  ( 21.56666275994539816, 0.9959460939976487737, -230.4474815061071240 ) ) ;
#222064=CYLINDRICAL_SURFACE ( 'NONE', #1404, 0.09999999999999939493 ) ;
#222069=CARTESIAN_POINT ( 'NONE',  ( 20.94999999999999574, 16.44800918141279311, -240.8068063186265135 ) ) ;
#222075=EDGE_CURVE ( 'NONE', #182052, #3876, #74396, .T. ) ;
#222085=ORIENTED_EDGE ( 'NONE', *, *, #92980, .T. ) ;
#222098=FACE_OUTER_BOUND ( 'NONE', #44571, .T. ) ;
#222101=AXIS2_PLACEMENT_3D ( 'NONE', #218710, #102598, #199169 ) ;
#222119=ORIENTED_EDGE ( 'NONE', *, *, #93708, .F. ) ;
#222184=ORIENTED_EDGE ( 'NONE', *, *, #22322, .T. ) ;
#222188=ORIENTED_EDGE ( 'NONE', *, *, #121224, .T. ) ;
#222221=B_SPLINE_CURVE_WITH_KNOTS ( 'NONE', 3,
 ( #58428, #158864, #40207, #183545, #84376, #81827, #221354, #180978 ),
 .UNSPECIFIED., .F., .F.,
 ( 4, 2, 2, 4 ),
 ( 0.000000000000000000, 0.0001049670497870005311, 0.0002099340995740010623, 0.0004198681991479908488 ),
 .UNSPECIFIED. ) ;
#222235=CARTESIAN_POINT ( 'NONE',  ( -20.94999999999999929, 36.22908226166886436, -236.0480061918409547 ) ) ;
#222249=EDGE_CURVE ( 'NONE', #46846, #202163, #199190, .T. ) ;
#222254=ORIENTED_EDGE ( 'NONE', *, *, #253872, .T. ) ;
#222290=ADVANCED_FACE ( 'NONE', ( #98756 ), #178364, .F. ) ;
#222327=CARTESIAN_POINT ( 'NONE',  ( 21.22070241538126467, 1.472315254537094553, -230.5904421098591968 ) ) ;
#222350=EDGE_LOOP ( 'NONE', ( #170025, #255938, #89043, #6560 ) ) ;
#222353=AXIS2_PLACEMENT_3D ( 'NONE', #136242, #20191, #37195 ) ;
#222362=LINE ( 'NONE', #240674, #116003 ) ;
#222391=EDGE_CURVE ( 'NONE', #44944, #178909, #167789, .T. ) ;
#222400=ORIENTED_EDGE ( 'NONE', *, *, #104047, .F. ) ;
#222432=AXIS2_PLACEMENT_3D ( 'NONE', #254382, #32840, #13248 ) ;
#222444=CARTESIAN_POINT ( 'NONE',  ( 20.04142135623730070, 2.319530388122574394, -217.8268657444419887 ) ) ;
#222447=ORIENTED_EDGE ( 'NONE', *, *, #5730, .F. ) ;
#222451=VERTEX_POINT ( 'NONE', #26993 ) ;
#222487=EDGE_LOOP ( 'NONE', ( #223874, #190358, #128155 ) ) ;
#222489=CARTESIAN_POINT ( 'NONE',  ( 18.50000000000000000, -7.714568254029292582, -236.5586399380298985 ) ) ;
#222497=AXIS2_PLACEMENT_3D ( 'NONE', #10607, #253051, #69304 ) ;
#222524=AXIS2_PLACEMENT_3D ( 'NONE', #34540, #158355, #155779 ) ;
#222533=CARTESIAN_POINT ( 'NONE',  ( -21.04999999999839133, 10.20950081962639544, -228.0124793259371359 ) ) ;
#222548=CARTESIAN_POINT ( 'NONE',  ( -20.85000000000000142, 42.92545512184477730, -254.1955779480491344 ) ) ;
#222562=VERTEX_POINT ( 'NONE', #128646 ) ;
#222591=CARTESIAN_POINT ( 'NONE',  ( -23.15000000000000213, 30.43677443282724937, -239.5249545687858870 ) ) ;
#222598=CIRCLE ( 'NONE', #80962, 3.999999999999994671 ) ;
#222640=CIRCLE ( 'NONE', #68554, 11.89999999999999858 ) ;
#222652=LINE ( 'NONE', #44038, #92748 ) ;
#222659=ORIENTED_EDGE ( 'NONE', *, *, #191264, .F. ) ;
#222662=AXIS2_PLACEMENT_3D ( 'NONE', #24451, #105195, #184771 ) ;
#222672=ADVANCED_FACE ( 'NONE', ( #159757 ), #28218, .T. ) ;
#222697=CARTESIAN_POINT ( 'NONE',  ( 22.50000000000000000, 7.128833340093095217, -233.7327013124392749 ) ) ;
#222715=CARTESIAN_POINT ( 'NONE',  ( -20.64999999999999858, 36.65892442174935439, -249.5511627012433848 ) ) ;
#222748=EDGE_LOOP ( 'NONE', ( #57690, #143487, #144719, #183823 ) ) ;
#222788=ORIENTED_EDGE ( 'NONE', *, *, #130836, .T. ) ;
#222797=FACE_OUTER_BOUND ( 'NONE', #28014, .T. ) ;
#222835=DIRECTION ( 'NONE',  ( -0.000000000000000000, -0.6052030477778852502, -0.7960711469211522173 ) ) ;
#222869=CARTESIAN_POINT ( 'NONE',  ( 20.95325940946048249, 18.76594065868512118, -228.0282680241705293 ) ) ;
#222908=ORIENTED_EDGE ( 'NONE', *, *, #80202, .T. ) ;
#222935=ADVANCED_FACE ( 'NONE', ( #181888 ), #94994, .T. ) ;
#222986=CIRCLE ( 'NONE', #185583, 3.900000000000020783 ) ;
#222987=CIRCLE ( 'NONE', #110574, 0.2000000000000058675 ) ;
#223000=DIRECTION ( 'NONE',  ( -1.000000000000000000, -0.000000000000000000, -0.000000000000000000 ) ) ;
#223008=CARTESIAN_POINT ( 'NONE',  ( -20.85000000000000142, 43.35377423437995503, -245.1717807829448930 ) ) ;
#223062=DIRECTION ( 'NONE',  ( -1.000000000000000000, -7.166229603267617241E-16, -4.447280054184918885E-16 ) ) ;
#223077=ORIENTED_EDGE ( 'NONE', *, *, #85777, .F. ) ;
#223089=VERTEX_POINT ( 'NONE', #59026 ) ;
#223103=CARTESIAN_POINT ( 'NONE',  ( -20.94999999999999929, 14.72981487416292623, -236.4853282537515895 ) ) ;
#223119=DIRECTION ( 'NONE',  ( -1.000000000000000000, -1.541880601228652843E-16, -2.878400969107353907E-16 ) ) ;
#223182=CARTESIAN_POINT ( 'NONE',  ( 21.00000000000000000, 30.46448808713892831, -235.1722212069449256 ) ) ;
#223188=VERTEX_POINT ( 'NONE', #211282 ) ;
#223192=CARTESIAN_POINT ( 'NONE',  ( 20.02499999999999858, 30.37633856152204359, -235.1250019192171408 ) ) ;
#223204=DIRECTION ( 'NONE',  ( 1.000000000000000000, -0.000000000000000000, -0.000000000000000000 ) ) ;
#223209=CARTESIAN_POINT ( 'NONE',  ( 20.94999999999999574, 13.63177590472475487, -238.5351604075707144 ) ) ;
#223216=AXIS2_PLACEMENT_3D ( 'NONE', #33538, #50454, #149611 ) ;
#223258=CARTESIAN_POINT ( 'NONE',  ( 20.94999999999999929, 43.24695311518262031, -245.0026972281755491 ) ) ;
#223260=ORIENTED_EDGE ( 'NONE', *, *, #177318, .T. ) ;
#223337=ORIENTED_EDGE ( 'NONE', *, *, #106194, .F. ) ;
#223367=CYLINDRICAL_SURFACE ( 'NONE', #68634, 0.09999999999999986677 ) ;
#223395=ORIENTED_EDGE ( 'NONE', *, *, #39946, .F. ) ;
#223461=ADVANCED_FACE ( 'NONE', ( #141519 ), #240627, .T. ) ;
#223483=CARTESIAN_POINT ( 'NONE',  ( -20.54999999999999716, 30.18746141061095045, -235.4776000216846796 ) ) ;
#223513=ORIENTED_EDGE ( 'NONE', *, *, #240691, .F. ) ;
#223518=PLANE ( 'NONE',  #147098 ) ;
#223536=ORIENTED_EDGE ( 'NONE', *, *, #254991, .F. ) ;
#223543=ADVANCED_FACE ( 'NONE', ( #89246 ), #30592, .T. ) ;
#223560=DIRECTION ( 'NONE',  ( -3.265361837132812600E-16, 0.4721928772777346239, 0.8814952561688430555 ) ) ;
#223562=CARTESIAN_POINT ( 'NONE',  ( 23.14999999999999858, 7.128833340093095217, -233.7327013124392749 ) ) ;
#223574=EDGE_CURVE ( 'NONE', #136977, #100199, #220083, .T. ) ;
#223580=DIRECTION ( 'NONE',  ( 0.000000000000000000, 0.8096735173027155286, -0.5868805631290315850 ) ) ;
#223593=VECTOR ( 'NONE', #155697, 1000.000000000000000 ) ;
#223597=AXIS2_PLACEMENT_3D ( 'NONE', #244909, #45431, #208378 ) ;
#223603=EDGE_LOOP ( 'NONE', ( #235890, #107234, #164639 ) ) ;
#223610=EDGE_CURVE ( 'NONE', #148687, #196126, #132600, .T. ) ;
#223624=ORIENTED_EDGE ( 'NONE', *, *, #36252, .F. ) ;
#223636=CARTESIAN_POINT ( 'NONE',  ( -20.94999999999999929, 18.27574494880468592, -237.6039235467692947 ) ) ;
#223660=EDGE_CURVE ( 'NONE', #15847, #207603, #91091, .T. ) ;
#223667=EDGE_CURVE ( 'NONE', #184576, #39196, #49586, .T. ) ;
#223669=CIRCLE ( 'NONE', #248626, 0.09999999999999528710 ) ;
#223674=ORIENTED_EDGE ( 'NONE', *, *, #219562, .T. ) ;
#223680=ORIENTED_EDGE ( 'NONE', *, *, #194839, .F. ) ;
#223720=CIRCLE ( 'NONE', #86328, 2.000000000000003553 ) ;
#223748=AXIS2_PLACEMENT_3D ( 'NONE', #28678, #129022, #186431 ) ;
#223751=CARTESIAN_POINT ( 'NONE',  ( -18.50000000000000000, 22.33586458086958615, -231.4986017528744071 ) ) ;
#223755=CARTESIAN_POINT ( 'NONE',  ( 20.94999999999999929, 18.18127959618848877, -237.5711165786817389 ) ) ;
#223842=DIRECTION ( 'NONE',  ( 1.000000000000000000, 0.000000000000000000, 0.000000000000000000 ) ) ;
#223845=VERTEX_POINT ( 'NONE', #59077 ) ;
#223874=ORIENTED_EDGE ( 'NONE', *, *, #106181, .F. ) ;
#223876=CIRCLE ( 'NONE', #115555, 11.65000000000000036 ) ;
#223891=TOROIDAL_SURFACE ( 'NONE', #119902, 7.791421356237335338, 0.1000000000000000056 ) ;
#223908=DIRECTION ( 'NONE',  ( -1.000000000000000000, -0.000000000000000000, -0.000000000000000000 ) ) ;
#223937=DIRECTION ( 'NONE',  ( 1.000000000000000000, 0.000000000000000000, 0.000000000000000000 ) ) ;
#223966=AXIS2_PLACEMENT_3D ( 'NONE', #164976, #65872, #201529 ) ;
#223974=ADVANCED_FACE ( 'NONE', ( #25156 ), #184188, .T. ) ;
#223982=CIRCLE ( 'NONE', #194803, 0.09999999999999568956 ) ;
#223989=DIRECTION ( 'NONE',  ( -1.000000000000000000, -0.000000000000000000, -0.000000000000000000 ) ) ;
#224049=B_SPLINE_CURVE_WITH_KNOTS ( 'NONE', 3,
 ( #40770, #103248, #39490, #137260, #120317, #199833, #119003 ),
 .UNSPECIFIED., .F., .F.,
 ( 4, 3, 4 ),
 ( 0.000000000000000000, 3.357501770815288591E-05, 5.199112466349617109E-05 ),
 .UNSPECIFIED. ) ;
#224050=DIRECTION ( 'NONE',  ( 1.000000000000000000, 1.541880601228652843E-16, 2.878400969107353907E-16 ) ) ;
#224069=AXIS2_PLACEMENT_3D ( 'NONE', #23880, #103362, #143784 ) ;
#224077=FACE_OUTER_BOUND ( 'NONE', #178823, .T. ) ;
#224156=CARTESIAN_POINT ( 'NONE',  ( 20.94999999999999929, 7.128833340093095217, -233.7327013124392749 ) ) ;
#224164=DIRECTION ( 'NONE',  ( 0.000000000000000000, 0.8814952561688442767, -0.4721928772777324035 ) ) ;
#224196=ORIENTED_EDGE ( 'NONE', *, *, #209290, .F. ) ;
#224209=ORIENTED_EDGE ( 'NONE', *, *, #187171, .T. ) ;
#224223=CARTESIAN_POINT ( 'NONE',  ( 21.05000000000000071, 7.128833340093095217, -233.7327013124392749 ) ) ;
#224251=EDGE_CURVE ( 'NONE', #209230, #52463, #137246, .T. ) ;
#224265=DIRECTION ( 'NONE',  ( -1.000000000000000000, -0.000000000000000000, -0.000000000000000000 ) ) ;
#224299=AXIS2_PLACEMENT_3D ( 'NONE', #131779, #168397, #211326 ) ;
#224325=EDGE_LOOP ( 'NONE', ( #163811, #7803, #85844 ) ) ;
#224327=CARTESIAN_POINT ( 'NONE',  ( -22.39999999999999858, 0.2612980822699374484, -230.0539506776466681 ) ) ;
#224343=DIRECTION ( 'NONE',  ( 0.000000000000000000, -0.8814952561688423893, 0.4721928772777359007 ) ) ;
#224345=ORIENTED_EDGE ( 'NONE', *, *, #5801, .T. ) ;
#224346=CARTESIAN_POINT ( 'NONE',  ( 23.25000000000000000, 28.50120599808395028, -258.2149742250584268 ) ) ;
#224406=ADVANCED_FACE ( 'NONE', ( #84756 ), #44402, .F. ) ;
#224411=CARTESIAN_POINT ( 'NONE',  ( -23.15000000000000213, 11.15983666280819975, -246.1019239270423213 ) ) ;
#224420=EDGE_CURVE ( 'NONE', #217322, #145739, #208172, .T. ) ;
#224422=ORIENTED_EDGE ( 'NONE', *, *, #49569, .F. ) ;
#224437=VERTEX_POINT ( 'NONE', #148640 ) ;
#224451=DIRECTION ( 'NONE',  ( 0.000000000000000000, -0.4721928772777813088, -0.8814952561688180754 ) ) ;
#224478=ORIENTED_EDGE ( 'NONE', *, *, #236536, .F. ) ;
#224493=CARTESIAN_POINT ( 'NONE',  ( -20.94999999999999929, 42.96960653111219131, -254.4772109693542745 ) ) ;
#224535=EDGE_CURVE ( 'NONE', #85650, #155390, #249027, .T. ) ;
#224553=LINE ( 'NONE', #6798, #200644 ) ;
#224562=ORIENTED_EDGE ( 'NONE', *, *, #250120, .F. ) ;
#224577=ADVANCED_FACE ( 'NONE', ( #153816 ), #233137, .F. ) ;
#224588=CARTESIAN_POINT ( 'NONE',  ( -21.14999999999999858, 1.363275264940686293, -230.6442496871288483 ) ) ;
#224606=CARTESIAN_POINT ( 'NONE',  ( -23.15000000000000213, 25.94586868676353575, -241.5435999122864530 ) ) ;
#224629=EDGE_LOOP ( 'NONE', ( #153646, #219741, #242776, #46397 ) ) ;
#224660=TOROIDAL_SURFACE ( 'NONE', #141283, 3.899999999999999467, 0.1000000000000000056 ) ;
#224682=CARTESIAN_POINT ( 'NONE',  ( 20.94999999999999929, 11.36448785225375424, -246.7787679937655980 ) ) ;
#224690=DIRECTION ( 'NONE',  ( 0.000000000000000000, 0.8814952561688438326, -0.4721928772777334582 ) ) ;
#224717=CARTESIAN_POINT ( 'NONE',  ( -21.07928932188134041, 1.596973512272247042, -230.6572452218044020 ) ) ;
#224721=LINE ( 'NONE', #164770, #203571 ) ;
#224736=DIRECTION ( 'NONE',  ( 1.000000000000000000, 0.000000000000000000, 0.000000000000000000 ) ) ;
#224782=DIRECTION ( 'NONE',  ( -0.000000000000000000, 0.5474227397873200340, -0.8368562265788217491 ) ) ;
#224830=DIRECTION ( 'NONE',  ( 0.000000000000000000, 0.8814952561688444987, -0.4721928772777320149 ) ) ;
#224860=LINE ( 'NONE', #46228, #160015 ) ;
#224897=CARTESIAN_POINT ( 'NONE',  ( 18.59999999999999787, 18.37021030142088662, -237.6367305148568221 ) ) ;
#224941=VERTEX_POINT ( 'NONE', #29682 ) ;
#224946=ADVANCED_FACE ( 'NONE', ( #192579 ), #248702, .T. ) ;
#224948=CARTESIAN_POINT ( 'NONE',  ( -21.55000000000000426, 29.43195280696657790, -236.8879924315548351 ) ) ;
#224950=DIRECTION ( 'NONE',  ( 1.000000000000000000, 0.000000000000000000, 0.000000000000000000 ) ) ;
#224953=EDGE_LOOP ( 'NONE', ( #161500, #232645, #188200, #5037 ) ) ;
#224968=ORIENTED_EDGE ( 'NONE', *, *, #11494, .T. ) ;
#224985=CARTESIAN_POINT ( 'NONE',  ( 21.14999999999999858, 1.363275264940683407, -230.6442496871288483 ) ) ;
#224986=DIRECTION ( 'NONE',  ( -1.000000000000000000, -1.394253735153569469E-16, -2.602809386958778209E-16 ) ) ;
#224994=ORIENTED_EDGE ( 'NONE', *, *, #160495, .F. ) ;
#225013=DIRECTION ( 'NONE',  ( 0.000000000000000000, -0.4721928772777383987, -0.8814952561688410571 ) ) ;
#225110=ADVANCED_FACE ( 'NONE', ( #142534 ), #43451, .F. ) ;
#225121=CARTESIAN_POINT ( 'NONE',  ( -20.85000000000000142, 45.93315328338058379, -256.6017782078560003 ) ) ;
#225123=TOROIDAL_SURFACE ( 'NONE', #183463, 0.2000000000000000111, 0.1000000000000000056 ) ;
#225130=ORIENTED_EDGE ( 'NONE', *, *, #117481, .T. ) ;
#225160=FACE_OUTER_BOUND ( 'NONE', #231744, .T. ) ;
#225172=CIRCLE ( 'NONE', #112778, 4.050000000000002487 ) ;
#225213=ORIENTED_EDGE ( 'NONE', *, *, #140857, .T. ) ;
#225273=FACE_OUTER_BOUND ( 'NONE', #230110, .T. ) ;
#225327=ADVANCED_FACE ( 'NONE', ( #13318 ), #96660, .T. ) ;
#225368=DIRECTION ( 'NONE',  ( -0.000000000000000000, 0.8814952561688430555, -0.4721928772777346239 ) ) ;
#225419=DIRECTION ( 'NONE',  ( -1.000000000000000000, 0.000000000000000000, 0.000000000000000000 ) ) ;
#225428=DIRECTION ( 'NONE',  ( 0.000000000000000000, 0.8814952561688436106, -0.4721928772777336247 ) ) ;
#225459=DIRECTION ( 'NONE',  ( 0.000000000000000000, -0.4721928772777346239, -0.8814952561688430555 ) ) ;
#225465=CARTESIAN_POINT ( 'NONE',  ( 20.94999999999999929, 24.12844930803501242, -253.0488546976795021 ) ) ;
#225521=AXIS2_PLACEMENT_3D ( 'NONE', #247851, #90048, #45796 ) ;
#225564=VERTEX_POINT ( 'NONE', #224346 ) ;
#225589=CARTESIAN_POINT ( 'NONE',  ( 23.14999999999999503, 23.34004772283015683, -229.2004250369967338 ) ) ;
#225590=CARTESIAN_POINT ( 'NONE',  ( 21.14999999999999858, 23.42819724844704155, -229.2476443247244902 ) ) ;
#225646=DIRECTION ( 'NONE',  ( -1.000000000000000000, 0.000000000000000000, 0.000000000000000000 ) ) ;
#225656=CARTESIAN_POINT ( 'NONE',  ( 18.49999999999999289, 30.78873405139468034, -234.7786928665882442 ) ) ;
#225675=DIRECTION ( 'NONE',  ( 0.000000000000000000, -0.9994937237965558774, -0.03181660087586650476 ) ) ;
#225688=VECTOR ( 'NONE', #251350, 1000.000000000000000 ) ;
#225708=ORIENTED_EDGE ( 'NONE', *, *, #251922, .T. ) ;
#225734=VECTOR ( 'NONE', #179565, 1000.000000000000000 ) ;
#225745=CARTESIAN_POINT ( 'NONE',  ( 20.94999999999999574, 13.59055429284667404, -238.6121134008722038 ) ) ;
#225766=DIRECTION ( 'NONE',  ( 0.000000000000000000, -0.8814952561688707000, 0.4721928772776828875 ) ) ;
#225784=ORIENTED_EDGE ( 'NONE', *, *, #1029, .T. ) ;
#225808=ORIENTED_EDGE ( 'NONE', *, *, #112233, .F. ) ;
#225823=EDGE_LOOP ( 'NONE', ( #194005, #82424, #39854, #30503 ) ) ;
#225827=CARTESIAN_POINT ( 'NONE',  ( 19.75857864376269291, 34.44688795055758845, -235.1500552906961730 ) ) ;
#225867=ORIENTED_EDGE ( 'NONE', *, *, #199886, .F. ) ;
#225877=CIRCLE ( 'NONE', #9422, 0.09999999999999983902 ) ;
#225887=FACE_OUTER_BOUND ( 'NONE', #126830, .T. ) ;
#225902=VECTOR ( 'NONE', #162468, 1000.000000000000000 ) ;
#225907=CARTESIAN_POINT ( 'NONE',  ( 20.85000000000000142, 43.08613539620618837, -254.3146655184800409 ) ) ;
#225940=AXIS2_PLACEMENT_3D ( 'NONE', #87511, #31448, #109648 ) ;
#225945=CARTESIAN_POINT ( 'NONE',  ( 23.14999999999999858, 19.82851818057134707, -235.1178474969725016 ) ) ;
#225948=ORIENTED_EDGE ( 'NONE', *, *, #178003, .T. ) ;
#225958=ORIENTED_EDGE ( 'NONE', *, *, #80214, .F. ) ;
#225964=CARTESIAN_POINT ( 'NONE',  ( 23.14999999999999503, 29.08883969319483498, -237.9520757887960940 ) ) ;
#225969=AXIS2_PLACEMENT_3D ( 'NONE', #152006, #174152, #196227 ) ;
#225976=CARTESIAN_POINT ( 'NONE',  ( 21.05000000000000071, 3.338403738567039980, -231.7022719401450104 ) ) ;
#225978=CARTESIAN_POINT ( 'NONE',  ( -22.39999999999999858, 10.71943444926882449, -226.8179467668883547 ) ) ;
#226050=AXIS2_PLACEMENT_3D ( 'NONE', #206384, #68152, #147693 ) ;
#226077=CARTESIAN_POINT ( 'NONE',  ( -23.15000000000000213, 12.67709964810647882, -223.3751320524553705 ) ) ;
#226091=VERTEX_POINT ( 'NONE', #214746 ) ;
#226134=ORIENTED_EDGE ( 'NONE', *, *, #169255, .F. ) ;
#226145=LINE ( 'NONE', #90514, #226455 ) ;
#226151=CARTESIAN_POINT ( 'NONE',  ( -23.15000000000000213, 36.02918351690956200, -236.0543695120161374 ) ) ;
#226157=ORIENTED_EDGE ( 'NONE', *, *, #212801, .F. ) ;
#226178=EDGE_CURVE ( 'NONE', #125839, #198947, #92938, .T. ) ;
#226188=CARTESIAN_POINT ( 'NONE',  ( -23.15000000000000213, 18.47808476326695626, -239.8121846073901224 ) ) ;
#226189=CIRCLE ( 'NONE', #55312, 0.1000000000000013933 ) ;
#226201=DIRECTION ( 'NONE',  ( 1.000000000000000000, 0.000000000000000000, 0.000000000000000000 ) ) ;
#226216=EDGE_CURVE ( 'NONE', #61591, #114424, #118222, .T. ) ;
#226220=AXIS2_PLACEMENT_3D ( 'NONE', #217907, #79686, #23627 ) ;
#226233=AXIS2_PLACEMENT_3D ( 'NONE', #117197, #132919, #151197 ) ;
#226236=PRODUCT_DEFINITION_SHAPE ( 'NONE', 'NONE',  #190348 ) ;
#226287=SURFACE_STYLE_FILL_AREA ( #184614 ) ;
#226289=AXIS2_PLACEMENT_3D ( 'NONE', #223562, #239297, #84016 ) ;
#226316=VERTEX_POINT ( 'NONE', #108914 ) ;
#226361=CYLINDRICAL_SURFACE ( 'NONE', #59269, 0.09999999999999986677 ) ;
#226416=EDGE_LOOP ( 'NONE', ( #30532, #115337, #238788, #176383 ) ) ;
#226417=CYLINDRICAL_SURFACE ( 'NONE', #212856, 0.1000000000000012546 ) ;
#226454=VECTOR ( 'NONE', #67167, 1000.000000000000000 ) ;
#226455=VECTOR ( 'NONE', #248317, 1000.000000000000000 ) ;
#226464=ORIENTED_EDGE ( 'NONE', *, *, #84400, .F. ) ;
#226482=CARTESIAN_POINT ( 'NONE',  ( -21.05000000000000071, 36.65892442174935439, -249.5511627012433848 ) ) ;
#226483=EDGE_LOOP ( 'NONE', ( #166058, #232630, #152999, #160236 ) ) ;
#226515=VERTEX_POINT ( 'NONE', #134873 ) ;
#226543=CARTESIAN_POINT ( 'NONE',  ( 21.14999999999999858, 17.83900070254454562, -239.4698447713637677 ) ) ;
#226549=AXIS2_PLACEMENT_3D ( 'NONE', #39158, #22160, #156549 ) ;
#226564=CIRCLE ( 'NONE', #18307, 0.09999999999999036049 ) ;
#226571=CARTESIAN_POINT ( 'NONE',  ( -20.85000000000000142, 42.15997144203495139, -239.2817429668763793 ) ) ;
#226582=CARTESIAN_POINT ( 'NONE',  ( -21.00448002041633444, 18.71387963086063166, -226.6088698288088779 ) ) ;
#226584=ORIENTED_EDGE ( 'NONE', *, *, #102335, .F. ) ;
#226605=EDGE_CURVE ( 'NONE', #85650, #240913, #109692, .T. ) ;
#226620=ADVANCED_FACE ( 'NONE', ( #136154 ), #77467, .F. ) ;
#226630=VERTEX_POINT ( 'NONE', #157055 ) ;
#226639=DIRECTION ( 'NONE',  ( 0.000000000000000000, 0.8855159391400395652, -0.4646089985449416981 ) ) ;
#226651=LINE ( 'NONE', #127568, #225688 ) ;
#226690=CARTESIAN_POINT ( 'NONE',  ( 20.94999999999999574, 14.81796439977981272, -236.5325475414793743 ) ) ;
#226713=CARTESIAN_POINT ( 'NONE',  ( -20.85000000000000142, 36.65892442174935439, -249.5511627012433848 ) ) ;
#226738=ORIENTED_EDGE ( 'NONE', *, *, #192733, .F. ) ;
#226746=CARTESIAN_POINT ( 'NONE',  ( -20.94999999999999929, 16.44800918141279666, -240.8068063186265135 ) ) ;
#226754=CIRCLE ( 'NONE', #76916, 0.09999999999999711897 ) ;
#226758=CIRCLE ( 'NONE', #22784, 11.70000000000000639 ) ;
#226772=CARTESIAN_POINT ( 'NONE',  ( -21.14999999999999858, 1.363275264940686293, -230.6442496871288483 ) ) ;
#226773=DIRECTION ( 'NONE',  ( -1.000000000000000000, -0.000000000000000000, -0.000000000000000000 ) ) ;
#226814=DIRECTION ( 'NONE',  ( 0.000000000000000000, -0.8814952561688320642, 0.4721928772777551075 ) ) ;
#226818=CARTESIAN_POINT ( 'NONE',  ( -18.59999999999999787, 18.81339837015603322, -226.7756228984618190 ) ) ;
#226820=( BOUNDED_CURVE ( )  B_SPLINE_CURVE ( 3, ( #139017, #159931, #197746, #81615 ),
 .UNSPECIFIED., .F., .F. ) 
 B_SPLINE_CURVE_WITH_KNOTS ( ( 4, 4 ),
 ( 3.141592653589793116, 4.712388980384689674 ),
 .UNSPECIFIED. ) 
 CURVE ( )  GEOMETRIC_REPRESENTATION_ITEM ( )  RATIONAL_B_SPLINE_CURVE ( ( 1.000000000000000000, 0.8047378541243649375, 0.8047378541243649375, 1.000000000000000000 ) ) 
 REPRESENTATION_ITEM ( '' )  );
#226862=CARTESIAN_POINT ( 'NONE',  ( 20.97239005616515328, 22.11792297137228758, -231.6940034657905301 ) ) ;
#226868=ORIENTED_EDGE ( 'NONE', *, *, #237263, .T. ) ;
#226872=DIRECTION ( 'NONE',  ( 0.000000000000000000, -0.4721928772777332917, -0.8814952561688437216 ) ) ;
#226879=EDGE_CURVE ( 'NONE', #209722, #218497, #226564, .T. ) ;
#226888=AXIS2_PLACEMENT_3D ( 'NONE', #196027, #177759, #38234 ) ;
#226894=DIRECTION ( 'NONE',  ( 0.000000000000000000, 0.8096735173027139743, -0.5868805631290339164 ) ) ;
#226912=AXIS2_PLACEMENT_3D ( 'NONE', #136279, #83989, #166187 ) ;
#226929=ADVANCED_FACE ( 'NONE', ( #12621 ), #137649, .F. ) ;
#226952=CIRCLE ( 'NONE', #214463, 11.74999999999999822 ) ;
#226959=AXIS2_PLACEMENT_3D ( 'NONE', #204372, #242216, #45313 ) ;
#226987=DIRECTION ( 'NONE',  ( -1.000000000000000000, 0.000000000000000000, 0.000000000000000000 ) ) ;
#227024=DIRECTION ( 'NONE',  ( 0.000000000000000000, -0.8814952561688629284, 0.4721928772776973204 ) ) ;
#227043=CARTESIAN_POINT ( 'NONE',  ( 22.49999999999999645, 12.54152817314150070, -223.4164406214577241 ) ) ;
#227052=ORIENTED_EDGE ( 'NONE', *, *, #89318, .T. ) ;
#227078=DIRECTION ( 'NONE',  ( -2.602085213965225788E-14, 0.8814952561688430555, -0.4721928772777346239 ) ) ;
#227085=AXIS2_PLACEMENT_3D ( 'NONE', #125138, #80840, #23493 ) ;
#227094=CARTESIAN_POINT ( 'NONE',  ( -18.39999999999999858, 8.841736820195469804, -245.4273993276876240 ) ) ;
#227109=VECTOR ( 'NONE', #213267, 1000.000000000000000 ) ;
#227126=VERTEX_POINT ( 'NONE', #19002 ) ;
#227134=ADVANCED_FACE ( 'NONE', ( #234194 ), #55532, .F. ) ;
#227137=DIRECTION ( 'NONE',  ( 1.000000000000000000, 0.000000000000000000, 0.000000000000000000 ) ) ;
#227159=VERTEX_POINT ( 'NONE', #235481 ) ;
#227171=AXIS2_PLACEMENT_3D ( 'NONE', #142173, #46906, #5202 ) ;
#227178=ORIENTED_EDGE ( 'NONE', *, *, #99711, .T. ) ;
#227212=EDGE_CURVE ( 'NONE', #146046, #171481, #97562, .T. ) ;
#227213=CARTESIAN_POINT ( 'NONE',  ( -21.14999999999999858, -3.140208063160686791, -228.2318569537739847 ) ) ;
#227219=FACE_OUTER_BOUND ( 'NONE', #19846, .T. ) ;
#227224=CYLINDRICAL_SURFACE ( 'NONE', #202876, 0.09999999999999939493 ) ;
#227227=CARTESIAN_POINT ( 'NONE',  ( 18.36493879433257348, 38.27493291353503935, -261.1939576383761050 ) ) ;
#227235=DIRECTION ( 'NONE',  ( 0.000000000000000000, -0.4721928772777366778, -0.8814952561688420563 ) ) ;
#227255=DIRECTION ( 'NONE',  ( 1.000000000000000000, -0.000000000000000000, -0.000000000000000000 ) ) ;
#227259=LINE ( 'NONE', #224682, #166815 ) ;
#227282=FACE_OUTER_BOUND ( 'NONE', #199529, .T. ) ;
#227288=CARTESIAN_POINT ( 'NONE',  ( -20.54999999999999716, 21.35054858842500281, -233.1262234518673893 ) ) ;
#227289=AXIS2_PLACEMENT_3D ( 'NONE', #230371, #169153, #210813 ) ;
#227296=CARTESIAN_POINT ( 'NONE',  ( -21.10320863425827298, 1.498834514567453757, -230.6884789221961398 ) ) ;
#227308=CARTESIAN_POINT ( 'NONE',  ( 23.14999999999999503, 35.97645343225767789, -235.9694016464868298 ) ) ;
#227335=DIRECTION ( 'NONE',  ( 1.000000000000000000, -0.000000000000000000, -0.000000000000000000 ) ) ;
#227339=PLANE ( 'NONE',  #190689 ) ;
#227375=SPHERICAL_SURFACE ( 'NONE', #161192, 0.1000000000000000056 ) ;
#227435=CARTESIAN_POINT ( 'NONE',  ( -23.25000000000000000, 7.128833340093095217, -233.7327013124392749 ) ) ;
#227439=EDGE_CURVE ( 'NONE', #31578, #211434, #168753, .T. ) ;
#227440=CARTESIAN_POINT ( 'NONE',  ( 18.59999999999999787, 43.02787096365918984, -254.3959382439171577 ) ) ;
#227446=EDGE_LOOP ( 'NONE', ( #165152, #210335, #35160, #155835 ) ) ;
#227460=ORIENTED_EDGE ( 'NONE', *, *, #168457, .F. ) ;
#227521=CARTESIAN_POINT ( 'NONE',  ( -22.59066674512257933, 12.65021040783261697, -223.3607282225494544 ) ) ;
#227522=AXIS2_PLACEMENT_3D ( 'NONE', #246095, #44034, #67437 ) ;
#227537=EDGE_CURVE ( 'NONE', #201330, #16880, #172843, .T. ) ;
#227538=( BOUNDED_CURVE ( )  B_SPLINE_CURVE ( 3, ( #253213, #211533, #113709, #97970 ),
 .UNSPECIFIED., .F., .F. ) 
 B_SPLINE_CURVE_WITH_KNOTS ( ( 4, 4 ),
 ( 1.570796326794901443, 3.141592653589853956 ),
 .UNSPECIFIED. ) 
 CURVE ( )  GEOMETRIC_REPRESENTATION_ITEM ( )  RATIONAL_B_SPLINE_CURVE ( ( 1.000000000000000000, 0.8047378541243517258, 0.8047378541243517258, 1.000000000000000000 ) ) 
 REPRESENTATION_ITEM ( '' )  );
#227548=CARTESIAN_POINT ( 'NONE',  ( 21.00000000000000000, 22.61918030723622408, -230.9697045991730988 ) ) ;
#227573=CIRCLE ( 'NONE', #189986, 0.09999999999999939493 ) ;
#227592=CIRCLE ( 'NONE', #127656, 0.1999999999999987899 ) ;
#227619=EDGE_LOOP ( 'NONE', ( #106846, #186165, #240361, #207657 ) ) ;
#227643=CARTESIAN_POINT ( 'NONE',  ( -18.50000000000000000, 43.08613539620618837, -254.3146655184800409 ) ) ;
#227652=CARTESIAN_POINT ( 'NONE',  ( 18.50000000000000000, 8.860057415267860392, -245.3237695635339719 ) ) ;
#227675=DIRECTION ( 'NONE',  ( 1.000000000000000000, 3.448943450116723568E-16, 6.438528483529607644E-16 ) ) ;
#227696=EDGE_CURVE ( 'NONE', #200406, #51015, #160352, .T. ) ;
#227700=CIRCLE ( 'NONE', #2852, 1.899999999999996136 ) ;
#227706=AXIS2_PLACEMENT_3D ( 'NONE', #248777, #190080, #209640 ) ;
#227771=CARTESIAN_POINT ( 'NONE',  ( 18.41789779300687258, 8.841737057899697660, -245.4273994550192697 ) ) ;
#227775=AXIS2_PLACEMENT_3D ( 'NONE', #249480, #27887, #147809 ) ;
#227779=CARTESIAN_POINT ( 'NONE',  ( 18.52643265882457868, 46.42459709376392851, -243.0752906381742662 ) ) ;
#227794=DIRECTION ( 'NONE',  ( 0.000000000000000000, -0.4721928772777346239, -0.8814952561688430555 ) ) ;
#227795=CIRCLE ( 'NONE', #177936, 0.1000000000000013933 ) ;
#227801=DIRECTION ( 'NONE',  ( 0.000000000000000000, 0.8814952561688629284, -0.4721928772776973204 ) ) ;
#227815=VERTEX_POINT ( 'NONE', #170131 ) ;
#227844=ORIENTED_EDGE ( 'NONE', *, *, #48872, .T. ) ;
#227874=VERTEX_POINT ( 'NONE', #78671 ) ;
#227917=ORIENTED_EDGE ( 'NONE', *, *, #157322, .T. ) ;
#227923=CARTESIAN_POINT ( 'NONE',  ( 22.49436431346199683, -3.108951784663558371, -228.1727023102511964 ) ) ;
#227951=VERTEX_POINT ( 'NONE', #215619 ) ;
#228010=DIRECTION ( 'NONE',  ( 0.000000000000000000, 0.8814952561688428334, -0.4721928772777350125 ) ) ;
#228020=ORIENTED_EDGE ( 'NONE', *, *, #243357, .T. ) ;
#228025=CIRCLE ( 'NONE', #195086, 0.3999999999999885869 ) ;
#228049=CARTESIAN_POINT ( 'NONE',  ( -23.15000000000000213, 26.22918441313017723, -241.0147027585851731 ) ) ;
#228062=DIRECTION ( 'NONE',  ( -0.000000000000000000, 0.8496786552930076786, 0.5273008465188218086 ) ) ;
#228097=CARTESIAN_POINT ( 'NONE',  ( -21.05000000000000426, 1.561552638127804205, -230.7743248509848399 ) ) ;
#228152=ORIENTED_EDGE ( 'NONE', *, *, #40329, .T. ) ;
#228154=ORIENTED_EDGE ( 'NONE', *, *, #160954, .F. ) ;
#228198=DIRECTION ( 'NONE',  ( 1.000000000000000000, 0.000000000000000000, 0.000000000000000000 ) ) ;
#228221=ADVANCED_FACE ( 'NONE', ( #229755 ), #130651, .T. ) ;
#228228=DIRECTION ( 'NONE',  ( -0.000000000000000000, 0.8814952561688428334, -0.4721928772777352346 ) ) ;
#228252=CARTESIAN_POINT ( 'NONE',  ( -21.15000000000000213, 1.363275264940683629, -230.6442496871288483 ) ) ;
#228261=CARTESIAN_POINT ( 'NONE',  ( -21.30740335185486245, 1.395886663891752866, -230.5494838277682845 ) ) ;
#228292=CONICAL_SURFACE ( 'NONE', #120177, 7.750000000000028422, 0.7853981633974531640 ) ;
#228304=CARTESIAN_POINT ( 'NONE',  ( 18.49999999999999289, 42.15997144203495139, -239.2817429668763793 ) ) ;
#228349=AXIS2_PLACEMENT_3D ( 'NONE', #34051, #171008, #112282 ) ;
#228367=CARTESIAN_POINT ( 'NONE',  ( 21.05000000000000071, 36.02367271998545561, -235.8812521208699309 ) ) ;
#228368=AXIS2_PLACEMENT_3D ( 'NONE', #3411, #161232, #101198 ) ;
#228413=EDGE_CURVE ( 'NONE', #48651, #63775, #203136, .T. ) ;
#228416=CARTESIAN_POINT ( 'NONE',  ( 23.24999999999999289, 30.38404434817536881, -239.4399867032565794 ) ) ;
#228430=DIRECTION ( 'NONE',  ( -1.000000000000000000, -0.000000000000000000, -0.000000000000000000 ) ) ;
#228433=CIRCLE ( 'NONE', #174293, 12.77500000000000036 ) ;
#228472=VECTOR ( 'NONE', #68567, 1000.000000000000000 ) ;
#228487=CARTESIAN_POINT ( 'NONE',  ( 21.14999999999999858, 22.16427325743960708, -231.8189304678590190 ) ) ;
#228497=ORIENTED_EDGE ( 'NONE', *, *, #136276, .F. ) ;
#228511=EDGE_LOOP ( 'NONE', ( #209784, #223260, #140999, #218656 ) ) ;
#228519=ORIENTED_EDGE ( 'NONE', *, *, #12578, .F. ) ;
#228522=ORIENTED_EDGE ( 'NONE', *, *, #203732, .T. ) ;
#228524=DIRECTION ( 'NONE',  ( -1.000000000000000000, -1.394253735153569469E-16, -2.602809386958778209E-16 ) ) ;
#228526=EDGE_CURVE ( 'NONE', #93557, #105209, #169181, .T. ) ;
#228533=CARTESIAN_POINT ( 'NONE',  ( 21.76363531954645936, 10.35302234425203949, -227.5040830337958937 ) ) ;
#228544=EDGE_CURVE ( 'NONE', #239499, #67751, #156449, .T. ) ;
#228554=VECTOR ( 'NONE', #177208, 1000.000000000000000 ) ;
#228604=FACE_OUTER_BOUND ( 'NONE', #142200, .T. ) ;
#228632=ORIENTED_EDGE ( 'NONE', *, *, #213544, .T. ) ;
#228642=VECTOR ( 'NONE', #51920, 1000.000000000000000 ) ;
#228654=DIRECTION ( 'NONE',  ( 1.000000000000000000, 0.000000000000000000, 0.000000000000000000 ) ) ;
#228665=TOROIDAL_SURFACE ( 'NONE', #149550, 0.4000000000000012990, 0.1000000000000000056 ) ;
#228667=EDGE_CURVE ( 'NONE', #140599, #119943, #17753, .T. ) ;
#228668=AXIS2_PLACEMENT_3D ( 'NONE', #16170, #72277, #194807 ) ;
#228702=CARTESIAN_POINT ( 'NONE',  ( 23.14999999999999858, 19.92792862942048870, -235.1286901285539841 ) ) ;
#228706=CIRCLE ( 'NONE', #37162, 0.09999999999999939493 ) ;
#228717=ORIENTED_EDGE ( 'NONE', *, *, #35771, .F. ) ;
#228761=AXIS2_PLACEMENT_3D ( 'NONE', #229946, #212956, #51277 ) ;
#228767=AXIS2_PLACEMENT_3D ( 'NONE', #124035, #99296, #101864 ) ;
#228768=AXIS2_PLACEMENT_3D ( 'NONE', #221908, #84956, #242771 ) ;
#228770=CARTESIAN_POINT ( 'NONE',  ( 22.50000000000000000, 0.3085173699977246109, -229.9658011520297975 ) ) ;
#228779=VECTOR ( 'NONE', #90971, 1000.000000000000000 ) ;
#228803=CARTESIAN_POINT ( 'NONE',  ( 18.49999999999999645, 7.128833340093095217, -233.7327013124392749 ) ) ;
#228812=TOROIDAL_SURFACE ( 'NONE', #253720, 12.97499999999999787, 0.1000000000000000056 ) ;
#228821=EDGE_CURVE ( 'NONE', #88893, #248473, #166313, .T. ) ;
#228834=EDGE_CURVE ( 'NONE', #251809, #29656, #85819, .T. ) ;
#228839=ORIENTED_EDGE ( 'NONE', *, *, #71658, .T. ) ;
#228861=DIRECTION ( 'NONE',  ( 0.000000000000000000, 0.8814952561688136345, -0.4721928772777895800 ) ) ;
#228934=ORIENTED_EDGE ( 'NONE', *, *, #14755, .F. ) ;
#228955=ADVANCED_FACE ( 'NONE', ( #191000 ), #82791, .T. ) ;
#228962=ORIENTED_EDGE ( 'NONE', *, *, #17488, .F. ) ;
#229037=AXIS2_PLACEMENT_3D ( 'NONE', #62901, #56766, #154651 ) ;
#229044=CARTESIAN_POINT ( 'NONE',  ( -21.46681500597906833, 1.083969783932762665, -230.4946333871049831 ) ) ;
#229050=DIRECTION ( 'NONE',  ( 1.000000000000000000, 0.000000000000000000, 0.000000000000000000 ) ) ;
#229060=DIRECTION ( 'NONE',  ( 0.000000000000000000, 0.4721928772777344574, 0.8814952561688431665 ) ) ;
#229089=DIRECTION ( 'NONE',  ( -1.000000000000000000, 0.000000000000000000, 0.000000000000000000 ) ) ;
#229121=VECTOR ( 'NONE', #161678, 1000.000000000000000 ) ;
#229163=ORIENTED_EDGE ( 'NONE', *, *, #51019, .F. ) ;
#229180=DIRECTION ( 'NONE',  ( 1.000000000000000000, 0.000000000000000000, 0.000000000000000000 ) ) ;
#229197=ORIENTED_EDGE ( 'NONE', *, *, #194663, .F. ) ;
#229215=DIRECTION ( 'NONE',  ( -1.000000000000000000, 0.000000000000000000, -0.000000000000000000 ) ) ;
#229221=DIRECTION ( 'NONE',  ( 0.000000000000000000, -0.8814952561688438326, 0.4721928772777334582 ) ) ;
#229225=ORIENTED_EDGE ( 'NONE', *, *, #133206, .T. ) ;
#229233=AXIS2_PLACEMENT_3D ( 'NONE', #189294, #188008, #231001 ) ;
#229253=DIRECTION ( 'NONE',  ( 1.000000000000000000, 1.394253735153569469E-16, 2.602809386958778209E-16 ) ) ;
#229265=DIRECTION ( 'NONE',  ( -1.000000000000000000, 0.000000000000000000, 0.000000000000000000 ) ) ;
#229267=AXIS2_PLACEMENT_3D ( 'NONE', #130476, #190487, #169658 ) ;
#229278=CARTESIAN_POINT ( 'NONE',  ( 22.60000000000000142, -3.180729737797944434, -228.0957332317254895 ) ) ;
#229296=LINE ( 'NONE', #72810, #217257 ) ;
#229301=CARTESIAN_POINT ( 'NONE',  ( -18.50000000000000000, 36.65892442174935439, -249.5511627012433848 ) ) ;
#229310=AXIS2_PLACEMENT_3D ( 'NONE', #158781, #235710, #255229 ) ;
#229318=EDGE_CURVE ( 'NONE', #114424, #71987, #69460, .T. ) ;
#229346=DIRECTION ( 'NONE',  ( 0.000000000000000000, 0.8814952561688431665, -0.4721928772777345129 ) ) ;
#229375=CARTESIAN_POINT ( 'NONE',  ( -23.15000000000000213, 2.272311100394799332, -217.9150152700588592 ) ) ;
#229390=LINE ( 'NONE', #188969, #110096 ) ;
#229420=VECTOR ( 'NONE', #24645, 1000.000000000000000 ) ;
#229428=VECTOR ( 'NONE', #34315, 1000.000000000000000 ) ;
#229442=CARTESIAN_POINT ( 'NONE',  ( 21.13461538461538325, 22.21093039075207898, -231.7318303787629930 ) ) ;
#229454=DIRECTION ( 'NONE',  ( 0.000000000000000000, 0.8814952561688430555, -0.4721928772777346239 ) ) ;
#229485=ORIENTED_EDGE ( 'NONE', *, *, #12355, .F. ) ;
#229486=ADVANCED_FACE ( 'NONE', ( #18455 ), #176273, .T. ) ;
#229490=VERTEX_POINT ( 'NONE', #156718 ) ;
#229494=CARTESIAN_POINT ( 'NONE',  ( -23.25000000000000000, 2.272311100394799332, -217.9150152700588592 ) ) ;
#229516=CIRCLE ( 'NONE', #62906, 0.1000000000000013933 ) ;
#229542=ORIENTED_EDGE ( 'NONE', *, *, #210732, .F. ) ;
#229563=CARTESIAN_POINT ( 'NONE',  ( -23.25000000000000000, 19.89303971870268839, -235.6353404070293038 ) ) ;
#229609=ADVANCED_FACE ( 'NONE', ( #238794 ), #61284, .T. ) ;
#229652=ORIENTED_EDGE ( 'NONE', *, *, #51400, .T. ) ;
#229664=ADVANCED_FACE ( 'NONE', ( #200943 ), #102955, .F. ) ;
#229717=DIRECTION ( 'NONE',  ( 1.000000000000000000, 0.000000000000000000, 0.000000000000000000 ) ) ;
#229719=ORIENTED_EDGE ( 'NONE', *, *, #53034, .F. ) ;
#229746=AXIS2_PLACEMENT_3D ( 'NONE', #224156, #2537, #45532 ) ;
#229755=FACE_OUTER_BOUND ( 'NONE', #213392, .T. ) ;
#229763=DIRECTION ( 'NONE',  ( 0.000000000000000000, 0.6052030477779125617, 0.7960711469211315672 ) ) ;
#229803=EDGE_CURVE ( 'NONE', #170728, #1479, #236425, .T. ) ;
#229809=EDGE_CURVE ( 'NONE', #6683, #175441, #169571, .T. ) ;
#229844=DIRECTION ( 'NONE',  ( -0.9880948137434723000, 0.07264505804272583522, 0.1356146547952018222 ) ) ;
#229854=ORIENTED_EDGE ( 'NONE', *, *, #104104, .T. ) ;
#229868=ORIENTED_EDGE ( 'NONE', *, *, #109231, .T. ) ;
#229893=ORIENTED_EDGE ( 'NONE', *, *, #113230, .F. ) ;
#229909=CARTESIAN_POINT ( 'NONE',  ( -21.52071067811865746, 29.53393254175612981, -236.9093933209877889 ) ) ;
#229914=CARTESIAN_POINT ( 'NONE',  ( 21.14999999999999858, 7.128833340093095217, -233.7327013124392749 ) ) ;
#229918=CARTESIAN_POINT ( 'NONE',  ( -20.64999999999999858, 21.35054858842500281, -233.1262234518673893 ) ) ;
#229923=LINE ( 'NONE', #154287, #61151 ) ;
#229939=SPHERICAL_SURFACE ( 'NONE', #75093, 0.1000000000000000056 ) ;
#229946=CARTESIAN_POINT ( 'NONE',  ( -23.15000000000000213, 28.50120599808395028, -258.2149742250584268 ) ) ;
#229958=DIRECTION ( 'NONE',  ( 0.000000000000000000, 0.8814952561688428334, -0.4721928772777349570 ) ) ;
#229968=AXIS2_PLACEMENT_3D ( 'NONE', #62594, #23497, #126404 ) ;
#229988=VERTEX_POINT ( 'NONE', #241065 ) ;
#229996=VERTEX_POINT ( 'NONE', #239773 ) ;
#230002=FACE_OUTER_BOUND ( 'NONE', #40516, .T. ) ;
#230003=CARTESIAN_POINT ( 'NONE',  ( -20.54999999999999716, 11.41170713998153019, -246.6906184681487559 ) ) ;
#230005=ORIENTED_EDGE ( 'NONE', *, *, #6477, .T. ) ;
#230023=CIRCLE ( 'NONE', #175885, 0.09999999999999939493 ) ;
#230029=ORIENTED_EDGE ( 'NONE', *, *, #34551, .T. ) ;
#230050=ORIENTED_EDGE ( 'NONE', *, *, #155652, .T. ) ;
#230054=CARTESIAN_POINT ( 'NONE',  ( 20.04142135623730070, 31.44980407958351165, -233.5445995079518866 ) ) ;
#230062=ORIENTED_EDGE ( 'NONE', *, *, #73375, .T. ) ;
#230068=DIRECTION ( 'NONE',  ( 0.000000000000000000, -0.4721928772777346239, -0.8814952561688430555 ) ) ;
#230075=EDGE_CURVE ( 'NONE', #188830, #151273, #148966, .T. ) ;
#230080=EDGE_CURVE ( 'NONE', #231806, #161820, #34599, .T. ) ;
#230098=EDGE_CURVE ( 'NONE', #177802, #121353, #57344, .T. ) ;
#230109=EDGE_CURVE ( 'NONE', #149301, #171330, #192307, .T. ) ;
#230110=EDGE_LOOP ( 'NONE', ( #15381, #14041, #131690, #47556 ) ) ;
#230156=EDGE_CURVE ( 'NONE', #67751, #215045, #107429, .T. ) ;
#230169=DIRECTION ( 'NONE',  ( 1.000000000000000000, 0.000000000000000000, 0.000000000000000000 ) ) ;
#230212=AXIS2_PLACEMENT_3D ( 'NONE', #66779, #147596, #247970 ) ;
#230215=VECTOR ( 'NONE', #83909, 1000.000000000000000 ) ;
#230227=LINE ( 'NONE', #133694, #21408 ) ;
#230232=CIRCLE ( 'NONE', #63633, 3.999999999999994671 ) ;
#230301=AXIS2_PLACEMENT_3D ( 'NONE', #129858, #12516, #251085 ) ;
#230307=CARTESIAN_POINT ( 'NONE',  ( -22.00411653889204899, 0.7817229495032812503, -230.2203756341760368 ) ) ;
#230320=ORIENTED_EDGE ( 'NONE', *, *, #116481, .F. ) ;
#230334=CARTESIAN_POINT ( 'NONE',  ( 18.50000000000000000, 9.063861706928131312, -245.4572825683437998 ) ) ;
#230367=DIRECTION ( 'NONE',  ( 1.000000000000000000, 0.000000000000000000, 0.000000000000000000 ) ) ;
#230371=CARTESIAN_POINT ( 'NONE',  ( -22.39999999999999858, 0.3085173699977072914, -229.9658011520297691 ) ) ;
#230423=DIRECTION ( 'NONE',  ( 0.000000000000000000, -0.4721928772777346239, -0.8814952561688430555 ) ) ;
#230425=DIRECTION ( 'NONE',  ( 1.000000000000000000, 0.000000000000000000, 0.000000000000000000 ) ) ;
#230435=ORIENTED_EDGE ( 'NONE', *, *, #144131, .T. ) ;
#230438=CARTESIAN_POINT ( 'NONE',  ( 21.14999999999999858, 7.081614052365321932, -233.8208508380561454 ) ) ;
#230445=CARTESIAN_POINT ( 'NONE',  ( -23.15000000000000213, 7.128833340093095217, -233.7327013124392749 ) ) ;
#230494=CARTESIAN_POINT ( 'NONE',  ( 22.46250603428203618, -3.130481585860003690, -228.2130804456526221 ) ) ;
#230514=VERTEX_POINT ( 'NONE', #94167 ) ;
#230551=CARTESIAN_POINT ( 'NONE',  ( -23.15000000000000213, 24.17260720300848931, -252.6908294531417027 ) ) ;
#230586=EDGE_CURVE ( 'NONE', #108268, #42982, #210290, .T. ) ;
#230593=CARTESIAN_POINT ( 'NONE',  ( -18.50000000000000711, 18.81339837015603322, -226.7756228984618190 ) ) ;
#230598=DIRECTION ( 'NONE',  ( -0.7071067811865473507, -0.3338907855510733769, -0.6233112732207618523 ) ) ;
#230680=CARTESIAN_POINT ( 'NONE',  ( 21.30000000000002558, 3.558777552609281081, -231.8203201594644725 ) ) ;
#230684=AXIS2_PLACEMENT_3D ( 'NONE', #187372, #47821, #145647 ) ;
#230706=CARTESIAN_POINT ( 'NONE',  ( 21.05000000000000071, 30.43677443282724937, -239.5249545687858870 ) ) ;
#230734=CARTESIAN_POINT ( 'NONE',  ( 21.03675099975490781, 22.18453705941069387, -231.7293054214682115 ) ) ;
#230744=CARTESIAN_POINT ( 'NONE',  ( -20.05000000000000426, 22.38308386859736032, -231.4104522272575082 ) ) ;
#230753=CIRCLE ( 'NONE', #164112, 0.09999999999999939493 ) ;
#230775=FACE_OUTER_BOUND ( 'NONE', #88202, .T. ) ;
#230788=AXIS2_PLACEMENT_3D ( 'NONE', #71698, #207352, #46956 ) ;
#230816=ORIENTED_EDGE ( 'NONE', *, *, #153884, .F. ) ;
#230843=EDGE_CURVE ( 'NONE', #92492, #152553, #202713, .T. ) ;
#230881=FACE_OUTER_BOUND ( 'NONE', #85644, .T. ) ;
#230883=DIRECTION ( 'NONE',  ( -0.000000000000000000, -0.8814952561688430555, 0.4721928772777346239 ) ) ;
#230886=CIRCLE ( 'NONE', #134967, 0.1000000000000092620 ) ;
#230925=EDGE_LOOP ( 'NONE', ( #111100, #90609, #20988, #24928 ) ) ;
#230975=CARTESIAN_POINT ( 'NONE',  ( -20.54999999999999716, 20.22419170005074918, -254.0771499268472553 ) ) ;
#230985=DIRECTION ( 'NONE',  ( 1.000000000000000000, 0.000000000000000000, 0.000000000000000000 ) ) ;
#230993=LINE ( 'NONE', #191877, #207208 ) ;
#231001=DIRECTION ( 'NONE',  ( 0.000000000000000000, 0.8814952561688437216, -0.4721928772777334582 ) ) ;
#231011=ORIENTED_EDGE ( 'NONE', *, *, #15570, .F. ) ;
#231037=CARTESIAN_POINT ( 'NONE',  ( 20.84451136049273146, 18.74944765725850004, -227.9096743945612502 ) ) ;
#231052=EDGE_LOOP ( 'NONE', ( #240840, #196648, #13007, #83764 ) ) ;
#231053=VECTOR ( 'NONE', #55623, 1000.000000000000000 ) ;
#231084=VERTEX_POINT ( 'NONE', #203493 ) ;
#231085=CARTESIAN_POINT ( 'NONE',  ( 23.14999999999999858, 38.50047664313251516, -246.1133312021848951 ) ) ;
#231097=ADVANCED_FACE ( 'NONE', ( #146070 ), #5255, .T. ) ;
#231105=CARTESIAN_POINT ( 'NONE',  ( 18.49999999999999289, 33.89924982463041658, -236.3385223663007366 ) ) ;
#231111=CARTESIAN_POINT ( 'NONE',  ( 18.43466021071393612, 38.00874357722931762, -261.0447760932440815 ) ) ;
#231114=AXIS2_PLACEMENT_3D ( 'NONE', #257504, #142739, #42374 ) ;
#231116=EDGE_CURVE ( 'NONE', #243045, #104543, #46961, .T. ) ;
#231124=DIRECTION ( 'NONE',  ( -2.252264143451593525E-15, 0.8127272543710891695, -0.5826443254700338636 ) ) ;
#231126=CARTESIAN_POINT ( 'NONE',  ( 21.07946286933444213, 1.586026531860189381, -230.6765785263235955 ) ) ;
#231154=CARTESIAN_POINT ( 'NONE',  ( 18.49999999999999289, 1.591682202823531123, -219.1856213577225105 ) ) ;
#231160=DIRECTION ( 'NONE',  ( 1.000000000000000000, 0.000000000000000000, 0.000000000000000000 ) ) ;
#231175=EDGE_LOOP ( 'NONE', ( #130300, #135459, #66358, #67115 ) ) ;
#231177=AXIS2_PLACEMENT_3D ( 'NONE', #237839, #155767, #158340 ) ;
#231184=DIRECTION ( 'NONE',  ( 0.000000000000000000, -0.8127272543710951647, 0.5826443254700257590 ) ) ;
#231197=VECTOR ( 'NONE', #68753, 1000.000000000000000 ) ;
#231200=CARTESIAN_POINT ( 'NONE',  ( -20.85000000000000142, 31.15787740146373253, -259.8205824356103903 ) ) ;
#231219=DIRECTION ( 'NONE',  ( 1.000000000000000000, 0.000000000000000000, 0.000000000000000000 ) ) ;
#231232=CARTESIAN_POINT ( 'NONE',  ( -21.05000000000000071, 10.91926294161908295, -235.7631306847335395 ) ) ;
#231237=EDGE_CURVE ( 'NONE', #119326, #109890, #132178, .T. ) ;
#231260=LINE ( 'NONE', #17338, #64793 ) ;
#231273=AXIS2_PLACEMENT_3D ( 'NONE', #67397, #146915, #126071 ) ;
#231288=EDGE_CURVE ( 'NONE', #12130, #120155, #103118, .T. ) ;
#231298=DIRECTION ( 'NONE',  ( 0.000000000000000000, 0.8814952561688476074, -0.4721928772777262417 ) ) ;
#231326=LINE ( 'NONE', #35704, #172768 ) ;
#231360=FACE_OUTER_BOUND ( 'NONE', #165936, .T. ) ;
#231392=CARTESIAN_POINT ( 'NONE',  ( -23.15000000000000213, 11.39998237908105416, -245.7725481090871540 ) ) ;
#231421=EDGE_CURVE ( 'NONE', #179081, #45747, #203085, .T. ) ;
#231433=DIRECTION ( 'NONE',  ( 1.000000000000000000, 0.000000000000000000, 0.000000000000000000 ) ) ;
#231435=ORIENTED_EDGE ( 'NONE', *, *, #145341, .F. ) ;
#231451=CARTESIAN_POINT ( 'NONE',  ( 21.11825140030058279, 1.450638645453875553, -230.6828758114810967 ) ) ;
#231452=CARTESIAN_POINT ( 'NONE',  ( -20.94999999999999929, 18.71344899777637494, -226.7788045585494103 ) ) ;
#231461=CARTESIAN_POINT ( 'NONE',  ( 20.94999999999999574, 14.68288696042412589, -236.3611559727223437 ) ) ;
#231463=CIRCLE ( 'NONE', #114750, 0.09999999999999939493 ) ;
#231468=AXIS2_PLACEMENT_3D ( 'NONE', #64841, #42719, #239646 ) ;
#231475=DIRECTION ( 'NONE',  ( 0.000000000000000000, 0.4797419643160688585, 0.8774096236502991752 ) ) ;
#231478=DIRECTION ( 'NONE',  ( 1.000000000000000000, -0.000000000000000000, -0.000000000000000000 ) ) ;
#231480=ORIENTED_EDGE ( 'NONE', *, *, #202453, .F. ) ;
#231516=DIRECTION ( 'NONE',  ( 0.000000000000000000, 0.8814952561688166321, -0.4721928772777839733 ) ) ;
#231524=EDGE_LOOP ( 'NONE', ( #244430, #208314, #186811, #254155 ) ) ;
#231551=FACE_OUTER_BOUND ( 'NONE', #33609, .T. ) ;
#231567=VECTOR ( 'NONE', #64731, 1000.000000000000000 ) ;
#231598=AXIS2_PLACEMENT_3D ( 'NONE', #142844, #161164, #15586 ) ;
#231601=CARTESIAN_POINT ( 'NONE',  ( 23.14999999999999858, 28.32080209959243788, -238.8452605374484676 ) ) ;
#231618=CARTESIAN_POINT ( 'NONE',  ( 20.94999999999999574, 4.360421613930905771, -245.4659189663672691 ) ) ;
#231700=CARTESIAN_POINT ( 'NONE',  ( 21.05000000000000071, 1.658775325997237315, -230.6916041481598540 ) ) ;
#231726=ORIENTED_EDGE ( 'NONE', *, *, #86801, .F. ) ;
#231732=VERTEX_POINT ( 'NONE', #135173 ) ;
#231744=EDGE_LOOP ( 'NONE', ( #116376, #93127, #32200, #63565 ) ) ;
#231755=CARTESIAN_POINT ( 'NONE',  ( 18.49999999999999289, 46.32970330538243786, -243.0551226933711746 ) ) ;
#231782=FACE_OUTER_BOUND ( 'NONE', #234915, .T. ) ;
#231806=VERTEX_POINT ( 'NONE', #102441 ) ;
#231807=CIRCLE ( 'NONE', #56419, 11.75000000000000355 ) ;
#231823=VECTOR ( 'NONE', #47597, 1000.000000000000000 ) ;
#231831=LINE ( 'NONE', #11502, #54327 ) ;
#231854=FACE_OUTER_BOUND ( 'NONE', #181329, .T. ) ;
#231868=VERTEX_POINT ( 'NONE', #140303 ) ;
#231880=CARTESIAN_POINT ( 'NONE',  ( -23.25000000000000000, 7.128833340093095217, -233.7327013124392749 ) ) ;
#231886=CARTESIAN_POINT ( 'NONE',  ( 21.09546886439511582, 22.10816305914821100, -231.6845674164850948 ) ) ;
#231897=DIRECTION ( 'NONE',  ( 0.000000000000000000, 0.8814952561688444987, -0.4721928772777320149 ) ) ;
#231909=CYLINDRICAL_SURFACE ( 'NONE', #164420, 0.1000000000000013933 ) ;
#231916=DIRECTION ( 'NONE',  ( 0.000000000000000000, -0.8127272543710951647, 0.5826443254700256480 ) ) ;
#231948=VERTEX_POINT ( 'NONE', #233681 ) ;
#231949=CARTESIAN_POINT ( 'NONE',  ( -21.05000000000000071, 14.77103648604101060, -236.4083752604501001 ) ) ;
#231974=DIRECTION ( 'NONE',  ( 1.000000000000000000, -0.000000000000000000, -0.000000000000000000 ) ) ;
#231979=ORIENTED_EDGE ( 'NONE', *, *, #150379, .F. ) ;
#231997=DIRECTION ( 'NONE',  ( 0.000000000000000000, 0.8814952561688428334, -0.4721928772777350125 ) ) ;
#232026=DIRECTION ( 'NONE',  ( 0.000000000000000000, -0.8814952561688476074, 0.4721928772777262417 ) ) ;
#232038=EDGE_LOOP ( 'NONE', ( #93824, #20576, #4214, #197265, #256745, #44081, #47269, #143014, #243373, #16384, #98424, #95229, #225213, #66173, #249997, #91292 ) ) ;
#232071=CARTESIAN_POINT ( 'NONE',  ( 23.14999999999999503, -0.1830918614494220220, -222.4987906021368360 ) ) ;
#232096=EDGE_LOOP ( 'NONE', ( #1156, #237237, #128500, #92714 ) ) ;
#232127=DIRECTION ( 'NONE',  ( -1.000000000000000000, -1.394253735153569469E-16, -2.602809386958778209E-16 ) ) ;
#232134=AXIS2_PLACEMENT_3D ( 'NONE', #184770, #239627, #180934 ) ;
#232146=DIRECTION ( 'NONE',  ( 0.000000000000000000, 0.5826443254699606999, 0.8127272543711416830 ) ) ;
#232160=EDGE_CURVE ( 'NONE', #192532, #142373, #37077, .T. ) ;
#232193=DIRECTION ( 'NONE',  ( -1.000000000000000000, 0.000000000000000000, -0.000000000000000000 ) ) ;
#232194=CARTESIAN_POINT ( 'NONE',  ( 23.24999999999999645, 37.65052946403260137, -247.7000226632887916 ) ) ;
#232245=LINE ( 'NONE', #37895, #51573 ) ;
#232288=EDGE_CURVE ( 'NONE', #195613, #223845, #137005, .T. ) ;
#232309=EDGE_CURVE ( 'NONE', #68656, #246412, #236756, .T. ) ;
#232318=AXIS2_PLACEMENT_3D ( 'NONE', #184739, #6097, #145609 ) ;
#232322=CARTESIAN_POINT ( 'NONE',  ( 20.51284917709620359, 18.76080927800072828, -228.2665908568477278 ) ) ;
#232343=CIRCLE ( 'NONE', #244774, 6.329289321881352848 ) ;
#232350=ORIENTED_EDGE ( 'NONE', *, *, #25297, .T. ) ;
#232354=DIRECTION ( 'NONE',  ( 0.000000000000000000, 0.8814952561688437216, -0.4721928772777334582 ) ) ;
#232367=ORIENTED_EDGE ( 'NONE', *, *, #222249, .F. ) ;
#232368=CARTESIAN_POINT ( 'NONE',  ( -21.05000000000000071, 10.19179799255971375, -228.2265004863033369 ) ) ;
#232375=CARTESIAN_POINT ( 'NONE',  ( 22.57320508075687115, 12.67709964810647882, -223.3751320524553705 ) ) ;
#232413=EDGE_LOOP ( 'NONE', ( #199198, #65479, #256504, #213779 ) ) ;
#232419=CYLINDRICAL_SURFACE ( 'NONE', #170526, 0.09999999999999986677 ) ;
#232424=CARTESIAN_POINT ( 'NONE',  ( 18.43565242384934777, 8.780520186313291120, -245.4165333277510115 ) ) ;
#232437=CYLINDRICAL_SURFACE ( 'NONE', #203637, 11.74999999999999112 ) ;
#232452=DIRECTION ( 'NONE',  ( 0.000000000000000000, 0.9421926911474418631, -0.3350715337779995862 ) ) ;
#232485=EDGE_CURVE ( 'NONE', #171481, #242741, #182990, .T. ) ;
#232523=AXIS2_PLACEMENT_3D ( 'NONE', #86203, #49674, #186633 ) ;
#232536=AXIS2_PLACEMENT_3D ( 'NONE', #255742, #114990, #39335 ) ;
#232550=AXIS2_PLACEMENT_3D ( 'NONE', #160952, #57958, #61841 ) ;
#232569=DIRECTION ( 'NONE',  ( -0.000000000000000000, 0.4721928772777345684, 0.8814952561688429444 ) ) ;
#232577=EDGE_CURVE ( 'NONE', #9313, #26083, #177096, .T. ) ;
#232587=AXIS2_PLACEMENT_3D ( 'NONE', #50120, #129666, #87943 ) ;
#232589=ADVANCED_FACE ( 'NONE', ( #53130 ), #234389, .F. ) ;
#232590=EDGE_CURVE ( 'NONE', #220389, #246715, #171839, .T. ) ;
#232591=ORIENTED_EDGE ( 'NONE', *, *, #44978, .T. ) ;
#232623=CARTESIAN_POINT ( 'NONE',  ( 18.59999999999999076, 28.91254064196106910, -237.8576372133405528 ) ) ;
#232630=ORIENTED_EDGE ( 'NONE', *, *, #33008, .T. ) ;
#232634=TOROIDAL_SURFACE ( 'NONE', #7768, 4.149999999999999467, 0.1000000000000000056 ) ;
#232636=EDGE_LOOP ( 'NONE', ( #252169, #53862, #245195, #77798 ) ) ;
#232645=ORIENTED_EDGE ( 'NONE', *, *, #130909, .F. ) ;
#232648=DIRECTION ( 'NONE',  ( 0.000000000000000000, 0.8814952561688416122, -0.4721928772777371219 ) ) ;
#232655=CARTESIAN_POINT ( 'NONE',  ( -18.48179518609190808, 38.23768179355963071, -261.1947912001946861 ) ) ;
#232657=AXIS2_PLACEMENT_3D ( 'NONE', #7268, #129788, #11136 ) ;
#232722=DIRECTION ( 'NONE',  ( 0.000000000000000000, 0.7965107556683636014, -0.6046243595031649543 ) ) ;
#232725=CARTESIAN_POINT ( 'NONE',  ( -21.05000000000000071, 10.05878724559879167, -228.1891859451582434 ) ) ;
#232736=CARTESIAN_POINT ( 'NONE',  ( 23.14999999999999503, 23.38726701055792745, -229.1122755113798348 ) ) ;
#232769=DIRECTION ( 'NONE',  ( -3.265361837132814079E-16, 0.4721928772777359007, 0.8814952561688425003 ) ) ;
#232785=ORIENTED_EDGE ( 'NONE', *, *, #244241, .F. ) ;
#232810=CYLINDRICAL_SURFACE ( 'NONE', #142008, 0.09999999999999939493 ) ;
#232815=EDGE_CURVE ( 'NONE', #226515, #246507, #123382, .T. ) ;
#232822=TOROIDAL_SURFACE ( 'NONE', #49632, 0.2000000000000000111, 0.1000000000000000056 ) ;
#232834=DIRECTION ( 'NONE',  ( 0.000000000000000000, -0.8496786552930077896, -0.5273008465188219196 ) ) ;
#232842=DIRECTION ( 'NONE',  ( 0.000000000000000000, -0.8814952561688428334, 0.4721928772777350680 ) ) ;
#232851=CARTESIAN_POINT ( 'NONE',  ( -18.59999999999999787, 18.11150788191476124, -237.7585516551410478 ) ) ;
#232904=EDGE_LOOP ( 'NONE', ( #187609, #106169, #73603, #140952 ) ) ;
#232909=ORIENTED_EDGE ( 'NONE', *, *, #99341, .F. ) ;
#232918=CIRCLE ( 'NONE', #20530, 0.1000000000000075273 ) ;
#232919=EDGE_CURVE ( 'NONE', #81287, #160449, #20679, .T. ) ;
#232927=ORIENTED_EDGE ( 'NONE', *, *, #68190, .F. ) ;
#232989=DIRECTION ( 'NONE',  ( 1.000000000000000000, 0.000000000000000000, 0.000000000000000000 ) ) ;
#233007=CARTESIAN_POINT ( 'NONE',  ( -18.50000000000000000, 23.34004772283014972, -229.2004250369967338 ) ) ;
#233024=ORIENTED_EDGE ( 'NONE', *, *, #19477, .T. ) ;
#233050=CARTESIAN_POINT ( 'NONE',  ( -23.25000000000000000, 42.94477010600543565, -254.3363632230312703 ) ) ;
#233065=EDGE_CURVE ( 'NONE', #71039, #54600, #248463, .T. ) ;
#233070=ORIENTED_EDGE ( 'NONE', *, *, #118194, .T. ) ;
#233093=DIRECTION ( 'NONE',  ( 0.000000000000000000, 0.8814952561688476074, -0.4721928772777262417 ) ) ;
#233103=VERTEX_POINT ( 'NONE', #117919 ) ;
#233126=CARTESIAN_POINT ( 'NONE',  ( -23.24999999999999645, 37.94390843806124991, -261.1300795796834109 ) ) ;
#233131=DIRECTION ( 'NONE',  ( -1.000000000000000000, -1.394253735153569469E-16, -2.602809386958778209E-16 ) ) ;
#233137=TOROIDAL_SURFACE ( 'NONE', #108210, 1.900000000000002576, 0.1000000000000000056 ) ;
#233174=AXIS2_PLACEMENT_3D ( 'NONE', #140003, #181727, #40958 ) ;
#233177=CIRCLE ( 'NONE', #187368, 0.09999999999999939493 ) ;
#233187=CARTESIAN_POINT ( 'NONE',  ( -18.59999999999999787, 22.29493434298047205, -231.3632329395297234 ) ) ;
#233204=UNCERTAINTY_MEASURE_WITH_UNIT (LENGTH_MEASURE( 1.000000000000000082E-05 ), #178182, 'distance_accuracy_value', 'NONE');
#233205=CARTESIAN_POINT ( 'NONE',  ( 18.59999999999999076, 18.18127959618848166, -237.5711165786817389 ) ) ;
#233227=CARTESIAN_POINT ( 'NONE',  ( 20.94999999999999574, 18.80454058543246276, -232.7833891117047074 ) ) ;
#233230=ADVANCED_FACE ( 'NONE', ( #65655 ), #145184, .F. ) ;
#233250=ADVANCED_FACE ( 'NONE', ( #160927, #43543 ), #42256, .F. ) ;
#233264=ORIENTED_EDGE ( 'NONE', *, *, #226178, .F. ) ;
#233282=DIRECTION ( 'NONE',  ( 3.469446951953727785E-14, -0.8496786552930157832, -0.5273008465188090410 ) ) ;
#233284=CARTESIAN_POINT ( 'NONE',  ( 21.05000000000000071, 16.44800918141279666, -240.8068063186265135 ) ) ;
#233312=DIRECTION ( 'NONE',  ( -0.000000000000000000, -0.8814952561688430555, 0.4721928772777346239 ) ) ;
#233318=LINE ( 'NONE', #131618, #67690 ) ;
#233343=ADVANCED_FACE ( 'NONE', ( #228604 ), #31705, .T. ) ;
#233359=DIRECTION ( 'NONE',  ( 0.000000000000000000, 0.8814952561688429444, -0.4721928772777349570 ) ) ;
#233378=DIRECTION ( 'NONE',  ( 0.000000000000000000, 0.8814952561688429444, -0.4721928772777345684 ) ) ;
#233401=CARTESIAN_POINT ( 'NONE',  ( -20.64999999999999858, 24.17260720300848931, -252.6908294531417027 ) ) ;
#233442=AXIS2_PLACEMENT_3D ( 'NONE', #51857, #188826, #66320 ) ;
#233452=CARTESIAN_POINT ( 'NONE',  ( 21.13461538461538325, 23.02743022372036918, -230.2075788195831763 ) ) ;
#233465=CARTESIAN_POINT ( 'NONE',  ( 21.14999999999999858, 7.216982865709976380, -233.7799206001670598 ) ) ;
#233487=FACE_OUTER_BOUND ( 'NONE', #249769, .T. ) ;
#233537=CARTESIAN_POINT ( 'NONE',  ( 20.94999999999999929, 30.48950451747912993, -239.6099224343151946 ) ) ;
#233554=DIRECTION ( 'NONE',  ( 0.000000000000000000, -0.8814952561688430555, 0.4721928772777346239 ) ) ;
#233561=CARTESIAN_POINT ( 'NONE',  ( 18.50000000000000000, 37.99112772578902764, -261.0419300540664835 ) ) ;
#233648=ORIENTED_EDGE ( 'NONE', *, *, #131007, .F. ) ;
#233664=CARTESIAN_POINT ( 'NONE',  ( -20.85000000000000142, 43.17747518314618560, -245.0773422074893233 ) ) ;
#233678=DIRECTION ( 'NONE',  ( 0.000000000000000000, 0.5868805631290353597, 0.8096735173027127530 ) ) ;
#233681=CARTESIAN_POINT ( 'NONE',  ( 23.24999999999999289, 21.06094381221970124, -233.8786389445302518 ) ) ;
#233684=ORIENTED_EDGE ( 'NONE', *, *, #136173, .F. ) ;
#233687=DIRECTION ( 'NONE',  ( -0.000000000000000000, -0.8814952561688432775, 0.4721928772777344019 ) ) ;
#233699=DIRECTION ( 'NONE',  ( 0.000000000000000000, 0.8127272543710951647, -0.5826443254700256480 ) ) ;
#233723=FACE_OUTER_BOUND ( 'NONE', #36861, .T. ) ;
#233726=DIRECTION ( 'NONE',  ( 0.000000000000000000, -0.8814952561688399468, 0.4721928772777404526 ) ) ;
#233730=EDGE_CURVE ( 'NONE', #142373, #251099, #231831, .T. ) ;
#233750=CIRCLE ( 'NONE', #179589, 11.65000000000000746 ) ;
#233753=AXIS2_PLACEMENT_3D ( 'NONE', #36007, #115518, #257542 ) ;
#233778=DIRECTION ( 'NONE',  ( 1.000000000000000000, 8.674042436075353235E-17, 1.619280515896125144E-16 ) ) ;
#233800=CARTESIAN_POINT ( 'NONE',  ( -20.93302460841142931, 46.41023286455059349, -243.0722154975327385 ) ) ;
#233828=FACE_OUTER_BOUND ( 'NONE', #125425, .T. ) ;
#233829=ORIENTED_EDGE ( 'NONE', *, *, #77312, .F. ) ;
#233852=CARTESIAN_POINT ( 'NONE',  ( -21.52071067811865746, 29.44578301613924154, -236.8621740332600041 ) ) ;
#233858=EDGE_CURVE ( 'NONE', #244837, #196423, #73593, .T. ) ;
#233867=CIRCLE ( 'NONE', #163146, 0.09999999999999939493 ) ;
#233926=ORIENTED_EDGE ( 'NONE', *, *, #131151, .F. ) ;
#233934=CARTESIAN_POINT ( 'NONE',  ( -20.64999999999999858, 29.19585636832770703, -237.3287400596392445 ) ) ;
#233935=AXIS2_PLACEMENT_3D ( 'NONE', #23994, #237880, #241732 ) ;
#233974=DIRECTION ( 'NONE',  ( 0.000000000000000000, 0.8814952561688476074, -0.4721928772777262417 ) ) ;
#233991=B_SPLINE_CURVE_WITH_KNOTS ( 'NONE', 3,
 ( #190957, #249632, #71009, #166264, #130956, #245772, #51378, #47541, #128392, #107530 ),
 .UNSPECIFIED., .F., .F.,
 ( 4, 2, 2, 2, 4 ),
 ( 0.000000000000000000, 4.221631689688079022E-05, 8.443263379376158043E-05, 0.0001688652675875276603, 0.0003377305351750620969 ),
 .UNSPECIFIED. ) ;
#233993=DIRECTION ( 'NONE',  ( 0.000000000000000000, -0.4721928772777346239, -0.8814952561688430555 ) ) ;
#234047=AXIS2_PLACEMENT_3D ( 'NONE', #231949, #207249, #247640 ) ;
#234052=EDGE_CURVE ( 'NONE', #250639, #98621, #125457, .T. ) ;
#234056=VERTEX_POINT ( 'NONE', #73740 ) ;
#234098=DIRECTION ( 'NONE',  ( -1.000000000000000000, 0.000000000000000000, 0.000000000000000000 ) ) ;
#234124=CARTESIAN_POINT ( 'NONE',  ( 20.85000000000000142, 36.22724532936083364, -235.9903003947922286 ) ) ;
#234135=ADVANCED_FACE ( 'NONE', ( #153290 ), #232810, .T. ) ;
#234176=DIRECTION ( 'NONE',  ( 0.000000000000000000, 0.8814952561688429444, -0.4721928772777345684 ) ) ;
#234187=ORIENTED_EDGE ( 'NONE', *, *, #173455, .T. ) ;
#234194=FACE_OUTER_BOUND ( 'NONE', #205094, .T. ) ;
#234217=CIRCLE ( 'NONE', #109312, 0.09999999999999700795 ) ;
#234232=CARTESIAN_POINT ( 'NONE',  ( 21.07954763557388489, 10.05941015404899375, -228.1223551902535576 ) ) ;
#234295=DIRECTION ( 'NONE',  ( -1.000000000000000000, 0.000000000000000000, 0.000000000000000000 ) ) ;
#234316=VECTOR ( 'NONE', #84257, 1000.000000000000000 ) ;
#234336=VERTEX_POINT ( 'NONE', #235340 ) ;
#234350=CARTESIAN_POINT ( 'NONE',  ( -21.05000000000000071, 36.65892442174935439, -249.5511627012433848 ) ) ;
#234357=ORIENTED_EDGE ( 'NONE', *, *, #136095, .T. ) ;
#234378=CARTESIAN_POINT ( 'NONE',  ( 21.00023020733437207, 10.14655627732183873, -228.0991803899404431 ) ) ;
#234389=( BOUNDED_SURFACE ( )  B_SPLINE_SURFACE ( 3, 2, ( 
 ( #128833, #31043, #71436 ),
 ( #150956, #191396, #68867 ),
 ( #50538, #33623, #110533 ),
 ( #212229, #190083, #111835 ) ),
 .UNSPECIFIED., .F., .F., .F. ) 
 B_SPLINE_SURFACE_WITH_KNOTS ( ( 4, 4 ),
 ( 3, 3 ),
 ( 0.04058434257139458684, 0.04256401539001586354 ),
 ( 0.000000000000000000, 1.000000000000000000 ),
 .UNSPECIFIED. ) 
 GEOMETRIC_REPRESENTATION_ITEM ( )  RATIONAL_B_SPLINE_SURFACE ( (
 ( 1.000000000000000000, 0.7103081912008379906, 1.000000000000000000),
 ( 1.000000000000000000, 0.7104998333555697654, 1.000000000000000000),
 ( 1.000000000000000000, 0.7107238315754171865, 1.000000000000000000),
 ( 1.000000000000000000, 0.7110073749539332910, 1.000000000000000000) ) ) 
 REPRESENTATION_ITEM ( '' )  SURFACE ( )  );
#234412=DIRECTION ( 'NONE',  ( 0.000000000000000000, 0.4721928772778128947, 0.8814952561688012000 ) ) ;
#234453=CIRCLE ( 'NONE', #151290, 0.1000000000000013933 ) ;
#234505=CARTESIAN_POINT ( 'NONE',  ( 18.59999999999999076, 34.53503747617446606, -235.1972745784239578 ) ) ;
#234517=CARTESIAN_POINT ( 'NONE',  ( -18.50000000000000000, 22.43030315632513094, -231.3223027016406093 ) ) ;
#234531=ORIENTED_EDGE ( 'NONE', *, *, #102683, .T. ) ;
#234543=VERTEX_POINT ( 'NONE', #140802 ) ;
#234557=ORIENTED_EDGE ( 'NONE', *, *, #5405, .T. ) ;
#234561=ORIENTED_EDGE ( 'NONE', *, *, #228834, .F. ) ;
#234574=CARTESIAN_POINT ( 'NONE',  ( 21.05000000000000071, 36.65892442174935439, -249.5511627012433848 ) ) ;
#234581=DIRECTION ( 'NONE',  ( 0.000000000000000000, -0.4721928772777346239, -0.8814952561688430555 ) ) ;
#234639=EDGE_CURVE ( 'NONE', #98749, #21212, #25676, .T. ) ;
#234669=DIRECTION ( 'NONE',  ( 0.000000000000000000, 0.8814952561688476074, -0.4721928772777262417 ) ) ;
#234674=TOROIDAL_SURFACE ( 'NONE', #105448, 0.2000000000000000111, 0.1000000000000000056 ) ;
#234677=FACE_OUTER_BOUND ( 'NONE', #188728, .T. ) ;
#234679=CARTESIAN_POINT ( 'NONE',  ( -20.85000000000000142, 36.17635217701698025, -235.9630383263116471 ) ) ;
#234687=VERTEX_POINT ( 'NONE', #186356 ) ;
#234725=DIRECTION ( 'NONE',  ( -2.602085213965225788E-14, -0.8814952561688430555, 0.4721928772777346239 ) ) ;
#234772=CIRCLE ( 'NONE', #188994, 0.09999999999999939493 ) ;
#234779=ORIENTED_EDGE ( 'NONE', *, *, #13722, .F. ) ;
#234783=DIRECTION ( 'NONE',  ( 1.000000000000000000, 0.000000000000000000, 0.000000000000000000 ) ) ;
#234810=DIRECTION ( 'NONE',  ( 1.000000000000000000, 1.394253735153569469E-16, 2.602809386958778209E-16 ) ) ;
#234833=ADVANCED_FACE ( 'NONE', ( #116749 ), #219692, .T. ) ;
#234839=CIRCLE ( 'NONE', #151660, 0.09999999999999983902 ) ;
#234850=AXIS2_PLACEMENT_3D ( 'NONE', #21921, #180998, #3616 ) ;
#234854=ORIENTED_EDGE ( 'NONE', *, *, #253371, .T. ) ;
#234855=EDGE_CURVE ( 'NONE', #155390, #143721, #82725, .T. ) ;
#234861=EDGE_CURVE ( 'NONE', #181985, #132235, #84059, .T. ) ;
#234874=CARTESIAN_POINT ( 'NONE',  ( 20.22894356738334309, 18.79873783012739352, -229.4580867665647759 ) ) ;
#234905=EDGE_CURVE ( 'NONE', #70426, #172562, #218399, .T. ) ;
#234908=ORIENTED_EDGE ( 'NONE', *, *, #214883, .F. ) ;
#234915=EDGE_LOOP ( 'NONE', ( #19597, #15013, #77601, #110513 ) ) ;
#234916=FACE_OUTER_BOUND ( 'NONE', #246710, .T. ) ;
#234951=ADVANCED_FACE ( 'NONE', ( #145291 ), #127028, .F. ) ;
#234958=VECTOR ( 'NONE', #170315, 1000.000000000000000 ) ;
#235003=ADVANCED_FACE ( 'NONE', ( #205263 ), #89177, .T. ) ;
#235053=DIRECTION ( 'NONE',  ( 1.000000000000000000, 0.000000000000000000, 0.000000000000000000 ) ) ;
#235056=CIRCLE ( 'NONE', #39449, 0.1000000000000013933 ) ;
#235061=CARTESIAN_POINT ( 'NONE',  ( -20.94999999999999929, 28.37802281961254636, -258.4449340416662722 ) ) ;
#235073=ADVANCED_FACE ( 'NONE', ( #149183 ), #50770, .F. ) ;
#235083=ORIENTED_EDGE ( 'NONE', *, *, #190761, .T. ) ;
#235109=EDGE_CURVE ( 'NONE', #134581, #39898, #242331, .T. ) ;
#235171=ORIENTED_EDGE ( 'NONE', *, *, #28529, .T. ) ;
#235196=CARTESIAN_POINT ( 'NONE',  ( 18.60000000000000142, 9.105964803472835101, -245.3658845043482586 ) ) ;
#235204=VECTOR ( 'NONE', #181720, 1000.000000000000114 ) ;
#235219=EDGE_LOOP ( 'NONE', ( #232909, #216377, #118847, #191874 ) ) ;
#235224=VERTEX_POINT ( 'NONE', #13513 ) ;
#235271=FACE_OUTER_BOUND ( 'NONE', #9135, .T. ) ;
#235273=CARTESIAN_POINT ( 'NONE',  ( 21.07954640115374900, 1.580764630276365823, -230.6858712634206370 ) ) ;
#235277=CARTESIAN_POINT ( 'NONE',  ( -21.45000000000000284, 21.65523568329831505, -232.7692078405380300 ) ) ;
#235302=CARTESIAN_POINT ( 'NONE',  ( -21.14999999999999858, -3.187427350888460076, -228.3200064793908837 ) ) ;
#235311=CARTESIAN_POINT ( 'NONE',  ( -18.41353343127311604, 8.841736820195469804, -245.4273993276876809 ) ) ;
#235313=VECTOR ( 'NONE', #46504, 1000.000000000000000 ) ;
#235328=CIRCLE ( 'NONE', #214484, 0.09999999999999939493 ) ;
#235340=CARTESIAN_POINT ( 'NONE',  ( 20.84999999999998721, 31.11065811373596190, -259.9087319612273177 ) ) ;
#235349=CIRCLE ( 'NONE', #122943, 2.099999999999998757 ) ;
#235354=EDGE_CURVE ( 'NONE', #17892, #40168, #221089, .T. ) ;
#235388=DIRECTION ( 'NONE',  ( -0.000000000000000000, 0.4721928772777347350, 0.8814952561688429444 ) ) ;
#235407=EDGE_CURVE ( 'NONE', #121993, #84354, #246054, .T. ) ;
#235408=ORIENTED_EDGE ( 'NONE', *, *, #174587, .T. ) ;
#235413=CARTESIAN_POINT ( 'NONE',  ( 23.25000000000000000, 1.627786319807483340, -244.0021210468063089 ) ) ;
#235418=CARTESIAN_POINT ( 'NONE',  ( -21.05000000000000071, 14.85285025691667293, -236.4388300032497057 ) ) ;
#235440=DIRECTION ( 'NONE',  ( 1.000000000000000000, -3.448943450116723568E-16, -6.438528483529607644E-16 ) ) ;
#235463=VERTEX_POINT ( 'NONE', #54866 ) ;
#235472=EDGE_CURVE ( 'NONE', #190272, #205178, #225172, .T. ) ;
#235481=CARTESIAN_POINT ( 'NONE',  ( -21.05000000000000071, 28.51339163295720169, -258.4040038037771865 ) ) ;
#235491=FACE_OUTER_BOUND ( 'NONE', #109792, .T. ) ;
#235501=DIRECTION ( 'NONE',  ( -1.000000000000000000, -0.000000000000000000, -0.000000000000000000 ) ) ;
#235509=VECTOR ( 'NONE', #252438, 999.9999999999998863 ) ;
#235516=CARTESIAN_POINT ( 'NONE',  ( 21.04999999999999716, 10.20944177074079562, -228.0128234210401104 ) ) ;
#235520=EDGE_CURVE ( 'NONE', #245302, #65949, #253072, .T. ) ;
#235544=CARTESIAN_POINT ( 'NONE',  ( 18.49999999999996803, 43.30036367478129478, -245.0872390055602352 ) ) ;
#235558=CARTESIAN_POINT ( 'NONE',  ( 20.12500000000000000, 18.88320179786139619, -228.9684431863134932 ) ) ;
#235578=AXIS2_PLACEMENT_3D ( 'NONE', #212899, #34289, #92933 ) ;
#235616=ORIENTED_EDGE ( 'NONE', *, *, #23990, .F. ) ;
#235635=FACE_OUTER_BOUND ( 'NONE', #32947, .T. ) ;
#235637=DIRECTION ( 'NONE',  ( -1.000000000000000000, 0.000000000000000000, 0.000000000000000000 ) ) ;
#235696=DIRECTION ( 'NONE',  ( 0.000000000000000000, -0.8814952561688430555, 0.4721928772777346239 ) ) ;
#235702=CARTESIAN_POINT ( 'NONE',  ( 21.12400222705899822, 22.07230102378213132, -231.7788474567792889 ) ) ;
#235707=EDGE_CURVE ( 'NONE', #202898, #218982, #217787, .T. ) ;
#235710=DIRECTION ( 'NONE',  ( 1.000000000000000000, 0.000000000000000000, 0.000000000000000000 ) ) ;
#235711=CYLINDRICAL_SURFACE ( 'NONE', #2060, 0.5000000000000008882 ) ;
#235719=EDGE_LOOP ( 'NONE', ( #191796, #246148, #239851 ) ) ;
#235730=DIRECTION ( 'NONE',  ( 0.000000000000000000, 0.8814952561688438326, -0.4721928772777331806 ) ) ;
#235731=PRODUCT_DEFINITION_CONTEXT ( 'detailed design', #152560, 'design' ) ;
#235749=CARTESIAN_POINT ( 'NONE',  ( 23.14999999999999147, 5.169232899390497238, -237.3909066255399978 ) ) ;
#235787=VERTEX_POINT ( 'NONE', #123856 ) ;
#235801=ORIENTED_EDGE ( 'NONE', *, *, #64395, .F. ) ;
#235806=EDGE_CURVE ( 'NONE', #135120, #84465, #234217, .T. ) ;
#235809=AXIS2_PLACEMENT_3D ( 'NONE', #152539, #228198, #189065 ) ;
#235832=ORIENTED_EDGE ( 'NONE', *, *, #159720, .F. ) ;
#235841=LINE ( 'NONE', #152496, #115858 ) ;
#235869=VERTEX_POINT ( 'NONE', #168154 ) ;
#235872=CARTESIAN_POINT ( 'NONE',  ( 20.84999999999999432, 43.08613539620618837, -254.3146655184800409 ) ) ;
#235890=ORIENTED_EDGE ( 'NONE', *, *, #179557, .F. ) ;
#235903=ADVANCED_FACE ( 'NONE', ( #250211 ), #34520, .T. ) ;
#235998=ADVANCED_FACE ( 'NONE', ( #37596 ), #184862, .T. ) ;
#236000=ORIENTED_EDGE ( 'NONE', *, *, #184693, .T. ) ;
#236026=( BOUNDED_SURFACE ( )  B_SPLINE_SURFACE ( 3, 2, ( 
 ( #73332, #172441, #208954 ),
 ( #69464, #227227, #189396 ),
 ( #10759, #70759, #151582 ),
 ( #231111, #111139, #12065 ),
 ( #250636, #48588, #72026 ),
 ( #207690, #150283, #147702 ),
 ( #152873, #47285, #52430 ),
 ( #131983, #211531, #32934 ),
 ( #29076, #88986, #92850 ),
 ( #112438, #191988, #168597 ) ),
 .UNSPECIFIED., .F., .F., .F. ) 
 B_SPLINE_SURFACE_WITH_KNOTS ( ( 4, 2, 2, 2, 4 ),
 ( 3, 3 ),
 ( 0.0001701955120502367041, 0.0002247052511886173890, 0.0002792149903269980468, 0.0003882344686037594167, 0.0006062734251572821564 ),
 ( 0.000000000000000000, 1.000000000000000000 ),
 .UNSPECIFIED. ) 
 GEOMETRIC_REPRESENTATION_ITEM ( )  RATIONAL_B_SPLINE_SURFACE ( (
 ( 1.000000000000000000, 0.2966190024561448646, 1.000000000000000000),
 ( 1.000000000000000000, 0.2964522492711734181, 1.000000000000000000),
 ( 1.000000000000000000, 0.3059923531884917169, 1.000000000000000000),
 ( 1.000000000000000000, 0.3355751146943816154, 1.000000000000000000),
 ( 1.000000000000000000, 0.3550672384963678430, 1.000000000000000000),
 ( 1.000000000000000000, 0.4157034672181950663, 1.000000000000000000),
 ( 1.000000000000000000, 0.4588031877658284574, 1.000000000000000000),
 ( 1.000000000000000000, 0.5771441759655042691, 1.000000000000000000),
 ( 1.000000000000000000, 0.6469377121777389883, 1.000000000000000000),
 ( 1.000000000000000000, 0.7071067811865509034, 1.000000000000000000) ) ) 
 REPRESENTATION_ITEM ( '' )  SURFACE ( )  );
#236029=CYLINDRICAL_SURFACE ( 'NONE', #93462, 0.1000000000000012546 ) ;
#236043=AXIS2_PLACEMENT_3D ( 'NONE', #118387, #100063, #205272 ) ;
#236045=CARTESIAN_POINT ( 'NONE',  ( -20.94999999999999929, 4.360421613930902218, -245.4659189663672691 ) ) ;
#236050=CARTESIAN_POINT ( 'NONE',  ( 23.14999999999999503, 31.44980407958351876, -233.5445995079518582 ) ) ;
#236080=EDGE_LOOP ( 'NONE', ( #176749, #160187, #17749, #216270 ) ) ;
#236083=ORIENTED_EDGE ( 'NONE', *, *, #61692, .T. ) ;
#236099=CARTESIAN_POINT ( 'NONE',  ( 20.95512840106822949, 22.90176656920205289, -230.1297528598131805 ) ) ;
#236106=EDGE_CURVE ( 'NONE', #20661, #57307, #180783, .T. ) ;
#236113=VERTEX_POINT ( 'NONE', #63546 ) ;
#236141=TOROIDAL_SURFACE ( 'NONE', #123731, 0.2000000000000000111, 0.1000000000000000056 ) ;
#236145=ORIENTED_EDGE ( 'NONE', *, *, #232309, .F. ) ;
#236156=EDGE_LOOP ( 'NONE', ( #210717, #177982, #175169, #178047 ) ) ;
#236157=ADVANCED_FACE ( 'NONE', ( #4834 ), #255553, .T. ) ;
#236171=ORIENTED_EDGE ( 'NONE', *, *, #247014, .F. ) ;
#236173=DIRECTION ( 'NONE',  ( 0.000000000000000000, 0.4721928772776973204, 0.8814952561688629284 ) ) ;
#236220=CARTESIAN_POINT ( 'NONE',  ( 21.07928932188134397, 1.596973512272234830, -230.6572452218043736 ) ) ;
#236239=DIRECTION ( 'NONE',  ( 0.000000000000000000, 0.4797419643160688585, 0.8774096236502991752 ) ) ;
#236249=DIRECTION ( 'NONE',  ( 0.000000000000000000, 0.5826443254699606999, 0.8127272543711416830 ) ) ;
#236272=DIRECTION ( 'NONE',  ( -0.7071067811865473507, -0.3338907855510732658, -0.6233112732207619633 ) ) ;
#236299=DIRECTION ( 'NONE',  ( 0.000000000000000000, -0.4721928772777344019, -0.8814952561688432775 ) ) ;
#236308=CARTESIAN_POINT ( 'NONE',  ( 21.14999999999999858, 2.319530388122574394, -217.8268657444419887 ) ) ;
#236346=EDGE_LOOP ( 'NONE', ( #52723, #124956, #24419 ) ) ;
#236367=ORIENTED_EDGE ( 'NONE', *, *, #205268, .F. ) ;
#236385=CARTESIAN_POINT ( 'NONE',  ( -23.25000000000000000, 45.93315328338058379, -256.6017782078560003 ) ) ;
#236395=CIRCLE ( 'NONE', #123979, 0.1000000000000013933 ) ;
#236398=AXIS2_PLACEMENT_3D ( 'NONE', #209326, #74991, #232769 ) ;
#236425=CIRCLE ( 'NONE', #107246, 0.09999999999999939493 ) ;
#236442=EDGE_CURVE ( 'NONE', #105430, #244837, #105918, .T. ) ;
#236455=AXIS2_PLACEMENT_3D ( 'NONE', #252625, #92270, #153590 ) ;
#236495=ORIENTED_EDGE ( 'NONE', *, *, #69283, .F. ) ;
#236505=CARTESIAN_POINT ( 'NONE',  ( -2.995603634470829482E-16, 20.31234122566763034, -254.1243692145750401 ) ) ;
#236513=CARTESIAN_POINT ( 'NONE',  ( 23.14999999999999503, 21.06723286205836487, -233.6551206055687260 ) ) ;
#236529=VECTOR ( 'NONE', #178246, 1000.000000000000000 ) ;
#236536=EDGE_CURVE ( 'NONE', #253511, #5127, #93457, .T. ) ;
#236550=DIRECTION ( 'NONE',  ( -0.000000000000000000, 0.9858629823651696711, 0.1675535138457361073 ) ) ;
#236551=CARTESIAN_POINT ( 'NONE',  ( 18.49999999999998934, 18.51212680383529374, -217.3114114048737520 ) ) ;
#236578=EDGE_CURVE ( 'NONE', #218718, #28211, #201798, .T. ) ;
#236580=SPHERICAL_SURFACE ( 'NONE', #170291, 0.1000000000000000056 ) ;
#236586=CARTESIAN_POINT ( 'NONE',  ( 20.94999999999999929, 4.481636728799211156, -245.1292951062512770 ) ) ;
#236604=FACE_OUTER_BOUND ( 'NONE', #238566, .T. ) ;
#236630=DIRECTION ( 'NONE',  ( 1.000000000000000000, 1.541880601228652843E-16, 2.878400969107353907E-16 ) ) ;
#236638=EDGE_CURVE ( 'NONE', #78910, #61591, #189157, .T. ) ;
#236644=CARTESIAN_POINT ( 'NONE',  ( 18.59999999999999076, 33.78581792236875003, -236.3841486493325874 ) ) ;
#236646=ORIENTED_EDGE ( 'NONE', *, *, #110966, .F. ) ;
#236665=ORIENTED_EDGE ( 'NONE', *, *, #93407, .F. ) ;
#236689=CIRCLE ( 'NONE', #120035, 0.09999999999999986677 ) ;
#236750=CIRCLE ( 'NONE', #132745, 0.09999999999999438505 ) ;
#236756=CIRCLE ( 'NONE', #82786, 0.1000000000000013933 ) ;
#236759=CIRCLE ( 'NONE', #199181, 11.64999999999999680 ) ;
#236785=CARTESIAN_POINT ( 'NONE',  ( -18.43599941264907471, 8.780520693175109415, -245.4165332560983757 ) ) ;
#236795=CARTESIAN_POINT ( 'NONE',  ( -22.50047199488166072, -3.207573401575996463, -228.1448281418072668 ) ) ;
#236798=CARTESIAN_POINT ( 'NONE',  ( 21.04999999999965610, 10.05849014890098303, -228.1548831405661986 ) ) ;
#236865=DIRECTION ( 'NONE',  ( 0.000000000000000000, -0.8814952561688476074, 0.4721928772777262417 ) ) ;
#236883=DIRECTION ( 'NONE',  ( 1.000000000000000000, 0.000000000000000000, 0.000000000000000000 ) ) ;
#236894=ORIENTED_EDGE ( 'NONE', *, *, #7611, .T. ) ;
#236895=CYLINDRICAL_SURFACE ( 'NONE', #66862, 0.1000000000000013933 ) ;
#236903=VERTEX_POINT ( 'NONE', #108186 ) ;
#236907=ORIENTED_EDGE ( 'NONE', *, *, #7036, .F. ) ;
#236917=CARTESIAN_POINT ( 'NONE',  ( 20.94999999999999929, 22.90266353732884497, -230.0169390150674076 ) ) ;
#236920=EDGE_CURVE ( 'NONE', #12413, #234336, #246407, .T. ) ;
#236925=CARTESIAN_POINT ( 'NONE',  ( 20.94999999999999574, 18.75483929237739744, -228.0790484105328630 ) ) ;
#236930=FACE_OUTER_BOUND ( 'NONE', #242962, .T. ) ;
#236948=CYLINDRICAL_SURFACE ( 'NONE', #187918, 0.1000000000000013933 ) ;
#236969=AXIS2_PLACEMENT_3D ( 'NONE', #101789, #86081, #183933 ) ;
#236977=EDGE_CURVE ( 'NONE', #123927, #201767, #35434, .T. ) ;
#236989=VERTEX_POINT ( 'NONE', #233284 ) ;
#237012=DIRECTION ( 'NONE',  ( 0.000000000000000000, -0.8096735173027155286, 0.5868805631290315850 ) ) ;
#237018=DIRECTION ( 'NONE',  ( 1.000000000000000000, 1.394253735153569469E-16, 2.602809386958778209E-16 ) ) ;
#237036=CARTESIAN_POINT ( 'NONE',  ( 22.39999999999999503, 0.2612980822699546568, -230.0539506776466965 ) ) ;
#237041=CARTESIAN_POINT ( 'NONE',  ( 18.59999999999999432, 38.30077178631847801, -261.1858881914067751 ) ) ;
#237059=AXIS2_PLACEMENT_3D ( 'NONE', #60894, #217394, #38785 ) ;
#237097=CARTESIAN_POINT ( 'NONE',  ( -22.49917693094574389, -3.100161397270361441, -228.1566209120988731 ) ) ;
#237115=CARTESIAN_POINT ( 'NONE',  ( 21.11701782572532693, 22.98544320335190605, -230.0636731943965287 ) ) ;
#237125=EDGE_LOOP ( 'NONE', ( #201663, #174837, #134392, #96653 ) ) ;
#237148=ORIENTED_EDGE ( 'NONE', *, *, #206773, .T. ) ;
#237152=VERTEX_POINT ( 'NONE', #83119 ) ;
#237163=EDGE_CURVE ( 'NONE', #11383, #243045, #127159, .T. ) ;
#237237=ORIENTED_EDGE ( 'NONE', *, *, #159042, .F. ) ;
#237239=DIRECTION ( 'NONE',  ( 0.000000000000000000, 0.8814952561688476074, -0.4721928772777262417 ) ) ;
#237241=EDGE_LOOP ( 'NONE', ( #34120, #187698, #165382, #198351, #87686 ) ) ;
#237252=TOROIDAL_SURFACE ( 'NONE', #216393, 0.6000000000000009770, 0.1000000000000000056 ) ;
#237263=EDGE_CURVE ( 'NONE', #186847, #46846, #38919, .T. ) ;
#237359=DIRECTION ( 'NONE',  ( 0.000000000000000000, 0.8814952561688429444, -0.4721928772777345684 ) ) ;
#237375=CARTESIAN_POINT ( 'NONE',  ( -18.39999999999999858, 8.794517532467699183, -245.5155488533044945 ) ) ;
#237461=EDGE_CURVE ( 'NONE', #97681, #110056, #256258, .T. ) ;
#237463=ORIENTED_EDGE ( 'NONE', *, *, #165420, .T. ) ;
#237464=CYLINDRICAL_SURFACE ( 'NONE', #40115, 0.1000000000000075273 ) ;
#237467=ORIENTED_EDGE ( 'NONE', *, *, #216948, .T. ) ;
#237468=EDGE_LOOP ( 'NONE', ( #219061, #179067, #252706, #146561, #33339 ) ) ;
#237476=ORIENTED_EDGE ( 'NONE', *, *, #212451, .F. ) ;
#237501=EDGE_LOOP ( 'NONE', ( #60048, #219019, #129358, #85914, #88835 ) ) ;
#237509=VECTOR ( 'NONE', #79766, 1000.000000000000000 ) ;
#237528=VERTEX_POINT ( 'NONE', #213364 ) ;
#237533=DIRECTION ( 'NONE',  ( 0.000000000000000000, -0.8814952561688437216, 0.4721928772777334582 ) ) ;
#237560=ADVANCED_FACE ( 'NONE', ( #81534 ), #201508, .T. ) ;
#237577=VECTOR ( 'NONE', #81847, 1000.000000000000000 ) ;
#237618=DIRECTION ( 'NONE',  ( 0.000000000000000000, 0.8814952561688430555, -0.4721928772777346239 ) ) ;
#237661=VERTEX_POINT ( 'NONE', #97235 ) ;
#237677=CARTESIAN_POINT ( 'NONE',  ( -23.15000000000000213, 35.97645343225767789, -235.9694016464868298 ) ) ;
#237681=EDGE_LOOP ( 'NONE', ( #95772, #212593, #210518, #239070 ) ) ;
#237694=EDGE_CURVE ( 'NONE', #182152, #227126, #189701, .T. ) ;
#237704=CARTESIAN_POINT ( 'NONE',  ( -23.25000000000000000, 20.06933876993645782, -235.7297789824848451 ) ) ;
#237726=AXIS2_PLACEMENT_3D ( 'NONE', #97878, #41816, #178775 ) ;
#237746=ORIENTED_EDGE ( 'NONE', *, *, #236106, .F. ) ;
#237801=EDGE_CURVE ( 'NONE', #35945, #213275, #72296, .T. ) ;
#237806=DIRECTION ( 'NONE',  ( 0.000000000000000000, -0.8814952561688430555, 0.4721928772777346239 ) ) ;
#237839=CARTESIAN_POINT ( 'NONE',  ( -23.25000000000000000, 36.65892442174935439, -249.5511627012433848 ) ) ;
#237850=DIRECTION ( 'NONE',  ( 2.952720810173290098E-16, -0.4721928772777333472, -0.8814952561688437216 ) ) ;
#237853=CARTESIAN_POINT ( 'NONE',  ( 21.08884785362045378, 10.08677120552972362, -228.1053582936064856 ) ) ;
#237857=ORIENTED_EDGE ( 'NONE', *, *, #77886, .T. ) ;
#237880=DIRECTION ( 'NONE',  ( 0.000000000000000000, -0.8814952561688430555, 0.4721928772777346239 ) ) ;
#237883=CARTESIAN_POINT ( 'NONE',  ( -23.15000000000000213, 38.42191493408704872, -250.4955484557988541 ) ) ;
#237890=CARTESIAN_POINT ( 'NONE',  ( -20.54999999999999716, 19.73066058418984170, -238.2142830767208466 ) ) ;
#237947=EDGE_LOOP ( 'NONE', ( #138193, #156126, #143213, #62979 ) ) ;
#237970=ORIENTED_EDGE ( 'NONE', *, *, #143698, .T. ) ;
#237984=PLANE ( 'NONE',  #79550 ) ;
#237988=DIRECTION ( 'NONE',  ( 0.000000000000000000, -0.8814952561688430555, 0.4721928772777346239 ) ) ;
#237996=DIRECTION ( 'NONE',  ( 1.000000000000000000, 0.000000000000000000, 0.000000000000000000 ) ) ;
#238032=PLANE ( 'NONE',  #104692 ) ;
#238038=CARTESIAN_POINT ( 'NONE',  ( -18.59999999999999787, 18.71344899777637494, -226.7788045585494103 ) ) ;
#238039=ORIENTED_EDGE ( 'NONE', *, *, #61382, .F. ) ;
#238058=CARTESIAN_POINT ( 'NONE',  ( 20.95512820512820440, 18.86447962780959386, -229.9497396848627204 ) ) ;
#238073=CARTESIAN_POINT ( 'NONE',  ( -18.50000000000000355, 9.122720154857383079, -245.4644708025848274 ) ) ;
#238075=FACE_OUTER_BOUND ( 'NONE', #130123, .T. ) ;
#238081=ORIENTED_EDGE ( 'NONE', *, *, #216150, .T. ) ;
#238086=AXIS2_PLACEMENT_3D ( 'NONE', #173521, #234725, #35279 ) ;
#238103=CARTESIAN_POINT ( 'NONE',  ( 22.49999999999999645, -3.092988775432923720, -228.1437074281570858 ) ) ;
#238105=ORIENTED_EDGE ( 'NONE', *, *, #52909, .T. ) ;
#238108=ORIENTED_EDGE ( 'NONE', *, *, #8061, .F. ) ;
#238113=ADVANCED_FACE ( 'NONE', ( #145212 ), #25298, .T. ) ;
#238122=CARTESIAN_POINT ( 'NONE',  ( 20.94999999999999929, 20.61385802457731131, -234.8303051839938007 ) ) ;
#238131=ORIENTED_EDGE ( 'NONE', *, *, #118099, .T. ) ;
#238146=ADVANCED_FACE ( 'NONE', ( #102209 ), #82648, .F. ) ;
#238218=ORIENTED_EDGE ( 'NONE', *, *, #70087, .F. ) ;
#238233=AXIS2_PLACEMENT_3D ( 'NONE', #63184, #240557, #102287 ) ;
#238248=DIRECTION ( 'NONE',  ( -0.000000000000000000, -0.8096735173027138632, 0.5868805631290339164 ) ) ;
#238257=CARTESIAN_POINT ( 'NONE',  ( 20.94999999999999929, 11.60058429089262333, -246.3380203656811887 ) ) ;
#238259=CYLINDRICAL_SURFACE ( 'NONE', #199138, 0.09999999999999986677 ) ;
#238262=CARTESIAN_POINT ( 'NONE',  ( 21.05000000000000071, 18.75483929237739389, -228.0790484105328630 ) ) ;
#238310=EDGE_LOOP ( 'NONE', ( #49811, #78301, #10060, #198615 ) ) ;
#238323=CARTESIAN_POINT ( 'NONE',  ( 20.94999999999999929, 28.32080209959243788, -238.8452605374484676 ) ) ;
#238367=VERTEX_POINT ( 'NONE', #151682 ) ;
#238414=ORIENTED_EDGE ( 'NONE', *, *, #136801, .T. ) ;
#238418=CARTESIAN_POINT ( 'NONE',  ( 20.87600722750343252, 46.46487552657982434, -243.0839400145317200 ) ) ;
#238435=ORIENTED_EDGE ( 'NONE', *, *, #72631, .T. ) ;
#238470=EDGE_LOOP ( 'NONE', ( #75782, #222659, #197562, #7309 ) ) ;
#238476=ORIENTED_EDGE ( 'NONE', *, *, #250710, .F. ) ;
#238484=CIRCLE ( 'NONE', #225969, 0.09999999999999036049 ) ;
#238510=CARTESIAN_POINT ( 'NONE',  ( 18.49999999999999645, 36.65892442174935439, -249.5511627012433848 ) ) ;
#238525=DIRECTION ( 'NONE',  ( 1.000000000000000000, 0.000000000000000000, 0.000000000000000000 ) ) ;
#238566=EDGE_LOOP ( 'NONE', ( #6220, #60808, #103342, #138270 ) ) ;
#238582=CARTESIAN_POINT ( 'NONE',  ( 22.50497660315938475, -3.265725704392756334, -228.2539210476268750 ) ) ;
#238587=FACE_OUTER_BOUND ( 'NONE', #66501, .T. ) ;
#238601=B_SPLINE_CURVE_WITH_KNOTS ( 'NONE', 3,
 ( #219507, #159559, #222054, #120458 ),
 .UNSPECIFIED., .F., .F.,
 ( 4, 4 ),
 ( 0.000000000000000000, 0.001767853679387109507 ),
 .UNSPECIFIED. ) ;
#238606=EDGE_CURVE ( 'NONE', #35113, #60388, #6687, .T. ) ;
#238617=ORIENTED_EDGE ( 'NONE', *, *, #86419, .T. ) ;
#238628=DIRECTION ( 'NONE',  ( 0.000000000000000000, -0.8814952561688437216, 0.4721928772777334582 ) ) ;
#238632=ORIENTED_EDGE ( 'NONE', *, *, #175577, .F. ) ;
#238648=EDGE_CURVE ( 'NONE', #240452, #167398, #86167, .T. ) ;
#238654=CARTESIAN_POINT ( 'NONE',  ( -18.50000000000000000, 12.71802988599559114, -223.5105008658000543 ) ) ;
#238681=CARTESIAN_POINT ( 'NONE',  ( -20.94999999999999929, 4.136903274969360389, -245.4596299165286268 ) ) ;
#238708=AXIS2_PLACEMENT_3D ( 'NONE', #114235, #118087, #197611 ) ;
#238778=ORIENTED_EDGE ( 'NONE', *, *, #147185, .T. ) ;
#238788=ORIENTED_EDGE ( 'NONE', *, *, #122490, .F. ) ;
#238794=FACE_OUTER_BOUND ( 'NONE', #83546, .T. ) ;
#238801=DIRECTION ( 'NONE',  ( -1.000000000000000000, 0.000000000000000000, 0.000000000000000000 ) ) ;
#238814=DIRECTION ( 'NONE',  ( -0.000000000000000000, -0.4721928772777346239, -0.8814952561688430555 ) ) ;
#238839=DIRECTION ( 'NONE',  ( 0.000000000000000000, -0.8814952561688431665, 0.4721928772777345129 ) ) ;
#238841=CARTESIAN_POINT ( 'NONE',  ( -21.45000000000000284, 29.50054346320101928, -236.9717244483098568 ) ) ;
#238850=SURFACE_STYLE_USAGE ( .BOTH. , #180177 ) ;
#238855=ORIENTED_EDGE ( 'NONE', *, *, #3042, .F. ) ;
#238865=LINE ( 'NONE', #137188, #254901 ) ;
#238889=VERTEX_POINT ( 'NONE', #54792 ) ;
#238890=AXIS2_PLACEMENT_3D ( 'NONE', #195637, #22134, #142049 ) ;
#238934=ORIENTED_EDGE ( 'NONE', *, *, #204216, .F. ) ;
#238939=CARTESIAN_POINT ( 'NONE',  ( 21.87500000000000355, 22.61918030723623119, -230.9697045991730988 ) ) ;
#238940=DIRECTION ( 'NONE',  ( -0.000000000000000000, 0.4721928772777345684, 0.8814952561688429444 ) ) ;
#239034=VECTOR ( 'NONE', #41770, 1000.000000000000000 ) ;
#239041=AXIS2_PLACEMENT_3D ( 'NONE', #84346, #144345, #205618 ) ;
#239070=ORIENTED_EDGE ( 'NONE', *, *, #11715, .F. ) ;
#239089=EDGE_CURVE ( 'NONE', #104599, #18238, #177978, .T. ) ;
#239163=DIRECTION ( 'NONE',  ( 1.000000000000000000, 0.000000000000000000, 0.000000000000000000 ) ) ;
#239166=EDGE_CURVE ( 'NONE', #212495, #70426, #105449, .T. ) ;
#239169=ORIENTED_EDGE ( 'NONE', *, *, #31655, .T. ) ;
#239197=CARTESIAN_POINT ( 'NONE',  ( -23.15000000000000213, 27.82649702422227733, -239.8850763025288870 ) ) ;
#239237=CIRCLE ( 'NONE', #251712, 0.1999999999999905742 ) ;
#239255=DIRECTION ( 'NONE',  ( 0.000000000000000000, 0.8814952561688437216, -0.4721928772777334582 ) ) ;
#239264=ORIENTED_EDGE ( 'NONE', *, *, #107403, .T. ) ;
#239297=DIRECTION ( 'NONE',  ( -1.000000000000000000, -1.394253735153569469E-16, -2.602809386958778209E-16 ) ) ;
#239314=DIRECTION ( 'NONE',  ( -0.000000000000000000, 0.03181660087583042251, -0.9994937237965568766 ) ) ;
#239333=FACE_OUTER_BOUND ( 'NONE', #159327, .T. ) ;
#239341=DIRECTION ( 'NONE',  ( 1.000000000000000000, 0.000000000000000000, 0.000000000000000000 ) ) ;
#239354=ORIENTED_EDGE ( 'NONE', *, *, #104950, .T. ) ;
#239359=EDGE_LOOP ( 'NONE', ( #139732, #200772, #234779, #128850 ) ) ;
#239385=EDGE_CURVE ( 'NONE', #81676, #211434, #28337, .T. ) ;
#239412=VERTEX_POINT ( 'NONE', #94277 ) ;
#239452=DIRECTION ( 'NONE',  ( -0.4999999999999797939, 0.7633972851576996677, -0.4089310272085914799 ) ) ;
#239469=DIRECTION ( 'NONE',  ( 1.000000000000000000, 0.000000000000000000, 0.000000000000000000 ) ) ;
#239499=VERTEX_POINT ( 'NONE', #31782 ) ;
#239513=DIRECTION ( 'NONE',  ( 0.000000000000000000, 0.8814952561688430555, -0.4721928772777346239 ) ) ;
#239523=CARTESIAN_POINT ( 'NONE',  ( -22.50000000000000000, 12.54152817314149715, -223.4164406214577241 ) ) ;
#239533=AXIS2_PLACEMENT_3D ( 'NONE', #148039, #72368, #232722 ) ;
#239566=ADVANCED_FACE ( 'NONE', ( #79831 ), #257153, .F. ) ;
#239588=ORIENTED_EDGE ( 'NONE', *, *, #250821, .T. ) ;
#239627=DIRECTION ( 'NONE',  ( -0.000000000000000000, -0.4721928772777346239, -0.8814952561688430555 ) ) ;
#239630=ORIENTED_EDGE ( 'NONE', *, *, #10092, .F. ) ;
#239639=DIRECTION ( 'NONE',  ( 1.000000000000000000, 0.000000000000000000, 0.000000000000000000 ) ) ;
#239646=DIRECTION ( 'NONE',  ( 1.000000000000000000, 0.000000000000000000, 0.000000000000000000 ) ) ;
#239661=ORIENTED_EDGE ( 'NONE', *, *, #215551, .F. ) ;
#239663=CARTESIAN_POINT ( 'NONE',  ( -22.45372860728439690, -3.133362159202385921, -228.2185976283504374 ) ) ;
#239664=AXIS2_PLACEMENT_3D ( 'NONE', #73626, #74910, #55277 ) ;
#239691=VERTEX_POINT ( 'NONE', #197235 ) ;
#239705=ORIENTED_EDGE ( 'NONE', *, *, #192162, .T. ) ;
#239709=CARTESIAN_POINT ( 'NONE',  ( -20.94999999999999929, 18.26942912180536638, -237.6183358664095238 ) ) ;
#239717=CARTESIAN_POINT ( 'NONE',  ( 23.15000000000000213, 28.42524210734032408, -258.3567845160494585 ) ) ;
#239741=VERTEX_POINT ( 'NONE', #104520 ) ;
#239773=CARTESIAN_POINT ( 'NONE',  ( -20.00857864376270001, 30.14024212288317628, -235.5657495473015501 ) ) ;
#239793=( BOUNDED_SURFACE ( )  B_SPLINE_SURFACE ( 3, 2, ( 
 ( #242110, #21802, #101267 ),
 ( #180872, #222533, #166467 ),
 ( #240844, #62205, #163875 ),
 ( #140437, #183438, #221252 ),
 ( #42632, #45199, #63469 ),
 ( #122183, #2205, #142991 ) ),
 .UNSPECIFIED., .F., .F., .T. ) 
 B_SPLINE_SURFACE_WITH_KNOTS ( ( 4, 2, 4 ),
 ( 3, 3 ),
 ( 0.0001300404313046688953, 0.0003183318589266743992, 0.0005066232865486798489 ),
 ( 0.000000000000000000, 1.000000000000000000 ),
 .UNSPECIFIED. ) 
 GEOMETRIC_REPRESENTATION_ITEM ( )  RATIONAL_B_SPLINE_SURFACE ( (
 ( 1.000000000000000000, 0.7071067811865352493, 1.000000000000000000),
 ( 1.000000000000000000, 0.7625113560533072210, 1.000000000000000000),
 ( 1.000000000000000000, 0.8126073484697884375, 1.000000000000000000),
 ( 1.000000000000000000, 0.8923049332722788884, 1.000000000000000000),
 ( 1.000000000000000000, 0.9231914937776775076, 1.000000000000000000),
 ( 1.000000000000000000, 0.9238795325113161594, 1.000000000000000000) ) ) 
 REPRESENTATION_ITEM ( '' )  SURFACE ( )  );
#239802=AXIS2_PLACEMENT_3D ( 'NONE', #32798, #254349, #194423 ) ;
#239803=VECTOR ( 'NONE', #129393, 1000.000000000000000 ) ;
#239805=EDGE_LOOP ( 'NONE', ( #58045, #118178, #69392, #180732, #151113 ) ) ;
#239846=DIRECTION ( 'NONE',  ( -1.000000000000000000, 0.000000000000000000, 0.000000000000000000 ) ) ;
#239851=ORIENTED_EDGE ( 'NONE', *, *, #116711, .F. ) ;
#239894=CARTESIAN_POINT ( 'NONE',  ( 21.14999999999999503, 12.62988036037871176, -223.4632815780722410 ) ) ;
#239933=VECTOR ( 'NONE', #193231, 1000.000000000000000 ) ;
#239943=CARTESIAN_POINT ( 'NONE',  ( -18.52643265882458579, 46.42459709376392851, -243.0752906381742662 ) ) ;
#239946=VECTOR ( 'NONE', #164506, 1000.000000000000000 ) ;
#239956=EDGE_CURVE ( 'NONE', #101453, #38568, #20116, .T. ) ;
#239964=DIRECTION ( 'NONE',  ( -1.000000000000000000, 0.000000000000000000, 0.000000000000000000 ) ) ;
#239976=AXIS2_PLACEMENT_3D ( 'NONE', #40181, #100091, #240920 ) ;
#239988=ORIENTED_EDGE ( 'NONE', *, *, #251910, .T. ) ;
#240003=EDGE_CURVE ( 'NONE', #167398, #195967, #211839, .T. ) ;
#240030=CARTESIAN_POINT ( 'NONE',  ( -21.05000000000000071, 7.128833340093095217, -233.7327013124392749 ) ) ;
#240055=DIRECTION ( 'NONE',  ( -1.000000000000000000, 0.000000000000000000, 0.000000000000000000 ) ) ;
#240089=AXIS2_PLACEMENT_3D ( 'NONE', #19486, #101541, #2461 ) ;
#240121=EDGE_CURVE ( 'NONE', #234687, #48376, #236750, .T. ) ;
#240130=VECTOR ( 'NONE', #196252, 1000.000000000000000 ) ;
#240134=AXIS2_PLACEMENT_3D ( 'NONE', #245200, #104368, #84794 ) ;
#240168=ORIENTED_EDGE ( 'NONE', *, *, #11765, .F. ) ;
#240188=AXIS2_PLACEMENT_3D ( 'NONE', #49203, #29675, #10079 ) ;
#240194=ORIENTED_EDGE ( 'NONE', *, *, #197493, .T. ) ;
#240223=ORIENTED_EDGE ( 'NONE', *, *, #40307, .T. ) ;
#240237=DIRECTION ( 'NONE',  ( 0.000000000000000000, 0.8814952561688476074, -0.4721928772777262417 ) ) ;
#240242=CARTESIAN_POINT ( 'NONE',  ( -18.59999999999999787, 31.36165455396662693, -233.4973802202241302 ) ) ;
#240250=EDGE_CURVE ( 'NONE', #235787, #192532, #171961, .T. ) ;
#240271=CIRCLE ( 'NONE', #23811, 0.5000000000000008882 ) ;
#240302=EDGE_CURVE ( 'NONE', #59204, #41196, #3719, .T. ) ;
#240306=AXIS2_PLACEMENT_3D ( 'NONE', #11280, #169107, #187360 ) ;
#240343=EDGE_LOOP ( 'NONE', ( #5520, #153223, #228934, #92073, #213363 ) ) ;
#240357=ORIENTED_EDGE ( 'NONE', *, *, #224535, .T. ) ;
#240361=ORIENTED_EDGE ( 'NONE', *, *, #254041, .F. ) ;
#240363=VERTEX_POINT ( 'NONE', #217436 ) ;
#240382=LINE ( 'NONE', #199978, #161986 ) ;
#240387=FACE_OUTER_BOUND ( 'NONE', #59851, .T. ) ;
#240409=ADVANCED_FACE ( 'NONE', ( #195359 ), #195294, .T. ) ;
#240425=CARTESIAN_POINT ( 'NONE',  ( 21.13498764882293557, 10.19455785685945948, -228.0060625952886824 ) ) ;
#240427=CIRCLE ( 'NONE', #69751, 0.1000000000000013933 ) ;
#240449=CARTESIAN_POINT ( 'NONE',  ( 21.05000000000000071, 20.61385802457731131, -234.8303051839938007 ) ) ;
#240452=VERTEX_POINT ( 'NONE', #182197 ) ;
#240457=CARTESIAN_POINT ( 'NONE',  ( -18.50000000000000000, 9.070041386091544311, -245.4580372780381765 ) ) ;
#240477=AXIS2_PLACEMENT_3D ( 'NONE', #123524, #203048, #24448 ) ;
#240486=AXIS2_PLACEMENT_3D ( 'NONE', #127485, #204437, #47932 ) ;
#240520=DIRECTION ( 'NONE',  ( 1.000000000000000000, 0.000000000000000000, 0.000000000000000000 ) ) ;
#240529=CARTESIAN_POINT ( 'NONE',  ( 21.05000000000000071, 28.32080209959243788, -238.8452605374484676 ) ) ;
#240536=CARTESIAN_POINT ( 'NONE',  ( -23.25000000000000000, 43.00579525902548994, -254.2551217332645876 ) ) ;
#240546=CARTESIAN_POINT ( 'NONE',  ( -20.00857864376270001, 30.09302283515540211, -235.6538990729184491 ) ) ;
#240557=DIRECTION ( 'NONE',  ( -0.000000000000000000, 0.4721928772777345684, 0.8814952561688429444 ) ) ;
#240580=VERTEX_POINT ( 'NONE', #100049 ) ;
#240606=DIRECTION ( 'NONE',  ( 2.694716079187276397E-16, -0.4721928772777353456, -0.8814952561688426114 ) ) ;
#240627=CYLINDRICAL_SURFACE ( 'NONE', #249324, 12.87500000000000178 ) ;
#240636=CARTESIAN_POINT ( 'NONE',  ( 21.78635804494511419, 0.9736806036678684606, -230.3232395766309537 ) ) ;
#240640=ORIENTED_EDGE ( 'NONE', *, *, #199886, .T. ) ;
#240654=DIRECTION ( 'NONE',  ( -1.000000000000000000, 0.000000000000000000, 0.000000000000000000 ) ) ;
#240674=CARTESIAN_POINT ( 'NONE',  ( -23.25000000000000000, 23.40438595358395091, -253.3416554127419431 ) ) ;
#240679=CARTESIAN_POINT ( 'NONE',  ( 22.45463910399148588, -3.140208065486764344, -228.2318569525289718 ) ) ;
#240691=EDGE_CURVE ( 'NONE', #196126, #149025, #165190, .T. ) ;
#240704=EDGE_CURVE ( 'NONE', #246187, #140884, #182431, .T. ) ;
#240717=EDGE_LOOP ( 'NONE', ( #198347, #147405, #170982, #12868 ) ) ;
#240733=EDGE_CURVE ( 'NONE', #21708, #214842, #135021, .T. ) ;
#240735=DIRECTION ( 'NONE',  ( 1.000000000000000000, 0.000000000000000000, 0.000000000000000000 ) ) ;
#240749=ADVANCED_FACE ( 'NONE', ( #254931 ), #253124, .F. ) ;
#240751=CIRCLE ( 'NONE', #236455, 0.09999999999999485689 ) ;
#240753=ORIENTED_EDGE ( 'NONE', *, *, #155652, .F. ) ;
#240767=CARTESIAN_POINT ( 'NONE',  ( -23.25000000000000000, 27.82020797438361370, -240.1085946414904413 ) ) ;
#240820=CIRCLE ( 'NONE', #128388, 4.049999999999994493 ) ;
#240840=ORIENTED_EDGE ( 'NONE', *, *, #32541, .T. ) ;
#240842=DIRECTION ( 'NONE',  ( -1.000000000000000000, 0.000000000000000000, 0.000000000000000000 ) ) ;
#240844=CARTESIAN_POINT ( 'NONE',  ( -21.11825140030083858, 10.16595892622148511, -228.0477036210933477 ) ) ;
#240857=VECTOR ( 'NONE', #113742, 1000.000000000000000 ) ;
#240878=VECTOR ( 'NONE', #186096, 1000.000000000000000 ) ;
#240882=CIRCLE ( 'NONE', #65908, 0.09999999999999834022 ) ;
#240901=VECTOR ( 'NONE', #55078, 1000.000000000000000 ) ;
#240910=ORIENTED_EDGE ( 'NONE', *, *, #49995, .F. ) ;
#240913=VERTEX_POINT ( 'NONE', #119346 ) ;
#240917=CONICAL_SURFACE ( 'NONE', #116040, 4.299999999999964295, 0.7853981633974466137 ) ;
#240920=DIRECTION ( 'NONE',  ( 0.7071067811865708874, -0.3338907855511046296, -0.6233112732207185536 ) ) ;
#240926=ADVANCED_FACE ( 'NONE', ( #642 ), #103601, .F. ) ;
#240948=CARTESIAN_POINT ( 'NONE',  ( -22.44366136229477249, -3.135927281448380732, -228.2235526381227260 ) ) ;
#240959=DIRECTION ( 'NONE',  ( 0.000000000000000000, 0.8814952561688430555, -0.4721928772777346239 ) ) ;
#240972=DIRECTION ( 'NONE',  ( 0.000000000000000000, 0.8814952561688428334, -0.4721928772777348460 ) ) ;
#240987=ADVANCED_FACE ( 'NONE', ( #43662 ), #82740, .T. ) ;
#240994=CARTESIAN_POINT ( 'NONE',  ( 20.94999999999999929, 46.32970330538243786, -243.0551226933711746 ) ) ;
#241007=LINE ( 'NONE', #41542, #228554 ) ;
#241065=CARTESIAN_POINT ( 'NONE',  ( -18.59999999999999787, 18.86061765788380740, -226.6874733728449485 ) ) ;
#241082=ORIENTED_EDGE ( 'NONE', *, *, #256839, .T. ) ;
#241097=ORIENTED_EDGE ( 'NONE', *, *, #49394, .T. ) ;
#241140=LINE ( 'NONE', #85861, #212903 ) ;
#241158=ORIENTED_EDGE ( 'NONE', *, *, #231116, .T. ) ;
#241180=CARTESIAN_POINT ( 'NONE',  ( -23.25000000000000000, 36.65892442174935439, -249.5511627012433848 ) ) ;
#241214=VERTEX_POINT ( 'NONE', #34395 ) ;
#241240=VECTOR ( 'NONE', #194704, 1000.000000000000000 ) ;
#241249=VECTOR ( 'NONE', #172906, 1000.000000000000000 ) ;
#241268=TOROIDAL_SURFACE ( 'NONE', #37246, 0.4000000000000010214, 0.1000000000000000056 ) ;
#241272=EDGE_CURVE ( 'NONE', #38568, #134779, #62604, .T. ) ;
#241289=DIRECTION ( 'NONE',  ( 0.000000000000000000, 0.8034013718071717491, -0.5954378521544919645 ) ) ;
#241318=ADVANCED_FACE ( 'NONE', ( #84683 ), #106842, .F. ) ;
#241327=EDGE_CURVE ( 'NONE', #254141, #244837, #3699, .T. ) ;
#241354=AXIS2_PLACEMENT_3D ( 'NONE', #130384, #153865, #233378 ) ;
#241401=PLANE ( 'NONE',  #38540 ) ;
#241409=ORIENTED_EDGE ( 'NONE', *, *, #74992, .T. ) ;
#241420=DIRECTION ( 'NONE',  ( 1.000000000000000000, 0.000000000000000000, 0.000000000000000000 ) ) ;
#241438=AXIS2_PLACEMENT_3D ( 'NONE', #71086, #11098, #170222 ) ;
#241455=DIRECTION ( 'NONE',  ( 0.000000000000000000, -0.9371753822965315228, 0.3488585713686134238 ) ) ;
#241480=DIRECTION ( 'NONE',  ( 0.000000000000000000, 0.8814952561688722543, -0.4721928772776801675 ) ) ;
#241482=DIRECTION ( 'NONE',  ( 1.000000000000000000, 0.000000000000000000, 0.000000000000000000 ) ) ;
#241528=ORIENTED_EDGE ( 'NONE', *, *, #62578, .T. ) ;
#241544=LINE ( 'NONE', #214587, #197930 ) ;
#241568=CIRCLE ( 'NONE', #245674, 11.65000000000000391 ) ;
#241593=AXIS2_PLACEMENT_3D ( 'NONE', #142079, #118697, #99085 ) ;
#241600=ADVANCED_FACE ( 'NONE', ( #3445 ), #23052, .F. ) ;
#241616=FACE_OUTER_BOUND ( 'NONE', #219497, .T. ) ;
#241636=EDGE_CURVE ( 'NONE', #126382, #107706, #257533, .T. ) ;
#241663=CIRCLE ( 'NONE', #208371, 0.09999999999999638345 ) ;
#241680=AXIS2_PLACEMENT_3D ( 'NONE', #164294, #185128, #41793 ) ;
#241693=DIRECTION ( 'NONE',  ( -0.000000000000000000, 0.4721928772777345684, 0.8814952561688429444 ) ) ;
#241707=CARTESIAN_POINT ( 'NONE',  ( 21.11927991906887669, 10.16575863945443459, -228.0440959703046246 ) ) ;
#241729=DIRECTION ( 'NONE',  ( 0.000000000000000000, 0.8814952561688430555, -0.4721928772777346239 ) ) ;
#241732=DIRECTION ( 'NONE',  ( 1.000000000000000000, 0.000000000000000000, 0.000000000000000000 ) ) ;
#241744=DIRECTION ( 'NONE',  ( -0.7071067811865303643, 0.3338907855507385891, 0.6233112732209604712 ) ) ;
#241757=CIRCLE ( 'NONE', #83514, 0.1000000000000013933 ) ;
#241766=EDGE_CURVE ( 'NONE', #13152, #105430, #178719, .T. ) ;
#241786=CIRCLE ( 'NONE', #91935, 0.1000000000000075273 ) ;
#241795=LINE ( 'NONE', #215794, #251762 ) ;
#241799=DIRECTION ( 'NONE',  ( 1.000000000000000000, 0.000000000000000000, 0.000000000000000000 ) ) ;
#241822=DIRECTION ( 'NONE',  ( 1.000000000000000000, 0.000000000000000000, 0.000000000000000000 ) ) ;
#241823=DIRECTION ( 'NONE',  ( 0.000000000000000000, -0.4721928772777347350, -0.8814952561688431665 ) ) ;
#241828=ADVANCED_FACE ( 'NONE', ( #205203 ), #4439, .F. ) ;
#241831=EDGE_LOOP ( 'NONE', ( #6674, #173273, #94121, #247753 ) ) ;
#241835=ORIENTED_EDGE ( 'NONE', *, *, #35771, .T. ) ;
#241840=CIRCLE ( 'NONE', #83592, 0.1000000000000013933 ) ;
#241841=CIRCLE ( 'NONE', #79332, 0.2000000000000002054 ) ;
#241911=CARTESIAN_POINT ( 'NONE',  ( 21.59780538579342135, 1.139892542176100809, -230.4123047064117316 ) ) ;
#241914=VERTEX_POINT ( 'NONE', #72153 ) ;
#241936=CARTESIAN_POINT ( 'NONE',  ( 20.95512820512820440, 22.03025613173517883, -231.6455594930189648 ) ) ;
#241939=ORIENTED_EDGE ( 'NONE', *, *, #86941, .T. ) ;
#241969=DIRECTION ( 'NONE',  ( -1.000000000000000000, 0.000000000000000000, 0.000000000000000000 ) ) ;
#241996=DIRECTION ( 'NONE',  ( 1.000000000000000000, 0.000000000000000000, 0.000000000000000000 ) ) ;
#242011=VECTOR ( 'NONE', #166384, 1000.000000000000000 ) ;
#242021=CIRCLE ( 'NONE', #58663, 0.1000000000000013933 ) ;
#242030=DIRECTION ( 'NONE',  ( 0.000000000000000000, 0.4721928772777331806, 0.8814952561688438326 ) ) ;
#242043=CYLINDRICAL_SURFACE ( 'NONE', #162318, 0.1000000000000012546 ) ;
#242077=ORIENTED_EDGE ( 'NONE', *, *, #179326, .T. ) ;
#242103=EDGE_CURVE ( 'NONE', #72605, #156710, #212195, .T. ) ;
#242108=DIRECTION ( 'NONE',  ( 0.000000000000000000, 0.8814952561688430555, -0.4721928772777346239 ) ) ;
#242110=CARTESIAN_POINT ( 'NONE',  ( -21.15000000000000213, 10.21728496540352360, -227.9671432372868765 ) ) ;
#242131=ORIENTED_EDGE ( 'NONE', *, *, #14686, .T. ) ;
#242145=CARTESIAN_POINT ( 'NONE',  ( -20.85000000000000142, 36.65892442174935439, -249.5511627012433848 ) ) ;
#242149=CARTESIAN_POINT ( 'NONE',  ( 18.59999999999999432, 13.71992543034163958, -238.5823796952984992 ) ) ;
#242155=PLANE ( 'NONE',  #108328 ) ;
#242157=CARTESIAN_POINT ( 'NONE',  ( 18.49999999999999645, 13.71992543034163781, -238.5823796952984992 ) ) ;
#242216=DIRECTION ( 'NONE',  ( -0.000000000000000000, 0.4721928772777346239, 0.8814952561688430555 ) ) ;
#242228=CARTESIAN_POINT ( 'NONE',  ( -20.94999999999999929, 28.63831050940605394, -258.0693639473472558 ) ) ;
#242239=DIRECTION ( 'NONE',  ( 1.000000000000000000, 0.000000000000000000, 0.000000000000000000 ) ) ;
#242254=DIRECTION ( 'NONE',  ( -1.000000000000000000, 0.000000000000000000, 0.000000000000000000 ) ) ;
#242286=ORIENTED_EDGE ( 'NONE', *, *, #86418, .T. ) ;
#242312=CARTESIAN_POINT ( 'NONE',  ( 21.05000000000000071, 18.65264709638147878, -228.0117735144100379 ) ) ;
#242313=ORIENTED_EDGE ( 'NONE', *, *, #166781, .T. ) ;
#242314=EDGE_LOOP ( 'NONE', ( #25894, #151427 ) ) ;
#242331=CIRCLE ( 'NONE', #167348, 0.09999999999999939493 ) ;
#242341=CARTESIAN_POINT ( 'NONE',  ( 18.49999999999999289, 30.76917518201224055, -234.8152055956155380 ) ) ;
#242349=EDGE_LOOP ( 'NONE', ( #25392, #23147, #171777, #124001 ) ) ;
#242373=EDGE_CURVE ( 'NONE', #19158, #45529, #199736, .T. ) ;
#242408=ORIENTED_EDGE ( 'NONE', *, *, #15294, .F. ) ;
#242412=ADVANCED_FACE ( 'NONE', ( #56084 ), #29058, .T. ) ;
#242430=CARTESIAN_POINT ( 'NONE',  ( 20.95265033839679347, 18.76182816757560445, -228.0387018287258911 ) ) ;
#242455=CARTESIAN_POINT ( 'NONE',  ( 22.39999999999999503, 0.2612980822699583205, -230.0539506776466681 ) ) ;
#242460=PLANE ( 'NONE',  #241593 ) ;
#242514=EDGE_CURVE ( 'NONE', #84354, #67400, #66627, .T. ) ;
#242564=EDGE_LOOP ( 'NONE', ( #160115, #120987 ) ) ;
#242567=EDGE_LOOP ( 'NONE', ( #19144, #196523, #161544, #165820 ) ) ;
#242579=FACE_OUTER_BOUND ( 'NONE', #59745, .T. ) ;
#242582=ORIENTED_EDGE ( 'NONE', *, *, #412, .F. ) ;
#242607=VECTOR ( 'NONE', #88802, 1000.000000000000114 ) ;
#242655=CIRCLE ( 'NONE', #167675, 4.299999999999957190 ) ;
#242712=ORIENTED_EDGE ( 'NONE', *, *, #118881, .F. ) ;
#242730=LINE ( 'NONE', #27591, #239946 ) ;
#242741=VERTEX_POINT ( 'NONE', #130189 ) ;
#242764=EDGE_CURVE ( 'NONE', #107904, #62992, #37591, .T. ) ;
#242765=FACE_OUTER_BOUND ( 'NONE', #15671, .T. ) ;
#242771=DIRECTION ( 'NONE',  ( 1.000000000000000000, 0.000000000000000000, 0.000000000000000000 ) ) ;
#242776=ORIENTED_EDGE ( 'NONE', *, *, #24863, .F. ) ;
#242813=EDGE_CURVE ( 'NONE', #235463, #245346, #158585, .T. ) ;
#242883=EDGE_CURVE ( 'NONE', #205599, #29656, #97463, .T. ) ;
#242901=EDGE_LOOP ( 'NONE', ( #255644, #55526, #172672, #154254, #26814, #52902 ) ) ;
#242948=CARTESIAN_POINT ( 'NONE',  ( 20.84999999999999432, 43.35377423437995503, -245.1717807829448930 ) ) ;
#242962=EDGE_LOOP ( 'NONE', ( #215052, #165991, #236145, #18091 ) ) ;
#242988=ORIENTED_EDGE ( 'NONE', *, *, #205662, .F. ) ;
#243019=CARTESIAN_POINT ( 'NONE',  ( 19.97071067811864609, 31.48319315813861863, -233.4822683806297903 ) ) ;
#243045=VERTEX_POINT ( 'NONE', #3513 ) ;
#243057=CARTESIAN_POINT ( 'NONE',  ( -20.94999999999999929, 16.52766025697963315, -240.8672687545768270 ) ) ;
#243066=AXIS2_PLACEMENT_3D ( 'NONE', #190914, #72233, #136014 ) ;
#243091=LINE ( 'NONE', #100963, #36421 ) ;
#243149=EDGE_LOOP ( 'NONE', ( #136578, #217893, #43219, #189676 ) ) ;
#243156=CIRCLE ( 'NONE', #130731, 0.09999999999999939493 ) ;
#243161=LINE ( 'NONE', #80201, #131596 ) ;
#243182=AXIS2_PLACEMENT_3D ( 'NONE', #82132, #106845, #239964 ) ;
#243226=DIRECTION ( 'NONE',  ( 1.000000000000000000, 0.000000000000000000, 0.000000000000000000 ) ) ;
#243228=DIRECTION ( 'NONE',  ( 0.000000000000000000, -0.8814952561688430555, 0.4721928772777346239 ) ) ;
#243279=ORIENTED_EDGE ( 'NONE', *, *, #167054, .F. ) ;
#243280=CIRCLE ( 'NONE', #243473, 4.100000000000009415 ) ;
#243302=LINE ( 'NONE', #167653, #242011 ) ;
#243324=AXIS2_PLACEMENT_3D ( 'NONE', #176741, #18924, #42354 ) ;
#243357=EDGE_CURVE ( 'NONE', #26265, #110056, #200145, .T. ) ;
#243373=ORIENTED_EDGE ( 'NONE', *, *, #55814, .T. ) ;
#243389=EDGE_LOOP ( 'NONE', ( #212182, #185509, #139436, #220783, #28726, #126457, #208359, #213559, #240194, #75461, #24162, #96046, #109694, #22704, #12054, #224422, #254186, #143349, #204424, #71258, #200791, #186501, #69882 ) ) ;
#243398=DIRECTION ( 'NONE',  ( 1.000000000000000000, 0.000000000000000000, 0.000000000000000000 ) ) ;
#243420=FACE_OUTER_BOUND ( 'NONE', #155074, .T. ) ;
#243431=AXIS2_PLACEMENT_3D ( 'NONE', #163221, #143637, #101919 ) ;
#243462=DIRECTION ( 'NONE',  ( 1.000000000000000000, -3.448943450116727512E-16, -6.438528483529605672E-16 ) ) ;
#243471=ORIENTED_EDGE ( 'NONE', *, *, #55181, .F. ) ;
#243473=AXIS2_PLACEMENT_3D ( 'NONE', #116014, #255451, #156446 ) ;
#243520=CARTESIAN_POINT ( 'NONE',  ( 20.85000000106542117, 36.17380055357438096, -235.9616714914856459 ) ) ;
#243535=CARTESIAN_POINT ( 'NONE',  ( -20.64999999999999858, 27.77927773649450316, -239.9732258281457860 ) ) ;
#243557=ORIENTED_EDGE ( 'NONE', *, *, #120311, .F. ) ;
#243669=EDGE_CURVE ( 'NONE', #72339, #18553, #63053, .T. ) ;
#243684=FACE_OUTER_BOUND ( 'NONE', #71896, .T. ) ;
#243731=CYLINDRICAL_SURFACE ( 'NONE', #145217, 7.899999999999994138 ) ;
#243746=EDGE_CURVE ( 'NONE', #74755, #141820, #163049, .T. ) ;
#243765=EDGE_CURVE ( 'NONE', #92704, #97681, #57228, .T. ) ;
#243773=CARTESIAN_POINT ( 'NONE',  ( 20.94999999999999929, 24.17260720300848575, -252.6908294531417027 ) ) ;
#243776=DIRECTION ( 'NONE',  ( 0.000000000000000000, 0.8814952561688438326, -0.4721928772777332362 ) ) ;
#243779=DIRECTION ( 'NONE',  ( 0.000000000000000000, -0.4721928772777242433, -0.8814952561688484955 ) ) ;
#243787=AXIS2_PLACEMENT_3D ( 'NONE', #206084, #23630, #103103 ) ;
#243799=DIRECTION ( 'NONE',  ( -0.8660254037843878594, 0.4407476280845205041, -0.2360964386388684777 ) ) ;
#243804=CIRCLE ( 'NONE', #239533, 0.09999999999999711897 ) ;
#243806=ORIENTED_EDGE ( 'NONE', *, *, #27008, .T. ) ;
#243829=CARTESIAN_POINT ( 'NONE',  ( 20.95429402530531959, 18.83316948772580091, -229.9329191065959037 ) ) ;
#243854=LINE ( 'NONE', #245150, #252135 ) ;
#243855=ORIENTED_EDGE ( 'NONE', *, *, #234639, .T. ) ;
#243863=CARTESIAN_POINT ( 'NONE',  ( 23.14999999999999503, 31.40887384169439756, -233.4092306946072313 ) ) ;
#243892=DIRECTION ( 'NONE',  ( -0.000000000000000000, 0.4721928772777345684, 0.8814952561688429444 ) ) ;
#243945=ADVANCED_FACE ( 'NONE', ( #16733 ), #204884, .F. ) ;
#243986=DIRECTION ( 'NONE',  ( -1.000000000000000000, -0.000000000000000000, -0.000000000000000000 ) ) ;
#243996=DIRECTION ( 'NONE',  ( 0.000000000000000000, -0.8814952561688476074, 0.4721928772777262417 ) ) ;
#244043=EDGE_CURVE ( 'NONE', #170331, #194531, #34249, .T. ) ;
#244161=DIRECTION ( 'NONE',  ( -0.000000000000000000, 0.4721928772777345684, 0.8814952561688429444 ) ) ;
#244176=ORIENTED_EDGE ( 'NONE', *, *, #213862, .T. ) ;
#244206=DIRECTION ( 'NONE',  ( 1.000000000000000000, 0.000000000000000000, 0.000000000000000000 ) ) ;
#244218=CARTESIAN_POINT ( 'NONE',  ( 21.14999999999999858, 12.37888392014804495, -249.8746333190754569 ) ) ;
#244225=ORIENTED_EDGE ( 'NONE', *, *, #33597, .F. ) ;
#244227=CARTESIAN_POINT ( 'NONE',  ( 20.94999999999999929, 42.96960653111219131, -254.4772109693542745 ) ) ;
#244230=EDGE_CURVE ( 'NONE', #217355, #188830, #146610, .T. ) ;
#244241=EDGE_CURVE ( 'NONE', #53873, #144717, #208997, .T. ) ;
#244275=EDGE_LOOP ( 'NONE', ( #47617, #111264, #31861, #60360 ) ) ;
#244281=CARTESIAN_POINT ( 'NONE',  ( -21.05000000000000071, 18.26942912180536638, -237.6183358664095238 ) ) ;
#244286=CARTESIAN_POINT ( 'NONE',  ( -21.64999999999999858, 29.33122518167236237, -237.2878098217501588 ) ) ;
#244288=ORIENTED_EDGE ( 'NONE', *, *, #104793, .F. ) ;
#244314=DIRECTION ( 'NONE',  ( 1.000000000000000000, 1.541880601228652843E-16, 2.878400969107353907E-16 ) ) ;
#244322=DIRECTION ( 'NONE',  ( 1.000000000000000000, 0.000000000000000000, 0.000000000000000000 ) ) ;
#244345=TOROIDAL_SURFACE ( 'NONE', #19518, 11.65000000000000036, 0.1000000000000000056 ) ;
#244364=EDGE_LOOP ( 'NONE', ( #239169, #61795, #105542, #127542, #245841, #224345, #102286, #207558, #83460, #141834, #103296, #228632 ) ) ;
#244384=EDGE_CURVE ( 'NONE', #186223, #238367, #155046, .T. ) ;
#244426=CARTESIAN_POINT ( 'NONE',  ( 18.59999999999999076, 33.98796489282361932, -236.2185561567993091 ) ) ;
#244430=ORIENTED_EDGE ( 'NONE', *, *, #131007, .T. ) ;
#244447=ORIENTED_EDGE ( 'NONE', *, *, #232919, .F. ) ;
#244453=TOROIDAL_SURFACE ( 'NONE', #140401, 0.6000000000000009770, 0.1000000000000000056 ) ;
#244458=CIRCLE ( 'NONE', #165374, 0.1000000000000013933 ) ;
#244484=CARTESIAN_POINT ( 'NONE',  ( 21.12642695952774119, 1.555420789734674569, -230.6349773343582115 ) ) ;
#244495=ORIENTED_EDGE ( 'NONE', *, *, #9093, .F. ) ;
#244506=CARTESIAN_POINT ( 'NONE',  ( 18.49999999999998934, 33.78581792236875003, -236.3841486493325874 ) ) ;
#244559=DIRECTION ( 'NONE',  ( 0.000000000000000000, 0.4721928772777346239, 0.8814952561688430555 ) ) ;
#244591=CARTESIAN_POINT ( 'NONE',  ( 23.24999999999999645, 36.65892442174935439, -249.5511627012433848 ) ) ;
#244610=DIRECTION ( 'NONE',  ( 0.000000000000000000, 0.9994937237965558774, 0.03181660087586650476 ) ) ;
#244657=DIRECTION ( 'NONE',  ( -1.000000000000000000, 0.000000000000000000, 0.000000000000000000 ) ) ;
#244683=AXIS2_PLACEMENT_3D ( 'NONE', #23371, #221514, #83280 ) ;
#244765=LINE ( 'NONE', #169133, #240878 ) ;
#244774=AXIS2_PLACEMENT_3D ( 'NONE', #50713, #29924, #10353 ) ;
#244777=CARTESIAN_POINT ( 'NONE',  ( 21.05000000000000071, 1.316055977212909456, -230.7323992127457473 ) ) ;
#244788=DIRECTION ( 'NONE',  ( -1.000000000000000000, -2.683427030341247466E-17, 8.429776912874270765E-16 ) ) ;
#244793=EDGE_CURVE ( 'NONE', #57931, #18553, #205722, .T. ) ;
#244795=FACE_OUTER_BOUND ( 'NONE', #247530, .T. ) ;
#244819=CIRCLE ( 'NONE', #174156, 0.09999999999999939493 ) ;
#244833=ORIENTED_EDGE ( 'NONE', *, *, #54504, .F. ) ;
#244837=VERTEX_POINT ( 'NONE', #214308 ) ;
#244847=EDGE_CURVE ( 'NONE', #158507, #57412, #209850, .T. ) ;
#244856=DIRECTION ( 'NONE',  ( -1.836970198721029441E-16, 0.4721928772777346239, 0.8814952561688430555 ) ) ;
#244860=ADVANCED_FACE ( 'NONE', ( #138578, #137315 ), #218128, .T. ) ;
#244887=ORIENTED_EDGE ( 'NONE', *, *, #48207, .F. ) ;
#244897=CIRCLE ( 'NONE', #149063, 0.1000000000000076522 ) ;
#244901=ORIENTED_EDGE ( 'NONE', *, *, #44978, .F. ) ;
#244909=CARTESIAN_POINT ( 'NONE',  ( -21.44999999999999929, 29.33122518167236237, -237.2878098217501588 ) ) ;
#244930=ORIENTED_EDGE ( 'NONE', *, *, #190558, .F. ) ;
#244972=CIRCLE ( 'NONE', #103479, 0.1000000000000015737 ) ;
#244991=CARTESIAN_POINT ( 'NONE',  ( 23.14999999999999858, 36.65892442174935439, -249.5511627012433848 ) ) ;
#245011=CARTESIAN_POINT ( 'NONE',  ( -23.25000000000000000, 36.65892442174935439, -249.5511627012433848 ) ) ;
#245024=AXIS2_PLACEMENT_3D ( 'NONE', #125335, #5351, #84875 ) ;
#245031=DIRECTION ( 'NONE',  ( 1.000000000000000000, 1.394253735153569469E-16, 2.602809386958778209E-16 ) ) ;
#245058=CARTESIAN_POINT ( 'NONE',  ( 20.94999999999999929, 36.65892442174935439, -249.5511627012433848 ) ) ;
#245068=AXIS2_PLACEMENT_3D ( 'NONE', #257305, #237806, #198671 ) ;
#245096=ORIENTED_EDGE ( 'NONE', *, *, #232160, .F. ) ;
#245104=DIRECTION ( 'NONE',  ( 0.000000000000000000, 0.4721928772777343464, 0.8814952561688431665 ) ) ;
#245131=EDGE_LOOP ( 'NONE', ( #193983, #165244 ) ) ;
#245135=CARTESIAN_POINT ( 'NONE',  ( -20.54999999999999716, 21.39147882631411335, -233.2615922652120730 ) ) ;
#245150=CARTESIAN_POINT ( 'NONE',  ( -18.50000000000000000, 30.31654117411694571, -235.6601881227570914 ) ) ;
#245180=VERTEX_POINT ( 'NONE', #216562 ) ;
#245191=DIRECTION ( 'NONE',  ( 1.000000000000000000, 0.000000000000000000, 0.000000000000000000 ) ) ;
#245195=ORIENTED_EDGE ( 'NONE', *, *, #24600, .F. ) ;
#245200=CARTESIAN_POINT ( 'NONE',  ( -20.64999999999999858, 36.65892442174935439, -249.5511627012433848 ) ) ;
#245240=ORIENTED_EDGE ( 'NONE', *, *, #102683, .F. ) ;
#245276=CIRCLE ( 'NONE', #82906, 12.77499999999999325 ) ;
#245299=DIRECTION ( 'NONE',  ( -0.000000000000000000, 0.4721928772777345684, 0.8814952561688429444 ) ) ;
#245302=VERTEX_POINT ( 'NONE', #152326 ) ;
#245308=CARTESIAN_POINT ( 'NONE',  ( -20.54999999999999716, 24.07562609839690992, -252.7152152143214892 ) ) ;
#245329=CIRCLE ( 'NONE', #132901, 0.1000000000000013933 ) ;
#245346=VERTEX_POINT ( 'NONE', #229278 ) ;
#245357=ORIENTED_EDGE ( 'NONE', *, *, #139206, .T. ) ;
#245393=CIRCLE ( 'NONE', #186961, 3.999999999999994671 ) ;
#245396=ORIENTED_EDGE ( 'NONE', *, *, #196282, .F. ) ;
#245397=CARTESIAN_POINT ( 'NONE',  ( 18.59999999999999787, 16.44800918141279311, -240.8068063186265135 ) ) ;
#245439=CARTESIAN_POINT ( 'NONE',  ( 19.80993210785516112, 34.50919645272388436, -235.0699886441803130 ) ) ;
#245443=CARTESIAN_POINT ( 'NONE',  ( 18.59999999999999076, 19.81721122307411420, -227.1998943584050039 ) ) ;
#245446=ORIENTED_EDGE ( 'NONE', *, *, #68219, .F. ) ;
#245455=DIRECTION ( 'NONE',  ( 0.000000000000000000, -0.8814952561688430555, 0.4721928772777346239 ) ) ;
#245478=CARTESIAN_POINT ( 'NONE',  ( 18.59999999999999076, 30.76917518201224055, -234.8152055956155380 ) ) ;
#245491=CIRCLE ( 'NONE', #149826, 2.099999999999998757 ) ;
#245492=ORIENTED_EDGE ( 'NONE', *, *, #33768, .T. ) ;
#245554=CARTESIAN_POINT ( 'NONE',  ( -18.59999999999999787, 36.65892442174935439, -249.5511627012433848 ) ) ;
#245555=EDGE_CURVE ( 'NONE', #195393, #220389, #218542, .T. ) ;
#245591=CARTESIAN_POINT ( 'NONE',  ( -21.08035267497491816, 1.586508777023655892, -230.6700248112038310 ) ) ;
#245640=DIRECTION ( 'NONE',  ( 0.000000000000000000, -0.4721928772777346239, -0.8814952561688430555 ) ) ;
#245674=AXIS2_PLACEMENT_3D ( 'NONE', #110859, #167021, #13070 ) ;
#245694=AXIS2_PLACEMENT_3D ( 'NONE', #97047, #218299, #176653 ) ;
#245697=ORIENTED_EDGE ( 'NONE', *, *, #176193, .T. ) ;
#245738=EDGE_CURVE ( 'NONE', #104063, #56714, #47291, .T. ) ;
#245746=CARTESIAN_POINT ( 'NONE',  ( 20.94999999999999929, 20.66107731230508548, -234.7421556583769302 ) ) ;
#245764=DIRECTION ( 'NONE',  ( 0.000000000000000000, 0.5341055959866798375, -0.8454177738465836756 ) ) ;
#245772=CARTESIAN_POINT ( 'NONE',  ( -18.46907102845856485, 38.07039079105120294, -261.0545844836100287 ) ) ;
#245774=DIRECTION ( 'NONE',  ( 0.000000000000000000, 0.8814952561688444987, -0.4721928772777320149 ) ) ;
#245808=CARTESIAN_POINT ( 'NONE',  ( 18.49999999999999645, -1.235880796157551309, -222.7862885752216471 ) ) ;
#245816=DIRECTION ( 'NONE',  ( 0.000000000000000000, 0.8814952561688429444, -0.4721928772777349570 ) ) ;
#245828=ORIENTED_EDGE ( 'NONE', *, *, #224535, .F. ) ;
#245832=CARTESIAN_POINT ( 'NONE',  ( 23.24999999999999645, 38.50047664313251516, -246.1133312021848951 ) ) ;
#245841=ORIENTED_EDGE ( 'NONE', *, *, #122966, .F. ) ;
#245846=AXIS2_PLACEMENT_3D ( 'NONE', #54425, #171853, #152274 ) ;
#245849=ORIENTED_EDGE ( 'NONE', *, *, #35882, .T. ) ;
#245874=ORIENTED_EDGE ( 'NONE', *, *, #138895, .F. ) ;
#245882=EDGE_CURVE ( 'NONE', #241214, #91747, #74623, .T. ) ;
#245902=CARTESIAN_POINT ( 'NONE',  ( -20.00857864376270001, 30.22839164850006455, -235.6129688350293350 ) ) ;
#245923=DIRECTION ( 'NONE',  ( 0.000000000000000000, 0.5868805631290315850, 0.8096735173027156396 ) ) ;
#245940=CARTESIAN_POINT ( 'NONE',  ( -21.05000000000000071, 14.85285025691667293, -236.4388300032497057 ) ) ;
#245954=CARTESIAN_POINT ( 'NONE',  ( 19.58285714285715073, 18.75808650758932217, -228.1810571460606241 ) ) ;
#246001=CIRCLE ( 'NONE', #229267, 0.1000000000000013933 ) ;
#246047=CARTESIAN_POINT ( 'NONE',  ( 18.59999999999999076, 33.76625905298630670, -236.4206613783598243 ) ) ;
#246054=CIRCLE ( 'NONE', #133614, 0.1000000000000075273 ) ;
#246095=CARTESIAN_POINT ( 'NONE',  ( -20.85000000000000142, 36.65892442174935439, -249.5511627012433848 ) ) ;
#246112=CARTESIAN_POINT ( 'NONE',  ( -22.45437739390954945, -3.140208066727175673, -228.2318569518635059 ) ) ;
#246130=FACE_OUTER_BOUND ( 'NONE', #172410, .T. ) ;
#246148=ORIENTED_EDGE ( 'NONE', *, *, #145049, .T. ) ;
#246166=CARTESIAN_POINT ( 'NONE',  ( -21.05000000000000071, 18.63703040626447205, -226.6960388224909764 ) ) ;
#246169=CIRCLE ( 'NONE', #8843, 0.1000000000000038081 ) ;
#246177=VECTOR ( 'NONE', #128257, 1000.000000000000000 ) ;
#246187=VERTEX_POINT ( 'NONE', #109273 ) ;
#246200=DIRECTION ( 'NONE',  ( 0.000000000000000000, -0.8814952561687010579, 0.4721928772779996342 ) ) ;
#246202=CARTESIAN_POINT ( 'NONE',  ( -20.85000000000000142, 36.65892442174935439, -249.5511627012433848 ) ) ;
#246208=DIRECTION ( 'NONE',  ( 1.000000000000000000, 0.000000000000000000, 0.000000000000000000 ) ) ;
#246279=CARTESIAN_POINT ( 'NONE',  ( 21.14999999999999503, -3.187427350888460076, -228.3200064793908837 ) ) ;
#246282=EDGE_CURVE ( 'NONE', #165408, #239412, #78999, .T. ) ;
#246298=DIRECTION ( 'NONE',  ( 0.000000000000000000, -0.8814952561688449428, 0.4721928772777310157 ) ) ;
#246333=EDGE_CURVE ( 'NONE', #16880, #194489, #145658, .T. ) ;
#246348=CARTESIAN_POINT ( 'NONE',  ( -20.64999999999999858, 19.98118924431957311, -235.6825596947570602 ) ) ;
#246365=DIRECTION ( 'NONE',  ( 0.000000000000000000, 0.9740678456249560746, -0.2262561206234139088 ) ) ;
#246368=EDGE_CURVE ( 'NONE', #91747, #190272, #137293, .T. ) ;
#246399=ORIENTED_EDGE ( 'NONE', *, *, #214076, .F. ) ;
#246407=LINE ( 'NONE', #205994, #114505 ) ;
#246411=DIRECTION ( 'NONE',  ( 1.000000000000000000, 0.000000000000000000, 0.000000000000000000 ) ) ;
#246412=VERTEX_POINT ( 'NONE', #114427 ) ;
#246417=DIRECTION ( 'NONE',  ( -0.000000000000000000, 0.9371753822965236402, -0.3488585713686349066 ) ) ;
#246442=CARTESIAN_POINT ( 'NONE',  ( -23.25000000000000000, 43.21392023178790964, -245.1418509714632421 ) ) ;
#246445=DIRECTION ( 'NONE',  ( 0.000000000000000000, -0.8814952561688430555, 0.4721928772777346239 ) ) ;
#246459=EDGE_LOOP ( 'NONE', ( #179770, #129, #90362, #88091 ) ) ;
#246474=CIRCLE ( 'NONE', #238086, 0.09999999999999939493 ) ;
#246507=VERTEX_POINT ( 'NONE', #101223 ) ;
#246528=DIRECTION ( 'NONE',  ( -3.265361837132812600E-16, 0.4721928772777346239, 0.8814952561688430555 ) ) ;
#246529=AXIS2_PLACEMENT_3D ( 'NONE', #106831, #142117, #140845 ) ;
#246573=EDGE_CURVE ( 'NONE', #6683, #136089, #40052, .T. ) ;
#246575=EDGE_LOOP ( 'NONE', ( #257999, #210951, #211392, #251007 ) ) ;
#246591=DIRECTION ( 'NONE',  ( 0.000000000000000000, 0.5273008465188072647, -0.8496786552930167824 ) ) ;
#246628=ORIENTED_EDGE ( 'NONE', *, *, #49141, .T. ) ;
#246691=ORIENTED_EDGE ( 'NONE', *, *, #181391, .F. ) ;
#246700=CARTESIAN_POINT ( 'NONE',  ( 19.86930884467611946, 34.45481642863170890, -235.1124302486271347 ) ) ;
#246701=ORIENTED_EDGE ( 'NONE', *, *, #244384, .T. ) ;
#246707=ORIENTED_EDGE ( 'NONE', *, *, #209350, .F. ) ;
#246710=EDGE_LOOP ( 'NONE', ( #87640, #99966, #75075, #229893 ) ) ;
#246715=VERTEX_POINT ( 'NONE', #191105 ) ;
#246729=ORIENTED_EDGE ( 'NONE', *, *, #34716, .T. ) ;
#246747=EDGE_LOOP ( 'NONE', ( #113063, #83496, #233024, #228962, #138302 ) ) ;
#246750=VERTEX_POINT ( 'NONE', #90684 ) ;
#246756=ORIENTED_EDGE ( 'NONE', *, *, #215335, .T. ) ;
#246782=SPHERICAL_SURFACE ( 'NONE', #161199, 0.1000000000000000056 ) ;
#246795=EDGE_CURVE ( 'NONE', #4633, #251099, #100034, .T. ) ;
#246847=AXIS2_PLACEMENT_3D ( 'NONE', #235749, #257834, #40160 ) ;
#246848=ADVANCED_FACE ( 'NONE', ( #1533 ), #225123, .F. ) ;
#246852=CARTESIAN_POINT ( 'NONE',  ( -21.08621493067320429, 1.558495345345466188, -230.6850742879884137 ) ) ;
#246867=CIRCLE ( 'NONE', #121974, 0.09999999999999939493 ) ;
#246873=CARTESIAN_POINT ( 'NONE',  ( 20.94999999999999574, 4.436385504674529301, -245.3241086753762659 ) ) ;
#246886=DIRECTION ( 'NONE',  ( 0.000000000000000000, 0.5868805631290340274, 0.8096735173027138632 ) ) ;
#246914=CARTESIAN_POINT ( 'NONE',  ( -18.59999999999999787, 2.319530388122570841, -217.8268657444419887 ) ) ;
#246916=FACE_OUTER_BOUND ( 'NONE', #214025, .T. ) ;
#246945=CARTESIAN_POINT ( 'NONE',  ( -18.59999999999999787, 18.81339837015603322, -226.7756228984618190 ) ) ;
#247003=CARTESIAN_POINT ( 'NONE',  ( 21.05000000000000071, 9.997527148596393687, -228.1702915402975407 ) ) ;
#247014=EDGE_CURVE ( 'NONE', #140654, #39363, #246001, .T. ) ;
#247023=LINE ( 'NONE', #171398, #98675 ) ;
#247039=CIRCLE ( 'NONE', #59771, 0.09999999999999939493 ) ;
#247061=VECTOR ( 'NONE', #164219, 1000.000000000000000 ) ;
#247076=EDGE_CURVE ( 'NONE', #114431, #223845, #108451, .T. ) ;
#247088=EDGE_LOOP ( 'NONE', ( #72963, #51040, #13604, #79852, #66610, #203371, #23622 ) ) ;
#247112=DIRECTION ( 'NONE',  ( 0.000000000000000000, 0.4721928772778128947, 0.8814952561688012000 ) ) ;
#247131=CIRCLE ( 'NONE', #193183, 0.1000000000000012546 ) ;
#247157=FACE_OUTER_BOUND ( 'NONE', #27003, .T. ) ;
#247216=LINE ( 'NONE', #227652, #129501 ) ;
#247217=VECTOR ( 'NONE', #176746, 1000.000000000000000 ) ;
#247238=DIRECTION ( 'NONE',  ( 0.000000000000000000, 0.8814952561688513821, -0.4721928772777189698 ) ) ;
#247317=ORIENTED_EDGE ( 'NONE', *, *, #93407, .T. ) ;
#247345=FACE_OUTER_BOUND ( 'NONE', #1917, .T. ) ;
#247348=( BOUNDED_SURFACE ( )  B_SPLINE_SURFACE ( 3, 2, ( 
 ( #255220, #14123, #34988 ),
 ( #76631, #156205, #235702 ),
 ( #57041, #231886, #111937 ),
 ( #53227, #37526, #91071 ),
 ( #170661, #250146, #132786 ),
 ( #131478, #211021, #32414 ) ),
 .UNSPECIFIED., .F., .F., .F. ) 
 B_SPLINE_SURFACE_WITH_KNOTS ( ( 4, 2, 4 ),
 ( 3, 3 ),
 ( 0.0001381104793128129277, 0.0002947094729387753141, 0.0004513084665647377276 ),
 ( 0.000000000000000000, 1.000000000000000000 ),
 .UNSPECIFIED. ) 
 GEOMETRIC_REPRESENTATION_ITEM ( )  RATIONAL_B_SPLINE_SURFACE ( (
 ( 1.000000000000000000, 0.7071067811864075736, 1.000000000000000000),
 ( 1.000000000000000000, 0.6919563088091734704, 1.000000000000000000),
 ( 1.000000000000000000, 0.6959445945726734362, 1.000000000000000000),
 ( 1.000000000000000000, 0.7137882985306041039, 1.000000000000000000),
 ( 1.000000000000000000, 0.7257496306101467454, 1.000000000000000000),
 ( 1.000000000000000000, 0.7250110520820811644, 1.000000000000000000) ) ) 
 REPRESENTATION_ITEM ( '' )  SURFACE ( )  );
#247443=CARTESIAN_POINT ( 'NONE',  ( -20.95613430942368538, 18.72165599329057883, -226.6130354132794480 ) ) ;
#247479=DIRECTION ( 'NONE',  ( 0.000000000000000000, -0.8814952561688428334, 0.4721928772777350680 ) ) ;
#247488=ADVANCED_FACE ( 'NONE', ( #68942 ), #108054, .T. ) ;
#247530=EDGE_LOOP ( 'NONE', ( #102798, #43302, #205853, #124938 ) ) ;
#247551=CARTESIAN_POINT ( 'NONE',  ( 21.05000000000000071, 20.42498087366621817, -235.1829032864613396 ) ) ;
#247565=CARTESIAN_POINT ( 'NONE',  ( -20.64999999999999858, 29.14863708059993286, -237.4168895852561434 ) ) ;
#247570=PLANE ( 'NONE',  #99555 ) ;
#247575=AXIS2_PLACEMENT_3D ( 'NONE', #214973, #36369, #195442 ) ;
#247579=CIRCLE ( 'NONE', #56015, 0.09999999999999791001 ) ;
#247595=DIRECTION ( 'NONE',  ( -0.000000000000000000, 0.8127272543711119290, -0.5826443254700023333 ) ) ;
#247640=DIRECTION ( 'NONE',  ( -1.000000000000000000, 0.000000000000000000, 0.000000000000000000 ) ) ;
#247657=VECTOR ( 'NONE', #106178, 1000.000000000000000 ) ;
#247708=ORIENTED_EDGE ( 'NONE', *, *, #126761, .T. ) ;
#247714=CARTESIAN_POINT ( 'NONE',  ( 20.95512820512820795, 22.07448326904560076, -231.6692507597321935 ) ) ;
#247753=ORIENTED_EDGE ( 'NONE', *, *, #100477, .T. ) ;
#247762=CARTESIAN_POINT ( 'NONE',  ( -20.85000000000000142, 36.65892442174935439, -249.5511627012433848 ) ) ;
#247772=DIRECTION ( 'NONE',  ( 0.000000000000000000, 0.4721928772777346239, 0.8814952561688430555 ) ) ;
#247810=DIRECTION ( 'NONE',  ( 0.000000000000000000, 0.8814952561688430555, -0.4721928772777346239 ) ) ;
#247842=DIRECTION ( 'NONE',  ( -0.000000000000000000, 0.03181660087582099256, -0.9994937237965573207 ) ) ;
#247849=CYLINDRICAL_SURFACE ( 'NONE', #38492, 0.09999999999999031886 ) ;
#247851=CARTESIAN_POINT ( 'NONE',  ( -21.64999999999999858, 21.48591740176965814, -233.0852932139783036 ) ) ;
#247869=EDGE_LOOP ( 'NONE', ( #108913, #161058, #140685 ) ) ;
#247935=AXIS2_PLACEMENT_3D ( 'NONE', #42706, #105199, #184775 ) ;
#247942=DIRECTION ( 'NONE',  ( -1.000000000000000000, -1.541880601228652843E-16, -2.878400969107353907E-16 ) ) ;
#247970=DIRECTION ( 'NONE',  ( 0.000000000000000000, -0.8814952561688476074, 0.4721928772777262417 ) ) ;
#247983=CIRCLE ( 'NONE', #77292, 0.09999999999999716060 ) ;
#247996=FACE_OUTER_BOUND ( 'NONE', #251503, .T. ) ;
#248040=AXIS2_PLACEMENT_3D ( 'NONE', #81786, #203047, #101331 ) ;
#248047=VERTEX_POINT ( 'NONE', #49038 ) ;
#248053=CYLINDRICAL_SURFACE ( 'NONE', #210559, 7.899999999999994138 ) ;
#248063=VECTOR ( 'NONE', #853, 1000.000000000000000 ) ;
#248068=DIRECTION ( 'NONE',  ( 0.000000000000000000, 0.4721928772777330696, 0.8814952561688439436 ) ) ;
#248167=EDGE_LOOP ( 'NONE', ( #246707, #118428, #15859, #117787 ) ) ;
#248168=EDGE_CURVE ( 'NONE', #18671, #197260, #92416, .T. ) ;
#248176=( BOUNDED_CURVE ( )  B_SPLINE_CURVE ( 3, ( #234124, #150749, #252391, #154630 ),
 .UNSPECIFIED., .F., .F. ) 
 B_SPLINE_CURVE_WITH_KNOTS ( ( 4, 4 ),
 ( 4.712388980384690562, 6.283185307179586232 ),
 .UNSPECIFIED. ) 
 CURVE ( )  GEOMETRIC_REPRESENTATION_ITEM ( )  RATIONAL_B_SPLINE_CURVE ( ( 1.000000000000000000, 0.8047378541243652705, 0.8047378541243652705, 1.000000000000000000 ) ) 
 REPRESENTATION_ITEM ( '' )  );
#248185=EDGE_CURVE ( 'NONE', #109684, #170534, #83996, .T. ) ;
#248190=DIRECTION ( 'NONE',  ( -1.000000000000000000, 0.000000000000000000, 0.000000000000000000 ) ) ;
#248204=CARTESIAN_POINT ( 'NONE',  ( -23.15000000000000213, 12.62988036037870643, -223.4632815780722410 ) ) ;
#248212=AXIS2_PLACEMENT_3D ( 'NONE', #177134, #139232, #57129 ) ;
#248224=CARTESIAN_POINT ( 'NONE',  ( -18.59999999999999787, 45.93315328338058379, -256.6017782078560003 ) ) ;
#248244=ORIENTED_EDGE ( 'NONE', *, *, #117927, .F. ) ;
#248249=DIRECTION ( 'NONE',  ( 0.000000000000000000, -0.8009761297185381546, 0.5986962832865355688 ) ) ;
#248282=ADVANCED_FACE ( 'NONE', ( #206530 ), #128287, .T. ) ;
#248290=CARTESIAN_POINT ( 'NONE',  ( 21.09551895715259207, 22.93116773457091284, -230.1482378004415352 ) ) ;
#248296=CARTESIAN_POINT ( 'NONE',  ( 21.30000000000002558, 10.69888912757691024, -235.6450824654141059 ) ) ;
#248298=EDGE_LOOP ( 'NONE', ( #177038, #227052, #238632 ) ) ;
#248317=DIRECTION ( 'NONE',  ( -0.000000000000000000, -0.8814952561688430555, 0.4721928772777346239 ) ) ;
#248330=DIRECTION ( 'NONE',  ( -0.000000000000000000, -0.3280696808754172689, -0.9446535261620008228 ) ) ;
#248333=CARTESIAN_POINT ( 'NONE',  ( 20.85000000000000142, 36.65892442174935439, -249.5511627012433848 ) ) ;
#248340=ORIENTED_EDGE ( 'NONE', *, *, #187398, .F. ) ;
#248362=ORIENTED_EDGE ( 'NONE', *, *, #161076, .T. ) ;
#248420=ORIENTED_EDGE ( 'NONE', *, *, #3142, .T. ) ;
#248431=CIRCLE ( 'NONE', #131731, 0.09999999999999939493 ) ;
#248436=CARTESIAN_POINT ( 'NONE',  ( -20.64999999999999858, 36.65892442174935439, -249.5511627012433848 ) ) ;
#248457=CARTESIAN_POINT ( 'NONE',  ( 20.94999999999999929, 36.65892442174935439, -249.5511627012433848 ) ) ;
#248459=DIRECTION ( 'NONE',  ( -4.239556034732055511E-17, -0.8127272543710951647, 0.5826443254700256480 ) ) ;
#248463=LINE ( 'NONE', #168967, #45618 ) ;
#248473=VERTEX_POINT ( 'NONE', #238939 ) ;
#248484=EDGE_CURVE ( 'NONE', #15834, #108480, #197233, .T. ) ;
#248508=CARTESIAN_POINT ( 'NONE',  ( 20.94999999999999574, 18.75483929237739744, -228.0790484105328630 ) ) ;
#248515=CARTESIAN_POINT ( 'NONE',  ( 20.94999999999999929, 18.47808476326695271, -239.8121846073901224 ) ) ;
#248516=AXIS2_PLACEMENT_3D ( 'NONE', #104425, #183989, #84850 ) ;
#248518=FACE_OUTER_BOUND ( 'NONE', #72356, .T. ) ;
#248534=CARTESIAN_POINT ( 'NONE',  ( -23.15000000000000213, 26.47476584046484049, -241.8269156386531051 ) ) ;
#248537=CARTESIAN_POINT ( 'NONE',  ( 21.11747605621531321, 22.06760108001729748, -231.7761073644578573 ) ) ;
#248599=DIRECTION ( 'NONE',  ( 1.836970198721029441E-16, -0.4721928772777346239, -0.8814952561688430555 ) ) ;
#248611=AXIS2_PLACEMENT_3D ( 'NONE', #74972, #241420, #95770 ) ;
#248619=ORIENTED_EDGE ( 'NONE', *, *, #170955, .T. ) ;
#248626=AXIS2_PLACEMENT_3D ( 'NONE', #207279, #9054, #226814 ) ;
#248630=CARTESIAN_POINT ( 'NONE',  ( 18.53317502108576420, 46.43483777265582546, -243.0774829958280918 ) ) ;
#248634=DIRECTION ( 'NONE',  ( 0.000000000000000000, -0.8814952561688444987, 0.4721928772777320149 ) ) ;
#248643=EDGE_CURVE ( 'NONE', #137151, #217322, #5091, .T. ) ;
#248691=CARTESIAN_POINT ( 'NONE',  ( -21.05000000000000071, 28.42524210734032053, -258.3567845160494585 ) ) ;
#248693=CARTESIAN_POINT ( 'NONE',  ( -18.59999999999999787, 22.38308386859736032, -231.4104522272575082 ) ) ;
#248702=CYLINDRICAL_SURFACE ( 'NONE', #37672, 7.899999999999994138 ) ;
#248754=EDGE_CURVE ( 'NONE', #39320, #58384, #113077, .T. ) ;
#248760=CIRCLE ( 'NONE', #148812, 0.1000000000000013933 ) ;
#248764=AXIS2_PLACEMENT_3D ( 'NONE', #68542, #201622, #205463 ) ;
#248777=CARTESIAN_POINT ( 'NONE',  ( -23.15000000000000213, 28.50120599808395028, -258.2149742250584268 ) ) ;
#248791=CARTESIAN_POINT ( 'NONE',  ( -18.50000000000000000, 9.783112580922244561, -245.9316685519929422 ) ) ;
#248838=VERTEX_POINT ( 'NONE', #19249 ) ;
#248855=DIRECTION ( 'NONE',  ( -1.000000000000000000, -8.674042436075353235E-17, -1.619280515896125144E-16 ) ) ;
#248870=VERTEX_POINT ( 'NONE', #119649 ) ;
#248872=AXIS2_PLACEMENT_3D ( 'NONE', #15431, #254009, #235730 ) ;
#248878=DIRECTION ( 'NONE',  ( 0.000000000000000000, 0.8814952561688476074, -0.4721928772777262417 ) ) ;
#248941=EDGE_LOOP ( 'NONE', ( #88584, #236367, #87076 ) ) ;
#248947=VERTEX_POINT ( 'NONE', #46495 ) ;
#248949=AXIS2_PLACEMENT_3D ( 'NONE', #137803, #76561, #14045 ) ;
#248952=CARTESIAN_POINT ( 'NONE',  ( -20.94999999999999929, 31.15787740146373253, -259.8205824356103903 ) ) ;
#248968=CARTESIAN_POINT ( 'NONE',  ( -18.50000000000000000, 23.38726701055792745, -229.1122755113798632 ) ) ;
#249025=ORIENTED_EDGE ( 'NONE', *, *, #158474, .T. ) ;
#249027=LINE ( 'NONE', #230744, #70819 ) ;
#249054=CARTESIAN_POINT ( 'NONE',  ( -23.15000000000000213, 11.60058429089262333, -246.3380203656811887 ) ) ;
#249073=FACE_OUTER_BOUND ( 'NONE', #73686, .T. ) ;
#249080=CARTESIAN_POINT ( 'NONE',  ( -23.25000000000000000, 1.580567032079710055, -244.0902705724231794 ) ) ;
#249089=AXIS2_PLACEMENT_3D ( 'NONE', #48560, #207659, #9433 ) ;
#249100=DIRECTION ( 'NONE',  ( -0.000000000000000000, 0.4721928772777346239, 0.8814952561688430555 ) ) ;
#249106=CARTESIAN_POINT ( 'NONE',  ( -21.04999999999997584, 1.442680752426173552, -230.7068865970040861 ) ) ;
#249115=CARTESIAN_POINT ( 'NONE',  ( 23.14999999999999503, 2.272311100394802885, -217.9150152700588592 ) ) ;
#249124=CARTESIAN_POINT ( 'NONE',  ( 18.59999999999999076, 30.76917518201224055, -234.8152055956155380 ) ) ;
#249188=VERTEX_POINT ( 'NONE', #27831 ) ;
#249199=DIRECTION ( 'NONE',  ( 0.000000000000000000, 0.8814952561688430555, -0.4721928772777346239 ) ) ;
#249242=VECTOR ( 'NONE', #193299, 1000.000000000000000 ) ;
#249251=DIRECTION ( 'NONE',  ( 0.000000000000000000, -0.8814952561688430555, 0.4721928772777346239 ) ) ;
#249265=CIRCLE ( 'NONE', #232536, 0.1999999999999959310 ) ;
#249274=CIRCLE ( 'NONE', #170196, 0.09999999999999605038 ) ;
#249281=PRODUCT ( 'Injection Molded Chain Links 8', 'Injection Molded Chain Links 8', '', ( #53511 ) ) ;
#249309=ADVANCED_FACE ( 'NONE', ( #68601 ), #103841, .T. ) ;
#249315=ORIENTED_EDGE ( 'NONE', *, *, #162874, .F. ) ;
#249324=AXIS2_PLACEMENT_3D ( 'NONE', #103658, #200221, #3278 ) ;
#249339=VECTOR ( 'NONE', #58358, 1000.000000000000000 ) ;
#249377=AXIS2_PLACEMENT_3D ( 'NONE', #153134, #111401, #115246 ) ;
#249443=DIRECTION ( 'NONE',  ( -1.000000000000000000, -0.000000000000000000, -0.000000000000000000 ) ) ;
#249480=CARTESIAN_POINT ( 'NONE',  ( -21.14999999999999858, 12.71802988599559292, -223.5105008658000258 ) ) ;
#249503=ORIENTED_EDGE ( 'NONE', *, *, #256019, .T. ) ;
#249538=CARTESIAN_POINT ( 'NONE',  ( -23.15000000000000213, 19.96675702282871256, -237.7735354486364088 ) ) ;
#249555=DIRECTION ( 'NONE',  ( 0.000000000000000000, 0.8814952561688438326, -0.4721928772777334582 ) ) ;
#249560=DIRECTION ( 'NONE',  ( 1.000000000000000000, 0.000000000000000000, 0.000000000000000000 ) ) ;
#249569=AXIS2_PLACEMENT_3D ( 'NONE', #55022, #254501, #137152 ) ;
#249571=CARTESIAN_POINT ( 'NONE',  ( 21.05000000000000071, 18.65488991999774271, -228.0822300706204544 ) ) ;
#249590=DIRECTION ( 'NONE',  ( 0.000000000000000000, -0.8814952561688423893, 0.4721928772777359007 ) ) ;
#249627=AXIS2_PLACEMENT_3D ( 'NONE', #153848, #114667, #75568 ) ;
#249632=CARTESIAN_POINT ( 'NONE',  ( -18.41418431465368144, 37.99112772578840236, -261.0419300540664267 ) ) ;
#249678=DIRECTION ( 'NONE',  ( 0.000000000000000000, 0.8814952561688442767, -0.4721928772777322925 ) ) ;
#249681=AXIS2_PLACEMENT_3D ( 'NONE', #181075, #7203, #2394 ) ;
#249769=EDGE_LOOP ( 'NONE', ( #223395, #41949, #72800 ) ) ;
#249772=CARTESIAN_POINT ( 'NONE',  ( -18.59999999999999787, 42.96960653111219131, -254.4772109693542745 ) ) ;
#249810=DIRECTION ( 'NONE',  ( 0.000000000000000000, -0.8814952561688429444, 0.4721928772777347905 ) ) ;
#249816=EDGE_CURVE ( 'NONE', #229988, #78573, #167413, .T. ) ;
#249856=CIRCLE ( 'NONE', #79148, 0.1000000000000075273 ) ;
#249867=CARTESIAN_POINT ( 'NONE',  ( 20.85000000000000142, 43.24695311518262031, -245.0026972281755491 ) ) ;
#249890=VERTEX_POINT ( 'NONE', #75994 ) ;
#249912=CARTESIAN_POINT ( 'NONE',  ( 18.49999999999997158, 9.105964803472787139, -245.3658845043482586 ) ) ;
#249924=DIRECTION ( 'NONE',  ( -1.000000000000000000, 0.000000000000000000, 0.000000000000000000 ) ) ;
#249926=EDGE_CURVE ( 'NONE', #215045, #123093, #216779, .T. ) ;
#249929=CARTESIAN_POINT ( 'NONE',  ( 21.05000000000000071, 18.81732247075047582, -230.0377732242114632 ) ) ;
#249966=TOROIDAL_SURFACE ( 'NONE', #166608, 0.2000000000000000111, 0.1000000000000000056 ) ;
#249991=FACE_OUTER_BOUND ( 'NONE', #134424, .T. ) ;
#249997=ORIENTED_EDGE ( 'NONE', *, *, #103249, .T. ) ;
#250005=ORIENTED_EDGE ( 'NONE', *, *, #53108, .F. ) ;
#250009=CARTESIAN_POINT ( 'NONE',  ( 23.15000000000000213, 12.37888392014804850, -249.8746333190754285 ) ) ;
#250010=ORIENTED_EDGE ( 'NONE', *, *, #149687, .F. ) ;
#250034=DIRECTION ( 'NONE',  ( 0.000000000000000000, -0.4721928772777346239, -0.8814952561688430555 ) ) ;
#250053=CARTESIAN_POINT ( 'NONE',  ( 22.49999999999999645, -3.098441969362629944, -228.1534806676847893 ) ) ;
#250072=EDGE_CURVE ( 'NONE', #198947, #248473, #113624, .T. ) ;
#250079=DIRECTION ( 'NONE',  ( -0.000000000000000000, 0.8096735173027155286, -0.5868805631290315850 ) ) ;
#250083=EDGE_LOOP ( 'NONE', ( #16051, #195851, #126203, #138110 ) ) ;
#250092=CIRCLE ( 'NONE', #141739, 7.800000000000009592 ) ;
#250111=EDGE_CURVE ( 'NONE', #223188, #107706, #146223, .T. ) ;
#250120=EDGE_CURVE ( 'NONE', #132943, #30797, #108400, .T. ) ;
#250146=CARTESIAN_POINT ( 'NONE',  ( 21.05000005001341989, 22.05259145179880420, -231.6630504590253565 ) ) ;
#250173=VECTOR ( 'NONE', #12762, 1000.000000000000000 ) ;
#250186=DIRECTION ( 'NONE',  ( -5.603264701231742896E-32, 0.8814952561688430555, -0.4721928772777344019 ) ) ;
#250188=VERTEX_POINT ( 'NONE', #190525 ) ;
#250211=FACE_OUTER_BOUND ( 'NONE', #190943, .T. ) ;
#250214=EDGE_CURVE ( 'NONE', #70494, #161523, #91406, .T. ) ;
#250266=DIRECTION ( 'NONE',  ( -0.000000000000000000, 0.4721928772777345684, 0.8814952561688429444 ) ) ;
#250267=VERTEX_POINT ( 'NONE', #136938 ) ;
#250328=CARTESIAN_POINT ( 'NONE',  ( 21.05000000000000071, 12.19249617487739812, -224.2797955561429148 ) ) ;
#250407=EDGE_CURVE ( 'NONE', #184383, #149228, #123803, .T. ) ;
#250416=EDGE_CURVE ( 'NONE', #18374, #191683, #83352, .T. ) ;
#250423=TOROIDAL_SURFACE ( 'NONE', #212841, 4.099999999999999645, 0.1000000000000000056 ) ;
#250469=ORIENTED_EDGE ( 'NONE', *, *, #52197, .T. ) ;
#250504=CARTESIAN_POINT ( 'NONE',  ( 23.14999999999999858, 20.70829660003285611, -234.6540061327600597 ) ) ;
#250509=CIRCLE ( 'NONE', #212926, 0.1000000000000013933 ) ;
#250513=FACE_OUTER_BOUND ( 'NONE', #242901, .T. ) ;
#250516=CARTESIAN_POINT ( 'NONE',  ( -23.25000000000000000, 20.01397631055648674, -237.6853859230195098 ) ) ;
#250565=CARTESIAN_POINT ( 'NONE',  ( 20.50589344624752286, 18.75447916118790914, -228.0677351699049495 ) ) ;
#250570=ORIENTED_EDGE ( 'NONE', *, *, #136672, .F. ) ;
#250592=VERTEX_POINT ( 'NONE', #115782 ) ;
#250636=CARTESIAN_POINT ( 'NONE',  ( 18.44206774312972641, 38.01831701715774869, -261.0463157240239980 ) ) ;
#250639=VERTEX_POINT ( 'NONE', #137889 ) ;
#250647=CARTESIAN_POINT ( 'NONE',  ( 21.13614978966382552, 1.399903376081983231, -230.6638703635511831 ) ) ;
#250686=DIRECTION ( 'NONE',  ( 0.000000000000000000, 0.8814952561688476074, -0.4721928772777262417 ) ) ;
#250690=ORIENTED_EDGE ( 'NONE', *, *, #11424, .F. ) ;
#250709=CARTESIAN_POINT ( 'NONE',  ( -21.55000000000000426, 29.41239393758413811, -236.9245051605820720 ) ) ;
#250710=EDGE_CURVE ( 'NONE', #19770, #226091, #5621, .T. ) ;
#250716=DIRECTION ( 'NONE',  ( 1.000000000000000000, 0.000000000000000000, 0.000000000000000000 ) ) ;
#250726=DIRECTION ( 'NONE',  ( 0.000000000000000000, 0.8496786552930111203, 0.5273008465188163685 ) ) ;
#250729=ADVANCED_FACE ( 'NONE', ( #38823 ), #53245, .F. ) ;
#250735=EDGE_CURVE ( 'NONE', #34617, #99386, #76366, .T. ) ;
#250750=DIRECTION ( 'NONE',  ( 1.000000000000000000, 0.000000000000000000, 0.000000000000000000 ) ) ;
#250751=DIRECTION ( 'NONE',  ( 0.000000000000000000, -0.8814952561688428334, 0.4721928772777349570 ) ) ;
#250755=CARTESIAN_POINT ( 'NONE',  ( 23.15000000000000213, 11.60058429089262333, -246.3380203656811887 ) ) ;
#250781=ORIENTED_EDGE ( 'NONE', *, *, #181940, .T. ) ;
#250821=EDGE_CURVE ( 'NONE', #88325, #53791, #72313, .T. ) ;
#250867=VECTOR ( 'NONE', #176596, 1000.000000000000000 ) ;
#250871=DIRECTION ( 'NONE',  ( 0.000000000000000000, 0.8814952561688407240, -0.4721928772777390093 ) ) ;
#250914=CARTESIAN_POINT ( 'NONE',  ( 18.59999999999999076, 34.58225676390223668, -235.1091250528070589 ) ) ;
#250963=CARTESIAN_POINT ( 'NONE',  ( 23.25000000000000000, -8.777002227904191045, -238.5420042644097975 ) ) ;
#251007=ORIENTED_EDGE ( 'NONE', *, *, #160343, .T. ) ;
#251061=DIRECTION ( 'NONE',  ( 1.000000000000000000, -0.000000000000000000, -0.000000000000000000 ) ) ;
#251085=DIRECTION ( 'NONE',  ( 0.000000000000000000, 0.8814952561688444987, -0.4721928772777320149 ) ) ;
#251089=CARTESIAN_POINT ( 'NONE',  ( 21.13920837816993270, 22.07453692459872130, -231.7746734506518749 ) ) ;
#251099=VERTEX_POINT ( 'NONE', #47151 ) ;
#251125=CYLINDRICAL_SURFACE ( 'NONE', #97591, 0.5000000000000008882 ) ;
#251199=PLANE ( 'NONE',  #80327 ) ;
#251213=CARTESIAN_POINT ( 'NONE',  ( -20.94560253601877164, 36.04561250502853653, -235.8930046631029711 ) ) ;
#251226=DIRECTION ( 'NONE',  ( 0.000000000000000000, -0.8814952561688476074, 0.4721928772777262417 ) ) ;
#251245=AXIS2_PLACEMENT_3D ( 'NONE', #139235, #63564, #103960 ) ;
#251262=ORIENTED_EDGE ( 'NONE', *, *, #209126, .F. ) ;
#251295=ORIENTED_EDGE ( 'NONE', *, *, #21185, .F. ) ;
#251308=AXIS2_PLACEMENT_3D ( 'NONE', #76321, #78884, #161031 ) ;
#251319=CARTESIAN_POINT ( 'NONE',  ( -20.94999999999999929, 28.50120599808395028, -258.2149742250584268 ) ) ;
#251324=CARTESIAN_POINT ( 'NONE',  ( -21.59780538579341425, 10.27473149069560243, -227.6502864689491048 ) ) ;
#251344=CARTESIAN_POINT ( 'NONE',  ( -18.59999999999999787, 16.50669723772569952, -240.7258389668962479 ) ) ;
#251350=DIRECTION ( 'NONE',  ( 1.000000000000000000, 8.855395344894292773E-17, 1.653135691717061729E-16 ) ) ;
#251471=FACE_OUTER_BOUND ( 'NONE', #102334, .T. ) ;
#251485=DIRECTION ( 'NONE',  ( 1.000000000000000000, 0.000000000000000000, 0.000000000000000000 ) ) ;
#251499=EDGE_CURVE ( 'NONE', #248870, #15247, #181004, .T. ) ;
#251503=EDGE_LOOP ( 'NONE', ( #257465, #135687, #249315, #28356, #17582, #33758, #28536, #203342, #104117, #151716, #193807, #130904 ) ) ;
#251505=AXIS2_PLACEMENT_3D ( 'NONE', #221323, #257855, #96253 ) ;
#251564=ORIENTED_EDGE ( 'NONE', *, *, #3776, .T. ) ;
#251565=ORIENTED_EDGE ( 'NONE', *, *, #242883, .F. ) ;
#251572=FACE_OUTER_BOUND ( 'NONE', #175357, .T. ) ;
#251588=VECTOR ( 'NONE', #8768, 1000.000000000000000 ) ;
#251655=CARTESIAN_POINT ( 'NONE',  ( -21.11833042828132889, 1.450380929312672817, -230.6828547334855841 ) ) ;
#251657=AXIS2_PLACEMENT_3D ( 'NONE', #156261, #175810, #177104 ) ;
#251691=EDGE_CURVE ( 'NONE', #159519, #3782, #14427, .T. ) ;
#251694=AXIS2_PLACEMENT_3D ( 'NONE', #111046, #147604, #188027 ) ;
#251712=AXIS2_PLACEMENT_3D ( 'NONE', #210731, #89483, #208182 ) ;
#251728=DIRECTION ( 'NONE',  ( 0.000000000000000000, -0.4721928772777352346, -0.8814952561688428334 ) ) ;
#251742=DIRECTION ( 'NONE',  ( -0.000000000000000000, 0.4721928772777345684, 0.8814952561688429444 ) ) ;
#251749=VERTEX_POINT ( 'NONE', #27348 ) ;
#251762=VECTOR ( 'NONE', #37200, 1000.000000000000000 ) ;
#251798=VECTOR ( 'NONE', #202361, 1000.000000000000000 ) ;
#251800=ORIENTED_EDGE ( 'NONE', *, *, #20177, .T. ) ;
#251809=VERTEX_POINT ( 'NONE', #33769 ) ;
#251825=ORIENTED_EDGE ( 'NONE', *, *, #55286, .F. ) ;
#251840=CARTESIAN_POINT ( 'NONE',  ( -18.59999999999999787, 45.93315328338058379, -256.6017782078560003 ) ) ;
#251842=DIRECTION ( 'NONE',  ( 0.000000000000000000, 0.8814952561688444987, -0.4721928772777320149 ) ) ;
#251850=CARTESIAN_POINT ( 'NONE',  ( 20.96937028524354929, 18.74928867235112051, -227.9046800076639840 ) ) ;
#251869=EDGE_LOOP ( 'NONE', ( #235408, #170719, #169955, #192626 ) ) ;
#251898=CARTESIAN_POINT ( 'NONE',  ( 20.95483826173899899, 18.85359715731150487, -229.9438933533002967 ) ) ;
#251910=EDGE_CURVE ( 'NONE', #2694, #181045, #235328, .T. ) ;
#251919=EDGE_CURVE ( 'NONE', #13152, #92492, #204327, .T. ) ;
#251922=EDGE_CURVE ( 'NONE', #246750, #146046, #160360, .T. ) ;
#251953=CARTESIAN_POINT ( 'NONE',  ( -18.59999999999999787, 43.26562470876307742, -245.1245614952171081 ) ) ;
#252020=ORIENTED_EDGE ( 'NONE', *, *, #212451, .T. ) ;
#252034=LINE ( 'NONE', #229909, #138696 ) ;
#252037=LINE ( 'NONE', #73436, #164611 ) ;
#252038=CIRCLE ( 'NONE', #31322, 0.09999999999999939493 ) ;
#252069=CIRCLE ( 'NONE', #68938, 0.1000000000000013933 ) ;
#252084=DIRECTION ( 'NONE',  ( -1.000000000000000000, -0.000000000000000000, -0.000000000000000000 ) ) ;
#252087=CARTESIAN_POINT ( 'NONE',  ( 23.14999999999999858, 18.47808476326694915, -239.8121846073901224 ) ) ;
#252111=AXIS2_PLACEMENT_3D ( 'NONE', #120702, #119398, #20307 ) ;
#252128=DIRECTION ( 'NONE',  ( 0.000000000000000000, -0.4721928772776434191, -0.8814952561688919053 ) ) ;
#252135=VECTOR ( 'NONE', #45664, 1000.000000000000000 ) ;
#252158=ORIENTED_EDGE ( 'NONE', *, *, #48714, .T. ) ;
#252166=EDGE_CURVE ( 'NONE', #231732, #54600, #85450, .T. ) ;
#252169=ORIENTED_EDGE ( 'NONE', *, *, #254840, .T. ) ;
#252170=CARTESIAN_POINT ( 'NONE',  ( 18.59999999999999076, 19.00443933019177223, -232.7770257915295531 ) ) ;
#252195=EDGE_CURVE ( 'NONE', #4633, #21708, #52958, .T. ) ;
#252209=EDGE_CURVE ( 'NONE', #231732, #114424, #143748, .T. ) ;
#252210=DIRECTION ( 'NONE',  ( 0.000000000000000000, -0.9424537609900501822, -0.3343365196859436339 ) ) ;
#252241=DIRECTION ( 'NONE',  ( 0.000000000000000000, -0.5273008465188072647, 0.8496786552930167824 ) ) ;
#252256=CARTESIAN_POINT ( 'NONE',  ( 21.05000000000000071, 28.67750504931771616, -258.3094128005139396 ) ) ;
#252278=SURFACE_STYLE_USAGE ( .BOTH. , #47652 ) ;
#252286=CARTESIAN_POINT ( 'NONE',  ( 18.59999999999999076, 29.00069016757795026, -237.9048565010683376 ) ) ;
#252289=CARTESIAN_POINT ( 'NONE',  ( -18.59999999999999787, 31.44980407958351165, -233.5445995079518866 ) ) ;
#252292=EDGE_LOOP ( 'NONE', ( #89636, #156754, #183335, #240357 ) ) ;
#252297=VERTEX_POINT ( 'NONE', #4537 ) ;
#252308=EDGE_LOOP ( 'NONE', ( #9520, #189664, #4783, #94606 ) ) ;
#252321=CARTESIAN_POINT ( 'NONE',  ( 20.94999999999999929, 18.81732247075047937, -230.0377732242114632 ) ) ;
#252335=ADVANCED_FACE ( 'NONE', ( #219736 ), #43684, .T. ) ;
#252371=CARTESIAN_POINT ( 'NONE',  ( -20.64999999999999858, 11.60058429089262333, -246.3380203656811887 ) ) ;
#252372=LINE ( 'NONE', #253661, #241249 ) ;
#252379=AXIS2_PLACEMENT_3D ( 'NONE', #125373, #221866, #64111 ) ;
#252391=CARTESIAN_POINT ( 'NONE',  ( 20.93284271247462414, 36.02367271998545561, -235.8812521208699309 ) ) ;
#252399=CIRCLE ( 'NONE', #177455, 0.6000000000000023093 ) ;
#252410=EDGE_CURVE ( 'NONE', #35945, #260, #10236, .T. ) ;
#252426=CARTESIAN_POINT ( 'NONE',  ( -21.07094088545368038, 1.604332817732114336, -230.6611890373810638 ) ) ;
#252437=DIRECTION ( 'NONE',  ( -7.304098846218136639E-16, -0.4721928772777346239, -0.8814952561688430555 ) ) ;
#252438=DIRECTION ( 'NONE',  ( -0.000000000000000000, 0.8127272543710951647, -0.5826443254700256480 ) ) ;
#252479=TOROIDAL_SURFACE ( 'NONE', #185851, 0.2000000000000000111, 0.1000000000000000056 ) ;
#252493=CARTESIAN_POINT ( 'NONE',  ( -23.15000000000000213, 11.60058429089262333, -246.3380203656811887 ) ) ;
#252496=DIRECTION ( 'NONE',  ( 0.000000000000000000, 0.8814952561688429444, -0.4721928772777345684 ) ) ;
#252498=EDGE_LOOP ( 'NONE', ( #245240, #196711, #24245, #142633 ) ) ;
#252501=ORIENTED_EDGE ( 'NONE', *, *, #228821, .T. ) ;
#252504=ORIENTED_EDGE ( 'NONE', *, *, #19889, .F. ) ;
#252531=ORIENTED_EDGE ( 'NONE', *, *, #257784, .F. ) ;
#252533=DIRECTION ( 'NONE',  ( 1.000000000000000000, 0.000000000000000000, 0.000000000000000000 ) ) ;
#252539=ORIENTED_EDGE ( 'NONE', *, *, #48207, .T. ) ;
#252601=CARTESIAN_POINT ( 'NONE',  ( -20.54999999999999716, 27.82649702422227733, -239.8850763025288870 ) ) ;
#252615=DIRECTION ( 'NONE',  ( 0.000000000000000000, -0.4721928772777346239, -0.8814952561688430555 ) ) ;
#252625=CARTESIAN_POINT ( 'NONE',  ( 23.15000000000000213, 28.50120599808395028, -258.2149742250584268 ) ) ;
#252654=CARTESIAN_POINT ( 'NONE',  ( 22.00411653962184033, 10.46655577782818369, -227.2920607449376575 ) ) ;
#252664=CARTESIAN_POINT ( 'NONE',  ( -20.54999999999999716, 24.04029978241812415, -253.0016354099517457 ) ) ;
#252686=CARTESIAN_POINT ( 'NONE',  ( 23.24999999999999289, 5.169232899390497238, -237.3909066255399978 ) ) ;
#252700=DIRECTION ( 'NONE',  ( -0.000000000000000000, -0.8814952561688430555, 0.4721928772777346239 ) ) ;
#252706=ORIENTED_EDGE ( 'NONE', *, *, #88881, .T. ) ;
#252712=CARTESIAN_POINT ( 'NONE',  ( 21.14999999999999503, -8.729782940176418649, -238.4538547387928986 ) ) ;
#252719=ORIENTED_EDGE ( 'NONE', *, *, #54190, .T. ) ;
#252725=DIRECTION ( 'NONE',  ( 0.000000000000000000, 0.4721928772777346239, 0.8814952561688430555 ) ) ;
#252750=DIRECTION ( 'NONE',  ( -1.836970198721029441E-16, 0.4721928772777346239, 0.8814952561688430555 ) ) ;
#252843=DIRECTION ( 'NONE',  ( 1.000000000000000000, 0.000000000000000000, 0.000000000000000000 ) ) ;
#252851=CYLINDRICAL_SURFACE ( 'NONE', #188293, 0.09999999999999939493 ) ;
#252855=DIRECTION ( 'NONE',  ( 0.000000000000000000, 0.8814952561688476074, -0.4721928772777262417 ) ) ;
#252859=ORIENTED_EDGE ( 'NONE', *, *, #206019, .T. ) ;
#252868=ORIENTED_EDGE ( 'NONE', *, *, #187968, .F. ) ;
#252895=ORIENTED_EDGE ( 'NONE', *, *, #48816, .T. ) ;
#252898=LINE ( 'NONE', #96375, #40533 ) ;
#252921=ORIENTED_EDGE ( 'NONE', *, *, #45469, .T. ) ;
#252951=ORIENTED_EDGE ( 'NONE', *, *, #70821, .F. ) ;
#252963=CARTESIAN_POINT ( 'NONE',  ( 18.52928932188133970, 33.79964813154141723, -236.3583302510377564 ) ) ;
#252970=EDGE_CURVE ( 'NONE', #160790, #149361, #69319, .T. ) ;
#252979=DIRECTION ( 'NONE',  ( 0.000000000000000000, 0.8814952561688476074, -0.4721928772777262417 ) ) ;
#252995=CARTESIAN_POINT ( 'NONE',  ( -22.50000000000000000, 0.3085173699977072914, -229.9658011520297691 ) ) ;
#253032=CIRCLE ( 'NONE', #140595, 0.8750000000000007772 ) ;
#253051=DIRECTION ( 'NONE',  ( 0.000000000000000000, 0.8855159391400492241, -0.4646089985449236570 ) ) ;
#253072=LINE ( 'NONE', #155305, #5250 ) ;
#253074=CYLINDRICAL_SURFACE ( 'NONE', #135537, 0.09999999999999986677 ) ;
#253088=DIRECTION ( 'NONE',  ( 0.000000000000000000, 0.8814952561688430555, -0.4721928772777346239 ) ) ;
#253095=DIRECTION ( 'NONE',  ( -1.000000000000000000, -8.855395344894292773E-17, -1.653135691717061729E-16 ) ) ;
#253105=ADVANCED_FACE ( 'NONE', ( #149589 ), #54645, .T. ) ;
#253117=EDGE_CURVE ( 'NONE', #114510, #35657, #185814, .T. ) ;
#253124=TOROIDAL_SURFACE ( 'NONE', #165681, 0.2000000000000000111, 0.1000000000000000056 ) ;
#253134=AXIS2_PLACEMENT_3D ( 'NONE', #236586, #198751, #137480 ) ;
#253147=ADVANCED_FACE ( 'NONE', ( #238075 ), #40103, .T. ) ;
#253175=DIRECTION ( 'NONE',  ( 0.000000000000000000, 0.8814952561688438326, -0.4721928772777330696 ) ) ;
#253213=CARTESIAN_POINT ( 'NONE',  ( 18.49999999999999289, 33.98796489282361932, -236.2185561567993091 ) ) ;
#253238=CARTESIAN_POINT ( 'NONE',  ( -18.39999999999999858, 8.812838127540084443, -245.4119190891508708 ) ) ;
#253241=VERTEX_POINT ( 'NONE', #116856 ) ;
#253250=CIRCLE ( 'NONE', #74230, 7.720710678118662074 ) ;
#253308=CARTESIAN_POINT ( 'NONE',  ( 21.00000000000000000, 30.37633856152204359, -235.1250019192171408 ) ) ;
#253337=VERTEX_POINT ( 'NONE', #226188 ) ;
#253338=CARTESIAN_POINT ( 'NONE',  ( -20.89192007715127986, 46.45729338110133710, -243.0823073233429170 ) ) ;
#253342=ADVANCED_FACE ( 'NONE', ( #167568 ), #48870, .F. ) ;
#253351=ADVANCED_FACE ( 'NONE', ( #82824 ), #52150, .T. ) ;
#253369=LINE ( 'NONE', #193420, #71733 ) ;
#253371=EDGE_CURVE ( 'NONE', #110689, #161820, #106293, .T. ) ;
#253439=CARTESIAN_POINT ( 'NONE',  ( 20.85000000000000142, 36.65892442174935439, -249.5511627012433848 ) ) ;
#253465=CARTESIAN_POINT ( 'NONE',  ( -18.54260524012581612, 38.05639603915591351, -261.2178114574803089 ) ) ;
#253472=ORIENTED_EDGE ( 'NONE', *, *, #82021, .F. ) ;
#253481=VERTEX_POINT ( 'NONE', #134807 ) ;
#253511=VERTEX_POINT ( 'NONE', #79960 ) ;
#253534=CYLINDRICAL_SURFACE ( 'NONE', #231177, 7.899999999999994138 ) ;
#253550=CARTESIAN_POINT ( 'NONE',  ( 21.13435531349839991, 1.404649027653016802, -230.6664124791826964 ) ) ;
#253622=CARTESIAN_POINT ( 'NONE',  ( -20.54999999999999716, 18.56623428888383387, -239.8594038951179073 ) ) ;
#253661=CARTESIAN_POINT ( 'NONE',  ( -23.15000000000000213, 26.18196512540240661, -241.1028522842020152 ) ) ;
#253673=ORIENTED_EDGE ( 'NONE', *, *, #157397, .T. ) ;
#253703=CARTESIAN_POINT ( 'NONE',  ( -21.44999999999999929, 21.39147882631411335, -233.2615922652120730 ) ) ;
#253713=ORIENTED_EDGE ( 'NONE', *, *, #46197, .T. ) ;
#253720=AXIS2_PLACEMENT_3D ( 'NONE', #224223, #26050, #166867 ) ;
#253739=VERTEX_POINT ( 'NONE', #125539 ) ;
#253740=EDGE_CURVE ( 'NONE', #51015, #176803, #60692, .T. ) ;
#253745=ORIENTED_EDGE ( 'NONE', *, *, #14755, .T. ) ;
#253780=EDGE_CURVE ( 'NONE', #116426, #110689, #131954, .T. ) ;
#253784=CIRCLE ( 'NONE', #208034, 0.4999999999999987232 ) ;
#253796=ADVANCED_FACE ( 'NONE', ( #111111 ), #248053, .T. ) ;
#253837=ORIENTED_EDGE ( 'NONE', *, *, #23845, .F. ) ;
#253848=DIRECTION ( 'NONE',  ( -4.448008912761041834E-16, 0.4721928772777335692, 0.8814952561688436106 ) ) ;
#253869=VECTOR ( 'NONE', #216389, 1000.000000000000000 ) ;
#253872=EDGE_CURVE ( 'NONE', #254486, #242741, #202189, .T. ) ;
#253884=DIRECTION ( 'NONE',  ( -1.000000000000000000, -0.000000000000000000, -0.000000000000000000 ) ) ;
#253905=DIRECTION ( 'NONE',  ( -1.000000000000000000, 0.000000000000000000, 0.000000000000000000 ) ) ;
#253927=DIRECTION ( 'NONE',  ( 0.000000000000000000, -0.8127272543710951647, 0.5826443254700257590 ) ) ;
#253937=CARTESIAN_POINT ( 'NONE',  ( 21.07016717456945187, 10.11353658153798563, -228.1608219491299678 ) ) ;
#253940=VERTEX_POINT ( 'NONE', #174989 ) ;
#253942=DIRECTION ( 'NONE',  ( 2.952720810173290098E-16, -0.4721928772777468364, -0.8814952561688365051 ) ) ;
#253981=CARTESIAN_POINT ( 'NONE',  ( 20.95512820512820440, 18.90192396791320562, -227.9871466877642661 ) ) ;
#254003=ORIENTED_EDGE ( 'NONE', *, *, #131381, .F. ) ;
#254009=DIRECTION ( 'NONE',  ( 1.000000000000000000, 0.000000000000000000, 0.000000000000000000 ) ) ;
#254033=DIRECTION ( 'NONE',  ( 0.000000000000000000, -0.4721928772777346239, -0.8814952561688430555 ) ) ;
#254041=EDGE_CURVE ( 'NONE', #136089, #195479, #102367, .T. ) ;
#254046=DIRECTION ( 'NONE',  ( 0.000000000000000000, 0.8814952561688439436, -0.4721928772777332362 ) ) ;
#254066=DIRECTION ( 'NONE',  ( 0.000000000000000000, 0.8814952561688476074, -0.4721928772777262417 ) ) ;
#254095=EDGE_CURVE ( 'NONE', #74203, #98621, #181544, .T. ) ;
#254126=CARTESIAN_POINT ( 'NONE',  ( 20.94999999999999574, 14.85285025691667293, -236.4388300032497057 ) ) ;
#254129=ORIENTED_EDGE ( 'NONE', *, *, #50259, .T. ) ;
#254141=VERTEX_POINT ( 'NONE', #189062 ) ;
#254147=ORIENTED_EDGE ( 'NONE', *, *, #167127, .F. ) ;
#254155=ORIENTED_EDGE ( 'NONE', *, *, #8015, .F. ) ;
#254186=ORIENTED_EDGE ( 'NONE', *, *, #139548, .T. ) ;
#254200=ORIENTED_EDGE ( 'NONE', *, *, #243746, .F. ) ;
#254208=ORIENTED_EDGE ( 'NONE', *, *, #219597, .F. ) ;
#254218=CARTESIAN_POINT ( 'NONE',  ( 18.59999999999999787, 26.26588584238432489, -255.7307459359297468 ) ) ;
#254225=VECTOR ( 'NONE', #20547, 1000.000000000000000 ) ;
#254230=ORIENTED_EDGE ( 'NONE', *, *, #248643, .T. ) ;
#254297=ORIENTED_EDGE ( 'NONE', *, *, #133454, .F. ) ;
#254323=CARTESIAN_POINT ( 'NONE',  ( 20.94999999999999929, 28.08470566095357057, -239.2860081655328770 ) ) ;
#254326=CARTESIAN_POINT ( 'NONE',  ( -21.00857864376268935, 18.71344899777637849, -226.7788045585494103 ) ) ;
#254348=EDGE_CURVE ( 'NONE', #21732, #84289, #85810, .T. ) ;
#254349=DIRECTION ( 'NONE',  ( -1.000000000000000000, 0.000000000000000000, 0.000000000000000000 ) ) ;
#254382=CARTESIAN_POINT ( 'NONE',  ( 18.59999999999999432, 13.71992543034163781, -238.5823796952984992 ) ) ;
#254412=ADVANCED_FACE ( 'NONE', ( #115949 ), #61078, .T. ) ;
#254416=AXIS2_PLACEMENT_3D ( 'NONE', #105752, #124077, #197482 ) ;
#254485=CARTESIAN_POINT ( 'NONE',  ( -18.59999999999999787, 14.81796439977981272, -236.5325475414793743 ) ) ;
#254486=VERTEX_POINT ( 'NONE', #245832 ) ;
#254496=ORIENTED_EDGE ( 'NONE', *, *, #129365, .F. ) ;
#254501=DIRECTION ( 'NONE',  ( 1.734723475976817192E-14, 0.8814952561688430555, -0.4721928772777346239 ) ) ;
#254516=CARTESIAN_POINT ( 'NONE',  ( -21.14999999999999858, 12.71802988599559292, -223.5105008658000258 ) ) ;
#254541=DIRECTION ( 'NONE',  ( 0.000000000000000000, 0.8814952561688428334, -0.4721928772777349570 ) ) ;
#254576=SPHERICAL_SURFACE ( 'NONE', #255210, 0.1000000000000000056 ) ;
#254579=EDGE_CURVE ( 'NONE', #85514, #205599, #19399, .T. ) ;
#254589=DIRECTION ( 'NONE',  ( -1.000000000000000000, 0.000000000000000000, 0.000000000000000000 ) ) ;
#254591=LINE ( 'NONE', #248515, #234958 ) ;
#254618=ADVANCED_FACE ( 'NONE', ( #110161 ), #40274, .F. ) ;
#254654=ORIENTED_EDGE ( 'NONE', *, *, #217702, .T. ) ;
#254680=LINE ( 'NONE', #33157, #110964 ) ;
#254710=DIRECTION ( 'NONE',  ( 0.000000000000000000, 0.8814952561688427224, -0.4721928772777352901 ) ) ;
#254714=CARTESIAN_POINT ( 'NONE',  ( -18.39999999999999858, 38.27493434228537694, -261.1939574891503639 ) ) ;
#254746=FACE_BOUND ( 'NONE', #203483, .T. ) ;
#254788=DIRECTION ( 'NONE',  ( -1.000000000000000000, -3.448943450116723568E-16, -6.438528483529607644E-16 ) ) ;
#254805=DIRECTION ( 'NONE',  ( 1.000000000000000000, 3.448943450116723568E-16, 6.438528483529607644E-16 ) ) ;
#254810=VERTEX_POINT ( 'NONE', #193267 ) ;
#254815=DIRECTION ( 'NONE',  ( -1.000000000000000000, -0.000000000000000000, -0.000000000000000000 ) ) ;
#254818=DIRECTION ( 'NONE',  ( 1.000000000000000000, 0.000000000000000000, 0.000000000000000000 ) ) ;
#254834=DIRECTION ( 'NONE',  ( 0.000000000000000000, -0.8814952561688430555, 0.4721928772777346239 ) ) ;
#254840=EDGE_CURVE ( 'NONE', #73105, #235787, #52881, .T. ) ;
#254853=CARTESIAN_POINT ( 'NONE',  ( -20.85000000000000142, 42.20719072976272912, -239.1935934412594804 ) ) ;
#254894=EDGE_CURVE ( 'NONE', #162422, #109178, #23707, .T. ) ;
#254901=VECTOR ( 'NONE', #81047, 1000.000000000000000 ) ;
#254916=VECTOR ( 'NONE', #181791, 1000.000000000000000 ) ;
#254931=FACE_OUTER_BOUND ( 'NONE', #35420, .T. ) ;
#254935=DIRECTION ( 'NONE',  ( 1.000000000000000000, 0.000000000000000000, 0.000000000000000000 ) ) ;
#254939=ORIENTED_EDGE ( 'NONE', *, *, #71764, .T. ) ;
#254969=DIRECTION ( 'NONE',  ( 1.000000000000000000, 0.000000000000000000, 0.000000000000000000 ) ) ;
#254978=ORIENTED_EDGE ( 'NONE', *, *, #216324, .T. ) ;
#254991=EDGE_CURVE ( 'NONE', #109178, #4633, #58855, .T. ) ;
#255011=CARTESIAN_POINT ( 'NONE',  ( -18.60000000000000142, 9.105964803472817337, -245.3658845043482586 ) ) ;
#255024=CARTESIAN_POINT ( 'NONE',  ( 21.05000000000000071, 10.12438351139595127, -228.1852649075067063 ) ) ;
#255050=DIRECTION ( 'NONE',  ( 0.000000000000000000, -0.8814952561688476074, 0.4721928772777262417 ) ) ;
#255059=CIRCLE ( 'NONE', #38650, 11.64999999999999503 ) ;
#255086=ORIENTED_EDGE ( 'NONE', *, *, #71200, .T. ) ;
#255091=DIRECTION ( 'NONE',  ( 1.000000000000000000, 0.000000000000000000, 0.000000000000000000 ) ) ;
#255099=CARTESIAN_POINT ( 'NONE',  ( 18.49999999999998934, 19.00443933019177223, -232.7770257915295531 ) ) ;
#255112=FACE_OUTER_BOUND ( 'NONE', #219338, .T. ) ;
#255122=LINE ( 'NONE', #212223, #108558 ) ;
#255140=CARTESIAN_POINT ( 'NONE',  ( 21.05000000000000071, 28.51339163295720525, -258.4040038037771865 ) ) ;
#255158=CIRCLE ( 'NONE', #63672, 0.09999999999999939493 ) ;
#255160=ADVANCED_FACE ( 'NONE', ( #46998 ), #164412, .F. ) ;
#255210=AXIS2_PLACEMENT_3D ( 'NONE', #95528, #116392, #235053 ) ;
#255220=CARTESIAN_POINT ( 'NONE',  ( 21.13461538461538680, 22.21093039075207543, -231.7318303787630214 ) ) ;
#255227=ORIENTED_EDGE ( 'NONE', *, *, #182508, .T. ) ;
#255229=DIRECTION ( 'NONE',  ( 0.000000000000000000, 0.8814952561688428334, -0.4721928772777350125 ) ) ;
#255246=CARTESIAN_POINT ( 'NONE',  ( -21.05000000000000071, 36.65892442174935439, -249.5511627012433848 ) ) ;
#255291=ORIENTED_EDGE ( 'NONE', *, *, #254579, .T. ) ;
#255329=AXIS2_PLACEMENT_3D ( 'NONE', #246945, #87856, #108732 ) ;
#255335=CARTESIAN_POINT ( 'NONE',  ( 21.05563370358598263, 22.93207528815513641, -230.0321118342242244 ) ) ;
#255363=VERTEX_POINT ( 'NONE', #76848 ) ;
#255370=ORIENTED_EDGE ( 'NONE', *, *, #27667, .F. ) ;
#255414=ORIENTED_EDGE ( 'NONE', *, *, #104047, .T. ) ;
#255451=DIRECTION ( 'NONE',  ( 1.000000000000000000, -0.000000000000000000, -0.000000000000000000 ) ) ;
#255453=AXIS2_PLACEMENT_3D ( 'NONE', #58824, #117541, #161834 ) ;
#255466=AXIS2_PLACEMENT_3D ( 'NONE', #160327, #138144, #2489 ) ;
#255470=LINE ( 'NONE', #234679, #253869 ) ;
#255473=VECTOR ( 'NONE', #92486, 1000.000000000000000 ) ;
#255492=CIRCLE ( 'NONE', #113513, 11.80000000000001670 ) ;
#255501=ORIENTED_EDGE ( 'NONE', *, *, #123269, .F. ) ;
#255525=DIRECTION ( 'NONE',  ( 0.000000000000000000, -0.8814952561688438326, 0.4721928772777332917 ) ) ;
#255553=TOROIDAL_SURFACE ( 'NONE', #239041, 11.65000000000000036, 0.1000000000000000056 ) ;
#255623=AXIS2_PLACEMENT_3D ( 'NONE', #147578, #42083, #43353 ) ;
#255644=ORIENTED_EDGE ( 'NONE', *, *, #183013, .F. ) ;
#255647=ADVANCED_FACE ( 'NONE', ( #110531 ), #10163, .T. ) ;
#255701=ORIENTED_EDGE ( 'NONE', *, *, #211360, .T. ) ;
#255724=ORIENTED_EDGE ( 'NONE', *, *, #17216, .T. ) ;
#255735=DIRECTION ( 'NONE',  ( 0.000000000000000000, -0.5868805631290325842, -0.8096735173027148624 ) ) ;
#255742=CARTESIAN_POINT ( 'NONE',  ( 21.05000000000000071, 4.436385504674529301, -245.3241086753762659 ) ) ;
#255846=AXIS2_PLACEMENT_3D ( 'NONE', #96811, #95557, #116421 ) ;
#255852=ORIENTED_EDGE ( 'NONE', *, *, #157063, .T. ) ;
#255877=DIRECTION ( 'NONE',  ( -0.000000000000000000, -0.4721928772777341798, -0.8814952561688433885 ) ) ;
#255911=EDGE_CURVE ( 'NONE', #92509, #201984, #162525, .T. ) ;
#255912=FACE_OUTER_BOUND ( 'NONE', #137015, .T. ) ;
#255931=VECTOR ( 'NONE', #135324, 1000.000000000000000 ) ;
#255938=ORIENTED_EDGE ( 'NONE', *, *, #234855, .F. ) ;
#255987=CARTESIAN_POINT ( 'NONE',  ( 20.94999999999999929, 36.65892442174935439, -249.5511627012433848 ) ) ;
#255995=EDGE_CURVE ( 'NONE', #205943, #79099, #109478, .T. ) ;
#256019=EDGE_CURVE ( 'NONE', #94806, #218203, #151202, .T. ) ;
#256029=DIRECTION ( 'NONE',  ( -1.000000000000000000, 0.000000000000000000, 0.000000000000000000 ) ) ;
#256058=CARTESIAN_POINT ( 'NONE',  ( -21.05000000000000426, 10.15197506655037429, -228.1685576039200498 ) ) ;
#256088=CARTESIAN_POINT ( 'NONE',  ( -20.94999999999999929, 7.128833340093095217, -233.7327013124392749 ) ) ;
#256091=DIRECTION ( 'NONE',  ( 1.000000000000000000, 0.000000000000000000, 0.000000000000000000 ) ) ;
#256102=VERTEX_POINT ( 'NONE', #75928 ) ;
#256122=DIRECTION ( 'NONE',  ( 1.000000000000000000, 0.000000000000000000, 0.000000000000000000 ) ) ;
#256164=LINE ( 'NONE', #93302, #240130 ) ;
#256185=ORIENTED_EDGE ( 'NONE', *, *, #16035, .F. ) ;
#256202=ORIENTED_EDGE ( 'NONE', *, *, #200290, .T. ) ;
#256242=EDGE_LOOP ( 'NONE', ( #75973, #97891, #12932, #180384 ) ) ;
#256258=CIRCLE ( 'NONE', #227289, 0.09999999999999939493 ) ;
#256263=ORIENTED_EDGE ( 'NONE', *, *, #235806, .F. ) ;
#256299=CARTESIAN_POINT ( 'NONE',  ( -22.59999970745345976, -3.233606324747438254, -228.1924402736483444 ) ) ;
#256319=AXIS2_PLACEMENT_3D ( 'NONE', #205629, #150805, #106518 ) ;
#256322=CARTESIAN_POINT ( 'NONE',  ( 22.45380639572256953, -3.229117443981163849, -228.1842304705649553 ) ) ;
#256325=ORIENTED_EDGE ( 'NONE', *, *, #135902, .T. ) ;
#256326=CIRCLE ( 'NONE', #143965, 11.90000000000000746 ) ;
#256344=ORIENTED_EDGE ( 'NONE', *, *, #103926, .T. ) ;
#256407=ORIENTED_EDGE ( 'NONE', *, *, #247076, .F. ) ;
#256421=CARTESIAN_POINT ( 'NONE',  ( 20.94999999999999929, 36.65892442174935439, -249.5511627012433848 ) ) ;
#256439=FACE_OUTER_BOUND ( 'NONE', #208236, .T. ) ;
#256452=CIRCLE ( 'NONE', #239976, 0.09999999999999438505 ) ;
#256486=DIRECTION ( 'NONE',  ( 1.000000000000000000, 0.000000000000000000, 0.000000000000000000 ) ) ;
#256498=CARTESIAN_POINT ( 'NONE',  ( -20.85000000000000142, 43.18640298906419162, -245.2812653309023574 ) ) ;
#256504=ORIENTED_EDGE ( 'NONE', *, *, #3338, .F. ) ;
#256520=ORIENTED_EDGE ( 'NONE', *, *, #32473, .F. ) ;
#256539=CARTESIAN_POINT ( 'NONE',  ( 18.52351027002947959, 38.02524580842611357, -261.2214809015557080 ) ) ;
#256548=DIRECTION ( 'NONE',  ( 0.000000000000000000, 0.8814952561688436106, -0.4721928772777334027 ) ) ;
#256553=CARTESIAN_POINT ( 'NONE',  ( -18.59999999999999787, 29.37215541956148002, -237.4231786350947857 ) ) ;
#256562=EDGE_CURVE ( 'NONE', #34543, #159519, #43232, .T. ) ;
#256599=ORIENTED_EDGE ( 'NONE', *, *, #233858, .T. ) ;
#256625=STYLED_ITEM ( 'NONE', ( #174091 ), #29580 ) ;
#256642=LINE ( 'NONE', #181035, #55539 ) ;
#256691=CARTESIAN_POINT ( 'NONE',  ( -20.64999999999999858, 36.65892442174935439, -249.5511627012433848 ) ) ;
#256710=VECTOR ( 'NONE', #172985, 1000.000000000000000 ) ;
#256744=DIRECTION ( 'NONE',  ( 0.000000000000000000, -0.4721928772777346239, -0.8814952561688430555 ) ) ;
#256745=ORIENTED_EDGE ( 'NONE', *, *, #48816, .F. ) ;
#256805=FACE_OUTER_BOUND ( 'NONE', #163029, .T. ) ;
#256839=EDGE_CURVE ( 'NONE', #44305, #89936, #172447, .T. ) ;
#256854=LINE ( 'NONE', #22175, #185788 ) ;
#256859=PLANE ( 'NONE',  #161690 ) ;
#256881=ORIENTED_EDGE ( 'NONE', *, *, #154410, .T. ) ;
#256897=DIRECTION ( 'NONE',  ( 0.000000000000000000, 0.8814952561688437216, -0.4721928772777334582 ) ) ;
#256923=TOROIDAL_SURFACE ( 'NONE', #144532, 11.90000000000000213, 0.1000000000000000056 ) ;
#256942=ORIENTED_EDGE ( 'NONE', *, *, #184069, .T. ) ;
#256947=VERTEX_POINT ( 'NONE', #189982 ) ;
#256951=ORIENTED_EDGE ( 'NONE', *, *, #47512, .F. ) ;
#257030=VERTEX_POINT ( 'NONE', #29654 ) ;
#257044=AXIS2_PLACEMENT_3D ( 'NONE', #154160, #54986, #255735 ) ;
#257049=CARTESIAN_POINT ( 'NONE',  ( -18.50000000000000000, 18.81339837015603322, -226.7756228984618190 ) ) ;
#257119=AXIS2_PLACEMENT_3D ( 'NONE', #37464, #17870, #58273 ) ;
#257120=CYLINDRICAL_SURFACE ( 'NONE', #2591, 0.09999999999999939493 ) ;
#257125=CARTESIAN_POINT ( 'NONE',  ( 19.92426406871192412, 34.58225676390223668, -235.1091250528070304 ) ) ;
#257138=ORIENTED_EDGE ( 'NONE', *, *, #122490, .T. ) ;
#257141=EDGE_CURVE ( 'NONE', #1463, #95344, #5966, .T. ) ;
#257142=AXIS2_PLACEMENT_3D ( 'NONE', #103955, #223908, #120558 ) ;
#257153=SPHERICAL_SURFACE ( 'NONE', #24222, 0.1000000000000000056 ) ;
#257164=ORIENTED_EDGE ( 'NONE', *, *, #139933, .F. ) ;
#257200=TOROIDAL_SURFACE ( 'NONE', #52850, 11.70000000000000107, 0.1000000000000000056 ) ;
#257249=DIRECTION ( 'NONE',  ( 0.000000000000000000, -0.8814952561688430555, 0.4721928772777346239 ) ) ;
#257278=ORIENTED_EDGE ( 'NONE', *, *, #114913, .T. ) ;
#257281=AXIS2_PLACEMENT_3D ( 'NONE', #168135, #3877, #65127 ) ;
#257289=ORIENTED_EDGE ( 'NONE', *, *, #104343, .F. ) ;
#257305=CARTESIAN_POINT ( 'NONE',  ( 22.39999999999999503, 1.666707276765596379, -230.6933463038365630 ) ) ;
#257355=AXIS2_PLACEMENT_3D ( 'NONE', #105770, #203613, #4125 ) ;
#257465=ORIENTED_EDGE ( 'NONE', *, *, #183512, .F. ) ;
#257480=VERTEX_POINT ( 'NONE', #170159 ) ;
#257501=CARTESIAN_POINT ( 'NONE',  ( 18.59999999999999432, -1.235880796157547756, -222.7862885752216471 ) ) ;
#257504=CARTESIAN_POINT ( 'NONE',  ( -20.64999999999999858, 23.68770167995059595, -252.8127582590406348 ) ) ;
#257526=ORIENTED_EDGE ( 'NONE', *, *, #16633, .F. ) ;
#257533=CIRCLE ( 'NONE', #195274, 0.09999999999999986677 ) ;
#257542=DIRECTION ( 'NONE',  ( 1.000000000000000000, 0.000000000000000000, 0.000000000000000000 ) ) ;
#257553=EDGE_CURVE ( 'NONE', #222451, #86057, #180971, .T. ) ;
#257561=DIRECTION ( 'NONE',  ( -0.000000000000000000, 0.4721928772777345684, 0.8814952561688429444 ) ) ;
#257582=CARTESIAN_POINT ( 'NONE',  ( -18.40000000000000213, 8.780520186313282238, -245.4165333277509831 ) ) ;
#257602=VERTEX_POINT ( 'NONE', #86059 ) ;
#257607=AXIS2_PLACEMENT_3D ( 'NONE', #245478, #244161, #88937 ) ;
#257653=AXIS2_PLACEMENT_3D ( 'NONE', #186953, #244314, #65686 ) ;
#257663=CIRCLE ( 'NONE', #103582, 0.09999999999999939493 ) ;
#257718=CARTESIAN_POINT ( 'NONE',  ( 18.49999999999998934, 21.15538238767524604, -233.7023398932965108 ) ) ;
#257725=AXIS2_PLACEMENT_3D ( 'NONE', #149412, #210643, #172854 ) ;
#257731=EDGE_CURVE ( 'NONE', #207618, #62655, #28740, .T. ) ;
#257734=CARTESIAN_POINT ( 'NONE',  ( -22.49231231312463208, 12.57605540120662901, -223.4344661467465301 ) ) ;
#257775=DIRECTION ( 'NONE',  ( 0.000000000000000000, -0.8814952561688437216, 0.4721928772777334582 ) ) ;
#257778=CARTESIAN_POINT ( 'NONE',  ( 21.05000000000000071, 18.80860808352057134, -227.8685889463688454 ) ) ;
#257784=EDGE_CURVE ( 'NONE', #110056, #43771, #127161, .T. ) ;
#257801=DIRECTION ( 'NONE',  ( -0.000000000000000000, 0.4721928772777345684, 0.8814952561688429444 ) ) ;
#257834=DIRECTION ( 'NONE',  ( 0.000000000000000000, 0.8814952561688431665, -0.4721928772777346794 ) ) ;
#257841=CARTESIAN_POINT ( 'NONE',  ( 21.05000000000000071, 36.65892442174935439, -249.5511627012433848 ) ) ;
#257849=LINE ( 'NONE', #216191, #218886 ) ;
#257855=DIRECTION ( 'NONE',  ( -1.000000000000000000, -1.394253735153569469E-16, -2.602809386958778209E-16 ) ) ;
#257858=FACE_OUTER_BOUND ( 'NONE', #231175, .T. ) ;
#257885=DIRECTION ( 'NONE',  ( -0.000000000000000000, 0.4721928772777345684, 0.8814952561688429444 ) ) ;
#257894=CARTESIAN_POINT ( 'NONE',  ( 20.95512820512820440, 18.90192396791320562, -227.9871466877642661 ) ) ;
#257896=CARTESIAN_POINT ( 'NONE',  ( 18.59999999999999076, 42.15997144203495139, -239.2817429668763793 ) ) ;
#257974=FACE_OUTER_BOUND ( 'NONE', #166071, .T. ) ;
#257999=ORIENTED_EDGE ( 'NONE', *, *, #217178, .T. ) ;
#258027=DIRECTION ( 'NONE',  ( -2.978066053179064300E-16, 0.4721928772777334582, 0.8814952561688436106 ) ) ;
#258049=CIRCLE ( 'NONE', #53909, 3.999999999999994671 ) ;
#258065=TOROIDAL_SURFACE ( 'NONE', #179041, 0.2000000000000000111, 0.1000000000000000056 ) ;
#258078=CARTESIAN_POINT ( 'NONE',  ( -23.15000000000000213, 26.42645436459467589, -241.9028176822583589 ) ) ;
ENDSEC;
END-ISO-10303-21;
